ISO-10303-21;
HEADER;
/* Generated by software containing ST-Developer
 * from STEP Tools, Inc. (www.steptools.com) 
 */

FILE_DESCRIPTION(
/* description */ (
'Independent guided parallel-jaw bracket clamp. Two12mm guide rods, re
placeable bronze sleeves, captured swiveling spindle, replaceable jaw 
pads and modeled M16x2 screw. Native slider/revolute joints linked2mm 
per revolution. Nominal opening0..122 with initial28mm. Base and two i
dentical supports welded. Standard fits, weld details and clamp load r
equire engineering selection.'),
/* implementation_level */ '2;1');

FILE_NAME(
/* name */ 'Socket head cap screw M6x25.step',
/* time_stamp */ '2026-11-14T09:15:44-08:00',
/* author */ (''),
/* organization */ (''),
/* preprocessor_version */ 'ST-DEVELOPER v20.2',
/* originating_system */ 'Autodesk Translation Framework v15.17.0.0',
/* authorisation */ '');

FILE_SCHEMA (('AUTOMOTIVE_DESIGN { 1 0 10303 214 3 1 1 }'));
ENDSEC;

DATA;
#10=MECHANICAL_DESIGN_GEOMETRIC_PRESENTATION_REPRESENTATION('',(#926),#105806);
#103=B_SPLINE_SURFACE_WITH_KNOTS('',3,3,((#104256,#104257,#104258,#104259,
#104260,#104261,#104262,#104263,#104264,#104265,#104266,#104267,#104268,
#104269,#104270,#104271,#104272,#104273,#104274,#104275,#104276,#104277,
#104278,#104279,#104280,#104281,#104282,#104283,#104284,#104285,#104286,
#104287,#104288,#104289,#104290,#104291,#104292,#104293,#104294,#104295,
#104296,#104297,#104298,#104299,#104300,#104301,#104302,#104303,#104304,
#104305,#104306,#104307,#104308,#104309,#104310,#104311,#104312,#104313,
#104314,#104315,#104316,#104317,#104318,#104319,#104320,#104321,#104322,
#104323,#104324,#104325,#104326,#104327,#104328,#104329,#104330,#104331,
#104332,#104333,#104334,#104335,#104336,#104337,#104338,#104339,#104340,
#104341,#104342,#104343,#104344,#104345,#104346,#104347,#104348,#104349,
#104350,#104351,#104352,#104353,#104354,#104355,#104356,#104357,#104358,
#104359,#104360,#104361,#104362,#104363,#104364,#104365,#104366,#104367,
#104368,#104369,#104370,#104371,#104372,#104373,#104374,#104375,#104376,
#104377,#104378,#104379,#104380,#104381,#104382,#104383,#104384,#104385,
#104386,#104387,#104388,#104389,#104390,#104391,#104392,#104393,#104394,
#104395,#104396,#104397,#104398,#104399,#104400,#104401,#104402,#104403,
#104404,#104405,#104406,#104407,#104408,#104409,#104410,#104411,#104412,
#104413),(#104414,#104415,#104416,#104417,#104418,#104419,#104420,#104421,
#104422,#104423,#104424,#104425,#104426,#104427,#104428,#104429,#104430,
#104431,#104432,#104433,#104434,#104435,#104436,#104437,#104438,#104439,
#104440,#104441,#104442,#104443,#104444,#104445,#104446,#104447,#104448,
#104449,#104450,#104451,#104452,#104453,#104454,#104455,#104456,#104457,
#104458,#104459,#104460,#104461,#104462,#104463,#104464,#104465,#104466,
#104467,#104468,#104469,#104470,#104471,#104472,#104473,#104474,#104475,
#104476,#104477,#104478,#104479,#104480,#104481,#104482,#104483,#104484,
#104485,#104486,#104487,#104488,#104489,#104490,#104491,#104492,#104493,
#104494,#104495,#104496,#104497,#104498,#104499,#104500,#104501,#104502,
#104503,#104504,#104505,#104506,#104507,#104508,#104509,#104510,#104511,
#104512,#104513,#104514,#104515,#104516,#104517,#104518,#104519,#104520,
#104521,#104522,#104523,#104524,#104525,#104526,#104527,#104528,#104529,
#104530,#104531,#104532,#104533,#104534,#104535,#104536,#104537,#104538,
#104539,#104540,#104541,#104542,#104543,#104544,#104545,#104546,#104547,
#104548,#104549,#104550,#104551,#104552,#104553,#104554,#104555,#104556,
#104557,#104558,#104559,#104560,#104561,#104562,#104563,#104564,#104565,
#104566,#104567,#104568,#104569,#104570,#104571),(#104572,#104573,#104574,
#104575,#104576,#104577,#104578,#104579,#104580,#104581,#104582,#104583,
#104584,#104585,#104586,#104587,#104588,#104589,#104590,#104591,#104592,
#104593,#104594,#104595,#104596,#104597,#104598,#104599,#104600,#104601,
#104602,#104603,#104604,#104605,#104606,#104607,#104608,#104609,#104610,
#104611,#104612,#104613,#104614,#104615,#104616,#104617,#104618,#104619,
#104620,#104621,#104622,#104623,#104624,#104625,#104626,#104627,#104628,
#104629,#104630,#104631,#104632,#104633,#104634,#104635,#104636,#104637,
#104638,#104639,#104640,#104641,#104642,#104643,#104644,#104645,#104646,
#104647,#104648,#104649,#104650,#104651,#104652,#104653,#104654,#104655,
#104656,#104657,#104658,#104659,#104660,#104661,#104662,#104663,#104664,
#104665,#104666,#104667,#104668,#104669,#104670,#104671,#104672,#104673,
#104674,#104675,#104676,#104677,#104678,#104679,#104680,#104681,#104682,
#104683,#104684,#104685,#104686,#104687,#104688,#104689,#104690,#104691,
#104692,#104693,#104694,#104695,#104696,#104697,#104698,#104699,#104700,
#104701,#104702,#104703,#104704,#104705,#104706,#104707,#104708,#104709,
#104710,#104711,#104712,#104713,#104714,#104715,#104716,#104717,#104718,
#104719,#104720,#104721,#104722,#104723,#104724,#104725,#104726,#104727,
#104728,#104729),(#104730,#104731,#104732,#104733,#104734,#104735,#104736,
#104737,#104738,#104739,#104740,#104741,#104742,#104743,#104744,#104745,
#104746,#104747,#104748,#104749,#104750,#104751,#104752,#104753,#104754,
#104755,#104756,#104757,#104758,#104759,#104760,#104761,#104762,#104763,
#104764,#104765,#104766,#104767,#104768,#104769,#104770,#104771,#104772,
#104773,#104774,#104775,#104776,#104777,#104778,#104779,#104780,#104781,
#104782,#104783,#104784,#104785,#104786,#104787,#104788,#104789,#104790,
#104791,#104792,#104793,#104794,#104795,#104796,#104797,#104798,#104799,
#104800,#104801,#104802,#104803,#104804,#104805,#104806,#104807,#104808,
#104809,#104810,#104811,#104812,#104813,#104814,#104815,#104816,#104817,
#104818,#104819,#104820,#104821,#104822,#104823,#104824,#104825,#104826,
#104827,#104828,#104829,#104830,#104831,#104832,#104833,#104834,#104835,
#104836,#104837,#104838,#104839,#104840,#104841,#104842,#104843,#104844,
#104845,#104846,#104847,#104848,#104849,#104850,#104851,#104852,#104853,
#104854,#104855,#104856,#104857,#104858,#104859,#104860,#104861,#104862,
#104863,#104864,#104865,#104866,#104867,#104868,#104869,#104870,#104871,
#104872,#104873,#104874,#104875,#104876,#104877,#104878,#104879,#104880,
#104881,#104882,#104883,#104884,#104885,#104886,#104887)),.UNSPECIFIED.,
 .F.,.F.,.F.,(4,4),(4,1,1,1,1,1,1,1,1,1,1,1,1,1,1,1,1,1,1,1,1,1,1,1,1,1,
1,1,1,1,1,1,1,1,1,1,1,1,1,1,1,1,1,1,1,1,1,1,1,1,1,1,1,1,1,1,1,1,1,1,1,1,
1,1,1,1,1,1,1,1,1,1,1,1,1,1,1,1,1,1,1,1,1,1,1,1,1,1,1,1,1,1,1,1,1,1,1,1,
1,1,1,1,1,1,1,1,1,1,1,1,1,1,1,1,1,1,1,1,1,1,1,1,1,1,1,1,1,1,1,1,1,1,1,1,
1,1,1,1,1,1,1,1,1,1,1,1,1,1,1,1,1,1,1,1,1,4),(-0.000442659764714567,0.0663381390438544),
(11.6145431713147,12.61338032228,13.6117277967416,14.6100752712031,15.6084227456647,
16.6067702201263,17.6051176945879,18.6034651690495,19.6018126435111,20.6001601179726,
21.5985075924342,22.5968550668958,23.5952025413574,24.593550015819,25.5918974902806,
26.5902449647422,27.5885924392037,28.5869399136653,29.5852873881269,30.5836348625885,
31.5819823370501,32.5803298115117,33.5786772859733,34.5770247604348,35.5753722348964,
36.573719709358,37.5720671838196,38.5704146582812,39.5687621327428,40.5671096072044,
41.5654570816659,42.5638045561275,43.5621520305891,44.5604995050507,45.5588469795123,
46.5571944539739,47.5555419284354,48.553889402897,49.5522368773586,50.5505843518202,
51.5489318262818,52.5472793007434,53.545626775205,54.5439742496665,55.5423217241281,
56.5406691985897,57.5390166730513,58.5373641475129,59.5357116219745,60.5340590964361,
61.5324065708976,62.5307540453592,63.5291015198208,64.5274489942824,65.525796468744,
66.5241439432056,67.5224914176672,68.5208388921287,69.5191863665903,70.5175338410519,
71.5158813155135,72.5142287899751,73.5125762644367,74.5109237388983,75.5092712133598,
76.5076186878214,77.505966162283,78.5043136367446,79.5026611112062,80.5010085856678,
81.4993560601293,82.4977035345909,83.4960510090525,84.4943984835141,85.4927459579757,
86.4910934324373,87.4894409068989,88.4877883813604,89.486135855822,90.4844833302836,
91.4828308047452,92.4811782792068,93.4795257536684,94.47787322813,95.4762207025915,
96.4745681770531,97.4729156515147,98.4712631259763,99.4696106004379,100.467958074899,
101.466305549361,102.464653023823,103.463000498284,104.461347972746,105.459695447207,
106.458042921669,107.456390396131,108.454737870592,109.453085345054,110.451432819515,
111.449780293977,112.448127768438,113.4464752429,114.444822717362,115.443170191823,
116.441517666285,117.439865140746,118.438212615208,119.43656008967,120.434907564131,
121.433255038593,122.431602513054,123.429949987516,124.428297461978,125.426644936439,
126.424992410901,127.423339885362,128.421687359824,129.420034834285,130.418382308747,
131.416729783209,132.41507725767,133.413424732132,134.411772206593,135.410119681055,
136.408467155517,137.406814629978,138.40516210444,139.403509578901,140.401857053363,
141.400204527824,142.398552002286,143.396899476748,144.395246951209,145.393594425671,
146.391941900132,147.390289374594,148.388636849056,149.386984323517,150.385331797979,
151.38367927244,152.382026746902,153.380374221363,154.378721695825,155.377069170287,
156.375416644748,157.37376411921,158.372111593671,159.370459068133,160.368806542595,
161.367154017056,162.365501491518,163.363848965979,164.362196440441,165.360543914903,
166.359382730207),.UNSPECIFIED.);
#104=B_SPLINE_SURFACE_WITH_KNOTS('',3,3,((#104979,#104980,#104981,#104982,
#104983,#104984,#104985,#104986,#104987,#104988,#104989,#104990,#104991,
#104992,#104993,#104994,#104995,#104996,#104997,#104998,#104999,#105000,
#105001,#105002,#105003,#105004,#105005,#105006,#105007,#105008,#105009,
#105010,#105011,#105012,#105013,#105014,#105015,#105016,#105017,#105018,
#105019,#105020,#105021,#105022,#105023,#105024,#105025,#105026,#105027,
#105028,#105029,#105030,#105031,#105032,#105033,#105034,#105035,#105036,
#105037,#105038,#105039,#105040,#105041,#105042,#105043,#105044,#105045,
#105046,#105047,#105048,#105049,#105050,#105051,#105052,#105053,#105054,
#105055,#105056,#105057,#105058,#105059,#105060,#105061,#105062,#105063,
#105064,#105065,#105066,#105067,#105068,#105069,#105070,#105071,#105072,
#105073,#105074,#105075,#105076,#105077,#105078,#105079,#105080,#105081,
#105082,#105083,#105084,#105085,#105086,#105087,#105088,#105089,#105090,
#105091,#105092,#105093,#105094,#105095,#105096,#105097,#105098,#105099,
#105100,#105101,#105102,#105103,#105104,#105105,#105106,#105107,#105108,
#105109,#105110,#105111,#105112,#105113,#105114,#105115,#105116,#105117,
#105118,#105119,#105120,#105121,#105122,#105123,#105124,#105125,#105126,
#105127,#105128,#105129,#105130,#105131,#105132,#105133,#105134,#105135,
#105136,#105137,#105138),(#105139,#105140,#105141,#105142,#105143,#105144,
#105145,#105146,#105147,#105148,#105149,#105150,#105151,#105152,#105153,
#105154,#105155,#105156,#105157,#105158,#105159,#105160,#105161,#105162,
#105163,#105164,#105165,#105166,#105167,#105168,#105169,#105170,#105171,
#105172,#105173,#105174,#105175,#105176,#105177,#105178,#105179,#105180,
#105181,#105182,#105183,#105184,#105185,#105186,#105187,#105188,#105189,
#105190,#105191,#105192,#105193,#105194,#105195,#105196,#105197,#105198,
#105199,#105200,#105201,#105202,#105203,#105204,#105205,#105206,#105207,
#105208,#105209,#105210,#105211,#105212,#105213,#105214,#105215,#105216,
#105217,#105218,#105219,#105220,#105221,#105222,#105223,#105224,#105225,
#105226,#105227,#105228,#105229,#105230,#105231,#105232,#105233,#105234,
#105235,#105236,#105237,#105238,#105239,#105240,#105241,#105242,#105243,
#105244,#105245,#105246,#105247,#105248,#105249,#105250,#105251,#105252,
#105253,#105254,#105255,#105256,#105257,#105258,#105259,#105260,#105261,
#105262,#105263,#105264,#105265,#105266,#105267,#105268,#105269,#105270,
#105271,#105272,#105273,#105274,#105275,#105276,#105277,#105278,#105279,
#105280,#105281,#105282,#105283,#105284,#105285,#105286,#105287,#105288,
#105289,#105290,#105291,#105292,#105293,#105294,#105295,#105296,#105297,
#105298),(#105299,#105300,#105301,#105302,#105303,#105304,#105305,#105306,
#105307,#105308,#105309,#105310,#105311,#105312,#105313,#105314,#105315,
#105316,#105317,#105318,#105319,#105320,#105321,#105322,#105323,#105324,
#105325,#105326,#105327,#105328,#105329,#105330,#105331,#105332,#105333,
#105334,#105335,#105336,#105337,#105338,#105339,#105340,#105341,#105342,
#105343,#105344,#105345,#105346,#105347,#105348,#105349,#105350,#105351,
#105352,#105353,#105354,#105355,#105356,#105357,#105358,#105359,#105360,
#105361,#105362,#105363,#105364,#105365,#105366,#105367,#105368,#105369,
#105370,#105371,#105372,#105373,#105374,#105375,#105376,#105377,#105378,
#105379,#105380,#105381,#105382,#105383,#105384,#105385,#105386,#105387,
#105388,#105389,#105390,#105391,#105392,#105393,#105394,#105395,#105396,
#105397,#105398,#105399,#105400,#105401,#105402,#105403,#105404,#105405,
#105406,#105407,#105408,#105409,#105410,#105411,#105412,#105413,#105414,
#105415,#105416,#105417,#105418,#105419,#105420,#105421,#105422,#105423,
#105424,#105425,#105426,#105427,#105428,#105429,#105430,#105431,#105432,
#105433,#105434,#105435,#105436,#105437,#105438,#105439,#105440,#105441,
#105442,#105443,#105444,#105445,#105446,#105447,#105448,#105449,#105450,
#105451,#105452,#105453,#105454,#105455,#105456,#105457,#105458),(#105459,
#105460,#105461,#105462,#105463,#105464,#105465,#105466,#105467,#105468,
#105469,#105470,#105471,#105472,#105473,#105474,#105475,#105476,#105477,
#105478,#105479,#105480,#105481,#105482,#105483,#105484,#105485,#105486,
#105487,#105488,#105489,#105490,#105491,#105492,#105493,#105494,#105495,
#105496,#105497,#105498,#105499,#105500,#105501,#105502,#105503,#105504,
#105505,#105506,#105507,#105508,#105509,#105510,#105511,#105512,#105513,
#105514,#105515,#105516,#105517,#105518,#105519,#105520,#105521,#105522,
#105523,#105524,#105525,#105526,#105527,#105528,#105529,#105530,#105531,
#105532,#105533,#105534,#105535,#105536,#105537,#105538,#105539,#105540,
#105541,#105542,#105543,#105544,#105545,#105546,#105547,#105548,#105549,
#105550,#105551,#105552,#105553,#105554,#105555,#105556,#105557,#105558,
#105559,#105560,#105561,#105562,#105563,#105564,#105565,#105566,#105567,
#105568,#105569,#105570,#105571,#105572,#105573,#105574,#105575,#105576,
#105577,#105578,#105579,#105580,#105581,#105582,#105583,#105584,#105585,
#105586,#105587,#105588,#105589,#105590,#105591,#105592,#105593,#105594,
#105595,#105596,#105597,#105598,#105599,#105600,#105601,#105602,#105603,
#105604,#105605,#105606,#105607,#105608,#105609,#105610,#105611,#105612,
#105613,#105614,#105615,#105616,#105617,#105618)),.UNSPECIFIED.,.F.,.F.,
 .F.,(4,4),(4,1,1,1,1,1,1,1,1,1,1,1,1,1,1,1,1,1,1,1,1,1,1,1,1,1,1,1,1,1,
1,1,1,1,1,1,1,1,1,1,1,1,1,1,1,1,1,1,1,1,1,1,1,1,1,1,1,1,1,1,1,1,1,1,1,1,
1,1,1,1,1,1,1,1,1,1,1,1,1,1,1,1,1,1,1,1,1,1,1,1,1,1,1,1,1,1,1,1,1,1,1,1,
1,1,1,1,1,1,1,1,1,1,1,1,1,1,1,1,1,1,1,1,1,1,1,1,1,1,1,1,1,1,1,1,1,1,1,1,
1,1,1,1,1,1,1,1,1,1,1,1,1,1,1,1,1,1,1,4),(-0.000490634837690153,0.0662903764834337),
(8.30725806501226,9.30628326397092,10.3050889755407,11.3038946871105,12.3027003986803,
13.30150611025,14.3003118218198,15.2991175333896,16.2979232449594,17.2967289565291,
18.2955346680989,19.2943403796687,20.2931460912385,21.2919518028082,22.290757514378,
23.2895632259478,24.2883689375176,25.2871746490874,26.2859803606571,27.2847860722269,
28.2835917837967,29.2823974953665,30.2812032069362,31.280008918506,32.2788146300758,
33.2776203416456,34.2764260532153,35.2752317647851,36.2740374763549,37.2728431879247,
38.2716488994945,39.2704546110642,40.269260322634,41.2680660342038,42.2668717457736,
43.2656774573433,44.2644831689131,45.2632888804829,46.2620945920527,47.2609003036224,
48.2597060151922,49.258511726762,50.2573174383318,51.2561231499016,52.2549288614713,
53.2537345730411,54.2525402846109,55.2513459961807,56.2501517077504,57.2489574193202,
58.24776313089,59.2465688424598,60.2453745540296,61.2441802655993,62.2429859771691,
63.2417916887389,64.2405974003087,65.2394031118784,66.2382088234482,67.237014535018,
68.2358202465878,69.2346259581576,70.2334316697273,71.2322373812971,72.2310430928669,
73.2298488044367,74.2286545160064,75.2274602275762,76.226265939146,77.2250716507158,
78.2238773622855,79.2226830738553,80.2214887854251,81.2202944969949,82.2191002085647,
83.2179059201344,84.2167116317042,85.215517343274,86.2143230548438,87.2131287664135,
88.2119344779833,89.2107401895531,90.2095459011229,91.2083516126927,92.2071573242624,
93.2059630358322,94.204768747402,95.2035744589718,96.2023801705415,97.2011858821113,
98.1999915936811,99.1987973052509,100.197603016821,101.19640872839,102.19521443996,
103.19402015153,104.1928258631,105.19163157467,106.190437286239,107.189242997809,
108.188048709379,109.186854420949,110.185660132518,111.184465844088,112.183271555658,
113.182077267228,114.180882978798,115.179688690367,116.178494401937,117.177300113507,
118.176105825077,119.174911536646,120.173717248216,121.172522959786,122.171328671356,
123.170134382926,124.168940094495,125.167745806065,126.166551517635,127.165357229205,
128.164162940774,129.162968652344,130.161774363914,131.160580075484,132.159385787054,
133.158191498623,134.156997210193,135.155802921763,136.154608633333,137.153414344902,
138.152220056472,139.151025768042,140.149831479612,141.148637191182,142.147442902751,
143.146248614321,144.145054325891,145.143860037461,146.14266574903,147.1414714606,
148.14027717217,149.13908288374,150.13788859531,151.136694306879,152.135500018449,
153.134305730019,154.133111441589,155.131917153158,156.130722864728,157.129528576298,
158.128334287868,159.127139999438,160.125945711007,161.124751422577,162.123557134147,
163.122362845717,164.121168557286,165.120464903694),.UNSPECIFIED.);
#106=CONICAL_SURFACE('',#7707,2.5,0.785398163397448);
#756=B_SPLINE_CURVE_WITH_KNOTS('',3,(#88858,#88859,#88860,#88861,#88862,
#88863,#88864,#88865,#88866,#88867,#88868,#88869,#88870,#88871,#88872,#88873,
#88874,#88875,#88876,#88877,#88878,#88879,#88880,#88881,#88882,#88883,#88884,
#88885,#88886,#88887,#88888,#88889,#88890,#88891,#88892,#88893,#88894,#88895,
#88896,#88897,#88898,#88899,#88900,#88901,#88902,#88903,#88904,#88905,#88906,
#88907,#88908,#88909,#88910,#88911,#88912,#88913,#88914,#88915,#88916,#88917,
#88918,#88919,#88920,#88921,#88922,#88923,#88924,#88925,#88926,#88927,#88928,
#88929,#88930,#88931,#88932,#88933,#88934,#88935,#88936,#88937,#88938,#88939,
#88940,#88941,#88942,#88943,#88944,#88945,#88946,#88947,#88948,#88949,#88950,
#88951,#88952,#88953,#88954,#88955,#88956,#88957,#88958,#88959,#88960,#88961,
#88962,#88963,#88964,#88965,#88966,#88967,#88968,#88969,#88970,#88971,#88972,
#88973,#88974,#88975,#88976,#88977,#88978,#88979,#88980,#88981,#88982,#88983,
#88984,#88985,#88986,#88987,#88988,#88989,#88990,#88991,#88992,#88993,#88994,
#88995,#88996,#88997,#88998,#88999,#89000,#89001,#89002,#89003,#89004,#89005,
#89006,#89007,#89008,#89009,#89010,#89011,#89012,#89013,#89014,#89015,#89016,
#89017,#89018,#89019,#89020,#89021,#89022,#89023,#89024,#89025,#89026,#89027),
 .UNSPECIFIED.,.F.,.F.,(4,2,2,2,2,2,2,2,2,2,2,2,2,2,2,2,2,2,2,2,2,2,2,2,
2,2,2,2,2,2,2,2,2,2,2,2,2,2,2,2,2,2,2,2,2,2,2,2,2,2,2,2,2,2,2,2,2,2,2,2,
2,2,2,2,2,2,2,2,2,2,2,2,2,2,2,2,2,2,2,2,2,2,2,2,4),(-1.2515673108366,-1.22435849913044,
-1.18111626973005,-1.17544558238588,-1.17313343276111,-1.17155791431562,
-1.16991884844908,-1.16738471241629,-1.15964630200229,-1.0993075393073,
-1.06370295787804,-1.05814004411266,-1.05464036190055,-1.05188693155765,
-1.0488117399633,-1.04367588385316,-1.02350567064026,-0.970063196322433,
-0.940627890269205,-0.936844402153188,-0.934908337774157,-0.933366910608549,
-0.931531482081231,-0.928126216997923,-0.90836141146552,-0.83602400114745,
-0.823461389161282,-0.818945364448262,-0.816296041589489,-0.813522380477069,
-0.809899489959606,-0.80211442928955,-0.771129890465391,-0.72688847713087,
-0.719255203577689,-0.702631820792681,-0.699554102394289,-0.697612420993421,
-0.696079488323228,-0.694276095606343,-0.690953296379212,-0.672420985195493,
-0.614755594276794,-0.602710917804209,-0.586308628129192,-0.581345526424109,
-0.578323752560248,-0.575586243211812,-0.572062671692218,-0.564690986793914,
-0.536582468568329,-0.5053700714835,-0.468380511459306,-0.46263404600946,
-0.460316384288055,-0.458886752268476,-0.457282481549026,-0.454916849166946,
-0.448470523637336,-0.409582319930846,-0.354306700297234,-0.345780899997678,
-0.342301711255695,-0.339718401676499,-0.336893078941839,-0.332987395763267,
-0.323623129832107,-0.310488980261098,-0.232900434545352,-0.225381943817547,
-0.222820600626815,-0.221171766935522,-0.219579718940233,-0.217955660179146,
-0.213743814124771,-0.177840686383126,-0.119019789569982,-0.110969718024,
-0.107306702527921,-0.104485004599358,-0.101440861244329,-0.0965944039422034,
-0.0802244065616758,-0.0518476034352533,-0.00381635513711168),
 .UNSPECIFIED.);
#757=B_SPLINE_CURVE_WITH_KNOTS('',3,(#89030,#89031,#89032,#89033,#89034,
#89035,#89036,#89037,#89038,#89039,#89040,#89041,#89042,#89043,#89044,#89045,
#89046,#89047,#89048,#89049,#89050,#89051,#89052,#89053,#89054,#89055,#89056,
#89057,#89058,#89059,#89060,#89061,#89062,#89063,#89064,#89065,#89066,#89067,
#89068,#89069,#89070,#89071,#89072,#89073,#89074,#89075,#89076,#89077,#89078,
#89079,#89080,#89081,#89082,#89083,#89084,#89085,#89086,#89087,#89088,#89089,
#89090,#89091,#89092,#89093,#89094,#89095,#89096,#89097,#89098,#89099,#89100,
#89101,#89102,#89103,#89104,#89105,#89106,#89107,#89108,#89109,#89110,#89111,
#89112,#89113,#89114,#89115,#89116,#89117,#89118,#89119,#89120,#89121,#89122,
#89123,#89124,#89125,#89126,#89127,#89128,#89129,#89130,#89131,#89132,#89133,
#89134,#89135,#89136,#89137,#89138,#89139,#89140,#89141,#89142,#89143,#89144,
#89145,#89146,#89147,#89148,#89149,#89150,#89151,#89152,#89153),
 .UNSPECIFIED.,.F.,.F.,(4,3,3,3,3,3,3,3,3,3,3,3,3,3,3,3,3,3,3,3,3,3,3,3,
3,3,3,3,3,3,3,3,3,3,3,3,3,3,3,3,3,4),(11.6150328478184,11.7178927810683,
11.8206900629369,11.9234772178892,12.0262624995802,12.129071156527,12.2319284566529,
12.3349398758623,12.4380321171329,12.5413259654438,12.61338032228,12.7128604993709,
12.8121804206787,12.9121238426866,13.0112337068811,13.1103017019409,13.2093602993827,
13.3099521737224,13.4091491768461,13.5104384867939,13.6117277967416,13.7123825153464,
13.8128920177283,13.913284058111,14.0136117411332,14.1139061000047,14.2141981264595,
14.3145876671349,14.4150241421376,14.5156398886915,14.6100752712031,14.7107559040164,
14.8112948220338,14.9117214609962,15.0120868840636,15.1124220794924,15.2127579970338,
15.3131959775761,15.4136834531212,15.5143539969786,15.6084227456647,15.635150476959),
 .UNSPECIFIED.);
#758=B_SPLINE_CURVE_WITH_KNOTS('',3,(#89158,#89159,#89160,#89161,#89162,
#89163,#89164,#89165,#89166,#89167,#89168,#89169,#89170,#89171,#89172,#89173,
#89174,#89175,#89176,#89177,#89178,#89179,#89180,#89181,#89182,#89183,#89184,
#89185,#89186,#89187,#89188,#89189,#89190,#89191,#89192,#89193,#89194,#89195,
#89196,#89197,#89198,#89199,#89200,#89201,#89202,#89203,#89204,#89205,#89206,
#89207,#89208,#89209,#89210,#89211,#89212,#89213,#89214,#89215,#89216,#89217,
#89218,#89219,#89220,#89221,#89222,#89223,#89224,#89225,#89226,#89227,#89228,
#89229,#89230,#89231,#89232,#89233,#89234,#89235,#89236,#89237,#89238,#89239,
#89240,#89241,#89242,#89243,#89244,#89245,#89246,#89247,#89248,#89249,#89250,
#89251,#89252,#89253,#89254,#89255,#89256,#89257,#89258,#89259,#89260,#89261,
#89262,#89263,#89264,#89265,#89266,#89267,#89268,#89269,#89270,#89271,#89272,
#89273,#89274,#89275,#89276,#89277,#89278,#89279,#89280,#89281,#89282,#89283,
#89284,#89285,#89286,#89287,#89288,#89289,#89290,#89291,#89292,#89293,#89294,
#89295,#89296,#89297,#89298,#89299,#89300,#89301,#89302,#89303,#89304,#89305,
#89306,#89307,#89308,#89309,#89310,#89311,#89312,#89313,#89314,#89315,#89316,
#89317,#89318,#89319,#89320,#89321,#89322,#89323,#89324,#89325,#89326,#89327,
#89328,#89329,#89330,#89331,#89332,#89333,#89334,#89335,#89336,#89337,#89338,
#89339,#89340,#89341,#89342,#89343,#89344,#89345,#89346,#89347,#89348,#89349,
#89350,#89351,#89352,#89353,#89354,#89355,#89356,#89357,#89358,#89359,#89360,
#89361,#89362,#89363,#89364,#89365,#89366,#89367,#89368,#89369,#89370,#89371,
#89372,#89373,#89374,#89375,#89376,#89377,#89378,#89379,#89380,#89381,#89382,
#89383,#89384,#89385,#89386,#89387,#89388,#89389,#89390,#89391,#89392,#89393,
#89394,#89395,#89396,#89397,#89398,#89399,#89400,#89401,#89402,#89403,#89404,
#89405,#89406,#89407,#89408,#89409),.UNSPECIFIED.,.F.,.F.,(4,2,2,2,2,2,
2,2,2,2,2,2,2,2,2,2,2,2,2,2,2,2,2,2,2,2,2,2,2,2,2,2,2,2,2,2,2,2,2,2,2,2,
2,2,2,2,2,2,2,2,2,2,2,2,2,2,2,2,2,2,2,2,2,2,2,2,2,2,2,2,2,2,2,2,2,2,2,2,
2,2,2,2,2,2,2,2,2,2,2,2,2,2,2,2,2,2,2,2,2,2,2,2,2,2,2,2,2,2,2,2,2,2,2,2,
2,2,2,2,2,2,2,2,2,2,2,4),(-2.74596130104751,-2.72684582105165,-2.72242131286312,
-2.71937229190755,-2.71679617626614,-2.71404945553218,-2.71060476704055,
-2.70522045400994,-2.67511637823372,-2.64750863656549,-2.62210270826699,
-2.60295764488784,-2.59955536128111,-2.59772558506206,-2.59618889512473,
-2.59425996079627,-2.59050191505979,-2.56264900107927,-2.49649139540665,
-2.48897828315974,-2.48299772668024,-2.47975463171809,-2.479725069868,-2.47969492845286,
-2.47966419244804,-2.47963284637204,-2.47960087428214,-2.47956825975468,
-2.47954544089104,-2.4795204642658,-2.47949312009591,-2.47946317725337,
-2.47943038095463,-2.47939445019257,-2.47935507489099,-2.47931191274788,
-2.47926458574908,-2.47921267633288,-2.47915572252463,-2.47909321448,-2.47633865405684,
-2.47281699864536,-2.4671774715544,-2.42019285991096,-2.38617755577876,
-2.36543234783292,-2.36199867938643,-2.36016225741302,-2.35862590846863,
-2.35670484273269,-2.35369425858519,-2.33829393891924,-2.32902161585575,
-2.26453017465292,-2.24896957980145,-2.2442582480386,-2.2412774355981,-2.2385001973981,
-2.23487548393799,-2.22683531039053,-2.16507749804811,-2.12899344642868,
-2.12484631392815,-2.12286498111636,-2.12133864671178,-2.11955425845572,
-2.11644591677456,-2.10375665387797,-2.03159606023987,-2.0120582258132,
-2.00697622583128,-2.003914474815,-2.00116117124945,-1.9976452849142,-1.99202345799012,
-1.94394477625816,-1.90581032736851,-1.88986575871525,-1.88665372202272,
-1.88486518882826,-1.88332503771993,-1.88134241604678,-1.87812717286299,
-1.85863339131255,-1.80809854872818,-1.77872668034899,-1.77116201148413,
-1.76758630099531,-1.76482521486805,-1.76179418482937,-1.75685342154035,
-1.74084672824851,-1.6721503775032,-1.65260031526199,-1.64921360143595,
-1.6473869560256,-1.6458493141535,-1.64391472338356,-1.64013375207598,-1.6106872258172,
-1.56008317041423,-1.5374741737023,-1.53215832280398,-1.52904379965535,
-1.52629694106275,-1.5228613199515,-1.51750907180911,-1.48825471392759,
-1.43322821497606,-1.41500050277623,-1.4116717250324,-1.40985749183632,
-1.40832052744295,-1.40637394901052,-1.4032756794298,-1.3861955666591,-1.38221198054699,
-1.34860598513101,-1.30151785999778,-1.29588783635578,-1.29237067383878,
-1.28961880804336,-1.28656118902796,-1.28149206889162,-1.26208531559498,
-1.2515673108366),.UNSPECIFIED.);
#759=B_SPLINE_CURVE_WITH_KNOTS('',3,(#89411,#89412,#89413,#89414),
 .UNSPECIFIED.,.F.,.F.,(4,4),(15.635150476959,15.707963267949),
 .UNSPECIFIED.);
#760=B_SPLINE_CURVE_WITH_KNOTS('',3,(#89415,#89416,#89417,#89418,#89419,
#89420,#89421,#89422,#89423,#89424,#89425,#89426,#89427,#89428,#89429,#89430,
#89431,#89432,#89433,#89434,#89435,#89436,#89437,#89438,#89439,#89440,#89441,
#89442,#89443,#89444,#89445,#89446,#89447,#89448,#89449,#89450,#89451,#89452,
#89453,#89454,#89455,#89456,#89457,#89458,#89459,#89460,#89461,#89462,#89463,
#89464,#89465,#89466,#89467,#89468,#89469,#89470,#89471,#89472,#89473,#89474,
#89475,#89476,#89477,#89478,#89479,#89480,#89481,#89482,#89483,#89484,#89485,
#89486,#89487,#89488,#89489,#89490,#89491,#89492,#89493,#89494,#89495,#89496,
#89497,#89498,#89499,#89500,#89501,#89502,#89503,#89504,#89505,#89506,#89507,
#89508,#89509,#89510,#89511,#89512,#89513,#89514,#89515,#89516,#89517,#89518,
#89519,#89520,#89521,#89522,#89523,#89524,#89525,#89526,#89527,#89528,#89529,
#89530,#89531,#89532,#89533,#89534,#89535,#89536,#89537,#89538,#89539,#89540,
#89541,#89542,#89543,#89544,#89545,#89546,#89547,#89548,#89549,#89550,#89551,
#89552,#89553,#89554,#89555,#89556,#89557,#89558,#89559,#89560,#89561,#89562,
#89563,#89564,#89565,#89566,#89567,#89568,#89569,#89570,#89571,#89572,#89573,
#89574,#89575,#89576,#89577,#89578,#89579,#89580,#89581,#89582,#89583,#89584,
#89585,#89586,#89587,#89588,#89589,#89590,#89591,#89592,#89593,#89594,#89595,
#89596,#89597,#89598,#89599,#89600,#89601,#89602,#89603,#89604,#89605,#89606,
#89607,#89608,#89609,#89610,#89611,#89612,#89613,#89614,#89615,#89616,#89617,
#89618),.UNSPECIFIED.,.F.,.F.,(4,2,2,2,2,2,2,2,2,2,2,2,2,2,2,2,2,2,2,2,
2,2,2,2,2,2,2,2,2,2,2,2,2,2,2,2,2,2,2,2,2,2,2,2,2,2,2,2,2,2,2,2,2,2,2,2,
2,2,2,2,2,2,2,2,2,2,2,2,2,2,2,2,2,2,2,2,2,2,2,2,2,2,2,2,2,2,2,2,2,2,2,2,
2,2,2,2,2,2,2,2,2,4),(-2.98957413435225,-2.92293074458371,-2.91013837221342,
-2.90095504915141,-2.89707614956163,-2.89425265569043,-2.8916588311148,
-2.88814692245246,-2.87941471369762,-2.82976411010901,-2.79796495390714,
-2.78670708167694,-2.78189848099851,-2.77925522439628,-2.77701460649494,
-2.77542935524957,-2.77397499015983,-2.77162826755696,-2.76587200822799,
-2.7250895086881,-2.68624164526005,-2.66590661028265,-2.66070453546092,
-2.657583278642,-2.65478404542381,-2.65121928814907,-2.64553714632705,-2.59911345921582,
-2.5656538196434,-2.54449388765869,-2.54100065660931,-2.539131123257,-2.53756832620688,
-2.53561287325283,-2.53181148645191,-2.50392182591024,-2.44655015813056,
-2.43470205020368,-2.42603259226309,-2.42222399796675,-2.41939553826342,
-2.41675696755446,-2.41312142376263,-2.40377442571152,-2.32699092878548,
-2.30690690240132,-2.30346565953354,-2.30161228261404,-2.30005438234876,
-2.29809519710445,-2.29500235210593,-2.27856838278559,-2.21653120644009,
-2.19198790275312,-2.18650101799731,-2.18332441100193,-2.18054514951452,
-2.17709774462248,-2.1717810293574,-2.1444143946996,-2.08175518424723,-2.07307842973623,
-2.06720084214376,-2.06490329017409,-2.06329879931526,-2.06182057908956,
-2.05975637643455,-2.05435462513705,-2.00506292444482,-1.95671257219573,
-1.94993615653964,-1.9464843251575,-1.9437008729984,-1.94051874492825,-1.93515983628363,
-1.91478867859304,-1.85745606031538,-1.84038620661764,-1.83398912462634,
-1.82933062865304,-1.82723546660552,-1.82566279584796,-1.82389601835563,
-1.82085558314271,-1.80964880205187,-1.73662019724725,-1.71652005577685,
-1.71134541138908,-1.70823523339447,-1.70544263040521,-1.70188190643201,
-1.69619781331851,-1.6493656260355,-1.61543123898372,-1.59466481383716,
-1.59119672964362,-1.58933758323233,-1.5877793337795,-1.58582545399308,
-1.58202341996452,-1.55346356205055,-1.51266683266716),.UNSPECIFIED.);
#761=B_SPLINE_CURVE_WITH_KNOTS('',3,(#89624,#89625,#89626,#89627,#89628,
#89629,#89630,#89631,#89632,#89633,#89634,#89635,#89636,#89637,#89638,#89639,
#89640,#89641,#89642,#89643,#89644,#89645,#89646,#89647,#89648,#89649,#89650,
#89651,#89652,#89653,#89654,#89655,#89656,#89657,#89658,#89659,#89660,#89661,
#89662,#89663,#89664,#89665,#89666,#89667,#89668,#89669,#89670,#89671,#89672,
#89673,#89674,#89675,#89676,#89677,#89678,#89679,#89680,#89681,#89682,#89683,
#89684,#89685,#89686,#89687,#89688,#89689,#89690,#89691,#89692,#89693,#89694,
#89695,#89696,#89697,#89698,#89699,#89700,#89701,#89702,#89703,#89704,#89705,
#89706,#89707,#89708,#89709,#89710,#89711,#89712,#89713,#89714,#89715,#89716,
#89717,#89718,#89719,#89720,#89721,#89722,#89723,#89724,#89725,#89726,#89727,
#89728,#89729,#89730,#89731,#89732,#89733,#89734,#89735,#89736,#89737,#89738,
#89739,#89740,#89741,#89742,#89743,#89744,#89745,#89746,#89747,#89748,#89749,
#89750,#89751,#89752,#89753,#89754,#89755,#89756,#89757,#89758,#89759,#89760,
#89761,#89762,#89763,#89764,#89765,#89766,#89767,#89768,#89769,#89770,#89771,
#89772,#89773,#89774,#89775,#89776,#89777,#89778,#89779,#89780,#89781,#89782,
#89783,#89784,#89785,#89786,#89787,#89788,#89789,#89790,#89791,#89792,#89793,
#89794,#89795,#89796,#89797,#89798,#89799,#89800,#89801,#89802,#89803,#89804,
#89805,#89806,#89807,#89808,#89809,#89810,#89811,#89812,#89813,#89814,#89815,
#89816,#89817,#89818,#89819,#89820,#89821),.UNSPECIFIED.,.F.,.F.,(4,2,2,
2,2,2,2,2,2,2,2,2,2,2,2,2,2,2,2,2,2,2,2,2,2,2,2,2,2,2,2,2,2,2,2,2,2,2,2,
2,2,2,2,2,2,2,2,2,2,2,2,2,2,2,2,2,2,2,2,2,2,2,2,2,2,2,2,2,2,2,2,2,2,2,2,
2,2,2,2,2,2,2,2,2,2,2,2,2,2,2,2,2,2,2,2,2,2,2,4),(-1.47789197491073,-1.41686972830544,
-1.3890785606746,-1.38378577682514,-1.38036862332489,-1.37762379445051,
-1.37449782019632,-1.36912803422488,-1.34571223404409,-1.29089043456906,
-1.26629215690005,-1.26258628142778,-1.26066824487321,-1.25913165025539,
-1.25729173874776,-1.25384320608642,-1.23271761582457,-1.19916887222781,
-1.15212999409321,-1.14649506710233,-1.14297416629817,-1.14021891174287,
-1.13715701829772,-1.13207953181691,-1.11262116564429,-1.07473851007211,
-1.0317097224467,-1.02602801879475,-1.02371246889212,-1.02213506388296,
-1.02049538514544,-1.01796062384299,-1.01022251912543,-0.949804493250946,
-0.914359309644795,-0.908802674216476,-0.905305390382556,-0.902552869647405,
-0.899477686147479,-0.894339483334249,-0.874130340155093,-0.824871239310694,
-0.791242054640749,-0.787436667388664,-0.785497327356098,-0.783959692472395,
-0.782137437032186,-0.778771768757833,-0.759722066915378,-0.697055384001429,
-0.675501602837159,-0.670097521078887,-0.666932728682255,-0.664465854178,
-0.661221898959827,-0.655306160101179,-0.620637967545861,-0.58343565599599,
-0.553605864413414,-0.549820438836707,-0.547885438263039,-0.54634815550498,
-0.544522670398463,-0.54114151121831,-0.521723963848347,-0.454754481856921,
-0.437210952171618,-0.432105725369859,-0.429038065690201,-0.426284563046816,
-0.422775450884152,-0.415560139825568,-0.365728839964459,-0.318575502838319,
-0.313080744137428,-0.311022519459302,-0.309558813370945,-0.307980585177986,
-0.305742110323364,-0.30013164023708,-0.291947760209732,-0.235751835887413,
-0.201450426413078,-0.195927412534167,-0.192440436493334,-0.18968923253603,
-0.187116094721187,-0.182798655480253,-0.169480225012182,-0.148209782927271,
-0.123966271616637,-0.0812834788924502,-0.0755919121589384,-0.0732749204249909,
-0.0716973995340425,-0.0700584881459055,-0.0675263830913471,-0.0598077889728894,
-0.000705296177145865),.UNSPECIFIED.);
#762=B_SPLINE_CURVE_WITH_KNOTS('',3,(#89822,#89823,#89824,#89825),
 .UNSPECIFIED.,.F.,.F.,(4,4),(-2.76352601725825,-2.74596130104751),
 .UNSPECIFIED.);
#763=B_SPLINE_CURVE_WITH_KNOTS('',3,(#89826,#89827,#89828,#89829,#89830,
#89831,#89832,#89833,#89834,#89835,#89836,#89837,#89838,#89839,#89840,#89841,
#89842,#89843,#89844,#89845,#89846,#89847,#89848,#89849,#89850,#89851,#89852,
#89853,#89854,#89855,#89856,#89857,#89858,#89859,#89860,#89861,#89862,#89863,
#89864,#89865,#89866,#89867,#89868,#89869,#89870,#89871,#89872,#89873,#89874,
#89875,#89876,#89877,#89878,#89879,#89880,#89881,#89882,#89883,#89884,#89885,
#89886,#89887,#89888,#89889,#89890,#89891,#89892,#89893,#89894,#89895,#89896,
#89897,#89898,#89899,#89900,#89901,#89902,#89903,#89904,#89905,#89906,#89907,
#89908,#89909,#89910,#89911,#89912,#89913,#89914,#89915,#89916,#89917,#89918,
#89919,#89920,#89921,#89922,#89923,#89924,#89925,#89926,#89927,#89928,#89929,
#89930,#89931,#89932,#89933,#89934,#89935,#89936,#89937,#89938,#89939,#89940,
#89941,#89942,#89943,#89944,#89945,#89946,#89947,#89948,#89949,#89950,#89951,
#89952,#89953,#89954,#89955,#89956,#89957,#89958,#89959,#89960,#89961,#89962,
#89963,#89964,#89965,#89966,#89967,#89968,#89969,#89970,#89971,#89972,#89973,
#89974,#89975,#89976,#89977,#89978,#89979,#89980,#89981,#89982,#89983,#89984,
#89985,#89986,#89987,#89988,#89989,#89990,#89991,#89992,#89993,#89994,#89995,
#89996,#89997,#89998,#89999,#90000,#90001,#90002,#90003,#90004,#90005,#90006,
#90007,#90008,#90009,#90010,#90011,#90012,#90013,#90014,#90015,#90016,#90017,
#90018,#90019,#90020,#90021,#90022,#90023,#90024,#90025,#90026,#90027,#90028,
#90029,#90030,#90031,#90032,#90033,#90034,#90035,#90036,#90037,#90038,#90039,
#90040,#90041),.UNSPECIFIED.,.F.,.F.,(4,2,2,2,2,2,2,2,2,2,2,2,2,2,2,2,2,
2,2,2,2,2,2,2,2,2,2,2,2,2,2,2,2,2,2,2,2,2,2,2,2,2,2,2,2,2,2,2,2,2,2,2,2,
2,2,2,2,2,2,2,2,2,2,2,2,2,2,2,2,2,2,2,2,2,2,2,2,2,2,2,2,2,2,2,2,2,2,2,2,
2,2,2,2,2,2,2,2,2,2,2,2,2,2,2,2,2,2,4),(-1.51266683266716,-1.49541993273005,
-1.47887900394735,-1.47383826195344,-1.47075792578449,-1.46795935128176,
-1.46434509020257,-1.45673382755789,-1.42732277547221,-1.37690379305642,
-1.35751191070546,-1.35427161457043,-1.35226722718299,-1.35070554134252,
-1.34888488141247,-1.34559673011018,-1.32882556253793,-1.28405894756381,
-1.24384138925538,-1.23814886308824,-1.23458554046803,-1.2317925740647,
-1.228683715852,-1.22351533459441,-1.20349466661584,-1.12479924966047,-1.11802999873483,
-1.11552204707489,-1.11403689096902,-1.11243596725831,-1.11016404529081,
-1.10446111773446,-1.07477621055012,-1.02636085301469,-1.00492336632276,
-0.999485136427048,-0.99628533626524,-0.993504442951504,-0.990078946256255,
-0.983429261080415,-0.93891371504645,-0.890248308468409,-0.881226647652229,
-0.878419126883371,-0.876704042247504,-0.875114867005384,-0.872908733303356,
-0.867610372549159,-0.842068436779016,-0.812474093608546,-0.769012227987209,
-0.763282595597802,-0.759707673875687,-0.756912777297084,-0.753809131882331,
-0.748666699039238,-0.728974028496135,-0.655267307637103,-0.644151324860056,
-0.641119220353837,-0.639354072386046,-0.637781175775374,-0.635683096670152,
-0.631006628918759,-0.593452676122721,-0.534578265305192,-0.526205644581475,
-0.522490001770164,-0.519665745794587,-0.516655958811039,-0.511943113518986,
-0.496762656941134,-0.471309941288985,-0.432312051694832,-0.421904247692991,
-0.40720777399811,-0.403922486841818,-0.402081965744691,-0.400521370479417,
-0.398541633628378,-0.394488972601381,-0.354679141705833,-0.297311951236022,
-0.289653552701159,-0.285532505422394,-0.282935446670138,-0.280073975073642,
-0.2761582401841,-0.266759380907634,-0.253502913961651,-0.213650866315259,
-0.173598485104228,-0.167826212493436,-0.165476509135714,-0.163876444538086,
-0.162212569742731,-0.159637534021854,-0.151749844139344,-0.0973616687214255,
-0.0778315392007462,-0.05520166125016,-0.0496731901416544,-0.0464523816290895,
-0.0436725378849232,-0.0410081735768323,-0.0376833416531648,-0.0326321706283457,
-0.0182824356155657),.UNSPECIFIED.);
#764=B_SPLINE_CURVE_WITH_KNOTS('',3,(#90046,#90047,#90048,#90049,#90050,
#90051,#90052,#90053,#90054,#90055,#90056,#90057,#90058,#90059,#90060,#90061,
#90062,#90063,#90064,#90065,#90066,#90067,#90068,#90069,#90070,#90071,#90072,
#90073,#90074,#90075,#90076,#90077,#90078,#90079,#90080,#90081,#90082,#90083,
#90084,#90085,#90086,#90087,#90088,#90089,#90090,#90091,#90092,#90093,#90094,
#90095,#90096,#90097,#90098,#90099,#90100,#90101,#90102,#90103,#90104,#90105,
#90106,#90107,#90108,#90109,#90110,#90111,#90112,#90113,#90114,#90115,#90116,
#90117,#90118,#90119,#90120,#90121,#90122,#90123,#90124,#90125,#90126,#90127,
#90128,#90129,#90130,#90131,#90132,#90133,#90134,#90135,#90136,#90137,#90138,
#90139,#90140,#90141,#90142,#90143,#90144,#90145,#90146,#90147,#90148,#90149,
#90150,#90151,#90152,#90153,#90154,#90155,#90156,#90157,#90158,#90159,#90160,
#90161,#90162,#90163,#90164,#90165,#90166,#90167,#90168,#90169,#90170,#90171,
#90172,#90173,#90174,#90175,#90176,#90177,#90178,#90179,#90180,#90181,#90182,
#90183,#90184,#90185,#90186,#90187,#90188,#90189,#90190,#90191,#90192,#90193,
#90194,#90195,#90196,#90197,#90198,#90199,#90200,#90201,#90202,#90203,#90204,
#90205,#90206,#90207,#90208,#90209,#90210,#90211,#90212,#90213,#90214,#90215,
#90216,#90217,#90218,#90219,#90220,#90221,#90222,#90223,#90224,#90225,#90226,
#90227,#90228,#90229,#90230,#90231,#90232,#90233,#90234,#90235,#90236,#90237,
#90238,#90239,#90240,#90241,#90242,#90243,#90244,#90245,#90246,#90247,#90248,
#90249,#90250,#90251,#90252,#90253,#90254,#90255,#90256,#90257,#90258,#90259,
#90260,#90261,#90262,#90263,#90264,#90265,#90266,#90267,#90268,#90269),
 .UNSPECIFIED.,.F.,.F.,(4,2,2,2,2,2,2,2,2,2,2,2,2,2,2,2,2,2,2,2,2,2,2,2,
2,2,2,2,2,2,2,2,2,2,2,2,2,2,2,2,2,2,2,2,2,2,2,2,2,2,2,2,2,2,2,2,2,2,2,2,
2,2,2,2,2,2,2,2,2,2,2,2,2,2,2,2,2,2,2,2,2,2,2,2,2,2,2,2,2,2,2,2,2,2,2,2,
2,2,2,2,2,2,2,2,2,2,2,2,2,2,2,4),(-2.97226061936036,-2.93571120009826,-2.9300133755847,
-2.92704069725888,-2.92450288252192,-2.92286304481359,-2.92128703398166,
-2.9189759449437,-2.91331717463684,-2.86978906514473,-2.84307833706508,
-2.81552463117315,-2.80917975508044,-2.80643072780928,-2.80363842954954,
-2.8010458400292,-2.79680191654852,-2.78599163095739,-2.73184172967793,
-2.69535892119586,-2.68918232910714,-2.68681249178123,-2.68520862080502,
-2.68377241594414,-2.68144652420498,-2.67569947722107,-2.63623164624101,
-2.59629359284983,-2.58269653659399,-2.57308582484009,-2.56915218791923,
-2.5663329067649,-2.5637730027392,-2.55970911135672,-2.55215496060649,-2.49369645592223,
-2.48635524258116,-2.45701243143504,-2.45137229878483,-2.44912944327533,
-2.44755067793458,-2.44608849875275,-2.44403521648086,-2.43857489856752,
-2.39058551447352,-2.34002729766112,-2.33379274488407,-2.33048206261321,
-2.32801070830146,-2.32490170506544,-2.31960651102622,-2.30023583327052,
-2.23526414462728,-2.22232643234466,-2.21446577695024,-2.2119165922906,
-2.21027406109759,-2.20869943688505,-2.20639651476276,-2.20078833151477,
-2.15574923301884,-2.11933978898649,-2.10677830203486,-2.0977326277979,
-2.09389184345349,-2.09108912431445,-2.08850963880315,-2.08501004938938,
-2.07630400456507,-2.02814016906202,-1.99294461293695,-1.98302729027546,
-1.97654929981374,-1.97418076725253,-1.97257700401845,-1.97114030670519,
-1.9688125247289,-1.96305534839698,-1.92606296108136,-1.89479507525905,
-1.86679742631814,-1.85941746979412,-1.85587660337223,-1.8531194768352,
-1.85006953463277,-1.84504447942937,-1.82826905093786,-1.76040994782724,
-1.74091882792873,-1.73753445580317,-1.7357082804195,-1.73417103188239,
-1.73223686204881,-1.72845536740707,-1.69892547868359,-1.66601412138072,
-1.63993181671569,-1.62453786004526,-1.6198433588336,-1.61686567692248,
-1.61408614175634,-1.61045093561083,-1.60235576604179,-1.5410249302819,
-1.50523850797559,-1.50064234217139,-1.49857626128058,-1.49702595603265,
-1.49528610268978,-1.49229901967879,-1.47984598605197,-1.47789197491073),
 .UNSPECIFIED.);
#765=B_SPLINE_CURVE_WITH_KNOTS('',3,(#90271,#90272,#90273,#90274),
 .UNSPECIFIED.,.F.,.F.,(4,4),(-0.0182824356155657,-0.000703321212415426),
 .UNSPECIFIED.);
#766=B_SPLINE_CURVE_WITH_KNOTS('',3,(#90275,#90276,#90277,#90278,#90279,
#90280,#90281,#90282,#90283,#90284),.UNSPECIFIED.,.F.,.F.,(4,1,1,1,1,1,
1,4),(28.2743402550742,28.5869399136653,29.5852873881269,30.5836348625885,
31.5819823370501,32.5803298115117,33.5786772859733,34.4839353288417),
 .UNSPECIFIED.);
#767=B_SPLINE_CURVE_WITH_KNOTS('',3,(#90290,#90291,#90292,#90293,#90294,
#90295,#90296,#90297,#90298,#90299),.UNSPECIFIED.,.F.,.F.,(4,1,1,1,1,1,
1,4),(34.5575191894877,35.2752317647851,36.2740374763549,37.2728431879247,
38.2716488994945,39.2704546110642,40.269260322634,40.7676704970196),
 .UNSPECIFIED.);
#768=B_SPLINE_CURVE_WITH_KNOTS('',3,(#90300,#90301,#90302,#90303),
 .UNSPECIFIED.,.F.,.F.,(4,4),(-2.98942133639523,-2.97226061936036),
 .UNSPECIFIED.);
#769=B_SPLINE_CURVE_WITH_KNOTS('',3,(#90305,#90306,#90307,#90308),
 .UNSPECIFIED.,.F.,.F.,(4,4),(34.4839353288417,34.5575163999847),
 .UNSPECIFIED.);
#770=B_SPLINE_CURVE_WITH_KNOTS('',3,(#90309,#90310,#90311,#90312,#90313,
#90314,#90315,#90316,#90317,#90318,#90319,#90320,#90321,#90322,#90323,#90324,
#90325,#90326,#90327,#90328,#90329,#90330,#90331,#90332,#90333,#90334,#90335,
#90336,#90337,#90338,#90339,#90340,#90341,#90342,#90343,#90344,#90345,#90346,
#90347,#90348,#90349,#90350,#90351,#90352,#90353,#90354,#90355,#90356,#90357,
#90358,#90359,#90360,#90361,#90362,#90363,#90364,#90365,#90366,#90367,#90368,
#90369,#90370,#90371,#90372,#90373,#90374,#90375,#90376,#90377,#90378,#90379,
#90380,#90381,#90382,#90383,#90384,#90385,#90386,#90387,#90388,#90389,#90390,
#90391,#90392,#90393,#90394,#90395,#90396,#90397,#90398,#90399,#90400,#90401,
#90402,#90403,#90404,#90405,#90406,#90407,#90408,#90409,#90410,#90411,#90412,
#90413,#90414,#90415,#90416,#90417,#90418,#90419,#90420,#90421,#90422,#90423,
#90424,#90425,#90426,#90427,#90428,#90429,#90430,#90431,#90432,#90433,#90434,
#90435,#90436,#90437,#90438,#90439,#90440,#90441,#90442,#90443,#90444,#90445,
#90446,#90447,#90448,#90449,#90450,#90451,#90452,#90453,#90454,#90455,#90456,
#90457,#90458,#90459,#90460,#90461,#90462,#90463,#90464,#90465,#90466,#90467,
#90468,#90469,#90470,#90471,#90472,#90473,#90474,#90475,#90476,#90477,#90478,
#90479,#90480,#90481,#90482,#90483,#90484,#90485,#90486,#90487,#90488,#90489,
#90490,#90491,#90492,#90493,#90494,#90495,#90496,#90497,#90498,#90499,#90500,
#90501,#90502,#90503,#90504,#90505,#90506,#90507,#90508,#90509,#90510,#90511,
#90512,#90513,#90514,#90515,#90516,#90517,#90518,#90519,#90520,#90521,#90522,
#90523,#90524),.UNSPECIFIED.,.F.,.F.,(4,2,2,2,2,2,2,2,2,2,2,2,2,2,2,2,2,
2,2,2,2,2,2,2,2,2,2,2,2,2,2,2,2,2,2,2,2,2,2,2,2,2,2,2,2,2,2,2,2,2,2,2,2,
2,2,2,2,2,2,2,2,2,2,2,2,2,2,2,2,2,2,2,2,2,2,2,2,2,2,2,2,2,2,2,2,2,2,2,2,
2,2,2,2,2,2,2,2,2,2,2,2,2,2,2,2,2,2,4),(-2.98932851488204,-2.98778835877455,
-2.98589440660087,-2.98439686001854,-2.98288940256014,-2.98026659780242,
-2.97269261178509,-2.92782104182352,-2.89563002419035,-2.87525617600293,
-2.87005949080672,-2.86694440682519,-2.86415265864336,-2.86060023505363,
-2.85494392054553,-2.80673551748508,-2.78518678448732,-2.75509075281792,
-2.75192043656174,-2.74992348108331,-2.74808722290459,-2.74655885834968,
-2.74463977046219,-2.74107596409357,-2.72071738393961,-2.67605240524974,
-2.64274404418098,-2.63463169078566,-2.63092348463791,-2.62811141703,-2.62507404972935,
-2.62023106865622,-2.60541488658953,-2.54284167972397,-2.52472911455355,
-2.51807754648573,-2.51327703918794,-2.51115710299689,-2.50958168586097,
-2.50782882661511,-2.50485046276057,-2.49426806185102,-2.42004704528794,
-2.40032273478815,-2.39517884838337,-2.3920754931402,-2.38928159844871,
-2.38570898279933,-2.37998507469446,-2.3366737105664,-2.30726025807467,
-2.2814023789362,-2.27607276993591,-2.273861822143,-2.27227219030427,-2.27055975911447,
-2.26776271370155,-2.25882483558985,-2.21013823319637,-2.16562853116848,
-2.15898081424815,-2.15555632788938,-2.15277624815042,-2.14957737625101,
-2.14414070234367,-2.12271077631613,-2.06600733106761,-2.04352541983092,
-2.03855563409326,-2.03640597754623,-2.03482632255464,-2.03308800308641,
-2.03017453908286,-2.02020927187821,-1.94569132525569,-1.92559604926915,
-1.92042237079454,-1.9173127347055,-1.91452059446957,-1.91096042740721,
-1.90527714587453,-1.8584728900673,-1.82457079751584,-1.80378100627075,
-1.80031222002498,-1.79845298352699,-1.79689477356601,-1.79494107725788,
-1.79113990096616,-1.76383992326005,-1.75466129094146,-1.7103790584558,
-1.68855634712395,-1.68325002215229,-1.68011120206541,-1.67732415884313,
-1.67381276485327,-1.66829122751587,-1.63556664395172,-1.58908035005274,
-1.56659251959106,-1.56306275472084,-1.56119056593201,-1.55963291817536,
-1.55769418818297,-1.55467093822223,-1.53951992506579,-1.5128189813854),
 .UNSPECIFIED.);
#771=B_SPLINE_CURVE_WITH_KNOTS('',3,(#90530,#90531,#90532,#90533,#90534,
#90535,#90536,#90537,#90538,#90539,#90540,#90541,#90542,#90543,#90544,#90545,
#90546,#90547,#90548,#90549,#90550,#90551,#90552,#90553,#90554,#90555,#90556,
#90557,#90558,#90559,#90560,#90561,#90562,#90563,#90564,#90565,#90566,#90567,
#90568,#90569,#90570,#90571,#90572,#90573,#90574,#90575,#90576,#90577,#90578,
#90579,#90580,#90581,#90582,#90583,#90584,#90585,#90586,#90587,#90588,#90589,
#90590,#90591,#90592,#90593,#90594,#90595,#90596,#90597,#90598,#90599,#90600,
#90601,#90602,#90603,#90604,#90605,#90606,#90607,#90608,#90609,#90610,#90611,
#90612,#90613,#90614,#90615,#90616,#90617,#90618,#90619,#90620,#90621,#90622,
#90623,#90624,#90625,#90626,#90627,#90628,#90629,#90630,#90631,#90632,#90633,
#90634,#90635,#90636,#90637,#90638,#90639,#90640,#90641,#90642,#90643,#90644,
#90645,#90646,#90647,#90648,#90649,#90650,#90651,#90652,#90653,#90654,#90655,
#90656,#90657,#90658,#90659,#90660,#90661,#90662,#90663,#90664,#90665,#90666,
#90667,#90668,#90669,#90670,#90671,#90672,#90673,#90674,#90675,#90676,#90677,
#90678,#90679,#90680,#90681,#90682,#90683,#90684,#90685,#90686,#90687,#90688,
#90689,#90690,#90691,#90692,#90693,#90694,#90695,#90696,#90697,#90698,#90699,
#90700,#90701,#90702,#90703,#90704,#90705,#90706,#90707,#90708,#90709,#90710,
#90711,#90712,#90713,#90714,#90715,#90716),.UNSPECIFIED.,.F.,.F.,(4,3,3,
3,3,3,3,3,3,3,3,3,3,3,3,3,3,3,3,3,3,3,3,3,3,3,3,3,3,3,3,3,3,3,3,3,3,3,3,
3,3,3,3,3,3,3,3,3,3,3,3,3,3,3,3,3,3,3,3,3,3,3,4),(40.8407044966673,40.949576446156,
41.0587417112112,41.16837803931,41.2680660342038,41.3685653530978,41.4689192022502,
41.5691560072746,41.6693287783783,41.7694687756258,41.8696072180232,41.9698456501707,
42.0701320477337,42.1706016493045,42.2668717457736,42.3673710646681,42.467724913821,
42.5679617188459,42.6681344899501,42.768274487198,42.8684129295959,42.9686513617439,
43.0689377593074,43.1694073608787,43.2656774573433,43.3661767762382,43.4665306253915,
43.5667674304169,43.6669402015215,43.7670801987699,43.8672186411682,43.9674570733167,
44.0677434708806,44.1682130724524,44.2644831689131,44.3649824878077,44.4653363369606,
44.5655731419856,44.6657459130898,44.7658859103379,44.8660243527359,44.9662627848839,
45.0665491824475,45.1670187840189,45.2632888804829,45.3637881993776,45.4641420485306,
45.5643788535557,45.66455162466,45.7646916219081,45.8648300643062,45.9650684964543,
46.065354894018,46.1658244955894,46.2620945920527,46.3611093540537,46.4599956905364,
46.5587866981655,46.657515345266,46.7562542414466,46.8549915856982,46.9538361689612,
47.049949307842),.UNSPECIFIED.);
#772=B_SPLINE_CURVE_WITH_KNOTS('',3,(#90717,#90718,#90719,#90720),
 .UNSPECIFIED.,.F.,.F.,(4,4),(40.7676704970196,40.8407044966673),
 .UNSPECIFIED.);
#773=B_SPLINE_CURVE_WITH_KNOTS('',3,(#90721,#90722,#90723,#90724,#90725,
#90726,#90727,#90728,#90729,#90730,#90731,#90732,#90733,#90734,#90735,#90736,
#90737,#90738,#90739,#90740,#90741,#90742,#90743,#90744,#90745,#90746,#90747,
#90748,#90749,#90750,#90751,#90752,#90753,#90754,#90755,#90756,#90757,#90758,
#90759,#90760,#90761,#90762,#90763,#90764,#90765,#90766,#90767,#90768,#90769,
#90770,#90771,#90772,#90773,#90774,#90775,#90776,#90777,#90778,#90779,#90780,
#90781,#90782,#90783,#90784,#90785,#90786,#90787,#90788,#90789,#90790,#90791,
#90792,#90793,#90794,#90795,#90796,#90797,#90798,#90799,#90800,#90801,#90802,
#90803,#90804,#90805,#90806,#90807,#90808,#90809,#90810,#90811,#90812,#90813,
#90814,#90815,#90816,#90817,#90818,#90819,#90820,#90821,#90822,#90823,#90824,
#90825,#90826,#90827,#90828,#90829,#90830,#90831,#90832,#90833,#90834,#90835,
#90836,#90837,#90838,#90839,#90840,#90841,#90842,#90843,#90844,#90845,#90846,
#90847,#90848,#90849,#90850,#90851,#90852,#90853,#90854,#90855,#90856,#90857,
#90858,#90859,#90860,#90861,#90862,#90863,#90864,#90865,#90866,#90867,#90868,
#90869,#90870,#90871,#90872,#90873,#90874,#90875,#90876,#90877,#90878,#90879,
#90880,#90881,#90882,#90883,#90884,#90885,#90886,#90887,#90888,#90889,#90890,
#90891,#90892,#90893,#90894,#90895,#90896,#90897,#90898,#90899,#90900,#90901,
#90902,#90903,#90904,#90905,#90906,#90907,#90908,#90909,#90910,#90911,#90912,
#90913,#90914,#90915,#90916,#90917,#90918,#90919,#90920,#90921,#90922,#90923,
#90924,#90925,#90926,#90927,#90928),.UNSPECIFIED.,.F.,.F.,(4,2,2,2,2,2,
2,2,2,2,2,2,2,2,2,2,2,2,2,2,2,2,2,2,2,2,2,2,2,2,2,2,2,2,2,2,2,2,2,2,2,2,
2,2,2,2,2,2,2,2,2,2,2,2,2,2,2,2,2,2,2,2,2,2,2,2,2,2,2,2,2,2,2,2,2,2,2,2,
2,2,2,2,2,2,2,2,2,2,2,2,2,2,2,2,2,2,2,2,2,2,2,2,2,4),(-1.5128189813854,
-1.49567083096832,-1.45307413227607,-1.44736432644523,-1.44379610752678,
-1.44100295746722,-1.43789765896982,-1.4327440554255,-1.41289821672349,
-1.33701941613466,-1.32788697449916,-1.32506672451318,-1.32334898447117,
-1.32176130779641,-1.31956287674903,-1.31430923522431,-1.28919559950112,
-1.24582570152713,-1.21514795299362,-1.20969473844147,-1.20620360258639,
-1.20341783775063,-1.20026467307552,-1.1948952554176,-1.17220056504091,
-1.1214208005053,-1.09233947219059,-1.08852903105112,-1.08657300928951,
-1.08501424812754,-1.08315589273124,-1.07969285460531,-1.05906965598642,
-1.02506056964473,-0.978207308870275,-0.972523453866462,-0.968962528771095,
-0.966169568558434,-0.963058785891341,-0.957882655229978,-0.937771449854287,
-0.864372594763722,-0.853422151304499,-0.850406491738569,-0.848645133083884,
-0.847071573671554,-0.84496709524445,-0.840254188388205,-0.796780174036855,
-0.744562915832417,-0.735925584321552,-0.732409061490226,-0.729800621453063,
-0.726950120965683,-0.723013448462171,-0.713590663040318,-0.700386264481193,
-0.622310256163776,-0.620474876710382,-0.614551381160995,-0.612176246324312,
-0.610716105446037,-0.609090785945978,-0.606696709856131,-0.600184952828215,
-0.560759598242131,-0.506859750039304,-0.498295110963134,-0.494790644250799,
-0.492184786597833,-0.489330885443234,-0.485378038386267,-0.475860154232796,
-0.462481936633166,-0.423841273510261,-0.382746826914453,-0.376997583257265,
-0.37465152618693,-0.373052024613091,-0.371386839631552,-0.368806489078964,
-0.360876691787964,-0.347834542404448,-0.281506227765355,-0.263572463419871,
-0.258382386911189,-0.255267911273333,-0.252530368026711,-0.249119868729723,
-0.245370897789706,-0.239294959532918,-0.227122340723278,-0.170103188138698,
-0.142247401274889,-0.138453019450219,-0.136500016020774,-0.134940853933661,
-0.133078683496536,-0.129599649296975,-0.1085837118209,-0.0399478565732092,
-0.025297919610965,-0.0204812965032507,-0.0181663831353254),
 .UNSPECIFIED.);
#774=B_SPLINE_CURVE_WITH_KNOTS('',3,(#90934,#90935,#90936,#90937,#90938,
#90939,#90940,#90941,#90942,#90943,#90944,#90945,#90946,#90947,#90948,#90949,
#90950,#90951,#90952,#90953,#90954,#90955,#90956,#90957,#90958,#90959,#90960,
#90961,#90962,#90963,#90964,#90965,#90966,#90967,#90968,#90969,#90970,#90971,
#90972,#90973,#90974,#90975,#90976,#90977,#90978,#90979,#90980,#90981,#90982,
#90983,#90984,#90985,#90986,#90987,#90988,#90989,#90990,#90991,#90992,#90993,
#90994,#90995,#90996,#90997,#90998,#90999,#91000,#91001,#91002,#91003,#91004,
#91005,#91006,#91007,#91008,#91009,#91010,#91011,#91012,#91013,#91014,#91015,
#91016,#91017,#91018,#91019,#91020,#91021,#91022,#91023,#91024,#91025,#91026,
#91027,#91028,#91029,#91030,#91031,#91032,#91033,#91034,#91035,#91036,#91037,
#91038,#91039,#91040,#91041,#91042,#91043,#91044,#91045,#91046,#91047,#91048,
#91049,#91050,#91051,#91052,#91053,#91054,#91055,#91056,#91057,#91058,#91059,
#91060,#91061,#91062,#91063,#91064,#91065,#91066,#91067,#91068,#91069,#91070,
#91071,#91072,#91073,#91074,#91075,#91076,#91077,#91078,#91079,#91080,#91081,
#91082,#91083,#91084,#91085,#91086,#91087,#91088,#91089,#91090,#91091,#91092,
#91093,#91094,#91095,#91096,#91097,#91098,#91099,#91100,#91101,#91102,#91103,
#91104,#91105,#91106,#91107,#91108,#91109,#91110,#91111,#91112,#91113,#91114,
#91115,#91116,#91117,#91118,#91119,#91120,#91121,#91122,#91123,#91124,#91125,
#91126,#91127,#91128,#91129,#91130,#91131,#91132,#91133,#91134,#91135,#91136,
#91137,#91138,#91139,#91140,#91141,#91142,#91143,#91144,#91145,#91146,#91147,
#91148,#91149,#91150,#91151,#91152,#91153,#91154,#91155,#91156,#91157,#91158,
#91159,#91160,#91161,#91162,#91163,#91164,#91165,#91166,#91167,#91168,#91169,
#91170,#91171,#91172,#91173,#91174,#91175,#91176,#91177,#91178,#91179,#91180,
#91181,#91182,#91183,#91184,#91185,#91186,#91187,#91188,#91189,#91190,#91191,
#91192,#91193,#91194,#91195,#91196,#91197,#91198,#91199,#91200,#91201,#91202,
#91203,#91204,#91205,#91206,#91207,#91208,#91209),.UNSPECIFIED.,.F.,.F.,
(4,2,2,2,2,2,2,2,2,2,2,2,2,2,2,2,2,2,2,2,2,2,2,2,2,2,2,2,2,2,2,2,2,2,2,
2,2,2,2,2,2,2,2,2,2,2,2,2,2,2,2,2,2,2,2,2,2,2,2,2,2,2,2,2,2,2,2,2,2,2,2,
2,2,2,2,2,2,2,2,2,2,2,2,2,2,2,2,2,2,2,2,2,2,2,2,2,2,2,2,2,2,2,2,2,2,2,2,
2,2,2,2,2,2,2,2,2,2,2,2,2,2,2,2,2,2,2,2,2,2,2,2,2,2,2,2,2,2,4),(-1.47769960275031,
-1.46520500159341,-1.46142137727949,-1.45948680831023,-1.45794960835698,
-1.45612391342727,-1.45274156019952,-1.4332930110912,-1.36591535240939,
-1.34874335194779,-1.34367663044156,-1.34061753337441,-1.33786243728151,
-1.33433847772105,-1.32704615043421,-1.31752105852131,-1.2940883761119,
-1.25441289907634,-1.24754491635115,-1.24111876512238,-1.2267007419593,
-1.22346408585819,-1.22165017544255,-1.22011224317267,-1.21816318023877,
-1.21418115139273,-1.17604671336282,-1.11648193926087,-1.10820249131097,
-1.10453502196883,-1.10175070383545,-1.09878704986067,-1.09415477188927,
-1.07932624361566,-1.05463844854815,-1.00914539150954,-0.989641672915569,
-0.986425397616695,-0.984442242198698,-0.982901697782013,-0.981112668817764,
-0.977899804998459,-0.961950601712537,-0.923800013111866,-0.875784311267044,
-0.870160873977159,-0.866643949024871,-0.863889828178817,-0.860827159537057,
-0.855743609812093,-0.836199808712195,-0.764026914480133,-0.751301368299504,
-0.748189306226988,-0.746403686550737,-0.744877047662869,-0.74289620513113,
-0.738752740054192,-0.70282407275373,-0.64089710965624,-0.633676407434816,
-0.630098858432703,-0.62749942820228,-0.624710463881338,-0.620951288372684,
-0.612381976041064,-0.600670317028426,-0.543274804524316,-0.514798191759316,
-0.511029197321451,-0.509097732002018,-0.507560670049986,-0.505732384282472,
-0.502337987520761,-0.482599900480575,-0.411100059020389,-0.397509597104142,
-0.39286025354986,-0.38989278275308,-0.38710986771861,-0.383387097114636,
-0.375023329403023,-0.339257224828324,-0.301153845763967,-0.291800206477809,
-0.276398616065952,-0.273387877947604,-0.271466793144273,-0.26993041987305,
-0.269924612150525,-0.269918890519476,-0.269913253570044,-0.269907699920863,
-0.269902228210771,-0.269896837100948,-0.269891525257584,-0.269886291415292,
-0.269881134297622,-0.269876052649428,-0.269870930532896,-0.269865824595588,
-0.269860734729688,-0.269855660845424,-0.269850602840557,-0.269845560625204,
-0.269840534111527,-0.269835523201754,-0.26983052780726,-0.269825547838814,
-0.2698205832146,-0.269815633823564,-0.269810699572557,-0.269805780380058,
-0.269800876165509,-0.269795986828172,-0.267935510432697,-0.264359503994271,
-0.25972102959401,-0.24900911340479,-0.208157785964817,-0.200942191983474,
-0.162927737791891,-0.157310175041958,-0.153794902006492,-0.151040825263961,
-0.14797691847449,-0.142888287428457,-0.123285334514095,-0.0751874841014997,
-0.0593794010607326,-0.0393101460320602,-0.0360714697423875,-0.0340815723064463,
-0.0325403404573989,-0.0310885058504802,-0.0293215905673413,-0.0266877338920759,
-0.000704083095801744),.UNSPECIFIED.);
#775=B_SPLINE_CURVE_WITH_KNOTS('',3,(#91210,#91211,#91212,#91213),
 .UNSPECIFIED.,.F.,.F.,(4,4),(47.049949307842,47.1238898036008),
 .UNSPECIFIED.);
#776=B_SPLINE_CURVE_WITH_KNOTS('',3,(#91215,#91216,#91217,#91218,#91219,
#91220,#91221,#91222,#91223,#91224,#91225,#91226),.UNSPECIFIED.,.F.,.F.,
(4,2,2,2,2,4),(-0.0181663831353254,-0.017448962707184,-0.0147685891677303,
-0.0120368289253415,-0.00702288019292292,-0.000702852059331679),
 .UNSPECIFIED.);
#777=B_SPLINE_CURVE_WITH_KNOTS('',3,(#91227,#91228,#91229,#91230,#91231,
#91232,#91233,#91234,#91235,#91236,#91237,#91238,#91239,#91240,#91241,#91242,
#91243,#91244,#91245,#91246,#91247,#91248,#91249,#91250,#91251,#91252,#91253,
#91254,#91255,#91256,#91257,#91258,#91259,#91260,#91261,#91262,#91263,#91264,
#91265,#91266,#91267,#91268,#91269,#91270,#91271,#91272,#91273,#91274,#91275,
#91276,#91277,#91278,#91279,#91280,#91281,#91282,#91283,#91284,#91285,#91286,
#91287,#91288,#91289,#91290,#91291,#91292,#91293,#91294,#91295,#91296,#91297,
#91298,#91299,#91300,#91301,#91302,#91303,#91304,#91305,#91306,#91307,#91308,
#91309,#91310,#91311,#91312,#91313,#91314,#91315,#91316,#91317,#91318,#91319,
#91320,#91321,#91322,#91323,#91324,#91325,#91326,#91327,#91328,#91329,#91330,
#91331,#91332,#91333,#91334,#91335,#91336,#91337,#91338,#91339,#91340,#91341,
#91342,#91343,#91344,#91345,#91346,#91347,#91348,#91349,#91350,#91351,#91352,
#91353,#91354,#91355,#91356,#91357,#91358,#91359,#91360,#91361,#91362,#91363,
#91364,#91365,#91366,#91367,#91368,#91369,#91370,#91371,#91372,#91373,#91374,
#91375,#91376,#91377,#91378,#91379,#91380,#91381,#91382,#91383,#91384,#91385,
#91386,#91387,#91388,#91389,#91390,#91391,#91392,#91393,#91394,#91395,#91396,
#91397,#91398,#91399,#91400,#91401,#91402,#91403,#91404,#91405,#91406,#91407,
#91408,#91409,#91410,#91411,#91412,#91413,#91414,#91415,#91416,#91417,#91418,
#91419,#91420,#91421,#91422,#91423,#91424,#91425,#91426,#91427,#91428,#91429,
#91430,#91431,#91432,#91433,#91434,#91435,#91436,#91437,#91438,#91439,#91440,
#91441,#91442,#91443,#91444,#91445,#91446,#91447,#91448,#91449,#91450,#91451,
#91452,#91453,#91454,#91455,#91456,#91457,#91458),.UNSPECIFIED.,.F.,.F.,
(4,2,2,2,2,2,2,2,2,2,2,2,2,2,2,2,2,2,2,2,2,2,2,2,2,2,2,2,2,2,2,2,2,2,2,
2,2,2,2,2,2,2,2,2,2,2,2,2,2,2,2,2,2,2,2,2,2,2,2,2,2,2,2,2,2,2,2,2,2,2,2,
2,2,2,2,2,2,2,2,2,2,2,2,2,2,2,2,2,2,2,2,2,2,2,2,2,2,2,2,2,2,2,2,2,2,2,2,
2,2,2,2,2,2,2,2,4),(-2.98920213316816,-2.91355244760858,-2.89256055197457,
-2.88908328851811,-2.88722191595717,-2.88566332840344,-2.88371093550557,
-2.87991742760162,-2.85201164884243,-2.79494528879838,-2.78287689151404,
-2.7768380820173,-2.77310477523359,-2.76969853623019,-2.7696512060653,-2.76960253933043,
-2.76955243875846,-2.7695007984547,-2.76944750285888,-2.76939242557052,
-2.76933542797915,-2.76927635769579,-2.76921504673341,-2.769151309392,-2.76911156297201,
-2.76906336463706,-2.76900459466037,-2.76893244416893,-2.76884310754945,
-2.76837809301476,-2.76563282238037,-2.76197012537908,-2.75388912669262,
-2.69233794823319,-2.65626527350994,-2.65208028375244,-2.6500749403872,
-2.6485127827839,-2.64669195604716,-2.64349185354238,-2.62996962525229,
-2.61661270449268,-2.55974451385223,-2.539576440405,-2.53439580388652,-2.53128403103742,
-2.5284912653393,-2.52493207766387,-2.51925395137538,-2.47234923391076,
-2.43822699481459,-2.41769586878694,-2.41423626310104,-2.41237863238761,
-2.41081981419016,-2.40886289163437,-2.40504828847699,-2.37562615832027,
-2.33099119488012,-2.31256918888605,-2.30445092556886,-2.29800714996462,
-2.29462413902028,-2.2921146254149,-2.28897782975844,-2.28368350035004,
-2.26466322980464,-2.20645409360217,-2.18283200059918,-2.17773645042245,
-2.17556470967348,-2.17398128192594,-2.17225211407082,-2.16938104854387,
-2.15980583077156,-2.08445323571059,-2.06464477732774,-2.05949361222313,
-2.05638845953858,-2.0535945966867,-2.0500243021211,-2.04430875089033,-2.00051510395259,
-1.9741853308782,-1.94601888246039,-1.94046026157136,-1.93821165745488,
-1.93661525445993,-1.935124746125,-1.9325880315953,-1.92562937001219,-1.84720915285884,
-1.8272084820429,-1.82204226805781,-1.81893416595458,-1.81614153235007,
-1.8125781609117,-1.80688454806761,-1.76065567559184,-1.72778263756613,
-1.70549511554985,-1.70197207976544,-1.70010129424701,-1.69854356529405,
-1.69660317414098,-1.69286413337185,-1.66826508452444,-1.62623090197975,
-1.59449671209507,-1.58658218442793,-1.58291072773492,-1.5801042526633,
-1.5770511491648,-1.57213522940316,-1.55670372546374,-1.51236511191743),
 .UNSPECIFIED.);
#778=B_SPLINE_CURVE_WITH_KNOTS('',3,(#91463,#91464,#91465,#91466,#91467,
#91468,#91469,#91470,#91471,#91472,#91473,#91474,#91475,#91476,#91477,#91478,
#91479,#91480,#91481,#91482,#91483,#91484,#91485,#91486,#91487,#91488,#91489,
#91490,#91491,#91492,#91493,#91494,#91495,#91496,#91497,#91498,#91499,#91500,
#91501,#91502,#91503,#91504,#91505,#91506,#91507,#91508,#91509,#91510,#91511,
#91512,#91513,#91514,#91515,#91516,#91517,#91518,#91519,#91520,#91521,#91522,
#91523,#91524,#91525,#91526,#91527,#91528,#91529,#91530,#91531,#91532,#91533,
#91534,#91535,#91536,#91537,#91538,#91539,#91540,#91541,#91542,#91543,#91544,
#91545,#91546,#91547,#91548,#91549,#91550,#91551,#91552,#91553,#91554,#91555,
#91556,#91557,#91558,#91559,#91560,#91561,#91562,#91563,#91564,#91565,#91566,
#91567,#91568,#91569,#91570,#91571,#91572,#91573,#91574,#91575,#91576,#91577,
#91578,#91579,#91580,#91581,#91582,#91583,#91584,#91585,#91586,#91587,#91588,
#91589,#91590,#91591,#91592,#91593,#91594,#91595,#91596,#91597,#91598,#91599,
#91600,#91601,#91602,#91603,#91604,#91605,#91606,#91607,#91608,#91609,#91610,
#91611,#91612,#91613,#91614,#91615,#91616,#91617,#91618,#91619,#91620,#91621,
#91622,#91623,#91624,#91625,#91626,#91627,#91628,#91629,#91630,#91631,#91632,
#91633,#91634,#91635,#91636,#91637,#91638,#91639,#91640,#91641,#91642,#91643,
#91644,#91645,#91646,#91647,#91648,#91649,#91650,#91651,#91652,#91653,#91654,
#91655,#91656,#91657,#91658,#91659,#91660,#91661,#91662,#91663,#91664,#91665,
#91666,#91667,#91668,#91669,#91670,#91671,#91672,#91673,#91674,#91675,#91676,
#91677,#91678,#91679,#91680,#91681,#91682,#91683,#91684,#91685,#91686,#91687,
#91688,#91689,#91690,#91691,#91692,#91693,#91694),.UNSPECIFIED.,.F.,.F.,
(4,2,2,2,2,2,2,2,2,2,2,2,2,2,2,2,2,2,2,2,2,2,2,2,2,2,2,2,2,2,2,2,2,2,2,
2,2,2,2,2,2,2,2,2,2,2,2,2,2,2,2,2,2,2,2,2,2,2,2,2,2,2,2,2,2,2,2,2,2,2,2,
2,2,2,2,2,2,2,2,2,2,2,2,2,2,2,2,2,2,2,2,2,2,2,2,2,2,2,2,2,2,2,2,2,2,2,2,
2,2,2,2,2,2,2,2,4),(-2.97246426759675,-2.94428574081794,-2.90996217957583,
-2.89016588973709,-2.88676899223866,-2.88494017514404,-2.88340314350309,
-2.8814723279444,-2.87770638484499,-2.84933895332952,-2.79212018654989,
-2.78027704843224,-2.77433950402829,-2.77066477541974,-2.7673103358639,
-2.76726337758087,-2.76721516593046,-2.76716560507966,-2.76711459057286,
-2.76706200825653,-2.767007733038,-2.76695162745497,-2.76689354001511,-2.76683330325438,
-2.76677073146232,-2.76673287228551,-2.76668710395592,-2.76663145067519,
-2.76656328640843,-2.76647903738856,-2.76380019796265,-2.76039106209135,
-2.75512389358505,-2.72781730867969,-2.66551997818784,-2.65647705482015,
-2.65042914807023,-2.64812309915009,-2.64653180714845,-2.64508307526343,
-2.64269159855483,-2.63655176890577,-2.55688483291798,-2.54364427703872,
-2.53422607934513,-2.53032334491243,-2.52750943466185,-2.52494297112302,
-2.52084390286609,-2.51315850818247,-2.45634544574622,-2.41565445024759,
-2.41175123235641,-2.4098177719378,-2.40842839237369,-2.40666147352304,
-2.4036305038161,-2.39185556380835,-2.31871669633103,-2.29909538488013,
-2.29400551909441,-2.29094145532281,-2.28818760734047,-2.28467313648524,
-2.27905783472003,-2.23081981948986,-2.20927589691354,-2.18050600425978,
-2.17491956195657,-2.17268517008435,-2.17110793180426,-2.16964360965937,
-2.16758246032872,-2.16206446171813,-2.11539806428787,-2.06401557545253,
-2.05752568542414,-2.05416201200345,-2.05142167411376,-2.04825821985294,
-2.04285785152711,-2.02134372432541,-1.95861752724636,-1.93956075356723,
-1.93619522147561,-1.93437323782737,-1.93283594686783,-1.93089719571369,
-1.92709341352371,-1.89311012534219,-1.84427006320665,-1.82406944758419,
-1.81893269899672,-1.81585822411878,-1.81310623374272,-1.80960948252501,
-1.80405335747445,-1.76860196801606,-1.70821883244269,-1.70043367452667,
-1.6978934053952,-1.69625268564684,-1.69467643079905,-1.69236591784739,
-1.68671321777781,-1.64268482863225,-1.60556522932953,-1.58633464690745,
-1.5812766338537,-1.57821925374063,-1.57546344230171,-1.57193543315433,
-1.56627604415298,-1.523915700132,-1.49489594417815,-1.47769960275031),
 .UNSPECIFIED.);
#779=B_SPLINE_CURVE_WITH_KNOTS('',3,(#91695,#91696,#91697,#91698,#91699,
#91700,#91701,#91702,#91703,#91704,#91705,#91706,#91707,#91708,#91709,#91710,
#91711,#91712,#91713,#91714,#91715,#91716,#91717,#91718,#91719,#91720,#91721,
#91722,#91723,#91724,#91725,#91726,#91727,#91728,#91729,#91730,#91731,#91732,
#91733,#91734,#91735,#91736,#91737,#91738,#91739,#91740,#91741,#91742,#91743,
#91744,#91745,#91746,#91747,#91748,#91749,#91750,#91751,#91752,#91753,#91754,
#91755,#91756,#91757,#91758,#91759,#91760,#91761,#91762,#91763,#91764,#91765,
#91766,#91767,#91768,#91769,#91770,#91771,#91772,#91773,#91774,#91775,#91776,
#91777,#91778,#91779,#91780,#91781,#91782,#91783,#91784,#91785,#91786,#91787,
#91788,#91789,#91790,#91791,#91792,#91793,#91794,#91795,#91796,#91797,#91798,
#91799,#91800,#91801,#91802,#91803,#91804,#91805,#91806,#91807,#91808,#91809,
#91810,#91811,#91812,#91813,#91814,#91815,#91816,#91817,#91818,#91819,#91820,
#91821,#91822,#91823,#91824,#91825,#91826,#91827,#91828,#91829,#91830,#91831,
#91832,#91833,#91834,#91835,#91836,#91837,#91838,#91839,#91840,#91841,#91842,
#91843,#91844,#91845,#91846,#91847,#91848,#91849,#91850,#91851,#91852,#91853,
#91854,#91855,#91856,#91857,#91858,#91859,#91860,#91861,#91862,#91863,#91864,
#91865,#91866,#91867,#91868,#91869,#91870,#91871,#91872,#91873,#91874,#91875,
#91876,#91877,#91878,#91879,#91880,#91881,#91882,#91883,#91884,#91885,#91886,
#91887,#91888,#91889,#91890,#91891,#91892,#91893,#91894,#91895,#91896,#91897,
#91898,#91899,#91900,#91901,#91902,#91903,#91904,#91905,#91906,#91907,#91908,
#91909,#91910,#91911,#91912,#91913,#91914,#91915,#91916,#91917,#91918,#91919,
#91920,#91921,#91922,#91923,#91924,#91925,#91926,#91927,#91928,#91929,#91930,
#91931,#91932,#91933,#91934,#91935,#91936,#91937,#91938,#91939,#91940,#91941,
#91942,#91943,#91944,#91945,#91946,#91947,#91948,#91949,#91950,#91951,#91952,
#91953,#91954,#91955,#91956,#91957,#91958,#91959,#91960,#91961,#91962,#91963,
#91964,#91965,#91966,#91967,#91968,#91969,#91970,#91971,#91972,#91973,#91974,
#91975,#91976),.UNSPECIFIED.,.F.,.F.,(4,2,2,2,2,2,2,2,2,2,2,2,2,2,2,2,2,
2,2,2,2,2,2,2,2,2,2,2,2,2,2,2,2,2,2,2,2,2,2,2,2,2,2,2,2,2,2,2,2,2,2,2,2,
2,2,2,2,2,2,2,2,2,2,2,2,2,2,2,2,2,2,2,2,2,2,2,2,2,2,2,2,2,2,2,2,2,2,2,2,
2,2,2,2,2,2,2,2,2,2,2,2,2,2,2,2,2,2,2,2,2,2,2,2,2,2,2,2,2,2,2,2,2,2,2,2,
2,2,2,2,2,2,2,2,2,2,2,2,2,2,2,4),(-1.51236511191743,-1.4948215896375,-1.49400362409459,
-1.4686262163764,-1.46486013725749,-1.46291377811845,-1.46135563468478,
-1.45948956840321,-1.45598953126205,-1.43436545784749,-1.40129123349152,
-1.35458738447322,-1.34890085264416,-1.34533935037137,-1.34254661797046,
-1.33943679163874,-1.33426391057615,-1.31418755447779,-1.23448407677383,
-1.22849661764815,-1.22611105486576,-1.22464927665935,-1.22302674714407,
-1.22064472822501,-1.21421409017876,-1.17585898450047,-1.12070349777977,
-1.11203193682353,-1.10860362801049,-1.10575787131501,-1.10284082721315,
-1.09856174584771,-1.08688270122094,-1.06930549682172,-1.03491814978669,
-0.996807934368717,-0.991010934055789,-0.98865733668245,-0.987056688094282,
-0.985394243751395,-0.982824932782483,-0.974982140855592,-0.962138488487206,
-0.89908744977156,-0.878132810000619,-0.87273123200272,-0.869539910067627,
-0.866758362868686,-0.863321748415991,-0.856617158496879,-0.810483160660005,
-0.758449072260833,-0.75330076096962,-0.75127590533753,-0.749807946169433,
-0.748192075076011,-0.74584281802364,-0.739635693809925,-0.730307904025884,
-0.698969649687284,-0.64601513080894,-0.637409505825225,-0.633898582092195,
-0.631291654220649,-0.628440227631647,-0.624497530493606,-0.615037113819034,
-0.601763357128723,-0.521701258400831,-0.515972104439006,-0.513629449386597,
-0.512030663291464,-0.510364636536567,-0.507780225697981,-0.499816170268663,
-0.4361905531141,-0.404217280394971,-0.398718201639703,-0.395212533062727,
-0.392424615825467,-0.389279062240039,-0.383947298396088,-0.361804048772071,
-0.33592991183649,-0.31582868044134,-0.281346117350063,-0.277517979809964,
-0.27555786474218,-0.273998501583353,-0.27399208436456,-0.27398575997803,
-0.273979526918604,-0.273973383679682,-0.273967328808087,-0.273961360891179,
-0.273955478513309,-0.27394968030636,-0.273943964918542,-0.273938331010769,
-0.273932777292616,-0.273927302477765,-0.273921905325855,-0.273916584600358,
-0.273911339076235,-0.273906167581931,-0.273901068930202,-0.273895873494243,
-0.273890693693645,-0.273885529409582,-0.273880380549952,-0.273875247030761,
-0.273870128752458,-0.273865025622705,-0.273859937564269,-0.273854864488639,
-0.273849806291677,-0.273844762893142,-0.273839734196123,-0.273834720113091,
-0.271942052655923,-0.26829690104547,-0.263555419882261,-0.216788032005356,
-0.171194387149065,-0.162436099933595,-0.158898774665211,-0.156285051731337,
-0.153438617003792,-0.14952552885499,-0.140245801416345,-0.115016960827674,
-0.0927781658392886,-0.0691895211035217,-0.0438288195000823,-0.0400623809339067,
-0.0381155615756425,-0.0365569009571547,-0.0350712717188883,-0.033225308262869,
-0.0304226243911011,-0.0178739340765507),.UNSPECIFIED.);
#780=B_SPLINE_CURVE_WITH_KNOTS('',3,(#91982,#91983,#91984,#91985,#91986,
#91987,#91988,#91989,#91990,#91991,#91992,#91993,#91994,#91995,#91996,#91997,
#91998,#91999,#92000,#92001,#92002,#92003,#92004,#92005,#92006,#92007,#92008,
#92009,#92010,#92011,#92012,#92013,#92014,#92015,#92016,#92017,#92018,#92019,
#92020,#92021,#92022,#92023,#92024,#92025,#92026,#92027,#92028,#92029,#92030,
#92031,#92032,#92033,#92034,#92035,#92036,#92037,#92038,#92039,#92040,#92041,
#92042,#92043,#92044,#92045,#92046,#92047,#92048,#92049,#92050,#92051,#92052,
#92053,#92054,#92055,#92056,#92057,#92058,#92059,#92060,#92061,#92062,#92063,
#92064,#92065,#92066,#92067,#92068,#92069,#92070,#92071,#92072,#92073,#92074,
#92075,#92076,#92077,#92078,#92079,#92080,#92081,#92082,#92083,#92084,#92085,
#92086,#92087,#92088,#92089,#92090,#92091,#92092,#92093,#92094,#92095,#92096,
#92097,#92098,#92099,#92100,#92101,#92102,#92103,#92104,#92105,#92106,#92107,
#92108,#92109,#92110,#92111,#92112,#92113,#92114,#92115,#92116,#92117,#92118,
#92119,#92120,#92121,#92122,#92123,#92124,#92125,#92126,#92127,#92128,#92129,
#92130,#92131,#92132,#92133,#92134,#92135,#92136,#92137,#92138,#92139,#92140,
#92141,#92142,#92143,#92144,#92145,#92146,#92147,#92148,#92149,#92150,#92151,
#92152,#92153,#92154,#92155,#92156,#92157,#92158,#92159,#92160,#92161,#92162,
#92163,#92164,#92165,#92166,#92167,#92168,#92169,#92170,#92171,#92172,#92173,
#92174,#92175,#92176,#92177,#92178,#92179,#92180,#92181,#92182,#92183,#92184,
#92185,#92186,#92187,#92188,#92189,#92190,#92191,#92192,#92193),
 .UNSPECIFIED.,.F.,.F.,(4,2,2,2,2,2,2,2,2,2,2,2,2,2,2,2,2,2,2,2,2,2,2,2,
2,2,2,2,2,2,2,2,2,2,2,2,2,2,2,2,2,2,2,2,2,2,2,2,2,2,2,2,2,2,2,2,2,2,2,2,
2,2,2,2,2,2,2,2,2,2,2,2,2,2,2,2,2,2,2,2,2,2,2,2,2,2,2,2,2,2,2,2,2,2,2,2,
2,2,2,2,2,2,2,2,2,4),(-1.47839118834467,-1.45095636912055,-1.44537329893961,
-1.44186857293672,-1.43911591034736,-1.43604649321691,-1.43093197654453,
-1.41100670082467,-1.33366421286716,-1.32560904346143,-1.32294356624872,
-1.32127520149056,-1.31969779651749,-1.31746385772411,-1.31188202252239,
-1.28317035018332,-1.26091841659239,-1.21338190405584,-1.20775267528002,
-1.20423360579058,-1.20147871739787,-1.19841613345648,-1.19333492704895,
-1.1738288454657,-1.10212440440244,-1.08892818122723,-1.08578077306755,
-1.08398682614121,-1.08244622254558,-1.0804684196035,-1.07634192919891,
-1.0410724444422,-0.978275102116205,-0.970361939853126,-0.966759401066234,
-0.963984821375909,-0.960992756106465,-0.956233341792901,-0.94022274305942,
-0.91255406991436,-0.873157454503169,-0.86906858727658,-0.851757904462305,
-0.848645297781779,-0.846692997117287,-0.845154475220216,-0.843342156957157,
-0.840023079864386,-0.822009788578399,-0.768673086976097,-0.737666115300506,
-0.732247079219614,-0.728791353776895,-0.726042973695466,-0.722942237806137,
-0.717688134252357,-0.695951476298799,-0.645206635634953,-0.614781252007789,
-0.610988811120715,-0.609052174384358,-0.607514622819395,-0.605690034427372,
-0.602313718855116,-0.58301847102543,-0.517581385307539,-0.498629697051033,
-0.49338592555714,-0.490287559847187,-0.487813871032943,-0.484486115670155,
-0.478172868897464,-0.423656670184969,-0.379935623237664,-0.374276825182988,
-0.37196509667068,-0.370388446901074,-0.368747734352966,-0.36620821980778,
-0.358431011873107,-0.298060309273393,-0.262608566949414,-0.257056554254677,
-0.253560672557908,-0.250883899562267,-0.247899377736921,-0.244772291537913,
-0.240157891697143,-0.231878246545897,-0.212829614210536,-0.170270027584861,
-0.139504304325582,-0.135708801052885,-0.13377159913348,-0.132234126686058,
-0.130410254847438,-0.12703689157107,-0.107806403759334,-0.0350839837826959,
-0.0220026728155107,-0.0174283316283289,-0.0144770441191171,-0.011853202522377,
-0.00913930033583054,-0.0051879348728483,-0.000704354964600651),
 .UNSPECIFIED.);
#781=B_SPLINE_CURVE_WITH_KNOTS('',3,(#92194,#92195,#92196,#92197),
 .UNSPECIFIED.,.F.,.F.,(4,4),(-2.98975612156922,-2.97246426759675),
 .UNSPECIFIED.);
#782=B_SPLINE_CURVE_WITH_KNOTS('',3,(#92199,#92200,#92201,#92202),
 .UNSPECIFIED.,.F.,.F.,(4,4),(-0.0178739340765507,-0.000702727300234043),
 .UNSPECIFIED.);
#783=B_SPLINE_CURVE_WITH_KNOTS('',3,(#92203,#92204,#92205,#92206,#92207,
#92208,#92209,#92210,#92211,#92212,#92213,#92214,#92215,#92216,#92217,#92218,
#92219,#92220,#92221,#92222,#92223,#92224,#92225,#92226,#92227,#92228,#92229,
#92230,#92231,#92232,#92233,#92234,#92235,#92236,#92237,#92238,#92239,#92240,
#92241,#92242,#92243,#92244,#92245,#92246,#92247,#92248,#92249,#92250,#92251,
#92252,#92253,#92254,#92255,#92256,#92257,#92258,#92259,#92260,#92261,#92262,
#92263,#92264,#92265,#92266,#92267,#92268,#92269,#92270,#92271,#92272,#92273,
#92274,#92275,#92276,#92277,#92278,#92279,#92280,#92281,#92282,#92283,#92284,
#92285,#92286,#92287,#92288,#92289,#92290,#92291,#92292,#92293,#92294,#92295,
#92296,#92297,#92298,#92299,#92300,#92301,#92302,#92303,#92304,#92305,#92306,
#92307,#92308,#92309,#92310,#92311,#92312,#92313,#92314,#92315,#92316,#92317,
#92318,#92319,#92320,#92321,#92322,#92323,#92324,#92325,#92326,#92327,#92328,
#92329,#92330,#92331,#92332,#92333,#92334,#92335,#92336,#92337,#92338,#92339,
#92340,#92341,#92342,#92343,#92344,#92345,#92346,#92347,#92348,#92349,#92350,
#92351,#92352,#92353,#92354,#92355,#92356,#92357,#92358,#92359,#92360,#92361,
#92362,#92363,#92364,#92365,#92366,#92367,#92368,#92369,#92370,#92371,#92372,
#92373,#92374,#92375,#92376,#92377,#92378,#92379,#92380,#92381,#92382,#92383,
#92384,#92385,#92386,#92387,#92388,#92389,#92390,#92391,#92392,#92393,#92394,
#92395,#92396,#92397,#92398,#92399,#92400,#92401,#92402,#92403,#92404,#92405,
#92406,#92407,#92408,#92409,#92410,#92411,#92412,#92413,#92414,#92415,#92416,
#92417,#92418,#92419,#92420,#92421,#92422),.UNSPECIFIED.,.F.,.F.,(4,2,2,
2,2,2,2,2,2,2,2,2,2,2,2,2,2,2,2,2,2,2,2,2,2,2,2,2,2,2,2,2,2,2,2,2,2,2,2,
2,2,2,2,2,2,2,2,2,2,2,2,2,2,2,2,2,2,2,2,2,2,2,2,2,2,2,2,2,2,2,2,2,2,2,2,
2,2,2,2,2,2,2,2,2,2,2,2,2,2,2,2,2,2,2,2,2,2,2,2,2,2,2,2,2,2,2,2,2,2,4),
(-2.99059624599852,-2.9242269223958,-2.91484635816592,-2.91091609311936,
-2.90806621662461,-2.9054555721249,-2.90193187652571,-2.89325567514184,
-2.84195233375899,-2.80933436231326,-2.7997928408015,-2.79549955961913,
-2.79217521726917,-2.79032884837834,-2.79031978580954,-2.79031065100499,
-2.79030144276184,-2.79029215985547,-2.79028280104057,-2.79027336503898,
-2.79026385053848,-2.78870416076414,-2.78674269667096,-2.78290918305818,
-2.75140408109271,-2.70262416901521,-2.68034235362197,-2.67500025006063,
-2.67185214251293,-2.6690641299345,-2.66556123485124,-2.66007212298071,
-2.62895195110776,-2.57592712444011,-2.56384755845483,-2.55878755814963,
-2.55490781320999,-2.55296243914939,-2.55155433979417,-2.54974801588207,
-2.54661335092271,-2.53395567319923,-2.46257647063955,-2.44245820461646,
-2.43728027403617,-2.43416837224634,-2.43137438113979,-2.42781210640301,
-2.42212597065061,-2.37519058377616,-2.34105416971642,-2.32054003592188,
-2.31708011969652,-2.31522201124306,-2.31366260861524,-2.31170472091216,
-2.30788756352151,-2.27187050128496,-2.23287930582103,-2.21502101546436,
-2.20320307331589,-2.1989039794478,-2.19598223686012,-2.19313874864965,
-2.18972143305987,-2.1811232000435,-2.12479050938735,-2.0838513959763,-2.07990508347753,
-2.07794634050091,-2.07653690611172,-2.07474031594477,-2.07164783240144,
-2.05948630112066,-1.98753123604281,-1.96741543148461,-1.9622378155508,
-1.95912604737941,-1.95633214113734,-1.95276992633491,-1.9470837886204,
-1.90019779637242,-1.86605451885922,-1.84550407659311,-1.84204282821988,
-1.84018447315634,-1.8386251401515,-1.8366676886051,-1.83285239514693,-1.80346600214544,
-1.75879938133016,-1.74035285224361,-1.732226303213,-1.72577686113148,-1.72239199172821,
-1.71988156547474,-1.71674423261773,-1.71145046261991,-1.69244815616754,
-1.62724459885455,-1.61426188279019,-1.60894437127265,-1.60491053696014,
-1.60293434433125,-1.60137377339904,-1.59953002350305,-1.5962311918276,
-1.58133402829854,-1.53724996492306,-1.51291820589149),.UNSPECIFIED.);
#784=B_SPLINE_CURVE_WITH_KNOTS('',3,(#92427,#92428,#92429,#92430,#92431,
#92432,#92433,#92434,#92435,#92436,#92437,#92438,#92439,#92440,#92441,#92442,
#92443,#92444,#92445,#92446,#92447,#92448,#92449,#92450,#92451,#92452,#92453,
#92454,#92455,#92456,#92457,#92458,#92459,#92460,#92461,#92462,#92463,#92464,
#92465,#92466,#92467,#92468,#92469,#92470,#92471,#92472,#92473,#92474,#92475,
#92476,#92477,#92478,#92479,#92480,#92481,#92482,#92483,#92484,#92485,#92486,
#92487,#92488,#92489,#92490,#92491,#92492,#92493,#92494,#92495,#92496,#92497,
#92498,#92499,#92500,#92501,#92502,#92503,#92504,#92505,#92506,#92507,#92508,
#92509,#92510,#92511,#92512,#92513,#92514,#92515,#92516,#92517,#92518,#92519,
#92520,#92521,#92522,#92523,#92524,#92525,#92526,#92527,#92528,#92529,#92530,
#92531,#92532,#92533,#92534,#92535,#92536,#92537,#92538,#92539,#92540,#92541,
#92542,#92543,#92544,#92545,#92546,#92547,#92548,#92549,#92550,#92551,#92552,
#92553,#92554,#92555,#92556,#92557,#92558,#92559,#92560,#92561,#92562,#92563,
#92564,#92565,#92566,#92567,#92568,#92569,#92570,#92571,#92572,#92573,#92574,
#92575,#92576,#92577,#92578,#92579,#92580,#92581,#92582,#92583,#92584,#92585,
#92586,#92587,#92588,#92589,#92590,#92591,#92592,#92593,#92594,#92595,#92596,
#92597,#92598,#92599,#92600,#92601,#92602,#92603,#92604,#92605,#92606,#92607,
#92608,#92609,#92610,#92611,#92612,#92613,#92614,#92615,#92616,#92617,#92618,
#92619,#92620,#92621,#92622,#92623,#92624,#92625,#92626,#92627,#92628,#92629,
#92630,#92631,#92632,#92633,#92634,#92635,#92636,#92637,#92638,#92639,#92640,
#92641,#92642),.UNSPECIFIED.,.F.,.F.,(4,2,2,2,2,2,2,2,2,2,2,2,2,2,2,2,2,
2,2,2,2,2,2,2,2,2,2,2,2,2,2,2,2,2,2,2,2,2,2,2,2,2,2,2,2,2,2,2,2,2,2,2,2,
2,2,2,2,2,2,2,2,2,2,2,2,2,2,2,2,2,2,2,2,2,2,2,2,2,2,2,2,2,2,2,2,2,2,2,2,
2,2,2,2,2,2,2,2,2,2,2,2,2,2,2,2,2,2,4),(-2.97248562834132,-2.97156067933371,
-2.92779150390965,-2.89482030744997,-2.88122261515143,-2.87161212394087,
-2.86767910884108,-2.86486045668559,-2.86230124776594,-2.85823872603261,
-2.85068782170555,-2.79219885096846,-2.75320557359479,-2.75037087584259,
-2.74795483399847,-2.74635691748857,-2.74482281563557,-2.74251618904016,
-2.73693120885304,-2.69188411114417,-2.65549220308016,-2.64293575198332,
-2.6338934714932,-2.6300539303029,-2.62725204622808,-2.62467327904287,-2.62117458734169,
-2.61247037738203,-2.56440112423484,-2.52915208832837,-2.51922798216468,
-2.51274719725168,-2.51037868804558,-2.50877525212609,-2.50733908456329,
-2.50501259985502,-2.49926082391095,-2.46296783804852,-2.45454866340838,
-2.40276126678399,-2.3955331936639,-2.39202237701551,-2.3892695476409,-2.3862047134983,
-2.38110908961234,-2.36364773451225,-2.35371713560661,-2.2957031459866,
-2.2771300555768,-2.27378642938069,-2.27196939875307,-2.27043212752409,
-2.26848811038663,-2.26540122916047,-2.24857803336442,-2.24445110911132,
-2.20289676623316,-2.16701696938553,-2.1586402971301,-2.15491575147548,
-2.1521330536444,-2.14952541671011,-2.14591428070777,-2.13652612784976,
-2.0755488971694,-2.07260000324708,-2.04311270407503,-2.03745930787644,
-2.03521444513661,-2.03363537947384,-2.03217381233665,-2.03012259874889,
-2.02467733277743,-1.97632597719324,-1.92650570480663,-1.9200385457438,
-1.91667975848291,-1.91393997325214,-1.91077332544168,-1.90535812303464,
-1.88363218370009,-1.82113371858248,-1.80835073044198,-1.80055751824542,
-1.79801660501411,-1.79637597061917,-1.7948002274363,-1.79249112890348,
-1.78684520515815,-1.74266300998612,-1.68862719191158,-1.68234608578561,
-1.67902568349406,-1.67655340916266,-1.67345153968695,-1.66818889860627,
-1.64902769629626,-1.59030518084118,-1.56710458084776,-1.56208332154418,
-1.55994244870059,-1.55838149760638,-1.55667828589076,-1.55385481097013,
-1.54448582904813,-1.49596156717328,-1.48741829385312,-1.47839118834467),
 .UNSPECIFIED.);
#785=B_SPLINE_CURVE_WITH_KNOTS('',3,(#92643,#92644,#92645,#92646,#92647,
#92648,#92649,#92650,#92651,#92652,#92653,#92654,#92655,#92656,#92657,#92658,
#92659,#92660,#92661,#92662,#92663,#92664,#92665,#92666,#92667,#92668,#92669,
#92670,#92671,#92672,#92673,#92674,#92675,#92676,#92677,#92678,#92679,#92680,
#92681,#92682,#92683,#92684,#92685,#92686,#92687,#92688,#92689,#92690,#92691,
#92692,#92693,#92694,#92695,#92696,#92697,#92698,#92699,#92700,#92701,#92702,
#92703,#92704,#92705,#92706,#92707,#92708,#92709,#92710,#92711,#92712,#92713,
#92714,#92715,#92716,#92717,#92718,#92719,#92720,#92721,#92722,#92723,#92724,
#92725,#92726,#92727,#92728,#92729,#92730,#92731,#92732,#92733,#92734,#92735,
#92736,#92737,#92738,#92739,#92740,#92741,#92742,#92743,#92744,#92745,#92746,
#92747,#92748,#92749,#92750,#92751,#92752,#92753,#92754,#92755,#92756,#92757,
#92758,#92759,#92760,#92761,#92762,#92763,#92764,#92765,#92766,#92767,#92768,
#92769,#92770,#92771,#92772,#92773,#92774,#92775,#92776,#92777,#92778,#92779,
#92780,#92781,#92782,#92783,#92784,#92785,#92786,#92787,#92788,#92789,#92790,
#92791,#92792,#92793,#92794,#92795,#92796,#92797,#92798,#92799,#92800,#92801,
#92802,#92803,#92804,#92805,#92806,#92807,#92808,#92809,#92810,#92811,#92812,
#92813,#92814,#92815,#92816,#92817,#92818,#92819,#92820,#92821,#92822,#92823,
#92824,#92825,#92826,#92827,#92828,#92829,#92830,#92831,#92832,#92833,#92834,
#92835,#92836,#92837,#92838,#92839,#92840,#92841,#92842,#92843,#92844,#92845,
#92846,#92847,#92848,#92849,#92850,#92851,#92852,#92853,#92854,#92855,#92856,
#92857,#92858,#92859,#92860,#92861,#92862,#92863,#92864),.UNSPECIFIED.,
 .F.,.F.,(4,2,2,2,2,2,2,2,2,2,2,2,2,2,2,2,2,2,2,2,2,2,2,2,2,2,2,2,2,2,2,
2,2,2,2,2,2,2,2,2,2,2,2,2,2,2,2,2,2,2,2,2,2,2,2,2,2,2,2,2,2,2,2,2,2,2,2,
2,2,2,2,2,2,2,2,2,2,2,2,2,2,2,2,2,2,2,2,2,2,2,2,2,2,2,2,2,2,2,2,2,2,2,2,
2,2,2,2,2,2,2,4),(-1.51291820589149,-1.4955978501673,-1.48868563564395,
-1.48515958090633,-1.48236927418393,-1.4792355956776,-1.47395934358364,
-1.45258156693988,-1.40774651121575,-1.39814287532211,-1.39125436101471,
-1.38469601357356,-1.37027237891115,-1.36700520915586,-1.36516865993728,
-1.36360747038655,-1.36162191430467,-1.35754059874169,-1.31506918560559,
-1.26071560156739,-1.25217413289291,-1.24867362219442,-1.24606869615536,
-1.24321384459742,-1.23925603562992,-1.22970817259507,-1.21627480175101,
-1.17735411016549,-1.13665444913826,-1.13089091199475,-1.12854244651807,
-1.12694244794468,-1.12527787594811,-1.12270043278592,-1.11479495463648,
-1.10180896135062,-1.03646880836714,-1.01762887845479,-1.0123507382666,
-1.00921685979573,-1.00670596413038,-1.0033162333797,-0.996843212778155,
-0.944436665893327,-0.929806331542807,-0.896218114977467,-0.892377260588701,
-0.890414330512949,-0.888854690317843,-0.887000759865873,-0.883560393997282,
-0.863532135212415,-0.787676746748735,-0.777698074474476,-0.773556075634001,
-0.770955404364455,-0.768097728760838,-0.764122082939013,-0.754461607785713,
-0.740819107303395,-0.70080783134114,-0.661610252602209,-0.655832266435037,
-0.653481690264618,-0.651881518153566,-0.650218012661907,-0.647644376192594,
-0.639767442918814,-0.626845996292329,-0.562559155746558,-0.542781723749043,
-0.537403610299997,-0.534248213692101,-0.531740845457862,-0.528382622219717,
-0.522059151776543,-0.46866436682011,-0.423915385958649,-0.418283072930048,
-0.416187484704163,-0.414700774212505,-0.413100850080367,-0.410834895896314,
-0.405170458648868,-0.375901850055044,-0.324134490002468,-0.30516131607259,
-0.299870942016026,-0.296734672891897,-0.294224573873341,-0.29156394675692,
-0.28634126755948,-0.264783519583157,-0.218837360639595,-0.183759298884581,
-0.179918406396861,-0.1779556362976,-0.176396218387824,-0.174542664724284,
-0.172561949813693,-0.164207609181587,-0.134872067375431,-0.106976169080335,
-0.0695224092823296,-0.0638646567633502,-0.0603111449863071,-0.0575184479006353,
-0.0544022074428103,-0.0511775410252991,-0.0463683924039305,-0.0183031829186653),
 .UNSPECIFIED.);
#786=B_SPLINE_CURVE_WITH_KNOTS('',3,(#92870,#92871,#92872,#92873,#92874,
#92875,#92876,#92877,#92878,#92879),.UNSPECIFIED.,.F.,.F.,(4,1,1,1,1,1,
1,4),(72.2566346161759,73.2298488044367,74.2286545160064,75.2274602275762,
76.226265939146,77.2250716507158,78.2238773622855,78.4676963535106),
 .UNSPECIFIED.);
#787=B_SPLINE_CURVE_WITH_KNOTS('',3,(#92880,#92881,#92882,#92883,#92884,
#92885,#92886,#92887,#92888,#92889,#92890,#92891,#92892,#92893,#92894,#92895),
 .UNSPECIFIED.,.F.,.F.,(4,2,2,2,2,2,2,4),(-2.98981850197706,-2.98825670069322,
-2.98643438083612,-2.98490201067196,-2.98342035314125,-2.98192681857162,
-2.97930338862327,-2.97248562834132),.UNSPECIFIED.);
#788=B_SPLINE_CURVE_WITH_KNOTS('',3,(#92897,#92898,#92899,#92900),
 .UNSPECIFIED.,.F.,.F.,(4,4),(-0.0183031829186653,-0.000703111691500607),
 .UNSPECIFIED.);
#789=B_SPLINE_CURVE_WITH_KNOTS('',3,(#92901,#92902,#92903,#92904,#92905,
#92906,#92907,#92908,#92909,#92910),.UNSPECIFIED.,.F.,.F.,(4,1,1,1,1,1,
1,4),(72.2566333488475,72.5142287899751,73.5125762644367,74.5109237388983,
75.5092712133598,76.5076186878214,77.505966162283,78.4665403893118),
 .UNSPECIFIED.);
#790=B_SPLINE_CURVE_WITH_KNOTS('',3,(#92916,#92917,#92918,#92919,#92920,
#92921,#92922,#92923,#92924,#92925,#92926,#92927,#92928,#92929,#92930,#92931,
#92932,#92933,#92934,#92935,#92936,#92937,#92938,#92939,#92940,#92941,#92942,
#92943,#92944,#92945,#92946,#92947,#92948,#92949,#92950,#92951,#92952,#92953,
#92954,#92955,#92956,#92957,#92958,#92959,#92960,#92961,#92962,#92963,#92964,
#92965,#92966,#92967,#92968,#92969,#92970,#92971,#92972,#92973,#92974,#92975,
#92976,#92977,#92978,#92979,#92980,#92981,#92982,#92983,#92984,#92985,#92986,
#92987,#92988,#92989,#92990,#92991,#92992,#92993,#92994,#92995,#92996,#92997,
#92998,#92999,#93000,#93001,#93002,#93003,#93004,#93005,#93006,#93007,#93008,
#93009,#93010,#93011,#93012,#93013,#93014,#93015,#93016,#93017,#93018,#93019,
#93020,#93021,#93022,#93023,#93024,#93025,#93026,#93027,#93028,#93029,#93030,
#93031,#93032,#93033,#93034,#93035,#93036,#93037,#93038,#93039,#93040,#93041,
#93042,#93043,#93044,#93045,#93046,#93047,#93048,#93049,#93050,#93051,#93052,
#93053,#93054,#93055,#93056,#93057,#93058,#93059,#93060,#93061,#93062,#93063,
#93064,#93065,#93066,#93067,#93068,#93069,#93070,#93071,#93072,#93073,#93074,
#93075,#93076,#93077,#93078,#93079,#93080,#93081,#93082,#93083,#93084,#93085,
#93086,#93087,#93088,#93089,#93090,#93091,#93092,#93093,#93094,#93095,#93096,
#93097,#93098,#93099,#93100,#93101,#93102,#93103,#93104,#93105),
 .UNSPECIFIED.,.F.,.F.,(4,3,3,3,3,3,3,3,3,3,3,3,3,3,3,3,3,3,3,3,3,3,3,3,
3,3,3,3,3,3,3,3,3,3,3,3,3,3,3,3,3,3,3,3,3,3,3,3,3,3,3,3,3,3,3,3,3,3,3,3,
3,3,3,4),(78.5398163397449,78.639625262068,78.7394070013408,78.8391931746706,
78.9390862524863,79.0390332714625,79.1391646313106,79.2226830738553,79.32318239275,
79.4235362419029,79.5237730469281,79.6239458180325,79.7240858152806,79.8242242576787,
79.9244626898268,80.0247490873905,80.125218688962,80.2214887854251,80.3219881043198,
80.4223419534728,80.5225787584979,80.6227515296023,80.7228915268504,80.8230299692488,
80.923268401397,81.0235547989607,81.1240244005322,81.2202944969949,81.3207938158895,
81.4211476650429,81.5213844700679,81.6215572411723,81.7216972384203,81.8218356808185,
81.9220741129666,82.0223605105304,82.1228301121019,82.2191002085647,82.3195995274593,
82.4199533766122,82.5201901816374,82.6203629527417,82.7205029499898,82.8206413923881,
82.9208798245363,83.0211662220999,83.1216358236714,83.2179059201344,83.318405239029,
83.4187590881821,83.5189958932072,83.6191686643116,83.7193086615596,83.8194471039578,
83.9196855361059,84.0199719336696,84.1204415352411,84.2167116317042,84.3185060059812,
84.4201415989636,84.5216223522047,84.6230133414407,84.7243377755445,84.7497329240609),
 .UNSPECIFIED.);
#791=B_SPLINE_CURVE_WITH_KNOTS('',3,(#93106,#93107,#93108,#93109),
 .UNSPECIFIED.,.F.,.F.,(4,4),(78.4676963535106,78.539809789393),
 .UNSPECIFIED.);
#792=B_SPLINE_CURVE_WITH_KNOTS('',3,(#93111,#93112,#93113,#93114,#93115),
 .UNSPECIFIED.,.F.,.F.,(4,1,4),(78.4665403893118,78.5043136367446,78.5398163397449),
 .UNSPECIFIED.);
#793=B_SPLINE_CURVE_WITH_KNOTS('',3,(#93116,#93117,#93118,#93119,#93120,
#93121,#93122,#93123,#93124,#93125,#93126,#93127,#93128,#93129,#93130,#93131,
#93132,#93133,#93134,#93135,#93136,#93137,#93138,#93139,#93140,#93141,#93142,
#93143,#93144,#93145,#93146,#93147,#93148,#93149,#93150,#93151,#93152,#93153,
#93154,#93155,#93156,#93157,#93158,#93159,#93160,#93161,#93162,#93163,#93164,
#93165,#93166,#93167,#93168,#93169,#93170,#93171,#93172,#93173,#93174,#93175,
#93176,#93177,#93178,#93179,#93180,#93181,#93182,#93183,#93184,#93185,#93186,
#93187,#93188,#93189,#93190,#93191,#93192,#93193,#93194,#93195,#93196,#93197,
#93198,#93199,#93200,#93201,#93202,#93203,#93204,#93205,#93206,#93207,#93208,
#93209,#93210,#93211,#93212,#93213,#93214,#93215,#93216,#93217,#93218,#93219,
#93220,#93221,#93222,#93223,#93224,#93225,#93226,#93227,#93228,#93229,#93230,
#93231,#93232,#93233,#93234,#93235,#93236,#93237,#93238,#93239,#93240,#93241,
#93242,#93243,#93244,#93245,#93246,#93247,#93248,#93249,#93250,#93251,#93252,
#93253,#93254,#93255,#93256,#93257,#93258,#93259,#93260,#93261,#93262,#93263,
#93264,#93265,#93266,#93267,#93268,#93269,#93270,#93271,#93272,#93273,#93274,
#93275,#93276,#93277,#93278,#93279,#93280,#93281,#93282,#93283,#93284,#93285,
#93286,#93287,#93288,#93289,#93290,#93291,#93292,#93293,#93294,#93295,#93296,
#93297,#93298,#93299,#93300,#93301,#93302,#93303,#93304,#93305,#93306,#93307,
#93308,#93309,#93310,#93311,#93312,#93313,#93314,#93315,#93316,#93317,#93318,
#93319,#93320,#93321,#93322,#93323,#93324,#93325,#93326,#93327,#93328,#93329,
#93330,#93331,#93332,#93333,#93334,#93335,#93336,#93337,#93338,#93339,#93340,
#93341,#93342,#93343,#93344,#93345,#93346,#93347,#93348,#93349,#93350,#93351,
#93352,#93353,#93354,#93355,#93356,#93357,#93358,#93359,#93360,#93361,#93362,
#93363,#93364,#93365,#93366,#93367,#93368,#93369,#93370,#93371,#93372,#93373,
#93374,#93375),.UNSPECIFIED.,.F.,.F.,(4,2,2,2,2,2,2,2,2,2,2,2,2,2,2,2,2,
2,2,2,2,2,2,2,2,2,2,2,2,2,2,2,2,2,2,2,2,2,2,2,2,2,2,2,2,2,2,2,2,2,2,2,2,
2,2,2,2,2,2,2,2,2,2,2,2,2,2,2,2,2,2,2,2,2,2,2,2,2,2,2,2,2,2,2,2,2,2,2,2,
2,2,2,2,2,2,2,2,2,2,2,2,2,2,2,2,2,2,2,2,2,2,2,2,2,2,2,2,2,2,2,2,2,2,2,2,
2,2,2,2,4),(-2.98918321660332,-2.95816385181088,-2.93577202507296,-2.89069523414431,
-2.88402815084895,-2.88059982146384,-2.87781962568173,-2.87462394209342,
-2.86920071949568,-2.84794758267391,-2.79111273857183,-2.77436136512357,
-2.76804493994685,-2.76483589798187,-2.76282311984763,-2.76097329392359,
-2.76096402969731,-2.76095470718103,-2.76094532512873,-2.76093588226905,
-2.7609263773134,-2.76091680891982,-2.76090717574813,-2.76089747640838,
-2.76088770946629,-2.76087787346166,-2.76086932728069,-2.76086049556672,
-2.76085136573228,-2.76084192443884,-2.76083215756958,-2.76082205013897,
-2.76081158621808,-2.7608007488897,-2.7607895201406,-2.76077788078478,-2.76076581036865,
-2.76075328703221,-2.76074028741406,-2.76072678651303,-2.76071275751994,
-2.76069817166731,-2.76068299803468,-2.75916438941005,-2.75714271292296,
-2.75377154592753,-2.73066323607994,-2.6878483444427,-2.65224654810353,
-2.64624469757052,-2.64295501287312,-2.64045364117898,-2.637244593841,-2.63176366149767,
-2.60979175848285,-2.56164472036491,-2.53224333909891,-2.5265678937192,
-2.5243007093267,-2.52270101597106,-2.52121539971995,-2.51912257331459,
-2.51350581557904,-2.46840195072964,-2.41553377784689,-2.40915183393897,
-2.40578216065481,-2.40327449972437,-2.40012954589255,-2.39479583053783,
-2.37535329006914,-2.31067656099045,-2.29773035565358,-2.28984414379551,
-2.28726989190211,-2.28560661485491,-2.28400719119716,-2.28165854850609,
-2.27588942505212,-2.23593615520927,-2.19654612010038,-2.17606815486324,
-2.17086317867483,-2.16774624553651,-2.16495480324629,-2.16140545397049,
-2.15575943518954,-2.1187804145423,-2.09649100125249,-2.05507100136872,
-2.05105560410942,-2.04908372342199,-2.04752422318301,-2.04567899266631,
-2.04237092389592,-2.02731246570253,-1.96394665140559,-1.93923412418153,
-1.93373316610162,-1.93055150887982,-1.92776963020741,-1.9243212759911,
-1.91900735559468,-1.89178198770894,-1.82898193403814,-1.82033144839511,
-1.81446611330096,-1.81216895684591,-1.81056348482962,-1.80908474756827,
-1.80701811608384,-1.80159887350359,-1.75258133540274,-1.70318405765312,
-1.69689975705287,-1.69355021613779,-1.69104415138619,-1.68788357484666,
-1.6824796494565,-1.66238598030677,-1.59841549512706,-1.58551109254505,
-1.57764280506907,-1.57507054090084,-1.57340756950339,-1.57180759641025,
-1.56945684072133,-1.56367600732907,-1.52672374711719,-1.51256178469963),
 .UNSPECIFIED.);
#794=B_SPLINE_CURVE_WITH_KNOTS('',3,(#93381,#93382,#93383,#93384,#93385,
#93386,#93387,#93388,#93389,#93390,#93391,#93392,#93393,#93394,#93395,#93396,
#93397,#93398,#93399,#93400,#93401,#93402,#93403,#93404,#93405,#93406,#93407,
#93408,#93409,#93410,#93411,#93412,#93413,#93414,#93415,#93416,#93417,#93418,
#93419,#93420,#93421,#93422,#93423,#93424,#93425,#93426,#93427,#93428,#93429,
#93430,#93431,#93432,#93433,#93434,#93435,#93436,#93437,#93438,#93439,#93440,
#93441,#93442,#93443,#93444,#93445,#93446,#93447,#93448,#93449,#93450,#93451,
#93452,#93453,#93454,#93455,#93456,#93457,#93458,#93459,#93460,#93461,#93462,
#93463,#93464,#93465,#93466,#93467,#93468,#93469,#93470,#93471,#93472,#93473,
#93474,#93475,#93476,#93477,#93478,#93479,#93480,#93481,#93482,#93483,#93484,
#93485,#93486,#93487,#93488,#93489,#93490,#93491,#93492,#93493,#93494,#93495,
#93496,#93497,#93498,#93499,#93500,#93501,#93502,#93503,#93504,#93505,#93506,
#93507,#93508,#93509,#93510,#93511,#93512,#93513,#93514,#93515,#93516,#93517,
#93518,#93519,#93520,#93521,#93522,#93523,#93524,#93525,#93526,#93527,#93528,
#93529,#93530,#93531,#93532,#93533,#93534,#93535,#93536,#93537,#93538,#93539,
#93540,#93541,#93542,#93543,#93544,#93545,#93546,#93547,#93548,#93549,#93550,
#93551,#93552,#93553,#93554,#93555,#93556,#93557,#93558,#93559,#93560,#93561,
#93562,#93563,#93564,#93565,#93566,#93567,#93568,#93569,#93570,#93571,#93572,
#93573,#93574,#93575,#93576,#93577,#93578,#93579,#93580,#93581,#93582),
 .UNSPECIFIED.,.F.,.F.,(4,2,2,2,2,2,2,2,2,2,2,2,2,2,2,2,2,2,2,2,2,2,2,2,
2,2,2,2,2,2,2,2,2,2,2,2,2,2,2,2,2,2,2,2,2,2,2,2,2,2,2,2,2,2,2,2,2,2,2,2,
2,2,2,2,2,2,2,2,2,2,2,2,2,2,2,2,2,2,2,2,2,2,2,2,2,2,2,2,2,2,2,2,2,2,2,2,
2,2,2,2,4),(-1.4782746125791,-1.4396509137331,-1.41159399107955,-1.40628973330349,
-1.40286868537309,-1.40012300583755,-1.39699852779614,-1.3916375036407,
-1.36836690740716,-1.31437602389714,-1.28881210494715,-1.28507576076022,
-1.28315093326428,-1.28161373742846,-1.27977885810151,-1.27635514245457,
-1.25590198451957,-1.22168177215044,-1.17457442239032,-1.16893949385635,
-1.16541820877157,-1.16266241707564,-1.15959968362865,-1.15452023412004,
-1.13504694935018,-1.09711966574836,-1.05413364404067,-1.04844892312133,
-1.04613258400297,-1.04455478918545,-1.04291485363532,-1.0403799469425,
-1.03264335259191,-0.972209102718155,-0.936755982197143,-0.931198172772021,
-0.927700156260857,-0.924947062848449,-0.921871243726662,-0.91673198898983,
-0.896518852237591,-0.847203909213429,-0.813612938747056,-0.80980672060834,
-0.807866968120856,-0.806329010124019,-0.804506375433296,-0.801140024185952,
-0.782086953227113,-0.7194138822926,-0.697849080511699,-0.692443387723308,
-0.689277817977244,-0.686810427920725,-0.683565905870787,-0.677649478975064,
-0.642990322382811,-0.605936247558776,-0.57593027932295,-0.572142086953887,
-0.570206256676715,-0.568668623658462,-0.566843086458597,-0.563462785564301,
-0.544078610861073,-0.477568156956744,-0.459593297823505,-0.454443469971658,
-0.451365585110331,-0.448888570037038,-0.445530546847995,-0.439071812309515,
-0.43090289350318,-0.412224336496224,-0.366525912809479,-0.338241789697379,
-0.334476140865227,-0.332545215609742,-0.331007957512597,-0.329178697386759,
-0.325780537942659,-0.305960178196428,-0.233163971478154,-0.220633266136224,
-0.216127716266159,-0.213484673222681,-0.210824921190773,-0.207403423127645,
-0.203612346312103,-0.197391716207418,-0.184740905258884,-0.147886959461409,
-0.103415661649691,-0.097779673451371,-0.0954718481460404,-0.0938960488671336,
-0.0922544327903232,-0.0897104128021005,-0.0818950365296063,-0.0690642949045764,
-0.000705350955375777),.UNSPECIFIED.);
#795=B_SPLINE_CURVE_WITH_KNOTS('',3,(#93583,#93584,#93585,#93586),
 .UNSPECIFIED.,.F.,.F.,(4,4),(84.7497329240609,84.8230016469245),
 .UNSPECIFIED.);
#796=B_SPLINE_CURVE_WITH_KNOTS('',3,(#93587,#93588,#93589,#93590,#93591,
#93592,#93593,#93594,#93595,#93596,#93597,#93598,#93599,#93600,#93601,#93602,
#93603,#93604,#93605,#93606,#93607,#93608,#93609,#93610,#93611,#93612,#93613,
#93614,#93615,#93616,#93617,#93618,#93619,#93620,#93621,#93622,#93623,#93624,
#93625,#93626,#93627,#93628,#93629,#93630,#93631,#93632,#93633,#93634,#93635,
#93636,#93637,#93638,#93639,#93640,#93641,#93642,#93643,#93644,#93645,#93646,
#93647,#93648,#93649,#93650,#93651,#93652,#93653,#93654,#93655,#93656,#93657,
#93658,#93659,#93660,#93661,#93662,#93663,#93664,#93665,#93666,#93667,#93668,
#93669,#93670,#93671,#93672,#93673,#93674,#93675,#93676,#93677,#93678,#93679,
#93680,#93681,#93682,#93683,#93684,#93685,#93686,#93687,#93688,#93689,#93690,
#93691,#93692,#93693,#93694,#93695,#93696,#93697,#93698,#93699,#93700,#93701,
#93702,#93703,#93704,#93705,#93706,#93707,#93708,#93709,#93710,#93711,#93712,
#93713,#93714,#93715,#93716,#93717,#93718,#93719,#93720,#93721,#93722,#93723,
#93724,#93725,#93726,#93727,#93728,#93729,#93730,#93731,#93732,#93733,#93734,
#93735,#93736,#93737,#93738,#93739,#93740,#93741,#93742,#93743,#93744,#93745,
#93746,#93747,#93748,#93749,#93750,#93751,#93752,#93753,#93754,#93755,#93756,
#93757,#93758,#93759,#93760,#93761,#93762,#93763,#93764,#93765,#93766,#93767,
#93768,#93769,#93770,#93771,#93772,#93773,#93774,#93775,#93776,#93777,#93778,
#93779,#93780,#93781,#93782,#93783,#93784,#93785,#93786,#93787,#93788,#93789,
#93790,#93791,#93792,#93793,#93794,#93795,#93796,#93797,#93798,#93799,#93800,
#93801,#93802,#93803,#93804,#93805,#93806,#93807,#93808,#93809,#93810,#93811,
#93812,#93813,#93814,#93815,#93816,#93817,#93818,#93819,#93820,#93821,#93822,
#93823,#93824,#93825,#93826,#93827,#93828,#93829,#93830,#93831,#93832,#93833,
#93834,#93835,#93836,#93837,#93838,#93839,#93840,#93841,#93842,#93843,#93844,
#93845,#93846,#93847,#93848,#93849,#93850),.UNSPECIFIED.,.F.,.F.,(4,2,2,
2,2,2,2,2,2,2,2,2,2,2,2,2,2,2,2,2,2,2,2,2,2,2,2,2,2,2,2,2,2,2,2,2,2,2,2,
2,2,2,2,2,2,2,2,2,2,2,2,2,2,2,2,2,2,2,2,2,2,2,2,2,2,2,2,2,2,2,2,2,2,2,2,
2,2,2,2,2,2,2,2,2,2,2,2,2,2,2,2,2,2,2,2,2,2,2,2,2,2,2,2,2,2,2,2,2,2,2,2,
2,2,2,2,2,2,2,2,2,2,2,2,2,2,2,2,2,2,2,2,4),(-1.51256178469963,-1.4953817432681,
-1.46535641570292,-1.45992811232076,-1.4564444474865,-1.45365919909592,
-1.45050077899404,-1.44510791761768,-1.42207541070932,-1.36957684230411,
-1.36267082421071,-1.35641004918383,-1.34170042859708,-1.33841484557679,
-1.33657453571175,-1.33501434807961,-1.3330354266082,-1.32898545107136,
-1.29127028662996,-1.23149065413333,-1.22321474078269,-1.21951695137761,
-1.21669631745552,-1.21368076972235,-1.20893867372257,-1.19348024252329,
-1.16732946253917,-1.12913811357486,-1.11955262173962,-1.10435781900799,
-1.10133118596885,-1.09939116450975,-1.09783308113571,-1.09596108380582,
-1.09243364227792,-1.07003186219425,-1.03726284074255,-1.03190196364829,
-0.991095807270734,-0.985398563845544,-0.981833587765332,-0.979040130457728,
-0.975931558386187,-0.970765622093367,-0.95078099329336,-0.872785101731417,
-0.871473754818147,-0.865115003611904,-0.862668727943834,-0.861195405537403,
-0.859584236328339,-0.857259614993989,-0.851218106252388,-0.842221997512537,
-0.81280549440489,-0.790498037522222,-0.753492259344454,-0.747844048750969,
-0.744293294130027,-0.741500750710934,-0.738382591858399,-0.733175584503152,
-0.712690808936499,-0.673287236015255,-0.633265797060171,-0.627489416205511,
-0.62513897910371,-0.623538729324841,-0.621874973125982,-0.619300655158341,
-0.611419341087762,-0.598488306619038,-0.53405684292646,-0.514407857441494,
-0.50904044571588,-0.505887212577665,-0.503379310200202,-0.50001747919903,
-0.493677621999187,-0.440481135368036,-0.395548432556467,-0.389917987387191,
-0.387822553849985,-0.386335800273472,-0.384735660403504,-0.382469123737077,
-0.376801811462389,-0.347505372594177,-0.311465281050975,-0.278344199223827,
-0.272807362596115,-0.269290200071955,-0.266501105205479,-0.266442339248896,
-0.266388517754334,-0.266339221063827,-0.266294064907373,-0.266252697649597,
-0.266214797660163,-0.266180070843758,-0.266148248330416,-0.266119084328322,
-0.266092354150027,-0.266067852387372,-0.266045391233553,-0.266012309899606,
-0.265979852850944,-0.265948005557679,-0.265916753853183,-0.265886083937673,
-0.262574527655244,-0.256380438170859,-0.248574457770508,-0.231170514684446,
-0.195300185456222,-0.158348933954051,-0.152563782509416,-0.150211871480349,
-0.148611320401091,-0.146947943124938,-0.144375406430151,-0.136508874639095,
-0.12361184137463,-0.0646289259588138,-0.0460606698494302,-0.036728761200554,
-0.0330955323476834,-0.0304574657994303,-0.027793538976715,-0.0250426290603577,
-0.0214416168447533,-0.0182274268811936),.UNSPECIFIED.);
#797=B_SPLINE_CURVE_WITH_KNOTS('',3,(#93855,#93856,#93857,#93858,#93859,
#93860,#93861,#93862,#93863,#93864,#93865,#93866,#93867,#93868,#93869,#93870,
#93871,#93872,#93873,#93874,#93875,#93876,#93877,#93878,#93879,#93880,#93881,
#93882,#93883,#93884,#93885,#93886,#93887,#93888,#93889,#93890,#93891,#93892,
#93893,#93894,#93895,#93896,#93897,#93898,#93899,#93900,#93901,#93902,#93903,
#93904,#93905,#93906,#93907,#93908,#93909,#93910,#93911,#93912,#93913,#93914,
#93915,#93916,#93917,#93918,#93919,#93920,#93921,#93922,#93923,#93924,#93925,
#93926,#93927,#93928,#93929,#93930,#93931,#93932,#93933,#93934,#93935,#93936,
#93937,#93938,#93939,#93940,#93941,#93942,#93943,#93944,#93945,#93946,#93947,
#93948,#93949,#93950,#93951,#93952,#93953,#93954,#93955,#93956,#93957,#93958,
#93959,#93960,#93961,#93962,#93963,#93964,#93965,#93966,#93967,#93968,#93969,
#93970,#93971,#93972,#93973,#93974,#93975,#93976,#93977,#93978,#93979,#93980,
#93981,#93982,#93983,#93984,#93985,#93986,#93987,#93988,#93989,#93990,#93991,
#93992,#93993,#93994,#93995,#93996,#93997,#93998,#93999,#94000,#94001,#94002,
#94003,#94004,#94005,#94006,#94007,#94008,#94009,#94010,#94011,#94012,#94013,
#94014,#94015,#94016,#94017,#94018,#94019,#94020,#94021,#94022,#94023,#94024,
#94025,#94026,#94027,#94028,#94029,#94030,#94031,#94032,#94033,#94034,#94035,
#94036,#94037,#94038,#94039,#94040,#94041,#94042,#94043,#94044,#94045,#94046,
#94047,#94048,#94049,#94050,#94051,#94052,#94053,#94054,#94055,#94056,#94057,
#94058,#94059,#94060,#94061,#94062,#94063,#94064,#94065,#94066,#94067,#94068,
#94069,#94070,#94071,#94072,#94073,#94074,#94075,#94076,#94077,#94078,#94079,
#94080,#94081,#94082,#94083,#94084),.UNSPECIFIED.,.F.,.F.,(4,2,2,2,2,2,
2,2,2,2,2,2,2,2,2,2,2,2,2,2,2,2,2,2,2,2,2,2,2,2,2,2,2,2,2,2,2,2,2,2,2,2,
2,2,2,2,2,2,2,2,2,2,2,2,2,2,2,2,2,2,2,2,2,2,2,2,2,2,2,2,2,2,2,2,2,2,2,2,
2,2,2,2,2,2,2,2,2,2,2,2,2,2,2,2,2,2,2,2,2,2,2,2,2,2,2,2,2,2,2,2,2,2,2,2,
4),(-2.97297727746947,-2.95221453996876,-2.9494940641458,-2.94769156185505,
-2.94623135474866,-2.94469390590804,-2.94275495456382,-2.93895077642154,
-2.9066755594628,-2.881763692486,-2.85564790422669,-2.83590801533075,-2.83079210636194,
-2.82772192694603,-2.82496862466811,-2.8214631449971,-2.8158789431899,-2.77942483221904,
-2.77068148341162,-2.71942709430567,-2.7122162238443,-2.70979726981379,
-2.70815401062335,-2.70657928892087,-2.70427714976083,-2.69867549839649,
-2.65360976955837,-2.61719653010085,-2.60463310989038,-2.59558590040179,
-2.59174434251351,-2.58894101455537,-2.5863609378248,-2.58286049904218,
-2.57415209617595,-2.52602673949374,-2.49078452476213,-2.48085910621145,
-2.47437682572526,-2.4720073621897,-2.47040315865921,-2.46896621122825,
-2.46663829189167,-2.46088211357877,-2.42245226969945,-2.38810801114708,
-2.37057840747024,-2.35895178203451,-2.35471577562704,-2.35183599458596,
-2.34903301644091,-2.34566440704953,-2.3371925427222,-2.27958809703861,
-2.27150050523808,-2.24213650914775,-2.23649330888341,-2.23424946028425,
-2.23267007327095,-2.23120738031702,-2.22915346080045,-2.22369210998522,
-2.17565708943197,-2.12510574928066,-2.11886905131563,-2.11555716575829,
-2.11308488597496,-2.10997468268039,-2.10467735616917,-2.08529777665042,
-2.02030338340487,-2.0073609083736,-1.99949734144815,-1.99694720355168,
-1.99530405588822,-1.99372883869859,-1.99142504635005,-1.98581472900864,
-1.94076624125344,-1.90433757449402,-1.89177025856211,-1.88272057092448,
-1.87887823905397,-1.87607444769401,-1.8734940151019,-1.8699932015744,-1.86128442662558,
-1.81304130268261,-1.777880790207,-1.7679670708958,-1.76149019258386,-1.75912127302491,
-1.75751701095387,-1.75607968673327,-1.75375055499176,-1.74798837224119,
-1.71004500748069,-1.67471632238995,-1.65748424215765,-1.64600276498108,
-1.64178658252846,-1.63891057835832,-1.6361038118058,-1.63272161135779,
-1.624165837611,-1.56758444947759,-1.54283849185021,-1.52563434545013,-1.5223540419327,
-1.52054989904816,-1.51901030199244,-1.51704635046194,-1.51389570332999,
-1.49580382761679,-1.4782746125791),.UNSPECIFIED.);
#798=B_SPLINE_CURVE_WITH_KNOTS('',3,(#94086,#94087,#94088,#94089,#94090,
#94091),.UNSPECIFIED.,.F.,.F.,(4,2,4),(-0.0182274268811936,-0.0134492786994115,
-0.000702675572520198),.UNSPECIFIED.);
#799=B_SPLINE_CURVE_WITH_KNOTS('',3,(#94092,#94093,#94094,#94095,#94096,
#94097,#94098,#94099,#94100,#94101,#94102,#94103,#94104,#94105,#94106,#94107,
#94108,#94109,#94110,#94111,#94112,#94113,#94114,#94115,#94116,#94117,#94118,
#94119,#94120,#94121,#94122,#94123,#94124,#94125,#94126,#94127,#94128,#94129,
#94130,#94131,#94132,#94133,#94134,#94135,#94136,#94137,#94138,#94139,#94140,
#94141,#94142,#94143,#94144,#94145,#94146,#94147,#94148,#94149,#94150,#94151,
#94152,#94153,#94154,#94155,#94156,#94157,#94158,#94159,#94160,#94161,#94162,
#94163,#94164,#94165,#94166,#94167,#94168,#94169,#94170,#94171,#94172,#94173,
#94174,#94175,#94176,#94177,#94178,#94179,#94180,#94181,#94182,#94183,#94184,
#94185,#94186,#94187,#94188,#94189,#94190,#94191,#94192,#94193,#94194,#94195,
#94196,#94197,#94198,#94199,#94200,#94201,#94202,#94203,#94204,#94205,#94206,
#94207,#94208,#94209,#94210,#94211,#94212,#94213,#94214,#94215,#94216,#94217,
#94218,#94219,#94220,#94221,#94222,#94223,#94224,#94225,#94226,#94227,#94228,
#94229,#94230,#94231,#94232,#94233,#94234,#94235,#94236,#94237,#94238,#94239,
#94240,#94241,#94242,#94243,#94244,#94245,#94246,#94247,#94248,#94249,#94250,
#94251,#94252,#94253,#94254,#94255,#94256,#94257,#94258,#94259,#94260,#94261,
#94262,#94263,#94264,#94265,#94266,#94267,#94268,#94269,#94270,#94271,#94272,
#94273,#94274,#94275,#94276,#94277,#94278,#94279,#94280,#94281,#94282,#94283,
#94284,#94285,#94286,#94287,#94288,#94289,#94290,#94291,#94292,#94293,#94294,
#94295,#94296,#94297),.UNSPECIFIED.,.F.,.F.,(4,2,2,2,2,2,2,2,2,2,2,2,2,
2,2,2,2,2,2,2,2,2,2,2,2,2,2,2,2,2,2,2,2,2,2,2,2,2,2,2,2,2,2,2,2,2,2,2,2,
2,2,2,2,2,2,2,2,2,2,2,2,2,2,2,2,2,2,2,2,2,2,2,2,2,2,2,2,2,2,2,2,2,2,2,2,
2,2,2,2,2,2,2,2,2,2,2,2,2,2,2,2,2,4),(-2.98887565051434,-2.924502732387,
-2.9116084080508,-2.90374471214077,-2.90117315191559,-2.89951043355443,
-2.89791052968358,-2.89555960578578,-2.88977701208323,-2.85291143240863,
-2.82172016481015,-2.80142529955388,-2.79275082837876,-2.786023203112,-2.78259492680106,
-2.77991850353311,-2.7768063029024,-2.77162327817418,-2.75374583182232,
-2.687348427526,-2.67430110292321,-2.66637058556449,-2.66379067400412,-2.6621259570535,
-2.66052705313884,-2.65818211698718,-2.65243678498901,-2.61135467233543,
-2.57276607095971,-2.55252580314062,-2.54733906489724,-2.54422577895641,
-2.54143301420749,-2.53787569303257,-2.53220431057548,-2.48534630200705,
-2.45141203101676,-2.43063988579794,-2.42717072049725,-2.42531096040646,
-2.4237521232111,-2.42179740320996,-2.4179935483166,-2.38939056749786,-2.35564728515263,
-2.3296602452943,-2.31426483236396,-2.30952922856423,-2.30651487625532,
-2.30369330975633,-2.29999132504619,-2.29169328771963,-2.23206647392036,
-2.22579654900007,-2.19653850833415,-2.19087543859783,-2.18860973878453,
-2.18700990119698,-2.18552319164231,-2.18342751216897,-2.17779417307367,
-2.13312923248987,-2.07970556899923,-2.07338163539794,-2.07002333369528,
-2.06751596896705,-2.0643606712224,-2.05898294882711,-2.03921090304679,
-1.98169539181991,-1.95824977221685,-1.95317307697667,-1.95100443971885,
-1.94942137778761,-1.94769058250375,-1.94481271288965,-1.93517823272047,
-1.85988337229967,-1.84007745313684,-1.8349261213889,-1.83182072207062,
-1.82902654434142,-1.82545571894948,-1.81973905678311,-1.77608387858558,
-1.74630057633959,-1.7210332881551,-1.71576381880236,-1.71356264241937,
-1.71197442681424,-1.71025761566779,-1.70744187570374,-1.69834880242274,
-1.62245283417048,-1.60934495296105,-1.59997468515844,-1.59604744091723,
-1.59319929301744,-1.59058991356684,-1.58706744303955,-1.5783918062132,
-1.52724399612353,-1.51202174447739),.UNSPECIFIED.);
#800=B_SPLINE_CURVE_WITH_KNOTS('',3,(#94303,#94304,#94305,#94306,#94307,
#94308,#94309,#94310,#94311,#94312,#94313,#94314,#94315,#94316,#94317,#94318,
#94319,#94320,#94321,#94322,#94323,#94324,#94325,#94326,#94327,#94328,#94329,
#94330,#94331,#94332,#94333,#94334,#94335,#94336,#94337,#94338,#94339,#94340,
#94341,#94342,#94343,#94344,#94345,#94346,#94347,#94348,#94349,#94350,#94351,
#94352,#94353,#94354,#94355,#94356,#94357,#94358,#94359,#94360,#94361,#94362,
#94363,#94364,#94365,#94366,#94367,#94368,#94369,#94370,#94371,#94372,#94373,
#94374,#94375,#94376,#94377,#94378,#94379,#94380,#94381,#94382,#94383,#94384,
#94385,#94386,#94387,#94388,#94389,#94390,#94391,#94392,#94393,#94394,#94395,
#94396,#94397,#94398,#94399,#94400,#94401,#94402,#94403,#94404,#94405,#94406,
#94407,#94408,#94409,#94410,#94411,#94412,#94413,#94414,#94415,#94416,#94417,
#94418,#94419,#94420,#94421,#94422,#94423,#94424,#94425,#94426,#94427,#94428,
#94429,#94430,#94431,#94432,#94433,#94434,#94435,#94436,#94437,#94438,#94439,
#94440,#94441,#94442,#94443,#94444,#94445,#94446,#94447,#94448,#94449,#94450,
#94451,#94452,#94453,#94454,#94455,#94456,#94457,#94458,#94459,#94460,#94461,
#94462,#94463,#94464,#94465,#94466,#94467,#94468,#94469,#94470,#94471,#94472,
#94473,#94474,#94475,#94476,#94477,#94478,#94479,#94480,#94481,#94482,#94483,
#94484,#94485,#94486,#94487,#94488,#94489,#94490,#94491,#94492,#94493,#94494,
#94495,#94496,#94497,#94498,#94499,#94500,#94501,#94502,#94503,#94504,#94505,
#94506,#94507,#94508,#94509,#94510,#94511,#94512,#94513,#94514),
 .UNSPECIFIED.,.F.,.F.,(4,2,2,2,2,2,2,2,2,2,2,2,2,2,2,2,2,2,2,2,2,2,2,2,
2,2,2,2,2,2,2,2,2,2,2,2,2,2,2,2,2,2,2,2,2,2,2,2,2,2,2,2,2,2,2,2,2,2,2,2,
2,2,2,2,2,2,2,2,2,2,2,2,2,2,2,2,2,2,2,2,2,2,2,2,2,2,2,2,2,2,2,2,2,2,2,2,
2,2,2,2,2,2,2,2,2,4),(-1.47775839119131,-1.4611779278763,-1.41924546235713,
-1.38795686037687,-1.38415872913402,-1.38222151583026,-1.38068473641341,
-1.37886251446716,-1.37549436186771,-1.35635671360715,-1.29265286538653,
-1.27212884030762,-1.26680917396854,-1.26366473802928,-1.26092356717381,
-1.25753666538795,-1.25093058139933,-1.20594092436458,-1.15599682897976,
-1.15440641496971,-1.14789817105003,-1.14545039208858,-1.14399134575219,
-1.14241063578823,-1.14015623704611,-1.13444097310608,-1.12605307584872,
-1.06320357555216,-1.0354849517325,-1.03019731993654,-1.02678271786948,
-1.02403943531407,-1.02091467672117,-1.0155456064936,-0.9921090339615,-0.937125568051097,
-0.926871617136693,-0.912026020893665,-0.909049117047158,-0.907138680987286,
-0.905603173256661,-0.903758575493711,-0.90028502239137,-0.878417209564425,
-0.845194532079808,-0.798648930300137,-0.79303062573563,-0.789515714665283,
-0.786762431963749,-0.783699934362523,-0.778614880008762,-0.759041904507518,
-0.686483927225724,-0.674144929703243,-0.671065463761088,-0.66928760085356,
-0.667900154196183,-0.665982939097033,-0.662159274111292,-0.65717523893782,
-0.645295636299193,-0.594038544143118,-0.5608257336881,-0.555336689632327,
-0.551860436297277,-0.549110945961338,-0.546024982760459,-0.540834749594743,
-0.51993979883592,-0.478969588224529,-0.440842122753212,-0.43507618958467,
-0.432747112309301,-0.431310303621506,-0.429707082188517,-0.427340519604145,
-0.420875072259536,-0.410984444704404,-0.375956862431396,-0.327644102324335,
-0.318942327777471,-0.315443707571479,-0.312864664618153,-0.31006216422699,
-0.306221221296459,-0.297483189667764,-0.285305251943957,-0.221868465436772,
-0.217342998222484,-0.199726635508437,-0.196592772698569,-0.19463436611401,
-0.193095842780582,-0.191639337613152,-0.188903092060043,-0.178963690163551,
-0.160699276119067,-0.133760562345111,-0.0860423214136049,-0.0804145980755769,
-0.0768963544657262,-0.0741420414966949,-0.0710800240874364,-0.0659995859047076,
-0.0599518565472093,-0.000705108085373342),.UNSPECIFIED.);
#801=B_SPLINE_CURVE_WITH_KNOTS('',3,(#94515,#94516,#94517,#94518),
 .UNSPECIFIED.,.F.,.F.,(4,4),(-2.99015346847395,-2.97297727746947),
 .UNSPECIFIED.);
#802=B_SPLINE_CURVE_WITH_KNOTS('',3,(#94519,#94520,#94521,#94522,#94523,
#94524,#94525,#94526,#94527,#94528,#94529,#94530,#94531,#94532,#94533,#94534,
#94535,#94536,#94537,#94538,#94539,#94540,#94541,#94542,#94543,#94544,#94545,
#94546,#94547,#94548,#94549,#94550,#94551,#94552,#94553,#94554,#94555,#94556,
#94557,#94558,#94559,#94560,#94561,#94562,#94563,#94564,#94565,#94566,#94567,
#94568,#94569,#94570,#94571,#94572,#94573,#94574,#94575,#94576,#94577,#94578,
#94579,#94580,#94581,#94582,#94583,#94584,#94585,#94586,#94587,#94588,#94589,
#94590,#94591,#94592,#94593,#94594,#94595,#94596,#94597,#94598,#94599,#94600,
#94601,#94602,#94603,#94604,#94605,#94606,#94607,#94608,#94609,#94610,#94611,
#94612,#94613,#94614,#94615,#94616,#94617,#94618,#94619,#94620,#94621,#94622,
#94623,#94624,#94625,#94626,#94627,#94628,#94629,#94630,#94631,#94632,#94633,
#94634,#94635,#94636,#94637,#94638,#94639,#94640,#94641,#94642,#94643,#94644,
#94645,#94646,#94647,#94648,#94649,#94650,#94651,#94652,#94653,#94654,#94655,
#94656,#94657,#94658,#94659,#94660,#94661,#94662,#94663,#94664,#94665,#94666,
#94667,#94668,#94669,#94670,#94671,#94672,#94673,#94674,#94675,#94676,#94677,
#94678,#94679,#94680,#94681,#94682,#94683,#94684,#94685,#94686,#94687,#94688,
#94689,#94690,#94691,#94692,#94693,#94694,#94695,#94696,#94697,#94698,#94699,
#94700,#94701,#94702,#94703,#94704,#94705,#94706,#94707,#94708,#94709,#94710,
#94711,#94712,#94713,#94714,#94715,#94716,#94717,#94718,#94719,#94720,#94721,
#94722,#94723,#94724,#94725,#94726,#94727,#94728,#94729,#94730,#94731,#94732,
#94733,#94734,#94735,#94736,#94737,#94738,#94739,#94740,#94741,#94742,#94743,
#94744,#94745,#94746),.UNSPECIFIED.,.F.,.F.,(4,2,2,2,2,2,2,2,2,2,2,2,2,
2,2,2,2,2,2,2,2,2,2,2,2,2,2,2,2,2,2,2,2,2,2,2,2,2,2,2,2,2,2,2,2,2,2,2,2,
2,2,2,2,2,2,2,2,2,2,2,2,2,2,2,2,2,2,2,2,2,2,2,2,2,2,2,2,2,2,2,2,2,2,2,2,
2,2,2,2,2,2,2,2,2,2,2,2,2,2,2,2,2,2,2,2,2,2,2,2,2,2,2,2,4),(-1.51202174447739,
-1.49454904547617,-1.48047647626758,-1.47723513990231,-1.47540506904566,
-1.47384419879638,-1.47185238202793,-1.46773586712831,-1.42890611890207,
-1.37057961537579,-1.3621608425291,-1.35843811289281,-1.35561371845074,
-1.35260881984386,-1.34791412522944,-1.33288540212958,-1.30780132189531,
-1.26541787817727,-1.2610243371997,-1.24348457387812,-1.24033348088928,
-1.23835577300944,-1.23679598327268,-1.23495547551074,-1.23157518761894,
-1.212916632683,-1.15447851769646,-1.12903790133968,-1.12331786150973,-1.12005434928619,
-1.11755551154115,-1.11432301604353,-1.10858765767323,-1.0796058035442,
-1.04353236837729,-1.03032647780455,-1.02184158158486,-1.00598788047094,
-1.00292536993841,-1.00097462449748,-0.999416446127392,-0.997554476047233,
-0.994073212571871,-0.97295471418744,-0.939315910191897,-0.892652793814085,
-0.886965413263028,-0.883403850123935,-0.880611361153735,-0.87750210641738,
-0.872330885185528,-0.852270457105418,-0.772842320038168,-0.766649953058824,
-0.7642308084342,-0.762762865528405,-0.761147214997645,-0.758798621887785,
-0.752595231872824,-0.74327471609675,-0.711977772137954,-0.658973867250021,
-0.650371263336323,-0.646861015091463,-0.644254387368612,-0.64140309232168,
-0.63746021466311,-0.627997588604397,-0.614719458818356,-0.53878994188948,
-0.52991546547017,-0.527125223894997,-0.525413832246053,-0.523822707501726,
-0.521606177441953,-0.516246404653856,-0.490106156189358,-0.45024763806163,
-0.417348804721315,-0.411819486184611,-0.408304694585921,-0.405515957460026,
-0.402376289526936,-0.397071119966351,-0.37529378405299,-0.33121177996708,
-0.317697977874013,-0.30997757874266,-0.293670360335373,-0.290581576561852,
-0.288622337688618,-0.287063039614836,-0.285206446211447,-0.281973279058032,
-0.264981414398109,-0.21866767413947,-0.180202739992224,-0.174526968883625,
-0.170968009066002,-0.168174669778125,-0.165061479275423,-0.16184120849513,
-0.150894364641724,-0.119680003097134,-0.0931455658162746,-0.0915427925875306,
-0.057017804551295,-0.0531777008401065,-0.0512150774252604,-0.0496556400471943,
-0.0478019023790041,-0.0458209384900077,-0.0426901689906602,-0.0178547436485936),
 .UNSPECIFIED.);
#803=B_SPLINE_CURVE_WITH_KNOTS('',3,(#94751,#94752,#94753,#94754,#94755,
#94756,#94757,#94758,#94759,#94760,#94761,#94762,#94763,#94764,#94765,#94766,
#94767,#94768,#94769,#94770,#94771,#94772,#94773,#94774,#94775,#94776,#94777,
#94778,#94779,#94780,#94781,#94782,#94783,#94784,#94785,#94786,#94787,#94788,
#94789,#94790,#94791,#94792,#94793,#94794,#94795,#94796,#94797,#94798,#94799,
#94800,#94801,#94802,#94803,#94804,#94805,#94806,#94807,#94808,#94809,#94810,
#94811,#94812,#94813,#94814,#94815,#94816,#94817,#94818,#94819,#94820,#94821,
#94822,#94823,#94824,#94825,#94826,#94827,#94828,#94829,#94830,#94831,#94832,
#94833,#94834,#94835,#94836,#94837,#94838,#94839,#94840,#94841,#94842,#94843,
#94844,#94845,#94846,#94847,#94848,#94849,#94850,#94851,#94852,#94853,#94854,
#94855,#94856,#94857,#94858,#94859,#94860,#94861,#94862,#94863,#94864,#94865,
#94866,#94867,#94868,#94869,#94870,#94871,#94872,#94873,#94874,#94875,#94876,
#94877,#94878,#94879,#94880,#94881,#94882,#94883,#94884,#94885,#94886,#94887,
#94888,#94889,#94890,#94891,#94892,#94893,#94894,#94895,#94896,#94897,#94898,
#94899,#94900,#94901,#94902,#94903,#94904,#94905,#94906,#94907,#94908,#94909,
#94910,#94911,#94912,#94913,#94914,#94915,#94916,#94917,#94918,#94919,#94920,
#94921,#94922,#94923,#94924,#94925,#94926,#94927,#94928,#94929,#94930,#94931,
#94932,#94933,#94934,#94935,#94936,#94937,#94938,#94939,#94940,#94941,#94942,
#94943,#94944,#94945,#94946,#94947,#94948,#94949,#94950,#94951,#94952,#94953,
#94954,#94955,#94956,#94957,#94958,#94959,#94960,#94961,#94962,#94963,#94964,
#94965,#94966,#94967,#94968,#94969,#94970,#94971,#94972,#94973,#94974,#94975,
#94976,#94977,#94978),.UNSPECIFIED.,.F.,.F.,(4,2,2,2,2,2,2,2,2,2,2,2,2,
2,2,2,2,2,2,2,2,2,2,2,2,2,2,2,2,2,2,2,2,2,2,2,2,2,2,2,2,2,2,2,2,2,2,2,2,
2,2,2,2,2,2,2,2,2,2,2,2,2,2,2,2,2,2,2,2,2,2,2,2,2,2,2,2,2,2,2,2,2,2,2,2,
2,2,2,2,2,2,2,2,2,2,2,2,2,2,2,2,2,2,2,2,2,2,2,2,2,2,2,2,4),(-2.97195118185969,
-2.9369490547122,-2.93226175452182,-2.92910505028776,-2.92604856518349,
-2.92329348615702,-2.91976631159245,-2.91410805118695,-2.87171596726723,
-2.84438886087576,-2.81388158733176,-2.81200237225385,-2.80897499325155,
-2.80714019892494,-2.80560398575201,-2.80368154244454,-2.80066588080868,
-2.78516978194972,-2.78288127370539,-2.77840688596625,-2.71511747190682,
-2.70283392999893,-2.69400861379573,-2.69016861850486,-2.68736648366754,
-2.68478754184567,-2.68128869912165,-2.67258455885489,-2.62442157915607,
-2.58924068632587,-2.57932654774481,-2.57285044962834,-2.57048248913528,
-2.5688790775123,-2.5674426679379,-2.56511530173446,-2.55935890187728,-2.52133832720534,
-2.48032483337261,-2.45941782231408,-2.45422698257092,-2.45114101134447,
-2.44839173050279,-2.44491603522207,-2.43942840241542,-2.40626182341202,
-2.35492215363733,-2.34303259120955,-2.3380459607788,-2.33422100921978,
-2.33230358111693,-2.33091616954396,-2.32913859240383,-2.32606019634413,
-2.31373242493805,-2.24120266433382,-2.22163486114178,-2.21655023855645,
-2.21348780229,-2.21073444624916,-2.20721926499839,-2.20160011642017,-2.15499582423271,
-2.12166369863531,-2.09990151012898,-2.09643142233339,-2.094587532026,-2.09305195578115,
-2.09114061966151,-2.08816088627562,-2.07326734853567,-2.06315909275528,
-2.00813713993986,-1.98469587966175,-1.97932644762113,-1.97620152933803,
-1.9734581344623,-1.97004342940281,-1.96475566167598,-1.93705056922101,
-1.87420237739287,-1.86577185686649,-1.86003505377718,-1.85777716225911,
-1.85619569101364,-1.85473728171475,-1.85269776521772,-1.84734106505971,
-1.79758790832624,-1.74910404224857,-1.74260775703456,-1.73924307800478,
-1.73650306472142,-1.7333412604279,-1.72794682195026,-1.70650610604253,
-1.64943223513945,-1.63283852572199,-1.62658239155219,-1.62201633952051,
-1.61995631612376,-1.61840739531866,-1.61666560062987,-1.61366749514505,
-1.60262207004701,-1.53561223692235,-1.50985417869354,-1.50434232731809,
-1.5011862949276,-1.49844594424172,-1.49507404219208,-1.48854212004445,
-1.48025519169541,-1.47775839119131),.UNSPECIFIED.);
#804=B_SPLINE_CURVE_WITH_KNOTS('',3,(#94980,#94981,#94982,#94983),
 .UNSPECIFIED.,.F.,.F.,(4,4),(-0.0178547436485936,-0.00070312019684868),
 .UNSPECIFIED.);
#805=B_SPLINE_CURVE_WITH_KNOTS('',3,(#94984,#94985,#94986,#94987,#94988,
#94989,#94990,#94991,#94992,#94993,#94994,#94995,#94996,#94997,#94998,#94999,
#95000,#95001,#95002,#95003,#95004,#95005,#95006,#95007,#95008,#95009,#95010,
#95011,#95012,#95013,#95014,#95015,#95016,#95017,#95018,#95019,#95020,#95021,
#95022,#95023,#95024,#95025,#95026,#95027,#95028,#95029,#95030,#95031,#95032,
#95033,#95034,#95035,#95036,#95037,#95038,#95039,#95040,#95041,#95042,#95043,
#95044,#95045,#95046,#95047,#95048,#95049,#95050,#95051,#95052,#95053,#95054,
#95055,#95056,#95057,#95058,#95059,#95060,#95061,#95062,#95063,#95064,#95065,
#95066,#95067,#95068,#95069,#95070,#95071,#95072,#95073,#95074,#95075,#95076,
#95077,#95078,#95079,#95080,#95081,#95082,#95083,#95084,#95085,#95086,#95087,
#95088,#95089,#95090,#95091,#95092,#95093,#95094,#95095,#95096,#95097,#95098,
#95099,#95100,#95101,#95102,#95103,#95104,#95105,#95106,#95107,#95108,#95109,
#95110,#95111,#95112,#95113,#95114,#95115,#95116,#95117,#95118,#95119,#95120,
#95121,#95122,#95123,#95124,#95125,#95126,#95127,#95128,#95129,#95130,#95131,
#95132,#95133,#95134,#95135,#95136,#95137,#95138,#95139,#95140,#95141,#95142,
#95143,#95144,#95145,#95146,#95147,#95148,#95149,#95150,#95151,#95152,#95153,
#95154,#95155,#95156,#95157,#95158,#95159,#95160,#95161,#95162,#95163,#95164,
#95165,#95166,#95167,#95168,#95169,#95170,#95171,#95172,#95173,#95174,#95175,
#95176,#95177,#95178,#95179,#95180,#95181,#95182,#95183,#95184,#95185,#95186,
#95187,#95188,#95189,#95190,#95191,#95192,#95193,#95194,#95195,#95196,#95197),
 .UNSPECIFIED.,.F.,.F.,(4,2,2,2,2,2,2,2,2,2,2,2,2,2,2,2,2,2,2,2,2,2,2,2,
2,2,2,2,2,2,2,2,2,2,2,2,2,2,2,2,2,2,2,2,2,2,2,2,2,2,2,2,2,2,2,2,2,2,2,2,
2,2,2,2,2,2,2,2,2,2,2,2,2,2,2,2,2,2,2,2,2,2,2,2,2,2,2,2,2,2,2,2,2,2,2,2,
2,2,2,2,2,2,2,2,2,2,4),(-2.98816441937799,-2.94356845749968,-2.92995261709646,
-2.92561308819106,-2.92170371885123,-2.91886101117686,-2.91625140995095,
-2.91272072754498,-2.90398440736828,-2.85659656848203,-2.82107533596852,
-2.80612646805003,-2.8030567042658,-2.80122445450541,-2.79966564044199,
-2.7976814659872,-2.79450556971702,-2.77639981707171,-2.7258598640443,-2.70374524833081,
-2.69455564951707,-2.68755673914181,-2.68400531139556,-2.68121618627363,
-2.67810593514233,-2.67292183735761,-2.65499867934137,-2.59028462549177,
-2.56946381304208,-2.5659958438401,-2.56413762103748,-2.56258059896764,
-2.56062881791686,-2.55756019794813,-2.54156297305539,-2.53342368024984,
-2.478054108746,-2.45452058110026,-2.44909850677268,-2.44593588457654,-2.44315470177134,
-2.43968634307538,-2.43430155823529,-2.4052501969039,-2.35036330524257,
-2.33212389796571,-2.3287649428226,-2.32692997772095,-2.3253711725584,-2.32338997682959,
-2.32022444583021,-2.30234234717104,-2.28172950497194,-2.24463311279488,
-2.22688011892884,-2.21896889385078,-2.21265736295332,-2.20930391364666,
-2.20679943500284,-2.20364679990158,-2.19827121263619,-2.17847615589279,
-2.11426408838042,-2.1013527822919,-2.0934834627502,-2.09091248942569,-2.08925076484646,
-2.08765234661296,-2.08530442556419,-2.07953330766194,-2.04215632577042,
-2.00088836693657,-1.98701845046527,-1.97723724975104,-1.97324470036676,
-1.97038614143557,-1.96779227443219,-1.96367749198135,-1.95603375647796,
-1.89852665416244,-1.8621035047574,-1.8558259994071,-1.85346765045097,-1.85185100906884,
-1.85038660168186,-1.84837219642747,-1.84327982078029,-1.79085276816924,
-1.76496169687726,-1.74281978611869,-1.73749235527656,-1.73434993836325,
-1.73156515427559,-1.7280638975639,-1.72257261421912,-1.69069730093992,
-1.62708123617219,-1.61908060655544,-1.61649349393351,-1.61482803034779,
-1.61323174362351,-1.61089578481211,-1.60519811378123,-1.56236171378938,
-1.54229641354551,-1.51864233044459,-1.5126710689066),.UNSPECIFIED.);
#806=B_SPLINE_CURVE_WITH_KNOTS('',3,(#95203,#95204,#95205,#95206,#95207,
#95208,#95209,#95210,#95211,#95212,#95213,#95214,#95215,#95216,#95217,#95218,
#95219,#95220,#95221,#95222,#95223,#95224,#95225,#95226,#95227,#95228,#95229,
#95230,#95231,#95232,#95233,#95234,#95235,#95236,#95237,#95238,#95239,#95240,
#95241,#95242,#95243,#95244,#95245,#95246,#95247,#95248,#95249,#95250,#95251,
#95252,#95253,#95254,#95255,#95256,#95257,#95258,#95259,#95260,#95261,#95262,
#95263,#95264,#95265,#95266,#95267,#95268,#95269,#95270,#95271,#95272,#95273,
#95274,#95275,#95276,#95277,#95278,#95279,#95280,#95281,#95282,#95283,#95284,
#95285,#95286,#95287,#95288,#95289,#95290,#95291,#95292,#95293,#95294,#95295,
#95296,#95297,#95298,#95299,#95300,#95301,#95302,#95303,#95304,#95305,#95306,
#95307,#95308,#95309,#95310,#95311,#95312,#95313,#95314,#95315,#95316,#95317,
#95318,#95319,#95320,#95321,#95322,#95323,#95324,#95325,#95326,#95327,#95328,
#95329,#95330,#95331,#95332,#95333,#95334,#95335,#95336,#95337,#95338,#95339,
#95340,#95341,#95342,#95343,#95344,#95345,#95346,#95347,#95348,#95349,#95350,
#95351,#95352,#95353,#95354,#95355,#95356,#95357,#95358,#95359,#95360,#95361,
#95362,#95363,#95364,#95365,#95366,#95367,#95368,#95369,#95370,#95371,#95372,
#95373,#95374,#95375,#95376,#95377,#95378,#95379,#95380,#95381,#95382,#95383,
#95384,#95385,#95386,#95387,#95388,#95389,#95390,#95391,#95392,#95393,#95394,
#95395,#95396,#95397,#95398,#95399,#95400,#95401,#95402,#95403,#95404,#95405,
#95406,#95407,#95408,#95409,#95410),.UNSPECIFIED.,.F.,.F.,(4,2,2,2,2,2,
2,2,2,2,2,2,2,2,2,2,2,2,2,2,2,2,2,2,2,2,2,2,2,2,2,2,2,2,2,2,2,2,2,2,2,2,
2,2,2,2,2,2,2,2,2,2,2,2,2,2,2,2,2,2,2,2,2,2,2,2,2,2,2,2,2,2,2,2,2,2,2,2,
2,2,2,2,2,2,2,2,2,2,2,2,2,2,2,2,2,2,2,2,2,2,2,2,2,4),(-1.47746825606646,
-1.47709627062028,-1.47209694916288,-1.44909236909339,-1.39051927519349,
-1.37113071817875,-1.36583512835576,-1.36272662260841,-1.36025606675236,
-1.35694695811006,-1.35071707483464,-1.30060828375161,-1.25211572248421,
-1.24667659591132,-1.24462642346029,-1.24316532322844,-1.24158644242032,
-1.23934132486027,-1.23368453375267,-1.20415745200467,-1.15601140840689,
-1.13403220163634,-1.12859984754024,-1.12542958831988,-1.12269054298271,
-1.11933754787313,-1.11289693191768,-1.06253539433096,-1.01467415296095,
-1.00920915638578,-1.00715548421374,-1.00569338472111,-1.00411509121056,
-1.00187354789131,-0.996239986142577,-0.966964557799699,-0.957057943040063,
-0.901504238793805,-0.893067141873779,-0.889614134086156,-0.887046719413081,
-0.88423539516573,-0.880342970013861,-0.870982853562216,-0.857846035403174,
-0.780930925816261,-0.77252883090844,-0.769819827658108,-0.768142060505955,
-0.766570123362722,-0.764364736072971,-0.758958064051164,-0.697625271886426,
-0.660150085066973,-0.654543497433236,-0.65103175909567,-0.648278389114548,
-0.645213141002927,-0.640117271690002,-0.62042043620004,-0.546354932893747,
-0.535405917794819,-0.532416574712538,-0.530676412952253,-0.529126522577678,
-0.527061956296651,-0.522472915608532,-0.516177212879489,-0.499429108935249,
-0.441627794874962,-0.421031982487848,-0.415705145876597,-0.412558268467668,
-0.409816072336617,-0.406429323415642,-0.399828132120443,-0.35504187528113,
-0.329502828303619,-0.299292561881776,-0.295503193983947,-0.29356747120792,
-0.29203029848529,-0.290205750324685,-0.287039153145369,-0.27053520969566,
-0.226969864796906,-0.185050931584614,-0.179396039097259,-0.175869509344014,
-0.173114060955056,-0.170056271022691,-0.166897805205537,-0.156299319948201,
-0.127170685538684,-0.101402950954814,-0.0616978449188197,-0.0579506763742791,
-0.0560239940333789,-0.0544873128780441,-0.0526554164545771,-0.0506965542130373,
-0.0475960528900393,-0.0415486408128117,-0.00070472459549365),
 .UNSPECIFIED.);
#807=B_SPLINE_CURVE_WITH_KNOTS('',3,(#95411,#95412,#95413,#95414),
 .UNSPECIFIED.,.F.,.F.,(4,4),(-2.98953857001745,-2.97195118185969),
 .UNSPECIFIED.);
#808=B_SPLINE_CURVE_WITH_KNOTS('',3,(#95415,#95416,#95417,#95418,#95419,
#95420,#95421,#95422,#95423,#95424,#95425,#95426,#95427,#95428,#95429,#95430,
#95431,#95432,#95433,#95434,#95435,#95436,#95437,#95438,#95439,#95440,#95441,
#95442,#95443,#95444,#95445,#95446,#95447,#95448,#95449,#95450,#95451,#95452,
#95453,#95454,#95455,#95456,#95457,#95458,#95459,#95460,#95461,#95462,#95463,
#95464,#95465,#95466,#95467,#95468,#95469,#95470,#95471,#95472,#95473,#95474,
#95475,#95476,#95477,#95478,#95479,#95480,#95481,#95482,#95483,#95484,#95485,
#95486,#95487,#95488,#95489,#95490,#95491,#95492,#95493,#95494,#95495,#95496,
#95497,#95498,#95499,#95500,#95501,#95502,#95503,#95504,#95505,#95506,#95507,
#95508,#95509,#95510,#95511,#95512,#95513,#95514,#95515,#95516,#95517,#95518,
#95519,#95520,#95521,#95522,#95523,#95524,#95525,#95526,#95527,#95528,#95529,
#95530,#95531,#95532,#95533,#95534,#95535,#95536,#95537,#95538,#95539,#95540,
#95541,#95542,#95543,#95544,#95545,#95546,#95547,#95548,#95549,#95550,#95551,
#95552,#95553,#95554,#95555,#95556,#95557,#95558,#95559,#95560,#95561,#95562,
#95563,#95564,#95565,#95566,#95567,#95568,#95569,#95570,#95571,#95572,#95573,
#95574,#95575,#95576,#95577,#95578,#95579,#95580,#95581,#95582,#95583,#95584,
#95585,#95586,#95587,#95588,#95589,#95590,#95591,#95592,#95593,#95594,#95595,
#95596,#95597,#95598,#95599,#95600,#95601,#95602,#95603,#95604,#95605,#95606,
#95607,#95608,#95609,#95610,#95611,#95612,#95613,#95614,#95615,#95616,#95617,
#95618,#95619,#95620,#95621,#95622,#95623,#95624,#95625,#95626),
 .UNSPECIFIED.,.F.,.F.,(4,2,2,2,2,2,2,2,2,2,2,2,2,2,2,2,2,2,2,2,2,2,2,2,
2,2,2,2,2,2,2,2,2,2,2,2,2,2,2,2,2,2,2,2,2,2,2,2,2,2,2,2,2,2,2,2,2,2,2,2,
2,2,2,2,2,2,2,2,2,2,2,2,2,2,2,2,2,2,2,2,2,2,2,2,2,2,2,2,2,2,2,2,2,2,2,2,
2,2,2,2,2,2,2,2,2,4),(-1.5126710689066,-1.50902900777726,-1.50166488034743,
-1.49809872716826,-1.49530672181284,-1.49220220991738,-1.48704876977966,
-1.46718852130175,-1.39101341317623,-1.38216756132172,-1.37938191037392,
-1.37767227012861,-1.37608193812814,-1.37386531542221,-1.36849960589727,
-1.31047961773172,-1.2699440296854,-1.2642510525941,-1.26068822557359,-1.25789613057838,
-1.25478874285753,-1.24962399348292,-1.22963356587977,-1.15141395098973,
-1.14427581272797,-1.14171299607487,-1.14021747513831,-1.13862473547355,
-1.13639587950957,-1.13095769957971,-1.10402316342254,-1.07807015851243,
-1.03253510520935,-1.02683637259012,-1.02327131396667,-1.02047831652466,
-1.01737079676933,-1.01220788206989,-0.992251840888327,-0.914684047025733,
-0.906987746394055,-0.904347839999176,-0.902836811919838,-0.901252426853539,
-0.899074679307156,-0.893943939462053,-0.86999723419399,-0.809797496904229,
-0.792799560897511,-0.787708460028692,-0.784616337296652,-0.781819307729638,
-0.778224216072073,-0.770717423751258,-0.742093109111218,-0.69515724074363,
-0.687180457292685,-0.671025128574803,-0.667945051528449,-0.665988693212269,
-0.664429872060102,-0.662571692219192,-0.659109636481321,-0.638513782347949,
-0.604483258052994,-0.557618787560536,-0.551934980463562,-0.548374014816828,
-0.545580979119142,-0.542470067262867,-0.537293615108414,-0.517179730856772,
-0.444484243736937,-0.432939215277158,-0.429866574029808,-0.42809261411862,
-0.426679611725878,-0.424687958781014,-0.420574238647885,-0.415121977240386,
-0.35140648672764,-0.319705044798057,-0.314215513623113,-0.310712992975402,
-0.307925707943216,-0.304778878344555,-0.299440071282056,-0.277535166898882,
-0.230267609507277,-0.196858781148106,-0.193018486480805,-0.191055880367547,
-0.189496517683828,-0.188014097360527,-0.185240673862887,-0.174870888381879,
-0.155486013627489,-0.128300830884341,-0.0826822284841619,-0.0769900749504804,
-0.0734263033018798,-0.0706325653283003,-0.0675224178842369,-0.062350886356143,
-0.0561881268009385,-0.0182968368378989),.UNSPECIFIED.);
#809=B_SPLINE_CURVE_WITH_KNOTS('',3,(#95631,#95632,#95633,#95634,#95635,
#95636,#95637,#95638,#95639,#95640,#95641,#95642,#95643,#95644,#95645,#95646,
#95647,#95648,#95649,#95650,#95651,#95652,#95653,#95654,#95655,#95656,#95657,
#95658,#95659,#95660,#95661,#95662,#95663,#95664,#95665,#95666,#95667,#95668,
#95669,#95670,#95671,#95672,#95673,#95674,#95675,#95676,#95677,#95678,#95679,
#95680,#95681,#95682,#95683,#95684,#95685,#95686,#95687,#95688,#95689,#95690,
#95691,#95692,#95693,#95694,#95695,#95696,#95697,#95698,#95699,#95700,#95701,
#95702,#95703,#95704,#95705,#95706,#95707,#95708,#95709,#95710,#95711,#95712,
#95713,#95714,#95715,#95716,#95717,#95718,#95719,#95720,#95721,#95722,#95723,
#95724,#95725,#95726,#95727,#95728,#95729,#95730,#95731,#95732,#95733,#95734,
#95735,#95736,#95737,#95738,#95739,#95740,#95741,#95742,#95743,#95744,#95745,
#95746,#95747,#95748,#95749,#95750,#95751,#95752,#95753,#95754,#95755,#95756,
#95757,#95758,#95759,#95760,#95761,#95762,#95763,#95764,#95765,#95766,#95767,
#95768,#95769,#95770,#95771,#95772,#95773,#95774,#95775,#95776,#95777,#95778,
#95779,#95780,#95781,#95782,#95783,#95784,#95785,#95786,#95787,#95788,#95789,
#95790,#95791,#95792,#95793,#95794,#95795,#95796,#95797,#95798,#95799,#95800,
#95801,#95802,#95803,#95804,#95805,#95806,#95807,#95808,#95809,#95810,#95811,
#95812,#95813,#95814,#95815,#95816,#95817,#95818,#95819,#95820,#95821,#95822,
#95823,#95824,#95825,#95826,#95827,#95828,#95829,#95830,#95831,#95832,#95833,
#95834,#95835,#95836,#95837,#95838,#95839,#95840,#95841,#95842,#95843,#95844,
#95845,#95846,#95847,#95848,#95849,#95850,#95851,#95852,#95853,#95854,#95855,
#95856,#95857,#95858,#95859,#95860,#95861,#95862,#95863,#95864,#95865,#95866,
#95867,#95868,#95869,#95870,#95871,#95872,#95873,#95874,#95875,#95876,#95877,
#95878,#95879,#95880,#95881,#95882),.UNSPECIFIED.,.F.,.F.,(4,2,2,2,2,2,
2,2,2,2,2,2,2,2,2,2,2,2,2,2,2,2,2,2,2,2,2,2,2,2,2,2,2,2,2,2,2,2,2,2,2,2,
2,2,2,2,2,2,2,2,2,2,2,2,2,2,2,2,2,2,2,2,2,2,2,2,2,2,2,2,2,2,2,2,2,2,2,2,
2,2,2,2,2,2,2,2,2,2,2,2,2,2,2,2,2,2,2,2,2,2,2,2,2,2,2,2,2,2,2,2,2,2,2,2,
2,2,2,2,2,2,2,2,2,2,2,4),(-2.97105222820656,-2.92530151267993,-2.91538079316817,
-2.90890247926954,-2.90653503873986,-2.90493237564454,-2.90349693776976,
-2.90117170463306,-2.895423370209,-2.85808058991527,-2.82613219202151,-2.80650998840188,
-2.7980623344165,-2.79149927038503,-2.78813138876897,-2.78808881943302,
-2.78804466416076,-2.78799882046067,-2.78795117695518,-2.78790161241877,
-2.78784999467852,-2.78779617937313,-2.7877400085451,-2.78768130904727,
-2.78761989071349,-2.78758617227167,-2.78754414668624,-2.78749157245197,
-2.78742549492871,-2.78734195753053,-2.78723555921924,-2.78448544777219,
-2.78098941248966,-2.77543107034222,-2.74046848892012,-2.69085164613979,
-2.67336026453325,-2.67006853388269,-2.66826319041914,-2.66672570013493,
-2.66476845273363,-2.66163617456593,-2.64387132620129,-2.62275903217099,
-2.59396029863855,-2.55950270680088,-2.55359849283462,-2.55035866590881,
-2.54789394517402,-2.54473057676797,-2.53932562865379,-2.51771679613077,
-2.46082157020576,-2.44426799892404,-2.43802286764056,-2.43346348980179,
-2.43140522404205,-2.42985709387879,-2.42811560093025,-2.42511671889659,
-2.41405442068574,-2.36690267704485,-2.3225272142909,-2.31637118902119,
-2.31307801114676,-2.31036803877725,-2.30715908430598,-2.30155446291995,
-2.27707308805575,-2.21742480722635,-2.20484233231857,-2.19965751723748,
-2.19571402444066,-2.19377329846871,-2.19223673643475,-2.19041830635657,
-2.18715890214725,-2.17237776118083,-2.16209775319349,-2.1071384565206,
-2.08371233434017,-2.07834506624147,-2.07522121730192,-2.07247864731743,
-2.06906482003752,-2.06377812615093,-2.03606778559913,-1.97321740707834,
-1.96481064081507,-1.95908646828845,-1.95683096579821,-1.95525030031179,
-1.95379194259511,-1.95175156690936,-1.94638537858148,-1.89678922401156,
-1.84773390010898,-1.84151491598415,-1.83820832487275,-1.83573824803327,
-1.83262851463997,-1.82732628710088,-1.80785737019362,-1.74302629120196,
-1.73010072077122,-1.7222462694604,-1.719698500221,-1.71805673138258,-1.7164827103165,
-1.71418047346966,-1.70857297528363,-1.66375602990719,-1.61032566586255,
-1.6040541270702,-1.60073639625711,-1.59826510340564,-1.59516314800567,
-1.58989712492058,-1.57068800126628,-1.51200201039136,-1.49475244590984,
-1.48532634065609,-1.48249699836122,-1.48079283551505,-1.47923295084144,
-1.47746825606646),.UNSPECIFIED.);
#810=B_SPLINE_CURVE_WITH_KNOTS('',3,(#95884,#95885,#95886,#95887),
 .UNSPECIFIED.,.F.,.F.,(4,4),(-0.0182968368378989,-0.000703552307223293),
 .UNSPECIFIED.);
#811=B_SPLINE_CURVE_WITH_KNOTS('',3,(#95888,#95889,#95890,#95891,#95892,
#95893,#95894,#95895,#95896,#95897,#95898),.UNSPECIFIED.,.F.,.F.,(4,1,1,
1,1,1,1,1,4),(116.238928182822,116.441517666285,117.439865140746,118.438212615208,
119.43656008967,120.434907564131,121.433255038593,122.431602513054,122.449185868852),
 .UNSPECIFIED.);
#812=B_SPLINE_CURVE_WITH_KNOTS('',3,(#95904,#95905,#95906,#95907,#95908,
#95909,#95910,#95911,#95912,#95913,#95914,#95915,#95916,#95917,#95918,#95919,
#95920,#95921,#95922,#95923,#95924,#95925,#95926,#95927,#95928,#95929,#95930,
#95931,#95932,#95933,#95934,#95935,#95936,#95937,#95938,#95939,#95940,#95941,
#95942,#95943,#95944,#95945,#95946,#95947,#95948,#95949,#95950,#95951,#95952,
#95953,#95954,#95955,#95956,#95957,#95958,#95959,#95960,#95961,#95962,#95963,
#95964,#95965,#95966,#95967,#95968,#95969,#95970,#95971,#95972,#95973,#95974,
#95975,#95976,#95977,#95978,#95979,#95980,#95981,#95982,#95983,#95984,#95985,
#95986,#95987,#95988,#95989,#95990,#95991,#95992,#95993,#95994,#95995,#95996,
#95997,#95998,#95999,#96000,#96001,#96002,#96003,#96004,#96005,#96006,#96007,
#96008,#96009,#96010,#96011,#96012,#96013,#96014,#96015,#96016,#96017,#96018,
#96019,#96020,#96021,#96022,#96023,#96024,#96025,#96026,#96027,#96028,#96029,
#96030,#96031,#96032,#96033,#96034,#96035,#96036,#96037,#96038,#96039,#96040,
#96041,#96042,#96043,#96044,#96045,#96046,#96047,#96048,#96049,#96050,#96051,
#96052,#96053,#96054,#96055,#96056,#96057,#96058,#96059,#96060,#96061,#96062,
#96063,#96064,#96065,#96066,#96067,#96068,#96069,#96070,#96071,#96072,#96073,
#96074,#96075,#96076,#96077,#96078,#96079,#96080,#96081,#96082,#96083,#96084,
#96085,#96086,#96087,#96088,#96089,#96090,#96091,#96092,#96093,#96094,#96095,
#96096,#96097,#96098,#96099,#96100,#96101,#96102,#96103,#96104,#96105,#96106,
#96107,#96108,#96109,#96110,#96111,#96112,#96113,#96114,#96115,#96116,#96117,
#96118,#96119,#96120,#96121,#96122,#96123,#96124,#96125),.UNSPECIFIED.,
 .F.,.F.,(4,2,2,2,2,2,2,2,2,2,2,2,2,2,2,2,2,2,2,2,2,2,2,2,2,2,2,2,2,2,2,
2,2,2,2,2,2,2,2,2,2,2,2,2,2,2,2,2,2,2,2,2,2,2,2,2,2,2,2,2,2,2,2,2,2,2,2,
2,2,2,2,2,2,2,2,2,2,2,2,2,2,2,2,2,2,2,2,2,2,2,2,2,2,2,2,2,2,2,2,2,2,2,2,
2,2,2,2,2,2,2,4),(-1.47793342396516,-1.47159962187165,-1.4660379402415,
-1.46283796696356,-1.46012649238102,-1.45682034373151,-1.45060631668525,
-1.40225134133357,-1.3517649051731,-1.34646836074566,-1.34443704887868,
-1.34298079575677,-1.34139744942583,-1.33912990428269,-1.33333118643874,
-1.32478081060184,-1.26208573097235,-1.23446978938446,-1.22918575339998,
-1.22577204759006,-1.22302855875104,-1.21990256045232,-1.21452882960185,
-1.19102770864582,-1.13568054371755,-1.12673892458363,-1.11109250659368,
-1.10806886204215,-1.1061440343247,-1.10460777071771,-1.10277511142929,
-1.09935848510082,-1.07904394878322,-1.04475288864464,-0.997633447767629,
-0.992002901482155,-0.988484110867937,-0.985730120867635,-0.98266923504059,
-0.977592486795252,-0.958124846283896,-0.886799042433985,-0.873268274774364,
-0.870095825806595,-0.868296558952147,-0.866757232702543,-0.864788611259076,
-0.86070699330488,-0.822718483866519,-0.763169229744586,-0.754888630349755,
-0.751221024377858,-0.748436749114557,-0.74547328146437,-0.74084158770654,
-0.726017511987287,-0.701340221735429,-0.655861797813584,-0.636332726975957,
-0.633115482879547,-0.631132068715903,-0.629591542299174,-0.627802786050468,
-0.624591025500221,-0.608660404659928,-0.570595614235536,-0.522455439561844,
-0.516843548249632,-0.513330148149617,-0.510576502270404,-0.50751200621222,
-0.502419881557107,-0.482770413072307,-0.409315563165325,-0.397799365546918,
-0.394791582528596,-0.393029988137725,-0.391639678682922,-0.389698299193982,
-0.38575559746242,-0.380573540307272,-0.368005628469173,-0.30859069759747,
-0.300150886308403,-0.282757436445097,-0.277667586959828,-0.274603287024916,
-0.271922614699323,-0.268515172002092,-0.261724008637028,-0.252935447257296,
-0.232146904518091,-0.184801719550013,-0.177466924465691,-0.160884594063012,
-0.157809361891572,-0.155868567865602,-0.154331049681059,-0.15251042605993,
-0.149151659557329,-0.130252418459665,-0.0770446139636898,-0.0588631097972616,
-0.0445357484533284,-0.0397921013985291,-0.0368039172630358,-0.0341622528282387,
-0.0314694229747601,-0.027975389799477,-0.0183619817347547,-0.000704113525364955),
 .UNSPECIFIED.);
#813=B_SPLINE_CURVE_WITH_KNOTS('',3,(#96126,#96127,#96128,#96129),
 .UNSPECIFIED.,.F.,.F.,(4,4),(-2.9882406571501,-2.97105222820656),
 .UNSPECIFIED.);
#814=B_SPLINE_CURVE_WITH_KNOTS('',3,(#96131,#96132,#96133,#96134),
 .UNSPECIFIED.,.F.,.F.,(4,4),(122.449185868852,122.522113490002),
 .UNSPECIFIED.);
#815=B_SPLINE_CURVE_WITH_KNOTS('',3,(#96135,#96136,#96137,#96138,#96139,
#96140,#96141,#96142,#96143,#96144,#96145,#96146,#96147,#96148,#96149,#96150,
#96151,#96152,#96153,#96154,#96155,#96156,#96157,#96158,#96159,#96160,#96161,
#96162,#96163,#96164,#96165,#96166,#96167,#96168,#96169,#96170,#96171,#96172,
#96173,#96174,#96175,#96176,#96177,#96178,#96179,#96180,#96181,#96182,#96183,
#96184,#96185,#96186,#96187,#96188,#96189,#96190,#96191,#96192,#96193,#96194,
#96195,#96196,#96197,#96198,#96199,#96200,#96201,#96202,#96203,#96204,#96205,
#96206,#96207,#96208,#96209,#96210,#96211,#96212,#96213,#96214,#96215,#96216,
#96217,#96218,#96219,#96220,#96221,#96222,#96223,#96224,#96225,#96226,#96227,
#96228,#96229,#96230,#96231,#96232,#96233,#96234,#96235,#96236,#96237,#96238,
#96239,#96240,#96241,#96242,#96243,#96244,#96245,#96246,#96247,#96248,#96249,
#96250,#96251,#96252,#96253,#96254,#96255,#96256,#96257,#96258,#96259,#96260,
#96261,#96262,#96263,#96264,#96265,#96266,#96267,#96268,#96269,#96270,#96271,
#96272,#96273,#96274,#96275,#96276,#96277,#96278,#96279,#96280,#96281,#96282,
#96283,#96284,#96285,#96286,#96287,#96288,#96289,#96290,#96291,#96292,#96293,
#96294,#96295,#96296,#96297,#96298,#96299,#96300,#96301,#96302,#96303,#96304,
#96305,#96306,#96307,#96308,#96309,#96310,#96311,#96312,#96313,#96314,#96315,
#96316,#96317,#96318,#96319,#96320,#96321,#96322,#96323,#96324,#96325,#96326,
#96327,#96328,#96329,#96330,#96331,#96332,#96333,#96334,#96335,#96336,#96337,
#96338,#96339,#96340,#96341,#96342),.UNSPECIFIED.,.F.,.F.,(4,2,2,2,2,2,
2,2,2,2,2,2,2,2,2,2,2,2,2,2,2,2,2,2,2,2,2,2,2,2,2,2,2,2,2,2,2,2,2,2,2,2,
2,2,2,2,2,2,2,2,2,2,2,2,2,2,2,2,2,2,2,2,2,2,2,2,2,2,2,2,2,2,2,2,2,2,2,2,
2,2,2,2,2,2,2,2,2,2,2,2,2,2,2,2,2,2,2,2,2,2,2,2,2,4),(-2.99000648890043,
-2.94584961950891,-2.91750563332864,-2.90119728980008,-2.89636597661476,
-2.89333076978242,-2.89051718050843,-2.88686488964828,-2.87884288406013,
-2.81678963173155,-2.79147746640786,-2.78325120439183,-2.77938364032968,
-2.77631785259106,-2.77453625899897,-2.7730700105066,-2.7711114424974,-2.76728997175505,
-2.73168083212128,-2.6923351469078,-2.67446276990647,-2.66263866834934,
-2.65833929055804,-2.65541792140491,-2.65257523007425,-2.64915939487085,
-2.64056774525176,-2.58418313772043,-2.54359038310803,-2.53946696465267,
-2.53747338372987,-2.53591189421763,-2.53408197125094,-2.53084296728536,
-2.51681167995195,-2.50699989596687,-2.45109292763761,-2.42745022026519,
-2.42201598502322,-2.41884816587808,-2.41606355259808,-2.41259241123449,
-2.40720618384692,-2.3782511272735,-2.32316628647195,-2.30488778050943,
-2.30152378009873,-2.29968630137048,-2.29812550910223,-2.29614197743889,
-2.29297307131489,-2.27508243189597,-2.21442327651552,-2.19005460165781,
-2.18457358753396,-2.18139552271497,-2.17861205906584,-2.17515559611704,
-2.16981747173299,-2.14203608715072,-2.08582675482622,-2.06741264787652,
-2.06404231129803,-2.06220345234582,-2.06064275690239,-2.05866097050875,
-2.05549790390484,-2.03772978845781,-1.97211757853999,-1.95198234233895,
-1.94680360034088,-1.94369182908404,-1.94089834619067,-1.93733725691012,
-1.9316541003244,-1.88461847257711,-1.85095469856973,-1.83010275215818,
-1.82663020595846,-1.8247695891278,-1.82321059541139,-1.82125638604744,
-1.81818402684617,-1.80216924694576,-1.79719936234036,-1.79068417392659,
-1.75149391529011,-1.71605893443987,-1.71006050617056,-1.70677068307643,
-1.70426830902027,-1.70105674514441,-1.6955685016196,-1.6735170599907,-1.61155431797976,
-1.59252469258765,-1.58912650580283,-1.58728162235004,-1.58572136219572,
-1.58374719215495,-1.58060947530326,-1.56336042347625,-1.55920972524322,
-1.51274127243884),.UNSPECIFIED.);
#816=B_SPLINE_CURVE_WITH_KNOTS('',3,(#96347,#96348,#96349,#96350,#96351,
#96352,#96353,#96354,#96355,#96356,#96357,#96358,#96359,#96360,#96361,#96362,
#96363,#96364,#96365,#96366,#96367,#96368,#96369,#96370,#96371,#96372,#96373,
#96374,#96375,#96376,#96377,#96378,#96379,#96380,#96381,#96382,#96383,#96384,
#96385,#96386,#96387,#96388,#96389,#96390,#96391,#96392,#96393,#96394,#96395,
#96396,#96397,#96398,#96399,#96400,#96401,#96402,#96403,#96404,#96405,#96406,
#96407,#96408,#96409,#96410,#96411,#96412,#96413,#96414,#96415,#96416,#96417,
#96418,#96419,#96420,#96421,#96422,#96423,#96424,#96425,#96426,#96427,#96428,
#96429,#96430,#96431,#96432,#96433,#96434,#96435,#96436,#96437,#96438,#96439,
#96440,#96441,#96442,#96443,#96444,#96445,#96446,#96447,#96448,#96449,#96450,
#96451,#96452,#96453,#96454,#96455,#96456,#96457,#96458,#96459,#96460,#96461,
#96462,#96463,#96464,#96465,#96466,#96467,#96468,#96469,#96470,#96471,#96472,
#96473,#96474,#96475,#96476,#96477,#96478,#96479,#96480,#96481,#96482,#96483,
#96484,#96485,#96486,#96487,#96488,#96489,#96490,#96491,#96492,#96493,#96494,
#96495,#96496,#96497,#96498,#96499,#96500,#96501,#96502,#96503,#96504,#96505,
#96506,#96507,#96508,#96509,#96510,#96511,#96512,#96513,#96514,#96515,#96516,
#96517,#96518,#96519,#96520,#96521,#96522,#96523,#96524,#96525,#96526,#96527,
#96528,#96529,#96530,#96531,#96532,#96533,#96534,#96535,#96536,#96537,#96538,
#96539,#96540,#96541,#96542,#96543,#96544,#96545,#96546,#96547,#96548,#96549,
#96550,#96551,#96552,#96553,#96554),.UNSPECIFIED.,.F.,.F.,(4,2,2,2,2,2,
2,2,2,2,2,2,2,2,2,2,2,2,2,2,2,2,2,2,2,2,2,2,2,2,2,2,2,2,2,2,2,2,2,2,2,2,
2,2,2,2,2,2,2,2,2,2,2,2,2,2,2,2,2,2,2,2,2,2,2,2,2,2,2,2,2,2,2,2,2,2,2,2,
2,2,2,2,2,2,2,2,2,2,2,2,2,2,2,2,2,2,2,2,2,2,2,2,2,4),(-2.97245970569877,
-2.92214142952578,-2.90540104299264,-2.89416444720541,-2.88998453515166,
-2.88711724732677,-2.88430654192965,-2.88026812300541,-2.87071750805123,
-2.80991567029712,-2.80366616555044,-2.78370546701035,-2.77664279248751,
-2.77318320814191,-2.77040254914006,-2.76869567365967,-2.76720286901453,
-2.76521015750593,-2.76188911393139,-2.73917838155429,-2.68275001270377,
-2.65906925382898,-2.65368384135151,-2.65055523597599,-2.64781196009358,
-2.64440178348323,-2.63912940350878,-2.6118240669353,-2.54952293218338,
-2.53600628326957,-2.53294353728047,-2.53118739644393,-2.52964148803829,
-2.52764075755106,-2.52429249396449,-2.50091202790177,-2.44508431901798,
-2.42150249536741,-2.4161231738138,-2.41299573356251,-2.41025205980173,
-2.40683953559697,-2.40155998275564,-2.37408241569683,-2.31155847385648,
-2.30278117696173,-2.29686733692576,-2.2945818746975,-2.29299488471608,
-2.29154227326443,-2.28952533861236,-2.28432614855628,-2.23288302457447,
-2.18612792754243,-2.17946190520251,-2.17606221906702,-2.17331938318625,
-2.17018254612168,-2.1648984297429,-2.14485078258701,-2.08663205782153,
-2.06971086020924,-2.06337243880631,-2.05875974429205,-2.05669098805927,
-2.05514066800377,-2.05340299282845,-2.05042444804163,-2.03958378307114,
-1.96544366575285,-1.9524356509498,-1.94314461485686,-1.93926320064969,
-1.93645352673468,-1.93388328167895,-1.93041992631652,-1.92192473051514,
-1.86727322850476,-1.82452161311394,-1.82069813992169,-1.81878092520041,
-1.81739344515303,-1.81561547293187,-1.81253570679418,-1.80019351885902,
-1.72767259544492,-1.70810452157173,-1.70301961625593,-1.6999569720883,
-1.69720340524019,-1.69368792191613,-1.68806822370022,-1.64145632923907,
-1.60811179656522,-1.5863614245952,-1.58289154700259,-1.58104761784714,
-1.57951192243395,-1.57760032957371,-1.57462000213366,-1.55971912451465,
-1.5554069349699,-1.49544486761083,-1.47793342396516),.UNSPECIFIED.);
#817=B_SPLINE_CURVE_WITH_KNOTS('',3,(#96555,#96556,#96557,#96558,#96559,
#96560,#96561,#96562,#96563,#96564,#96565,#96566,#96567,#96568,#96569,#96570,
#96571,#96572,#96573,#96574,#96575,#96576,#96577,#96578,#96579,#96580,#96581,
#96582,#96583,#96584,#96585,#96586,#96587,#96588,#96589,#96590,#96591,#96592,
#96593,#96594,#96595,#96596,#96597,#96598,#96599,#96600,#96601,#96602,#96603,
#96604,#96605,#96606,#96607,#96608,#96609,#96610,#96611,#96612,#96613,#96614,
#96615,#96616,#96617,#96618,#96619,#96620,#96621,#96622,#96623,#96624,#96625,
#96626,#96627,#96628,#96629,#96630,#96631,#96632,#96633,#96634,#96635,#96636,
#96637,#96638,#96639,#96640,#96641,#96642,#96643,#96644,#96645,#96646,#96647,
#96648,#96649,#96650,#96651,#96652,#96653,#96654,#96655,#96656,#96657,#96658,
#96659,#96660,#96661,#96662,#96663,#96664,#96665,#96666,#96667,#96668,#96669,
#96670,#96671,#96672,#96673,#96674,#96675,#96676,#96677,#96678,#96679,#96680,
#96681,#96682,#96683,#96684,#96685,#96686,#96687,#96688,#96689,#96690,#96691,
#96692,#96693,#96694,#96695,#96696,#96697,#96698,#96699,#96700,#96701,#96702,
#96703,#96704,#96705,#96706,#96707,#96708,#96709,#96710,#96711,#96712,#96713,
#96714,#96715,#96716,#96717,#96718,#96719,#96720,#96721,#96722,#96723,#96724,
#96725,#96726,#96727,#96728,#96729,#96730,#96731,#96732,#96733,#96734,#96735,
#96736,#96737,#96738,#96739,#96740,#96741,#96742,#96743,#96744,#96745,#96746,
#96747,#96748,#96749,#96750,#96751,#96752,#96753,#96754,#96755,#96756,#96757,
#96758,#96759,#96760,#96761,#96762,#96763,#96764,#96765,#96766,#96767,#96768,
#96769,#96770,#96771,#96772,#96773,#96774,#96775,#96776,#96777,#96778,#96779,
#96780,#96781,#96782,#96783,#96784,#96785,#96786,#96787,#96788,#96789,#96790,
#96791,#96792,#96793,#96794,#96795,#96796,#96797,#96798,#96799,#96800,#96801,
#96802,#96803,#96804,#96805,#96806,#96807,#96808,#96809,#96810),
 .UNSPECIFIED.,.F.,.F.,(4,2,2,2,2,2,2,2,2,2,2,2,2,2,2,2,2,2,2,2,2,2,2,2,
2,2,2,2,2,2,2,2,2,2,2,2,2,2,2,2,2,2,2,2,2,2,2,2,2,2,2,2,2,2,2,2,2,2,2,2,
2,2,2,2,2,2,2,2,2,2,2,2,2,2,2,2,2,2,2,2,2,2,2,2,2,2,2,2,2,2,2,2,2,2,2,2,
2,2,2,2,2,2,2,2,2,2,2,2,2,2,2,2,2,2,2,2,2,2,2,2,2,2,2,2,2,2,2,4),(-1.51274127243884,
-1.49549398668246,-1.47715139789912,-1.47191936647955,-1.46879576988828,
-1.46628350754593,-1.46287932608243,-1.45633549067589,-1.40341849350104,
-1.35854339385021,-1.35291250969525,-1.35081696648587,-1.34933015024703,
-1.34772995972947,-1.34546337878145,-1.33979609649977,-1.3105010996305,
-1.30598427432574,-1.24433015989774,-1.23626162848646,-1.23260049860598,
-1.22978512106834,-1.22675293215949,-1.22193708368748,-1.20578588627485,
-1.17785593043212,-1.14521375320881,-1.13837746412902,-1.13192657775694,
-1.11740099292549,-1.11412732626893,-1.11228950905734,-1.11072876593191,
-1.10874572729469,-1.1046760509969,-1.06517436595889,-1.00750043041296,
-0.999127436817403,-0.995690764935652,-0.992842645836684,-0.989927835918512,
-0.985660663950069,-0.974068680490885,-0.956670052802494,-0.92081829779567,
-0.883849468738206,-0.878065502341966,-0.875713933138073,-0.874113567733765,
-0.872450337143972,-0.86987794744299,-0.862011242166212,-0.849113273710083,
-0.785210006884101,-0.765059982366121,-0.75965734035212,-0.75649657246078,
-0.753989847298627,-0.750638761412244,-0.744349423434949,-0.694626261157236,
-0.645892577052872,-0.640451299269309,-0.638381326364837,-0.636901453009344,
-0.635296153212917,-0.633001575103994,-0.627155225252009,-0.618543660064297,
-0.555722423090365,-0.528472500800093,-0.523156782458076,-0.519707287692145,
-0.516924525973986,-0.513741899032524,-0.508239375172271,-0.48352385291504,
-0.420214970398746,-0.405033773951311,-0.402007472732476,-0.40006729161317,
-0.398508819011127,-0.396636041380429,-0.393106278093656,-0.370656799772542,
-0.321193150647477,-0.291215968601058,-0.285788658773259,-0.282304906209567,
-0.279519121306193,-0.279467355042463,-0.279419976725557,-0.27937660280131,
-0.279336884477936,-0.27930050452084,-0.279267174318047,-0.279236631205406,
-0.279208636042033,-0.279182971010811,-0.279159437620457,-0.279137854908755,
-0.279104992352874,-0.279072745814695,-0.279041100108549,-0.279010040475174,
-0.278979552569855,-0.275673812187924,-0.269521690979313,-0.261771545500601,
-0.244546376309817,-0.203779465665771,-0.168494842914406,-0.164653168898947,
-0.162690190869913,-0.161130709281989,-0.159277199984235,-0.155838226582873,
-0.135837036075348,-0.0919629954157552,-0.0729435991846148,-0.0527102775772208,
-0.0472999482011549,-0.0441372506986406,-0.041630390480389,-0.0389781980499252,
-0.0356992516244263,-0.0307588796484749,-0.0182762009540131),
 .UNSPECIFIED.);
#818=B_SPLINE_CURVE_WITH_KNOTS('',3,(#96816,#96817,#96818,#96819,#96820,
#96821,#96822,#96823,#96824,#96825,#96826,#96827,#96828,#96829,#96830,#96831,
#96832,#96833,#96834,#96835,#96836,#96837,#96838,#96839,#96840,#96841,#96842,
#96843,#96844,#96845,#96846,#96847,#96848,#96849,#96850,#96851,#96852,#96853,
#96854,#96855,#96856,#96857,#96858,#96859,#96860,#96861,#96862,#96863,#96864,
#96865,#96866,#96867,#96868,#96869,#96870,#96871,#96872,#96873,#96874,#96875,
#96876,#96877,#96878,#96879,#96880,#96881,#96882,#96883,#96884,#96885,#96886,
#96887,#96888,#96889,#96890,#96891,#96892,#96893,#96894,#96895,#96896,#96897,
#96898,#96899,#96900,#96901,#96902,#96903,#96904,#96905,#96906,#96907,#96908,
#96909,#96910,#96911,#96912,#96913,#96914,#96915,#96916,#96917,#96918,#96919,
#96920,#96921,#96922,#96923,#96924,#96925,#96926,#96927,#96928,#96929,#96930,
#96931,#96932,#96933,#96934,#96935,#96936,#96937,#96938,#96939,#96940,#96941,
#96942,#96943,#96944,#96945,#96946,#96947,#96948,#96949,#96950,#96951,#96952,
#96953,#96954,#96955,#96956,#96957,#96958,#96959,#96960,#96961,#96962,#96963,
#96964,#96965,#96966,#96967,#96968,#96969,#96970,#96971,#96972,#96973,#96974,
#96975,#96976,#96977,#96978,#96979,#96980,#96981,#96982,#96983,#96984,#96985,
#96986,#96987,#96988,#96989,#96990,#96991,#96992,#96993,#96994,#96995,#96996,
#96997,#96998,#96999,#97000,#97001,#97002,#97003,#97004,#97005,#97006,#97007,
#97008,#97009,#97010,#97011,#97012,#97013,#97014,#97015,#97016,#97017,#97018,
#97019,#97020,#97021,#97022,#97023,#97024,#97025,#97026,#97027,#97028,#97029),
 .UNSPECIFIED.,.F.,.F.,(4,2,2,2,2,2,2,2,2,2,2,2,2,2,2,2,2,2,2,2,2,2,2,2,
2,2,2,2,2,2,2,2,2,2,2,2,2,2,2,2,2,2,2,2,2,2,2,2,2,2,2,2,2,2,2,2,2,2,2,2,
2,2,2,2,2,2,2,2,2,2,2,2,2,2,2,2,2,2,2,2,2,2,2,2,2,2,2,2,2,2,2,2,2,2,2,2,
2,2,2,2,2,2,2,2,2,2,4),(-1.47765371799144,-1.45142745756412,-1.44576112899101,
-1.44344851691512,-1.44187199792082,-1.4402321442346,-1.43769521092576,
-1.42993567632337,-1.3695627018735,-1.33412821553208,-1.32857313560911,
-1.32507682309873,-1.32232506213325,-1.31925072262929,-1.31411391864714,
-1.2939101260195,-1.24470366157367,-1.2110448045594,-1.20724049397964,-1.20530169388443,
-1.20376448058945,-1.20194271617302,-1.19857794039293,-1.17953286531276,
-1.11687703999204,-1.09533530595162,-1.0899331425105,-1.08676931348704,
-1.08430310269733,-1.08105991289151,-1.07514523528644,-1.04047048631585,
-1.00423675424185,-0.973490342597509,-0.969696136292642,-0.967759570096034,
-0.966222588323663,-0.964399282199045,-0.961026922533679,-0.94180090162142,
-0.877116019589753,-0.857518254725743,-0.852203753372913,-0.849090639811394,
-0.846619964327545,-0.843315226846412,-0.837108518188459,-0.78942467591477,
-0.738138697120928,-0.732920383228218,-0.730900565727312,-0.729447288336196,
-0.727861170436274,-0.725579644421702,-0.719690659690047,-0.710963148971715,
-0.648434678628104,-0.620936979259781,-0.6156573651419,-0.612244899571475,
-0.609501356501994,-0.606374155623114,-0.600995481362829,-0.577422260160876,
-0.521657765063854,-0.514091564330872,-0.497642949625792,-0.494575201808842,
-0.492636894586785,-0.491099827876407,-0.48927794940316,-0.485912213763665,
-0.466840042870094,-0.403880221409232,-0.38263106354139,-0.377255299656835,
-0.374097682196106,-0.371357191622453,-0.367986694848489,-0.361462530434708,
-0.307377819699041,-0.263615346754291,-0.25796110247614,-0.2556506714107,
-0.254074718260244,-0.252467481373426,-0.250015012302373,-0.247123966559145,
-0.241647450292063,-0.228023513600522,-0.193676029608931,-0.146529591470678,
-0.140899171299612,-0.137380330053458,-0.134626220580472,-0.131565119861788,
-0.126487822606833,-0.107015575728412,-0.0356453510311497,-0.0240297605022315,
-0.0196655814877161,-0.0176643188754654,-0.016163978162886,-0.0147204199484846,
-0.0129967245031383,-0.0104687631420757,-0.000704102697230447),
 .UNSPECIFIED.);
#819=B_SPLINE_CURVE_WITH_KNOTS('',3,(#97030,#97031,#97032,#97033),
 .UNSPECIFIED.,.F.,.F.,(4,4),(-2.98994510152635,-2.97245970569877),
 .UNSPECIFIED.);
#820=B_SPLINE_CURVE_WITH_KNOTS('',3,(#97035,#97036,#97037,#97038),
 .UNSPECIFIED.,.F.,.F.,(4,4),(-0.0182762009540131,-0.000702744675276971),
 .UNSPECIFIED.);
#821=B_SPLINE_CURVE_WITH_KNOTS('',3,(#97039,#97040,#97041,#97042,#97043,
#97044,#97045,#97046,#97047,#97048,#97049,#97050,#97051,#97052,#97053,#97054,
#97055,#97056,#97057,#97058,#97059,#97060,#97061,#97062,#97063,#97064,#97065,
#97066,#97067,#97068,#97069,#97070,#97071,#97072,#97073,#97074,#97075,#97076,
#97077,#97078,#97079,#97080,#97081,#97082,#97083,#97084,#97085,#97086,#97087,
#97088,#97089,#97090,#97091,#97092,#97093,#97094,#97095,#97096,#97097,#97098,
#97099,#97100,#97101,#97102,#97103,#97104,#97105,#97106,#97107,#97108,#97109,
#97110,#97111,#97112,#97113,#97114,#97115,#97116,#97117,#97118,#97119,#97120,
#97121,#97122,#97123,#97124,#97125,#97126,#97127,#97128,#97129,#97130,#97131,
#97132,#97133,#97134,#97135,#97136,#97137,#97138,#97139,#97140,#97141,#97142,
#97143,#97144,#97145,#97146,#97147,#97148,#97149,#97150,#97151,#97152,#97153,
#97154,#97155,#97156,#97157,#97158,#97159,#97160,#97161,#97162,#97163,#97164,
#97165,#97166,#97167,#97168,#97169,#97170,#97171,#97172,#97173,#97174,#97175,
#97176,#97177,#97178,#97179,#97180,#97181,#97182,#97183,#97184,#97185,#97186,
#97187,#97188,#97189,#97190,#97191,#97192,#97193,#97194,#97195,#97196,#97197,
#97198,#97199,#97200,#97201,#97202,#97203,#97204,#97205,#97206,#97207,#97208,
#97209,#97210,#97211,#97212,#97213,#97214,#97215,#97216,#97217,#97218,#97219,
#97220,#97221,#97222,#97223,#97224,#97225,#97226,#97227,#97228,#97229,#97230,
#97231,#97232,#97233,#97234,#97235,#97236,#97237,#97238,#97239,#97240,#97241,
#97242,#97243,#97244,#97245,#97246,#97247,#97248,#97249,#97250,#97251,#97252,
#97253,#97254,#97255,#97256),.UNSPECIFIED.,.F.,.F.,(4,2,2,2,2,2,2,2,2,2,
2,2,2,2,2,2,2,2,2,2,2,2,2,2,2,2,2,2,2,2,2,2,2,2,2,2,2,2,2,2,2,2,2,2,2,2,
2,2,2,2,2,2,2,2,2,2,2,2,2,2,2,2,2,2,2,2,2,2,2,2,2,2,2,2,2,2,2,2,2,2,2,2,
2,2,2,2,2,2,2,2,2,2,2,2,2,2,2,2,2,2,2,2,2,2,2,2,2,2,4),(-2.98990986834267,
-2.92589827377045,-2.91790264009375,-2.91531455028523,-2.91364780976403,
-2.912049745725,-2.90971033311418,-2.90399996945836,-2.86133972365879,-2.8358616406499,
-2.81552684940263,-2.80683975774228,-2.80012033891742,-2.79668688038249,
-2.79664121284996,-2.79659394193871,-2.79654496529467,-2.79649417193831,
-2.79644144135315,-2.79393060958563,-2.79079685546178,-2.7855190211026,
-2.76668177341165,-2.70130235832172,-2.68830972825382,-2.68040211965345,
-2.67782439675567,-2.67615976402111,-2.67455979966933,-2.67221154322354,
-2.66644925829432,-2.62561756680326,-2.58683368139395,-2.5665315003627,
-2.56133853346357,-2.55822317057154,-2.55542959105554,-2.5518726697505,
-2.54620482473542,-2.49937304034869,-2.46614000274728,-2.44463981483692,
-2.44114253579803,-2.43927640933814,-2.43771731915679,-2.43576866035675,
-2.43271528995482,-2.41705837521584,-2.40829076098589,-2.3491724791566,
-2.33585493713671,-2.32636910338221,-2.32242149275693,-2.31956851121527,
-2.31696152383361,-2.31345257279434,-2.30486215254651,-2.251435761258,-2.22037896474988,
-2.21109722379226,-2.20491304405002,-2.20256673849671,-2.20095109613951,
-2.19948193293225,-2.19705843365786,-2.1908426855805,-2.11143997697347,
-2.09137763858312,-2.08620460210324,-2.08309398493847,-2.08030009829476,
-2.07673651367095,-2.07104536623521,-2.02432779106774,-1.99062780407669,
-1.96952019868146,-1.96603786829361,-1.96417511781295,-1.96261615803266,
-1.96066428129978,-1.95687460803613,-1.92928588836175,-1.87727573845112,
-1.85433604069524,-1.84894877038702,-1.84579113836016,-1.84300507484848,
-1.83951839423567,-1.834081469451,-1.80386739892158,-1.74997563501545,-1.73184606268024,
-1.72848895140245,-1.72665290844792,-1.72509191096596,-1.72310629399625,
-1.71993061397123,-1.70190013653771,-1.68106279015895,-1.64414960195492,
-1.62643469254374,-1.61468657719638,-1.61039729347355,-1.6074776821537,
-1.60463278844666,-1.60120957906441,-1.59257343486644,-1.53678204388997,
-1.51273582755968),.UNSPECIFIED.);
#822=B_SPLINE_CURVE_WITH_KNOTS('',3,(#97261,#97262,#97263,#97264,#97265,
#97266,#97267,#97268,#97269,#97270,#97271,#97272,#97273,#97274,#97275,#97276,
#97277,#97278,#97279,#97280,#97281,#97282,#97283,#97284,#97285,#97286,#97287,
#97288,#97289,#97290,#97291,#97292,#97293,#97294,#97295,#97296,#97297,#97298,
#97299,#97300,#97301,#97302,#97303,#97304,#97305,#97306,#97307,#97308,#97309,
#97310,#97311,#97312,#97313,#97314,#97315,#97316,#97317,#97318,#97319,#97320,
#97321,#97322,#97323,#97324,#97325,#97326,#97327,#97328,#97329,#97330,#97331,
#97332,#97333,#97334,#97335,#97336,#97337,#97338,#97339,#97340,#97341,#97342,
#97343,#97344,#97345,#97346,#97347,#97348,#97349,#97350,#97351,#97352,#97353,
#97354,#97355,#97356,#97357,#97358,#97359,#97360,#97361,#97362,#97363,#97364,
#97365,#97366,#97367,#97368,#97369,#97370,#97371,#97372,#97373,#97374,#97375,
#97376,#97377,#97378,#97379,#97380,#97381,#97382,#97383,#97384,#97385,#97386,
#97387,#97388,#97389,#97390,#97391,#97392,#97393,#97394,#97395,#97396,#97397,
#97398,#97399,#97400,#97401,#97402,#97403,#97404,#97405,#97406,#97407,#97408,
#97409,#97410,#97411,#97412,#97413,#97414,#97415,#97416,#97417,#97418,#97419,
#97420,#97421,#97422,#97423,#97424,#97425,#97426,#97427,#97428,#97429,#97430,
#97431,#97432,#97433,#97434,#97435,#97436,#97437,#97438,#97439,#97440,#97441,
#97442,#97443,#97444,#97445,#97446,#97447,#97448,#97449,#97450,#97451,#97452,
#97453,#97454,#97455,#97456,#97457,#97458,#97459,#97460,#97461,#97462,#97463,
#97464,#97465,#97466),.UNSPECIFIED.,.F.,.F.,(4,2,2,2,2,2,2,2,2,2,2,2,2,
2,2,2,2,2,2,2,2,2,2,2,2,2,2,2,2,2,2,2,2,2,2,2,2,2,2,2,2,2,2,2,2,2,2,2,2,
2,2,2,2,2,2,2,2,2,2,2,2,2,2,2,2,2,2,2,2,2,2,2,2,2,2,2,2,2,2,2,2,2,2,2,2,
2,2,2,2,2,2,2,2,2,2,2,2,2,2,2,2,2,4),(-2.97176568216088,-2.96872105170352,
-2.95972050146067,-2.89185505033743,-2.87284393448954,-2.86948173076718,
-2.8676610454326,-2.86612454991605,-2.8641864205224,-2.86038272706146,-2.8249595191706,
-2.78535439701824,-2.76745110893685,-2.75564547704731,-2.75242182978618,
-2.74981077156188,-2.74712833812788,-2.7440165420145,-2.73865994653809,
-2.71713973115572,-2.65445810896365,-2.63541092860209,-2.63204685973361,
-2.63022564381836,-2.62868898578821,-2.6267510142312,-2.62294870739234,
-2.58913854524189,-2.57486177967326,-2.5222255774948,-2.51580519899522,
-2.51245648550289,-2.50971780318085,-2.5065444412584,-2.50109807983616,
-2.47891791216427,-2.41690490556003,-2.3979197705736,-2.39455816612544,
-2.39273738008213,-2.39120054274797,-2.38926165728933,-2.38619141726884,
-2.36968571550571,-2.36230251816553,-2.30649141213079,-2.28291548056584,
-2.27753738106449,-2.27441063358931,-2.27166755699529,-2.26825576168443,
-2.26297731000146,-2.23550445328324,-2.17299232357434,-2.16421886532137,
-2.15830728918988,-2.15602247394333,-2.15443585900521,-2.15298353266008,
-2.15096691627438,-2.14576808682149,-2.09434363735776,-2.04730393459202,
-2.04081535582008,-2.03745233306374,-2.03471251090759,-2.0315496360009,
-2.02615021759127,-2.00463924706465,-1.94192572650429,-1.92287261387068,
-1.91950771747663,-1.91768607683776,-1.91614907456029,-1.91421068658743,
-1.91040761448511,-1.87643881418507,-1.82759975911285,-1.80740297745391,
-1.80226719670048,-1.79919329988616,-1.79644182618105,-1.79294573042378,
-1.78739064478555,-1.75194577298051,-1.69157119874507,-1.68378982592072,
-1.68125031576849,-1.67960996578412,-1.67803396282162,-1.67572365929685,
-1.67007067408029,-1.62614751802524,-1.58896448683082,-1.57625022918979,
-1.56712029874236,-1.56326549549487,-1.56046041912332,-1.55788422801519,
-1.55439743863851,-1.5457342247264,-1.49481472321863,-1.47765371799144),
 .UNSPECIFIED.);
#823=B_SPLINE_CURVE_WITH_KNOTS('',3,(#97467,#97468,#97469,#97470,#97471,
#97472,#97473,#97474,#97475,#97476,#97477,#97478,#97479,#97480,#97481,#97482,
#97483,#97484,#97485,#97486,#97487,#97488,#97489,#97490,#97491,#97492,#97493,
#97494,#97495,#97496,#97497,#97498,#97499,#97500,#97501,#97502,#97503,#97504,
#97505,#97506,#97507,#97508,#97509,#97510,#97511,#97512,#97513,#97514,#97515,
#97516,#97517,#97518,#97519,#97520,#97521,#97522,#97523,#97524,#97525,#97526,
#97527,#97528,#97529,#97530,#97531,#97532,#97533,#97534,#97535,#97536,#97537,
#97538,#97539,#97540,#97541,#97542,#97543,#97544,#97545,#97546,#97547,#97548,
#97549,#97550,#97551,#97552,#97553,#97554,#97555,#97556,#97557,#97558,#97559,
#97560,#97561,#97562,#97563,#97564,#97565,#97566,#97567,#97568,#97569,#97570,
#97571,#97572,#97573,#97574,#97575,#97576,#97577,#97578,#97579,#97580,#97581,
#97582,#97583,#97584,#97585,#97586,#97587,#97588,#97589,#97590,#97591,#97592,
#97593,#97594,#97595,#97596,#97597,#97598,#97599,#97600,#97601,#97602,#97603,
#97604,#97605,#97606,#97607,#97608,#97609,#97610,#97611,#97612,#97613,#97614,
#97615,#97616,#97617,#97618,#97619,#97620,#97621,#97622,#97623,#97624,#97625,
#97626,#97627,#97628,#97629,#97630,#97631,#97632,#97633,#97634,#97635,#97636,
#97637,#97638,#97639,#97640,#97641,#97642,#97643,#97644,#97645,#97646,#97647,
#97648,#97649,#97650,#97651,#97652,#97653,#97654,#97655,#97656,#97657,#97658,
#97659,#97660,#97661,#97662,#97663,#97664,#97665,#97666,#97667,#97668,#97669,
#97670,#97671,#97672,#97673,#97674,#97675,#97676,#97677,#97678,#97679,#97680,
#97681,#97682),.UNSPECIFIED.,.F.,.F.,(4,2,2,2,2,2,2,2,2,2,2,2,2,2,2,2,2,
2,2,2,2,2,2,2,2,2,2,2,2,2,2,2,2,2,2,2,2,2,2,2,2,2,2,2,2,2,2,2,2,2,2,2,2,
2,2,2,2,2,2,2,2,2,2,2,2,2,2,2,2,2,2,2,2,2,2,2,2,2,2,2,2,2,2,2,2,2,2,2,2,
2,2,2,2,2,2,2,2,2,2,2,2,2,2,2,2,2,2,4),(-1.51273582755968,-1.49533009439322,
-1.49145300152984,-1.4894823103939,-1.48792216612365,-1.48607430729772,
-1.48266259777879,-1.46332313891588,-1.39785925583083,-1.37913500448887,
-1.37386797111017,-1.37073657882099,-1.36822537979251,-1.36483224077331,
-1.35834249433802,-1.30952180667387,-1.26014662303698,-1.25474526821147,
-1.25268042986114,-1.25120174885727,-1.24959493319984,-1.24729353762033,
-1.24140485726079,-1.2327108801626,-1.16995571829231,-1.14275634338727,
-1.13744191572076,-1.1339924830641,-1.13120926399711,-1.12802555896641,
-1.1225197558781,-1.09776291714441,-1.03413794464092,-1.01926034253567,
-1.01596275186856,-1.01411930237346,-1.01255872680346,-1.01058221077209,
-1.00654666027565,-1.0012266938936,-0.988236036753984,-0.922820106098911,
-0.904047660223555,-0.898775862710917,-0.895643321881228,-0.893132142281531,
-0.889740258144957,-0.883257099179764,-0.831450284803719,-0.785271298367369,
-0.779700350307255,-0.7776130450655,-0.776128337169116,-0.774526255956581,
-0.772250174779494,-0.766523891281055,-0.758146659589103,-0.702018719648352,
-0.668137691632259,-0.662577046371655,-0.659052510502516,-0.656262457136877,
-0.65312806524388,-0.647848197781125,-0.626420093698929,-0.581375938007835,
-0.577020946712195,-0.545132634245399,-0.541293187550638,-0.539330490903698,
-0.537770778091171,-0.53591645591085,-0.532474561284134,-0.512412442043688,
-0.435892584727484,-0.426414620254934,-0.422758399284,-0.420114404713707,
-0.417289066016605,-0.413500260763577,-0.404944110542066,-0.367919035203341,
-0.352959483710124,-0.310422040261175,-0.304706512188651,-0.302366261786151,
-0.300768059649106,-0.299101595237071,-0.296514683807388,-0.288747587277735,
-0.228300376322557,-0.19316411950662,-0.187566764711083,-0.184031504253709,
-0.181240831796681,-0.178113990707515,-0.173217453633384,-0.154668976338493,
-0.119786530530212,-0.0726714303882921,-0.0671620863195167,-0.0650831649812104,
-0.0636008725397968,-0.0619974234875304,-0.0597128594454045,-0.0571189548369731,
-0.0486132338801387,-0.0178597978295153),.UNSPECIFIED.);
#824=B_SPLINE_CURVE_WITH_KNOTS('',3,(#97688,#97689,#97690,#97691,#97692,
#97693,#97694,#97695,#97696,#97697,#97698,#97699,#97700,#97701,#97702,#97703,
#97704,#97705,#97706,#97707,#97708,#97709,#97710,#97711,#97712,#97713,#97714,
#97715,#97716,#97717,#97718,#97719,#97720,#97721,#97722,#97723,#97724,#97725,
#97726,#97727,#97728,#97729,#97730,#97731,#97732,#97733,#97734,#97735,#97736,
#97737,#97738,#97739,#97740,#97741,#97742,#97743,#97744,#97745,#97746,#97747,
#97748,#97749,#97750,#97751,#97752,#97753,#97754,#97755,#97756,#97757,#97758,
#97759,#97760,#97761,#97762,#97763,#97764,#97765,#97766,#97767,#97768,#97769,
#97770,#97771,#97772,#97773,#97774,#97775,#97776,#97777,#97778,#97779,#97780,
#97781,#97782,#97783,#97784,#97785,#97786,#97787,#97788,#97789,#97790,#97791,
#97792,#97793,#97794,#97795,#97796,#97797,#97798,#97799,#97800,#97801,#97802,
#97803,#97804,#97805,#97806,#97807,#97808,#97809,#97810,#97811,#97812,#97813,
#97814,#97815,#97816,#97817,#97818,#97819,#97820,#97821,#97822,#97823,#97824,
#97825,#97826,#97827,#97828,#97829,#97830,#97831,#97832,#97833,#97834,#97835,
#97836,#97837,#97838,#97839,#97840,#97841,#97842,#97843,#97844,#97845,#97846,
#97847,#97848,#97849,#97850,#97851,#97852,#97853,#97854,#97855,#97856,#97857,
#97858,#97859,#97860,#97861,#97862,#97863,#97864,#97865,#97866,#97867,#97868,
#97869,#97870,#97871,#97872,#97873,#97874,#97875,#97876,#97877,#97878,#97879,
#97880,#97881,#97882,#97883,#97884,#97885,#97886,#97887,#97888,#97889,#97890,
#97891,#97892,#97893,#97894,#97895,#97896,#97897,#97898,#97899,#97900,#97901,
#97902,#97903,#97904,#97905,#97906,#97907,#97908,#97909,#97910,#97911,#97912,
#97913,#97914,#97915,#97916,#97917,#97918,#97919,#97920,#97921),
 .UNSPECIFIED.,.F.,.F.,(4,2,2,2,2,2,2,2,2,2,2,2,2,2,2,2,2,2,2,2,2,2,2,2,
2,2,2,2,2,2,2,2,2,2,2,2,2,2,2,2,2,2,2,2,2,2,2,2,2,2,2,2,2,2,2,2,2,2,2,2,
2,2,2,2,2,2,2,2,2,2,2,2,2,2,2,2,2,2,2,2,2,2,2,2,2,2,2,2,2,2,2,2,2,2,2,2,
2,2,2,2,2,2,2,2,2,2,2,2,2,2,2,2,2,2,2,2,4),(-1.47803507761506,-1.4374382166583,
-1.42902327118118,-1.42566395721682,-1.42286355569726,-1.41998113674546,
-1.41573133860918,-1.40400284259666,-1.38626022836868,-1.34933916660219,
-1.32835208862582,-1.3102866655161,-1.30713792004883,-1.30517484722609,
-1.30363577175521,-1.30183205387249,-1.29855184675731,-1.28132977592769,
-1.25652702998621,-1.2001283038934,-1.1917446170029,-1.18830021066431,-1.18573435123345,
-1.18291997774264,-1.17901453134801,-1.16957959344572,-1.15630656989121,
-1.08170717121051,-1.07158472945669,-1.06867871926907,-1.06695688576749,
-1.06540167930469,-1.06330024680825,-1.05850693628611,-1.05184653958829,
-1.03361023354797,-0.969184367184311,-0.955827057811356,-0.95120815174358,
-0.948247057246169,-0.945460903105427,-0.941719724616904,-0.933253648008918,
-0.896613958422921,-0.853537293916598,-0.835069355832113,-0.83188894335215,
-0.829916348242102,-0.82837645503442,-0.826579441268595,-0.823330778887602,
-0.806728306024424,-0.762718975575585,-0.721312156487068,-0.715659828246629,
-0.712133841846288,-0.709378168350001,-0.706319462222812,-0.701255805482828,
-0.681960396031265,-0.644622824114802,-0.600836007622749,-0.595178876073316,
-0.592867515410677,-0.591291012797656,-0.589650367743824,-0.587110774356832,
-0.579331891156864,-0.518968595377029,-0.48352882298928,-0.477972731526719,
-0.474475768804785,-0.471723487626494,-0.468648558179329,-0.463510747875674,
-0.443302727661449,-0.394142336559927,-0.360421489890999,-0.356616502027983,
-0.354677346967185,-0.353139846597439,-0.351317735677201,-0.347952306769623,
-0.328903169174258,-0.266230682763259,-0.24469571757594,-0.239334067050411,
-0.236220014883805,-0.233740028253042,-0.233655368160887,-0.233587204057685,
-0.233530493093196,-0.233482156739802,-0.233360576876392,-0.233241224047959,
-0.233123063555533,-0.233005218496759,-0.23288692072389,-0.232767476824585,
-0.232646243675562,-0.23252261029551,-0.232395983961024,-0.232265779279798,
-0.228405497879208,-0.21866179705136,-0.169602741123395,-0.125606219698173,
-0.119951956199722,-0.117641164493793,-0.116064847083046,-0.114424174022154,
-0.11188419698253,-0.104101477988992,-0.0437464108273202,-0.00971125300947028,
-0.00384469650073024,-0.000705366426058919),.UNSPECIFIED.);
#825=B_SPLINE_CURVE_WITH_KNOTS('',3,(#97922,#97923,#97924,#97925,#97926,
#97927,#97928,#97929,#97930,#97931,#97932,#97933),.UNSPECIFIED.,.F.,.F.,
(4,2,2,2,2,4),(-2.9891191772697,-2.98772513884422,-2.98543450742337,-2.98285334584464,
-2.97881195257422,-2.97176568216088),.UNSPECIFIED.);
#826=B_SPLINE_CURVE_WITH_KNOTS('',3,(#97935,#97936,#97937,#97938),
 .UNSPECIFIED.,.F.,.F.,(4,4),(-0.0178597978295153,-0.000703565759050232),
 .UNSPECIFIED.);
#827=B_SPLINE_CURVE_WITH_KNOTS('',3,(#97939,#97940,#97941,#97942,#97943,
#97944,#97945,#97946,#97947,#97948,#97949,#97950,#97951,#97952,#97953,#97954,
#97955,#97956,#97957,#97958,#97959,#97960,#97961,#97962,#97963,#97964,#97965,
#97966,#97967,#97968,#97969,#97970,#97971,#97972,#97973,#97974,#97975,#97976,
#97977,#97978,#97979,#97980,#97981,#97982,#97983,#97984,#97985,#97986,#97987,
#97988,#97989,#97990,#97991,#97992,#97993,#97994,#97995,#97996,#97997,#97998,
#97999,#98000,#98001,#98002,#98003,#98004,#98005,#98006,#98007,#98008,#98009,
#98010,#98011,#98012,#98013,#98014,#98015,#98016,#98017,#98018,#98019,#98020,
#98021,#98022,#98023,#98024,#98025,#98026,#98027,#98028,#98029,#98030,#98031,
#98032,#98033,#98034,#98035,#98036,#98037,#98038,#98039,#98040,#98041,#98042,
#98043,#98044,#98045,#98046,#98047,#98048,#98049,#98050,#98051,#98052,#98053,
#98054,#98055,#98056,#98057,#98058,#98059,#98060,#98061,#98062,#98063,#98064,
#98065,#98066,#98067,#98068,#98069,#98070,#98071,#98072,#98073,#98074,#98075,
#98076,#98077,#98078,#98079,#98080,#98081,#98082,#98083,#98084,#98085,#98086,
#98087,#98088,#98089,#98090,#98091,#98092,#98093,#98094,#98095,#98096,#98097,
#98098,#98099,#98100,#98101,#98102,#98103,#98104,#98105,#98106,#98107,#98108,
#98109,#98110,#98111,#98112,#98113,#98114,#98115,#98116,#98117,#98118,#98119,
#98120,#98121,#98122,#98123,#98124,#98125,#98126,#98127,#98128,#98129,#98130,
#98131,#98132,#98133,#98134,#98135,#98136,#98137,#98138,#98139,#98140,#98141,
#98142,#98143,#98144,#98145,#98146,#98147,#98148),.UNSPECIFIED.,.F.,.F.,
(4,2,2,2,2,2,2,2,2,2,2,2,2,2,2,2,2,2,2,2,2,2,2,2,2,2,2,2,2,2,2,2,2,2,2,
2,2,2,2,2,2,2,2,2,2,2,2,2,2,2,2,2,2,2,2,2,2,2,2,2,2,2,2,2,2,2,2,2,2,2,2,
2,2,2,2,2,2,2,2,2,2,2,2,2,2,2,2,2,2,2,2,2,2,2,2,2,2,2,2,2,2,2,2,2,4),(-2.98869725023108,
-2.94478634572554,-2.93996525139911,-2.93673637914376,-2.93361763812439,
-2.93082743710486,-2.92728357025766,-2.92165410752704,-2.88528881974124,
-2.85699877390433,-2.82713274602364,-2.81861194066847,-2.81662066431204,
-2.81476000028187,-2.81320199906365,-2.81125033216377,-2.80745821492658,
-2.77956042165103,-2.72251147978083,-2.70432593050842,-2.69940406275812,
-2.6962962254929,-2.69350407822626,-2.68994166929962,-2.68425028701077,
-2.64408074789386,-2.59970276303459,-2.5825051973328,-2.57919547841962,
-2.57737042573491,-2.57580951260509,-2.57381206574106,-2.57059468046712,
-2.55172952614159,-2.53155636551345,-2.49501275335206,-2.47727105002767,
-2.46551208427408,-2.46122315176185,-2.45830503385862,-2.45546255770236,
-2.45204342034472,-2.44342394195459,-2.38751742307331,-2.37793658340261,
-2.34879338056555,-2.3431425529687,-2.34087948847909,-2.33928073111228,
-2.337587610471,-2.3348768564197,-2.32663681141175,-2.24978037870746,-2.22987711381173,
-2.22471964514284,-2.22161392193877,-2.2188215966232,-2.21525609684678,
-2.20955396767431,-2.16765007521875,-2.13857941870352,-2.11118390042684,
-2.10570135757225,-2.10346564575699,-2.10187204706687,-2.10016969644309,
-2.09741656709454,-2.08883686713255,-2.01239439569718,-1.99252056878035,
-1.98736607473593,-1.98426132086768,-1.9814693445828,-1.97790356908542,
-1.97219953347957,-1.92996558713754,-1.88690798812862,-1.87043773092777,
-1.86716667405698,-1.86535025335834,-1.8637887506722,-1.86178019927249,
-1.85852487050036,-1.83874640873644,-1.79775591495437,-1.76084327726368,
-1.75230337524243,-1.74851948686979,-1.74569692363156,-1.74305487433179,
-1.73940030820839,-1.72992048911928,-1.65344896115047,-1.63339647369863,
-1.62995710641481,-1.62810429239469,-1.62654592952984,-1.6245850490982,
-1.62074950432182,-1.58892893328139,-1.55838625006236,-1.53248072178885,
-1.51712033679016,-1.5123901083176,-1.51231102550938),.UNSPECIFIED.);
#828=B_SPLINE_CURVE_WITH_KNOTS('',3,(#98153,#98154,#98155,#98156,#98157,
#98158,#98159,#98160,#98161,#98162,#98163,#98164,#98165,#98166,#98167,#98168,
#98169,#98170,#98171,#98172,#98173,#98174,#98175,#98176,#98177,#98178,#98179,
#98180,#98181,#98182,#98183,#98184,#98185,#98186,#98187,#98188,#98189,#98190,
#98191,#98192,#98193,#98194,#98195,#98196,#98197,#98198,#98199,#98200,#98201,
#98202,#98203,#98204,#98205,#98206,#98207,#98208,#98209,#98210,#98211,#98212,
#98213,#98214,#98215,#98216,#98217,#98218,#98219,#98220,#98221,#98222,#98223,
#98224,#98225,#98226,#98227,#98228,#98229,#98230,#98231,#98232,#98233,#98234,
#98235,#98236,#98237,#98238,#98239,#98240,#98241,#98242,#98243,#98244,#98245,
#98246,#98247,#98248,#98249,#98250,#98251,#98252,#98253,#98254,#98255,#98256,
#98257,#98258,#98259,#98260,#98261,#98262,#98263,#98264,#98265,#98266,#98267,
#98268,#98269,#98270,#98271,#98272,#98273,#98274,#98275,#98276,#98277,#98278,
#98279,#98280,#98281,#98282,#98283,#98284,#98285,#98286,#98287,#98288,#98289,
#98290,#98291,#98292,#98293,#98294,#98295,#98296,#98297,#98298,#98299,#98300,
#98301,#98302,#98303,#98304,#98305,#98306,#98307,#98308,#98309,#98310,#98311,
#98312,#98313,#98314,#98315,#98316,#98317,#98318,#98319,#98320,#98321,#98322,
#98323,#98324,#98325,#98326,#98327,#98328,#98329,#98330,#98331,#98332,#98333,
#98334,#98335,#98336,#98337,#98338,#98339,#98340,#98341,#98342,#98343,#98344,
#98345,#98346,#98347,#98348,#98349,#98350,#98351,#98352,#98353,#98354,#98355,
#98356,#98357,#98358,#98359,#98360,#98361,#98362,#98363,#98364,#98365,#98366,
#98367,#98368,#98369,#98370,#98371,#98372,#98373,#98374,#98375,#98376,#98377,
#98378,#98379,#98380,#98381,#98382,#98383,#98384,#98385,#98386,#98387,#98388,
#98389,#98390,#98391,#98392,#98393,#98394,#98395,#98396,#98397,#98398,#98399,
#98400,#98401,#98402,#98403,#98404,#98405,#98406,#98407,#98408,#98409,#98410,
#98411,#98412,#98413,#98414,#98415,#98416,#98417,#98418,#98419,#98420,#98421,
#98422,#98423,#98424,#98425,#98426,#98427,#98428,#98429,#98430,#98431,#98432,
#98433,#98434,#98435,#98436,#98437,#98438,#98439,#98440,#98441,#98442,#98443,
#98444,#98445,#98446,#98447,#98448,#98449,#98450,#98451,#98452,#98453,#98454,
#98455,#98456,#98457,#98458),.UNSPECIFIED.,.F.,.F.,(4,2,2,2,2,2,2,2,2,2,
2,2,2,2,2,2,2,2,2,2,2,2,2,2,2,2,2,2,2,2,2,2,2,2,2,2,2,2,2,2,2,2,2,2,2,2,
2,2,2,2,2,2,2,2,2,2,2,2,2,2,2,2,2,2,2,2,2,2,2,2,2,2,2,2,2,2,2,2,2,2,2,2,
2,2,2,2,2,2,2,2,2,2,2,2,2,2,2,2,2,2,2,2,2,2,2,2,2,2,2,2,2,2,2,2,2,2,2,2,
2,2,2,2,2,2,2,2,2,2,2,2,2,2,2,2,2,2,2,2,2,2,2,2,2,2,2,2,2,2,2,2,2,2,4),
(-2.9723526798557,-2.97147367758802,-2.96947216547705,-2.96795877905284,
-2.96646860463858,-2.96474477447139,-2.96182936926877,-2.95161537306312,
-2.93951555371508,-2.87673067507901,-2.85699506679948,-2.8518879152199,
-2.84881533186768,-2.84605492998145,-2.84253348732493,-2.83690935729481,
-2.79041241366749,-2.7512981176478,-2.74054688101143,-2.73589267366465,
-2.73229897861837,-2.73044204480278,-2.73043710560119,-2.73043215127893,
-2.73042718173856,-2.73042219688213,-2.73041719664725,-2.73041218094353,
-2.73040714966964,-2.73040210274658,-2.73039704008575,-2.73039196158955,
-2.73038686716928,-2.7303817567387,-2.73037663021558,-2.73037148749642,
-2.73036641433062,-2.73036126587527,-2.73035604091821,-2.73035073820319,
-2.73034535647939,-2.73033989445168,-2.73033435080217,-2.73032872420341,
-2.73032301330493,-2.73031721671264,-2.73031133302377,-2.73030536080352,
-2.73029929859911,-2.7302931449125,-2.73028689823818,-2.73028055702682,
-2.73027411970475,-2.73026758468242,-2.73026095031405,-2.73025421494658,
-2.73024737690837,-2.73024043447437,-2.73023338588709,-2.73022622936283,
-2.73021896308281,-2.73021158520149,-2.730204093834,-2.73019648706117,-2.7301887629238,
-2.72873979435687,-2.7268035292362,-2.72301764881134,-2.69332078750982,
-2.64021484433467,-2.62005479049749,-2.61492071620485,-2.61184641371106,
-2.6090936652735,-2.60559469433469,-2.60003254616515,-2.56442148225037,
-2.50406726932473,-2.49632694258815,-2.49379287875546,-2.49215405179859,
-2.49057891793114,-2.48826758809657,-2.48260013316845,-2.43937872987733,
-2.40168845675221,-2.38229308990374,-2.37722558143666,-2.37416865470849,
-2.37141723149979,-2.36790038581627,-2.36227030904764,-2.31516642473108,
-2.28153888883397,-2.26048297906383,-2.25704058779779,-2.25520365962458,
-2.25366833314637,-2.25175074997344,-2.2480455406783,-2.22343732013175,
-2.18108013194337,-2.14941496686595,-2.14155074734815,-2.13791800614312,
-2.13514809809557,-2.13251089763286,-2.12803679210106,-2.11572883732265,
-2.04270739292887,-2.02287505417673,-2.01947542767887,-2.0176453950244,
-2.01610790732421,-2.0141770156478,-2.01041108729613,-1.98204701900106,
-1.92479075014335,-1.91297925358472,-1.90435293890396,-1.90058395495811,
-1.89779349219172,-1.89519678345639,-1.89162944270307,-1.88251996069581,
-1.81266254311245,-1.78796889419894,-1.78278779448989,-1.78061963283496,
-1.77905408186768,-1.77757188155018,-1.7750072647872,-1.76770119044484,
-1.72488378750006,-1.68850174997462,-1.67594545340269,-1.66690264559348,
-1.66306239326959,-1.66025982027577,-1.65768030369917,-1.65418042343413,
-1.64547240122963,-1.59743633690341,-1.56212688730419,-1.55219198877646,
-1.5457054738535,-1.54333576803615,-1.54173178298661,-1.54029511554569,
-1.53796820681521,-1.53221741670429,-1.49562193104974,-1.47803507761506),
 .UNSPECIFIED.);
#829=B_SPLINE_CURVE_WITH_KNOTS('',3,(#98459,#98460,#98461,#98462,#98463,
#98464,#98465,#98466,#98467,#98468,#98469,#98470,#98471,#98472,#98473,#98474,
#98475,#98476,#98477,#98478,#98479,#98480,#98481,#98482,#98483,#98484,#98485,
#98486,#98487,#98488,#98489,#98490,#98491,#98492,#98493,#98494,#98495,#98496,
#98497,#98498,#98499,#98500,#98501,#98502,#98503,#98504,#98505,#98506,#98507,
#98508,#98509,#98510,#98511,#98512,#98513,#98514,#98515,#98516,#98517,#98518,
#98519,#98520,#98521,#98522,#98523,#98524,#98525,#98526,#98527,#98528,#98529,
#98530,#98531,#98532,#98533,#98534,#98535,#98536,#98537,#98538,#98539,#98540,
#98541,#98542,#98543,#98544,#98545,#98546,#98547,#98548,#98549,#98550,#98551,
#98552,#98553,#98554,#98555,#98556,#98557,#98558,#98559,#98560,#98561,#98562,
#98563,#98564,#98565,#98566,#98567,#98568,#98569,#98570,#98571,#98572,#98573,
#98574,#98575,#98576,#98577,#98578,#98579,#98580,#98581,#98582,#98583,#98584,
#98585,#98586,#98587,#98588,#98589,#98590,#98591,#98592,#98593,#98594,#98595,
#98596,#98597,#98598,#98599,#98600,#98601,#98602,#98603,#98604,#98605,#98606,
#98607,#98608,#98609,#98610,#98611,#98612,#98613,#98614,#98615,#98616,#98617,
#98618,#98619,#98620,#98621,#98622,#98623,#98624,#98625,#98626,#98627,#98628,
#98629,#98630,#98631,#98632,#98633,#98634,#98635,#98636,#98637,#98638,#98639,
#98640,#98641,#98642,#98643,#98644,#98645,#98646,#98647,#98648,#98649,#98650,
#98651,#98652,#98653,#98654,#98655,#98656,#98657,#98658,#98659,#98660,#98661,
#98662,#98663,#98664,#98665,#98666,#98667,#98668,#98669,#98670,#98671,#98672,
#98673,#98674),.UNSPECIFIED.,.F.,.F.,(4,2,2,2,2,2,2,2,2,2,2,2,2,2,2,2,2,
2,2,2,2,2,2,2,2,2,2,2,2,2,2,2,2,2,2,2,2,2,2,2,2,2,2,2,2,2,2,2,2,2,2,2,2,
2,2,2,2,2,2,2,2,2,2,2,2,2,2,2,2,2,2,2,2,2,2,2,2,2,2,2,2,2,2,2,2,2,2,2,2,
2,2,2,2,2,2,2,2,2,2,2,2,2,2,2,2,2,2,4),(-1.51231102550938,-1.50937795378451,
-1.5065575892059,-1.5028559415549,-1.4948704996413,-1.46173491400937,-1.41883717248856,
-1.41381874968353,-1.39625132694891,-1.39309937667654,-1.39112162685282,
-1.38956208308337,-1.3877221529687,-1.38434387898383,-1.36572181637724,
-1.30758876903333,-1.28187577983948,-1.27664570300112,-1.27322342327221,
-1.27044385722297,-1.26724415740081,-1.26165858777699,-1.23550874200421,
-1.16433896777091,-1.15715537125209,-1.15458032033267,-1.15308240502432,
-1.15149145486357,-1.1492717954386,-1.14388803196606,-1.1174941258089,-1.11399542278392,
-1.06582504404247,-1.04399981113337,-1.03853007460249,-1.03532393679724,
-1.03254494112992,-1.02913122264479,-1.02253455089204,-1.01417128633876,
-0.99492975249179,-0.960975205301778,-0.941888522027811,-0.921800609081408,
-0.918532314651245,-0.916519650731639,-0.914957441929174,-0.913143056947562,
-0.909882772945706,-0.893621379949587,-0.854143268104672,-0.80806810645506,
-0.802376332445633,-0.798813489944883,-0.79602091190884,-0.792912501232409,
-0.787744906062139,-0.76772795930744,-0.689058446235256,-0.682276588338172,
-0.679766776138107,-0.678281276463881,-0.676679806042403,-0.674407929542478,
-0.668710084178113,-0.639088837451255,-0.590721339391454,-0.569242800693029,
-0.563800563178923,-0.560599182519575,-0.557817368010485,-0.554391296161003,
-0.547742215746839,-0.503284418711376,-0.454771575717138,-0.445576276743383,
-0.442748356083229,-0.441028689960377,-0.43944296094844,-0.437250912072291,
-0.432027220060372,-0.407182439707801,-0.356593571960495,-0.332167885948443,
-0.326514170286668,-0.323267244046988,-0.320519058481895,-0.31717151635646,
-0.310888269430139,-0.261295333244967,-0.212345008996586,-0.206966340545937,
-0.204906089468333,-0.203429754876905,-0.201953601928911,-0.19978898497157,
-0.194808303689184,-0.187706196878368,-0.167678666386733,-0.150885307902492,
-0.0995906345809307,-0.0909097994206186,-0.0873849550592839,-0.0847737139333753,
-0.081923428716779,-0.0779930536770725,-0.0686142555213277,-0.0182935576830915),
 .UNSPECIFIED.);
#830=B_SPLINE_CURVE_WITH_KNOTS('',3,(#98678,#98679,#98680,#98681,#98682,
#98683),.UNSPECIFIED.,.F.,.F.,(4,1,1,4),(-4.09293042013064,-3.99338989784634,
-2.99504242338476,-2.06901289643202),.UNSPECIFIED.);
#831=B_SPLINE_CURVE_WITH_KNOTS('',3,(#98687,#98688,#98689,#98690,#98691,
#98692,#98693,#98694,#98695,#98696,#98697,#98698,#98699,#98700,#98701,#98702,
#98703,#98704,#98705,#98706,#98707,#98708,#98709,#98710,#98711,#98712,#98713,
#98714,#98715,#98716,#98717,#98718,#98719,#98720,#98721,#98722,#98723),
 .UNSPECIFIED.,.F.,.F.,(4,3,3,3,3,3,3,3,3,3,3,3,4),(0.,0.0974621470036353,
0.194867321320676,0.295359620101813,0.39274979403887,0.490157456371112,
0.587604110657141,0.685111293680858,0.78276525835489,0.880505077811792,
0.978410992324384,0.998805711569776,1.11730040836826),.UNSPECIFIED.);
#832=B_SPLINE_CURVE_WITH_KNOTS('',3,(#98725,#98726,#98727,#98728,#98729,
#98730,#98731,#98732,#98733,#98734,#98735,#98736,#98737,#98738,#98739,#98740,
#98741,#98742,#98743,#98744,#98745,#98746,#98747,#98748,#98749,#98750,#98751,
#98752,#98753,#98754,#98755,#98756,#98757,#98758,#98759,#98760,#98761,#98762,
#98763,#98764,#98765,#98766,#98767,#98768,#98769,#98770,#98771,#98772,#98773,
#98774,#98775,#98776,#98777,#98778,#98779,#98780,#98781,#98782,#98783,#98784,
#98785,#98786,#98787,#98788,#98789,#98790,#98791,#98792,#98793,#98794,#98795,
#98796,#98797,#98798,#98799,#98800,#98801,#98802,#98803,#98804,#98805,#98806,
#98807,#98808,#98809,#98810,#98811,#98812,#98813,#98814,#98815,#98816,#98817,
#98818,#98819,#98820,#98821,#98822,#98823,#98824,#98825,#98826,#98827,#98828,
#98829,#98830,#98831,#98832,#98833,#98834,#98835,#98836,#98837,#98838,#98839,
#98840,#98841,#98842,#98843,#98844,#98845,#98846,#98847,#98848,#98849,#98850,
#98851,#98852,#98853,#98854,#98855,#98856,#98857,#98858,#98859,#98860,#98861,
#98862,#98863,#98864,#98865,#98866,#98867,#98868,#98869,#98870,#98871,#98872,
#98873,#98874,#98875,#98876,#98877,#98878,#98879,#98880,#98881,#98882,#98883,
#98884,#98885,#98886,#98887,#98888,#98889,#98890,#98891,#98892,#98893,#98894,
#98895,#98896,#98897,#98898,#98899,#98900,#98901,#98902,#98903,#98904,#98905,
#98906,#98907,#98908,#98909,#98910,#98911,#98912,#98913,#98914,#98915,#98916,
#98917,#98918,#98919,#98920,#98921,#98922,#98923,#98924,#98925,#98926,#98927,
#98928,#98929,#98930,#98931,#98932),.UNSPECIFIED.,.F.,.F.,(4,3,3,3,3,3,
3,3,3,3,3,3,3,3,3,3,3,3,3,3,3,3,3,3,3,3,3,3,3,3,3,3,3,3,3,3,3,3,3,3,3,3,
3,3,3,3,3,3,3,3,3,3,3,3,3,3,3,3,3,3,3,3,3,3,3,3,3,3,3,4),(1.11730040857369,
1.21026936232094,1.30311793855996,1.39587642027055,1.48858757671237,1.58127988763124,
1.67398180531496,1.76677948692346,1.85963092734075,1.9526328138594,1.99761142313956,
2.09298165155123,2.188220560694,2.28335751558291,2.37842514156716,2.47345765340052,
2.56848143150041,2.66352284114503,2.75866633648478,2.85386709030249,2.94921898643841,
2.99641713470934,3.09181289507372,3.1870804966658,3.28224925142725,3.37735319725211,
3.47242482594695,3.56749048050769,3.66257649114042,3.75776847975029,3.85302001444509,
3.94842577423536,3.99522284627912,4.09032351438071,4.18529104306171,4.28015519178503,
4.37494905104444,4.46970730681924,4.56445668469983,4.65922389510171,4.75409518218335,
4.84902445655776,4.94410867188475,4.9940285578489,5.08928497076329,5.18441006852906,
5.27943338437871,5.37438813325423,5.46930829119369,5.564220388636,5.65915094149034,
5.75418553061646,5.84927833113956,5.9445248238826,5.99283426941868,6.08808320371743,
6.18320112491135,6.27821757512862,6.37316595376636,6.4680800519387,6.56298640897521,
6.65791154995309,6.75294126289703,6.8480294847337,6.94327190966745,6.99163998098847,
7.09673724801162,7.20153978237807,7.30582428634004,7.4004855048612),
 .UNSPECIFIED.);
#833=B_SPLINE_CURVE_WITH_KNOTS('',3,(#98934,#98935,#98936,#98937,#98938,
#98939,#98940,#98941,#98942,#98943),.UNSPECIFIED.,.F.,.F.,(4,1,1,1,1,1,
1,4),(7.40048571554784,7.99044569255824,8.98925140412801,9.98805711569779,
10.9868628272676,11.9856685388373,12.9844742504071,13.6836710227274),
 .UNSPECIFIED.);
#834=B_SPLINE_CURVE_WITH_KNOTS('',3,(#98945,#98946,#98947,#98948,#98949,
#98950,#98951,#98952,#98953,#98954,#98955,#98956,#98957,#98958,#98959,#98960,
#98961,#98962,#98963,#98964,#98965,#98966,#98967,#98968,#98969,#98970,#98971,
#98972,#98973,#98974,#98975,#98976,#98977,#98978,#98979,#98980,#98981,#98982,
#98983,#98984,#98985,#98986,#98987,#98988,#98989,#98990,#98991,#98992,#98993,
#98994,#98995,#98996,#98997,#98998,#98999,#99000,#99001,#99002,#99003,#99004,
#99005,#99006,#99007,#99008,#99009,#99010,#99011,#99012,#99013,#99014,#99015,
#99016,#99017,#99018,#99019,#99020,#99021,#99022,#99023,#99024,#99025,#99026,
#99027,#99028,#99029,#99030,#99031,#99032,#99033,#99034,#99035,#99036,#99037,
#99038,#99039,#99040,#99041,#99042,#99043,#99044,#99045,#99046,#99047,#99048,
#99049,#99050,#99051,#99052,#99053,#99054,#99055,#99056,#99057,#99058,#99059,
#99060,#99061,#99062,#99063,#99064,#99065,#99066,#99067,#99068,#99069,#99070,
#99071,#99072,#99073,#99074,#99075,#99076,#99077,#99078,#99079,#99080,#99081,
#99082,#99083,#99084,#99085,#99086,#99087,#99088,#99089,#99090,#99091,#99092,
#99093,#99094,#99095,#99096,#99097,#99098,#99099,#99100,#99101,#99102,#99103,
#99104,#99105,#99106,#99107,#99108,#99109,#99110,#99111,#99112,#99113,#99114,
#99115,#99116,#99117,#99118,#99119,#99120,#99121,#99122,#99123,#99124,#99125,
#99126,#99127,#99128,#99129,#99130,#99131,#99132,#99133,#99134,#99135,#99136,
#99137,#99138,#99139,#99140,#99141,#99142,#99143,#99144,#99145,#99146,#99147,
#99148,#99149,#99150,#99151,#99152),.UNSPECIFIED.,.F.,.F.,(4,3,3,3,3,3,
3,3,3,3,3,3,3,3,3,3,3,3,3,3,3,3,3,3,3,3,3,3,3,3,3,3,3,3,3,3,3,3,3,3,3,3,
3,3,3,3,3,3,3,3,3,3,3,3,3,3,3,3,3,3,3,3,3,3,3,3,3,3,3,4),(13.6836712041916,
13.797991322231,13.9138835030568,13.9832799619769,14.0785092135632,14.1736070391483,
14.2686030110431,14.3635304257209,14.4584232661345,14.55330809716,14.6482114691976,
14.7432191749856,14.8382852213964,14.9335054242281,14.9820856735467,15.0773147893924,
15.1724124783643,15.2674083129692,15.3623355899308,15.4572282924156,15.5521129854716,
15.6470162196709,15.7420237886646,15.8370896986706,15.9323097670429,15.9808913851164,
16.0761204340477,16.1712180545898,16.2662138193526,16.3611410246546,16.4560336543772,
16.5509182736553,16.645821433147,16.7408289264676,16.8358947601386,16.9311147518851,
16.9796970966862,17.0749262208139,17.1700239176513,17.2650197596961,17.3599470434276,
17.4548397522635,17.5497244512421,17.6446276909254,17.7396352646988,17.834701179091,
17.9299212511898,17.978502808256,18.0737319081004,18.1688295804472,18.2638253978294,
18.3587526567462,18.4536453406822,18.5485300147066,18.6434332294124,18.7384407783249,
18.8335066678857,18.9287267154421,18.9773085198258,19.0723820620226,19.1673242839475,
19.2621649731371,19.3569377633092,19.4516766625256,19.5464084270052,19.6411597992607,
19.7360155760681,19.8309310201432,19.925997941627,19.966856329907),
 .UNSPECIFIED.);
#835=B_SPLINE_CURVE_WITH_KNOTS('',3,(#99154,#99155,#99156,#99157,#99158,
#99159,#99160,#99161,#99162,#99163,#99164,#99165),.UNSPECIFIED.,.F.,.F.,
(4,2,1,1,1,1,1,1,4),(19.966856329907,19.9761142313955,20.9749199429653,
21.9737256545351,22.9725313661049,23.9713370776747,24.9701427892444,25.9689485008142,
26.2500372664898),.UNSPECIFIED.);
#836=B_SPLINE_CURVE_WITH_KNOTS('',3,(#99167,#99168,#99169,#99170,#99171,
#99172,#99173,#99174,#99175,#99176,#99177,#99178,#99179,#99180,#99181,#99182,
#99183,#99184,#99185,#99186,#99187,#99188,#99189,#99190,#99191,#99192,#99193,
#99194,#99195,#99196,#99197,#99198,#99199,#99200,#99201,#99202,#99203,#99204,
#99205,#99206,#99207,#99208,#99209,#99210,#99211,#99212,#99213,#99214,#99215,
#99216,#99217,#99218,#99219,#99220,#99221,#99222,#99223,#99224,#99225,#99226,
#99227,#99228,#99229,#99230,#99231,#99232,#99233,#99234,#99235,#99236,#99237,
#99238,#99239,#99240,#99241,#99242,#99243,#99244,#99245,#99246,#99247,#99248,
#99249,#99250,#99251,#99252,#99253,#99254,#99255,#99256,#99257,#99258,#99259,
#99260,#99261,#99262,#99263,#99264,#99265,#99266,#99267,#99268,#99269,#99270,
#99271,#99272,#99273,#99274,#99275,#99276,#99277,#99278,#99279,#99280,#99281,
#99282,#99283,#99284,#99285,#99286,#99287,#99288,#99289,#99290,#99291,#99292,
#99293,#99294,#99295,#99296,#99297,#99298,#99299,#99300,#99301,#99302,#99303,
#99304,#99305,#99306,#99307,#99308,#99309,#99310,#99311,#99312,#99313,#99314,
#99315,#99316,#99317,#99318,#99319,#99320,#99321,#99322,#99323,#99324,#99325,
#99326,#99327,#99328,#99329,#99330,#99331,#99332,#99333,#99334,#99335,#99336,
#99337,#99338,#99339,#99340,#99341,#99342,#99343,#99344,#99345,#99346,#99347,
#99348,#99349,#99350,#99351,#99352,#99353,#99354,#99355,#99356,#99357,#99358,
#99359,#99360,#99361,#99362,#99363,#99364,#99365,#99366,#99367,#99368,#99369,
#99370,#99371,#99372,#99373,#99374),.UNSPECIFIED.,.F.,.F.,(4,3,3,3,3,3,
3,3,3,3,3,3,3,3,3,3,3,3,3,3,3,3,3,3,3,3,3,3,3,3,3,3,3,3,3,3,3,3,3,3,3,3,
3,3,3,3,3,3,3,3,3,3,3,3,3,3,3,3,3,3,3,3,3,3,3,3,3,3,3,4),(26.2500416370866,
26.3441968333611,26.4383096251651,26.5324074449842,26.6265177047687,26.7207282412848,
26.8149931960284,26.9094154392851,26.967754212384,27.0629833121013,27.1580809842519,
27.2530768013692,27.3480040599197,27.4428967434264,27.5377814169589,27.6326846311107,
27.7276921793768,27.8227580682378,27.9179781150178,27.9665599239538,28.0617890236771,
28.1568866958333,28.2518825129561,28.3468097715119,28.4417024550238,28.5365871285611,
28.6314903427171,28.7264978909876,28.8215637798526,28.9167838266362,28.9653656355235,
29.060594735272,29.155692407454,29.2506882246028,29.3456154831852,29.440508166724,
29.5353928402884,29.6302960544723,29.7253036027704,29.8203694916634,29.9155895384748,
29.9641713470933,30.0594004468259,30.1544981189915,30.2494939361243,30.3444211946902,
30.4393138782123,30.5341985517602,30.6291017659269,30.7241093142081,30.8191752030844,
30.914395249879,30.9629770586631,31.0582061583978,31.1533038305661,31.2482996477012,
31.3432269062693,31.4381195897934,31.5330042633433,31.6279074775115,31.7229150257946,
31.8179809146729,31.9132009614694,31.9617827702329,32.0592107277751,32.1564851134588,
32.253594530523,32.3506070134981,32.4475346235577,32.5332269442662),
 .UNSPECIFIED.);
#837=B_SPLINE_CURVE_WITH_KNOTS('',3,(#99376,#99377,#99378,#99379,#99380,
#99381,#99382,#99383,#99384,#99385),.UNSPECIFIED.,.F.,.F.,(4,1,1,1,1,1,
1,4),(32.5332323413119,32.9605884818027,33.9593941933724,34.9581999049422,
35.957005616512,36.9558113280818,37.9546170396515,38.8164122514458),
 .UNSPECIFIED.);
#838=B_SPLINE_CURVE_WITH_KNOTS('',3,(#99387,#99388,#99389,#99390,#99391,
#99392,#99393,#99394,#99395,#99396,#99397),.UNSPECIFIED.,.F.,.F.,(4,1,1,
1,1,1,1,1,4),(38.8164122514458,38.9534227512213,39.9522284627911,40.9510341743609,
41.9498398859306,42.9486455975004,43.9474513090702,44.94625702064,45.0995975586254),
 .UNSPECIFIED.);
#839=B_SPLINE_CURVE_WITH_KNOTS('',3,(#99399,#99400,#99401,#99402,#99403,
#99404,#99405,#99406,#99407,#99408),.UNSPECIFIED.,.F.,.F.,(4,1,1,1,1,1,
1,4),(45.0995975586254,45.9450627322098,46.9438684437795,47.9426741553493,
48.9414798669191,49.9402855784889,50.9390912900586,51.3827784970663),
 .UNSPECIFIED.);
#840=B_SPLINE_CURVE_WITH_KNOTS('',3,(#99410,#99411,#99412,#99413,#99414,
#99415,#99416,#99417,#99418,#99419,#99420,#99421,#99422,#99423,#99424,#99425,
#99426,#99427,#99428,#99429,#99430,#99431,#99432,#99433,#99434,#99435,#99436,
#99437,#99438,#99439,#99440,#99441,#99442,#99443,#99444,#99445,#99446,#99447,
#99448,#99449,#99450,#99451,#99452,#99453,#99454,#99455,#99456,#99457,#99458,
#99459,#99460,#99461,#99462,#99463,#99464,#99465,#99466,#99467,#99468,#99469,
#99470,#99471,#99472,#99473,#99474,#99475,#99476,#99477,#99478,#99479,#99480,
#99481,#99482,#99483,#99484,#99485,#99486,#99487,#99488,#99489,#99490,#99491,
#99492,#99493,#99494,#99495,#99496,#99497,#99498,#99499,#99500,#99501,#99502,
#99503,#99504,#99505,#99506,#99507,#99508,#99509,#99510,#99511,#99512,#99513,
#99514,#99515,#99516,#99517,#99518,#99519,#99520,#99521,#99522,#99523,#99524,
#99525,#99526,#99527,#99528,#99529,#99530,#99531,#99532,#99533,#99534,#99535,
#99536,#99537,#99538,#99539,#99540,#99541,#99542,#99543,#99544,#99545,#99546,
#99547,#99548,#99549,#99550,#99551,#99552,#99553,#99554,#99555,#99556,#99557,
#99558,#99559,#99560,#99561,#99562,#99563,#99564,#99565,#99566,#99567,#99568,
#99569,#99570,#99571,#99572,#99573,#99574,#99575,#99576,#99577,#99578,#99579,
#99580,#99581,#99582,#99583,#99584,#99585,#99586,#99587,#99588,#99589,#99590,
#99591,#99592,#99593,#99594,#99595,#99596,#99597,#99598,#99599,#99600,#99601,
#99602,#99603,#99604,#99605,#99606,#99607,#99608,#99609,#99610,#99611,#99612,
#99613,#99614,#99615,#99616,#99617),.UNSPECIFIED.,.F.,.F.,(4,3,3,3,3,3,
3,3,3,3,3,3,3,3,3,3,3,3,3,3,3,3,3,3,3,3,3,3,3,3,3,3,3,3,3,3,3,3,3,3,3,3,
3,3,3,3,3,3,3,3,3,3,3,3,3,3,3,3,3,3,3,3,3,3,3,3,3,3,3,4),(51.382782865805,
51.4801713722121,51.5776322272777,51.6752689470314,51.772999404316,51.8709376684413,
51.9378970016284,52.0331261013645,52.1282237735339,52.2232195906702,52.3181468492396,
52.4130395327654,52.5079242063168,52.6028274204872,52.6978349687721,52.7929008576518,
52.88812090445,52.9367027131982,53.0319318129343,53.1270294851035,53.2220253022398,
53.3169525608094,53.4118452443351,53.5067299178866,53.601633132057,53.6966406803419,
53.7917065692213,53.8869266160196,53.935508424768,54.0307375245042,54.1258351966735,
54.2208310138099,54.3157582723794,54.4106509559052,54.5055356294566,54.6004388436268,
54.6954463919116,54.7905122807912,54.8857323275893,54.9343141363377,55.0295432360737,
55.1246409082431,55.2196367253796,55.3145639839491,55.4094566674749,55.5043413410262,
55.5992445551964,55.6942521034812,55.7893179923608,55.884538039159,55.9331198479075,
56.0283489476435,56.1234466198129,56.2184424369491,56.3133696955187,56.4082623790445,
56.503147052596,56.5980502667659,56.6930578150508,56.7881237039302,56.8833437507283,
56.9319255594773,57.0261632540803,57.1202810694238,57.2143068149925,57.3082681983479,
57.4022166769982,57.4961537969889,57.5901558500571,57.6659681729846),
 .UNSPECIFIED.);
#841=B_SPLINE_CURVE_WITH_KNOTS('',3,(#99619,#99620,#99621,#99622,#99623,
#99624,#99625,#99626,#99627,#99628,#99629,#99630,#99631,#99632,#99633,#99634,
#99635,#99636,#99637,#99638,#99639,#99640,#99641,#99642,#99643,#99644,#99645,
#99646,#99647,#99648,#99649,#99650,#99651,#99652,#99653,#99654,#99655,#99656,
#99657,#99658,#99659,#99660,#99661,#99662,#99663,#99664,#99665,#99666,#99667,
#99668,#99669,#99670,#99671,#99672,#99673,#99674,#99675,#99676,#99677,#99678,
#99679,#99680,#99681,#99682,#99683,#99684,#99685,#99686,#99687,#99688,#99689,
#99690,#99691,#99692,#99693,#99694,#99695,#99696,#99697,#99698,#99699,#99700,
#99701,#99702,#99703,#99704,#99705,#99706,#99707,#99708,#99709,#99710,#99711,
#99712,#99713,#99714,#99715,#99716,#99717,#99718,#99719,#99720,#99721,#99722,
#99723,#99724,#99725,#99726,#99727,#99728,#99729,#99730,#99731,#99732,#99733,
#99734,#99735,#99736,#99737,#99738,#99739,#99740,#99741,#99742,#99743,#99744,
#99745,#99746,#99747,#99748,#99749,#99750,#99751,#99752,#99753,#99754,#99755,
#99756,#99757,#99758,#99759,#99760,#99761,#99762,#99763,#99764,#99765,#99766,
#99767,#99768,#99769,#99770,#99771,#99772,#99773,#99774,#99775,#99776,#99777,
#99778,#99779,#99780,#99781,#99782,#99783,#99784,#99785,#99786,#99787,#99788,
#99789,#99790,#99791,#99792,#99793,#99794,#99795,#99796,#99797,#99798,#99799,
#99800,#99801,#99802,#99803,#99804,#99805,#99806,#99807,#99808,#99809,#99810,
#99811,#99812,#99813,#99814,#99815,#99816,#99817,#99818,#99819,#99820,#99821,
#99822,#99823,#99824,#99825,#99826,#99827,#99828,#99829),.UNSPECIFIED.,
 .F.,.F.,(4,3,3,3,3,3,3,3,3,3,3,3,3,3,3,3,3,3,3,3,3,3,3,3,3,3,3,3,3,3,3,
3,3,3,3,3,3,3,3,3,3,3,3,3,3,3,3,3,3,3,3,3,3,3,3,3,3,3,3,3,3,3,3,3,3,3,3,
3,3,3,4),(57.6659681731688,57.7852696288089,57.9069205713756,57.9307312710471,
58.0259603707832,58.1210580429527,58.2160538600891,58.3109811186587,58.4058738021845,
58.500758475736,58.5956616899063,58.6906692381912,58.7857351270709,58.8809551738691,
58.9295369826169,59.024766082353,59.1198637545224,59.2148595716588,59.3097868302282,
59.404679513754,59.4995641873054,59.5944674014757,59.6894749497605,59.7845408386401,
59.8797608854383,59.9283426941866,60.0235717939227,60.1186694660922,60.2136652832285,
60.308592541798,60.4034852253238,60.4983698988752,60.5932731130455,60.6882806613303,
60.78334655021,60.8785665970082,60.9271484057564,61.0223775054925,61.1174751776619,
61.2124709947983,61.3073982533678,61.4022909368936,61.497175610445,61.5920788246154,
61.6870863729002,61.7821522617799,61.8773723085781,61.9259541173262,62.0211832170623,
62.1162808892317,62.211276706368,62.3062039649375,62.4010966484633,62.4959813220147,
62.5908845361849,62.6858920844697,62.7809579733493,62.8761780201476,62.924759828896,
63.0199889286321,63.1150866008014,63.2100824179378,63.3050096765074,63.3999023600331,
63.4947870335845,63.5896902477548,63.6846977960397,63.7797636849193,63.8749837317175,
63.9235655404658,63.9491534801642),.UNSPECIFIED.);
#842=B_SPLINE_CURVE_WITH_KNOTS('',3,(#99831,#99832,#99833,#99834,#99835,
#99836,#99837,#99838,#99839,#99840,#99841,#99842,#99843,#99844,#99845,#99846,
#99847,#99848,#99849,#99850,#99851,#99852,#99853,#99854,#99855,#99856,#99857,
#99858,#99859,#99860,#99861,#99862,#99863,#99864,#99865,#99866,#99867,#99868,
#99869,#99870,#99871,#99872,#99873,#99874,#99875,#99876,#99877,#99878,#99879,
#99880,#99881,#99882,#99883,#99884,#99885,#99886,#99887,#99888,#99889,#99890,
#99891,#99892,#99893,#99894,#99895,#99896,#99897,#99898,#99899,#99900,#99901,
#99902,#99903,#99904,#99905,#99906,#99907,#99908,#99909,#99910,#99911,#99912,
#99913,#99914,#99915,#99916,#99917,#99918,#99919,#99920,#99921,#99922,#99923,
#99924,#99925,#99926,#99927,#99928,#99929,#99930,#99931,#99932,#99933,#99934,
#99935,#99936,#99937,#99938,#99939,#99940,#99941,#99942,#99943,#99944,#99945,
#99946,#99947,#99948,#99949,#99950,#99951,#99952,#99953,#99954,#99955,#99956,
#99957,#99958,#99959,#99960,#99961,#99962,#99963,#99964,#99965,#99966,#99967,
#99968,#99969,#99970,#99971,#99972,#99973,#99974,#99975,#99976,#99977,#99978,
#99979,#99980,#99981,#99982,#99983,#99984,#99985,#99986,#99987,#99988,#99989,
#99990,#99991,#99992,#99993,#99994,#99995,#99996,#99997,#99998,#99999,#100000,
#100001,#100002,#100003,#100004,#100005,#100006,#100007,#100008,#100009,
#100010,#100011,#100012,#100013,#100014,#100015,#100016,#100017,#100018,
#100019,#100020,#100021,#100022,#100023,#100024,#100025,#100026,#100027,
#100028,#100029,#100030,#100031,#100032,#100033,#100034,#100035,#100036,
#100037,#100038),.UNSPECIFIED.,.F.,.F.,(4,3,3,3,3,3,3,3,3,3,3,3,3,3,3,3,
3,3,3,3,3,3,3,3,3,3,3,3,3,3,3,3,3,3,3,3,3,3,3,3,3,3,3,3,3,3,3,3,3,3,3,3,
3,3,3,3,3,3,3,3,3,3,3,3,3,3,3,3,3,4),(63.9491534803492,64.0439714327274,
64.1386592433009,64.2366232443927,64.3311438921143,64.4256335614288,64.5201192947624,
64.6146281237261,64.7092427149105,64.8039206481598,64.8987448593486,64.9223712520355,
65.0176003517715,65.1126980239411,65.2076938410773,65.3026210996469,65.3975137831726,
65.4923984567238,65.587301670894,65.6823092191788,65.7773751080585,65.8725951548567,
65.9211769636053,66.0164060633414,66.1115037355109,66.2064995526472,66.3014268112167,
66.3963194947426,66.4912041682941,66.5861073824644,66.6811149307493,66.7761808196289,
66.8714008664272,66.9199826751751,67.0152117749112,67.1103094470804,67.2053052642169,
67.3002325227864,67.3951252063121,67.4900098798635,67.5849130940337,67.6799206423185,
67.7749865311982,67.8702065779964,67.9187883867448,68.0140174864809,68.1091151586503,
68.2041109757866,68.2990382343561,68.3939309178818,68.4888155914332,68.5837188056033,
68.6787263538881,68.7737922427677,68.8690122895659,68.9175940983146,69.0128231980508,
69.1079208702203,69.202916687357,69.2978439459265,69.3927366294522,69.4876213030037,
69.5825245171741,69.6775320654589,69.7725979543382,69.8678180011363,69.9163998098844,
70.0302968077158,70.1429109804956,70.232338577275),.UNSPECIFIED.);
#843=B_SPLINE_CURVE_WITH_KNOTS('',3,(#100040,#100041,#100042,#100043,#100044,
#100045,#100046,#100047,#100048,#100049),.UNSPECIFIED.,.F.,.F.,(4,1,1,1,
1,1,1,4),(70.2323387873437,70.9152055214542,71.9140112330239,72.9128169445937,
73.9116226561635,74.9104283677333,75.9092340793031,76.5155240945233),
 .UNSPECIFIED.);
#844=B_SPLINE_CURVE_WITH_KNOTS('',3,(#100051,#100052,#100053,#100054,#100055,
#100056,#100057,#100058,#100059,#100060),.UNSPECIFIED.,.F.,.F.,(4,1,1,1,
1,1,1,4),(76.5155240945233,76.9080397908728,77.9068455024426,78.9056512140124,
79.9044569255822,80.903262637152,81.9020683487218,82.7987004857864),
 .UNSPECIFIED.);
#845=B_SPLINE_CURVE_WITH_KNOTS('',3,(#100062,#100063,#100064,#100065,#100066,
#100067,#100068,#100069,#100070,#100071,#100072,#100073,#100074,#100075,
#100076,#100077,#100078,#100079,#100080,#100081,#100082,#100083,#100084,
#100085,#100086,#100087,#100088,#100089,#100090,#100091,#100092,#100093,
#100094,#100095,#100096,#100097,#100098,#100099,#100100,#100101,#100102,
#100103,#100104,#100105,#100106,#100107,#100108,#100109,#100110,#100111,
#100112,#100113,#100114,#100115,#100116,#100117,#100118,#100119,#100120,
#100121,#100122,#100123,#100124,#100125,#100126,#100127,#100128,#100129,
#100130,#100131,#100132,#100133,#100134,#100135,#100136,#100137,#100138,
#100139,#100140,#100141,#100142,#100143,#100144,#100145,#100146,#100147,
#100148,#100149,#100150,#100151,#100152,#100153,#100154,#100155,#100156,
#100157,#100158,#100159,#100160,#100161,#100162,#100163,#100164,#100165,
#100166,#100167,#100168,#100169,#100170,#100171,#100172,#100173,#100174,
#100175,#100176,#100177,#100178,#100179,#100180,#100181,#100182,#100183,
#100184,#100185,#100186,#100187,#100188,#100189,#100190,#100191,#100192,
#100193,#100194,#100195,#100196,#100197,#100198,#100199,#100200,#100201,
#100202,#100203,#100204,#100205,#100206,#100207,#100208,#100209,#100210,
#100211,#100212,#100213,#100214,#100215,#100216,#100217,#100218,#100219,
#100220,#100221,#100222,#100223,#100224,#100225,#100226,#100227,#100228,
#100229,#100230,#100231,#100232,#100233,#100234,#100235,#100236,#100237,
#100238,#100239,#100240,#100241,#100242,#100243,#100244,#100245,#100246,
#100247,#100248,#100249,#100250,#100251,#100252,#100253,#100254,#100255,
#100256,#100257,#100258,#100259,#100260,#100261,#100262,#100263,#100264,
#100265,#100266,#100267,#100268,#100269),.UNSPECIFIED.,.F.,.F.,(4,3,3,3,
3,3,3,3,3,3,3,3,3,3,3,3,3,3,3,3,3,3,3,3,3,3,3,3,3,3,3,3,3,3,3,3,3,3,3,3,
3,3,3,3,3,3,3,3,3,3,3,3,3,3,3,3,3,3,3,3,3,3,3,3,3,3,3,3,3,4),(82.7987094017029,
82.9008740602915,82.9961031600276,83.091200832197,83.1861966493334,83.2811239079029,
83.3760165914286,83.47090126498,83.5658044791504,83.6608120274352,83.7558779163149,
83.8510979631131,83.8996797718613,83.9949088715974,84.0900065437669,84.1850023609033,
84.2799296194728,84.3748223029986,84.46970697655,84.5646101907203,84.6596177390052,
84.7546836278848,84.8499036746831,84.8984854834311,84.9937145831671,85.0888122553365,
85.1838080724728,85.2787353310423,85.373628014568,85.4685126881194,85.5634159022897,
85.6584234505745,85.7534893394541,85.8487093862523,85.8972911950008,85.9925202947369,
86.0876179669063,86.1826137840427,86.2775410426122,86.3724337261379,86.4673183996893,
86.5622216138596,86.6572291621444,86.7522950510241,86.8475150978223,86.8960969065706,
86.9913260063067,87.0864236784762,87.1814194956125,87.276346754182,87.3712394377078,
87.4661241112593,87.5610273254296,87.6560348737144,87.7511007625941,87.8463208093923,
87.8949026181404,87.9901317178765,88.0852293900459,88.1802252071822,88.2751524657517,
88.3700451492774,88.4649298228288,88.5598330369991,88.6548405852839,88.7499064741636,
88.8451265209618,88.8937083297102,89.03459316754,89.0818947088825),
 .UNSPECIFIED.);
#846=B_SPLINE_CURVE_WITH_KNOTS('',3,(#100271,#100272,#100273,#100274,#100275,
#100276,#100277,#100278,#100279,#100280),.UNSPECIFIED.,.F.,.F.,(4,1,1,1,
1,1,1,4),(89.08189908702,89.8925140412799,90.8913197528497,91.8901254644195,
92.8889311759893,93.8877368875591,94.8865425991288,95.365078400473),
 .UNSPECIFIED.);
#847=B_SPLINE_CURVE_WITH_KNOTS('',3,(#100282,#100283,#100284,#100285,#100286,
#100287,#100288,#100289,#100290,#100291,#100292,#100293,#100294,#100295,
#100296,#100297,#100298,#100299,#100300,#100301,#100302,#100303,#100304,
#100305,#100306,#100307,#100308,#100309,#100310,#100311,#100312,#100313,
#100314,#100315,#100316,#100317,#100318,#100319,#100320,#100321,#100322,
#100323,#100324,#100325,#100326,#100327,#100328,#100329,#100330,#100331,
#100332,#100333,#100334,#100335,#100336,#100337,#100338,#100339,#100340,
#100341,#100342,#100343,#100344,#100345,#100346,#100347,#100348,#100349,
#100350,#100351,#100352,#100353,#100354,#100355,#100356,#100357,#100358,
#100359,#100360,#100361,#100362,#100363,#100364,#100365,#100366,#100367,
#100368,#100369,#100370,#100371,#100372,#100373,#100374,#100375,#100376,
#100377,#100378,#100379,#100380,#100381,#100382,#100383,#100384,#100385,
#100386,#100387,#100388,#100389,#100390,#100391,#100392,#100393,#100394,
#100395,#100396,#100397,#100398,#100399,#100400,#100401,#100402,#100403,
#100404,#100405,#100406,#100407,#100408,#100409,#100410,#100411,#100412,
#100413,#100414,#100415,#100416,#100417,#100418,#100419,#100420,#100421,
#100422,#100423,#100424,#100425,#100426,#100427,#100428,#100429,#100430,
#100431,#100432,#100433,#100434,#100435,#100436,#100437,#100438,#100439,
#100440,#100441,#100442,#100443,#100444,#100445,#100446,#100447,#100448,
#100449,#100450,#100451,#100452,#100453,#100454,#100455,#100456,#100457,
#100458,#100459,#100460,#100461,#100462,#100463,#100464,#100465,#100466,
#100467,#100468,#100469,#100470,#100471,#100472,#100473,#100474,#100475,
#100476,#100477,#100478,#100479,#100480,#100481,#100482,#100483,#100484,
#100485,#100486,#100487,#100488,#100489,#100490,#100491,#100492),
 .UNSPECIFIED.,.F.,.F.,(4,3,3,3,3,3,3,3,3,3,3,3,3,3,3,3,3,3,3,3,3,3,3,3,
3,3,3,3,3,3,3,3,3,3,3,3,3,3,3,3,3,3,3,3,3,3,3,3,3,3,3,3,3,3,3,3,3,3,3,3,
3,3,3,3,3,3,3,3,3,3,4),(95.3650800160621,95.463654469693,95.5623452628044,
95.6612541125098,95.7602864476327,95.8595327072477,95.8853483106986,95.9805774104347,
96.075675082604,96.1706708997406,96.2655981583101,96.3604908418358,96.4553755153873,
96.5502787295579,96.6452862778428,96.7403521667226,96.8355722135207,96.8841540222684,
96.9793831220044,97.0744807941739,97.1694766113103,97.2644038698798,97.3592965534056,
97.4541812269571,97.5490844411273,97.6440919894121,97.7391578782916,97.8343779250898,
97.8829597338382,97.9781888335742,98.0732865057437,98.1682823228801,98.2632095814496,
98.3581022649753,98.4529869385267,98.5478901526971,98.6428977009819,98.7379635898615,
98.8331836366598,98.881765445408,98.976994545144,99.0720922173134,99.16708803445,
99.2620152930194,99.356907976545,99.4517926500964,99.5466958642667,99.6417034125515,
99.736769301431,99.8319893482292,99.8805711569777,99.9758002567139,100.070897928884,
100.16589374602,100.26082100459,100.355713688116,100.450598361667,100.545501575838,
100.640509124123,100.735575013002,100.830795059801,100.879376868548,100.975487925385,
101.06932774662,101.163078924259,101.256769403842,101.354643383692,101.448325851882,
101.542026129326,101.635804369266,101.648265323242),.UNSPECIFIED.);
#848=B_SPLINE_CURVE_WITH_KNOTS('',3,(#100494,#100495,#100496,#100497,#100498,
#100499,#100500,#100501,#100502,#100503,#100504),.UNSPECIFIED.,.F.,.F.,
(4,1,1,1,1,1,1,1,4),(101.648265323242,101.878182580117,102.876988291687,
103.875794003257,104.874599714827,105.873405426396,106.872211137966,107.871016849536,
107.931450630421),.UNSPECIFIED.);
#849=B_SPLINE_CURVE_WITH_KNOTS('',3,(#100506,#100507,#100508,#100509,#100510,
#100511,#100512,#100513,#100514,#100515,#100516,#100517,#100518,#100519,
#100520,#100521,#100522,#100523,#100524,#100525,#100526,#100527,#100528,
#100529,#100530,#100531,#100532,#100533,#100534,#100535,#100536,#100537,
#100538,#100539,#100540,#100541,#100542,#100543,#100544,#100545,#100546,
#100547,#100548,#100549,#100550,#100551,#100552,#100553,#100554,#100555,
#100556,#100557,#100558,#100559,#100560,#100561,#100562,#100563,#100564,
#100565,#100566,#100567,#100568,#100569,#100570,#100571,#100572,#100573,
#100574,#100575,#100576,#100577,#100578,#100579,#100580,#100581,#100582,
#100583,#100584,#100585,#100586,#100587,#100588,#100589,#100590,#100591,
#100592,#100593,#100594,#100595,#100596,#100597,#100598,#100599,#100600,
#100601,#100602,#100603,#100604,#100605,#100606,#100607,#100608,#100609,
#100610,#100611,#100612,#100613,#100614,#100615,#100616,#100617,#100618,
#100619,#100620,#100621,#100622,#100623,#100624,#100625,#100626,#100627,
#100628,#100629,#100630,#100631,#100632,#100633,#100634,#100635,#100636,
#100637,#100638,#100639,#100640,#100641,#100642,#100643,#100644,#100645,
#100646,#100647,#100648,#100649,#100650,#100651,#100652,#100653,#100654,
#100655,#100656,#100657,#100658,#100659,#100660,#100661,#100662,#100663,
#100664,#100665,#100666,#100667,#100668,#100669,#100670,#100671,#100672,
#100673,#100674,#100675,#100676,#100677,#100678,#100679,#100680,#100681,
#100682,#100683,#100684,#100685,#100686,#100687,#100688,#100689,#100690,
#100691,#100692,#100693,#100694,#100695,#100696,#100697,#100698,#100699,
#100700,#100701,#100702,#100703,#100704,#100705,#100706,#100707,#100708,
#100709,#100710,#100711,#100712,#100713),.UNSPECIFIED.,.F.,.F.,(4,3,3,3,
3,3,3,3,3,3,3,3,3,3,3,3,3,3,3,3,3,3,3,3,3,3,3,3,3,3,3,3,3,3,3,3,3,3,3,3,
3,3,3,3,3,3,3,3,3,3,3,3,3,3,3,3,3,3,3,3,3,3,3,3,3,3,3,3,3,4),(107.931450630421,
108.025811128759,108.120045947231,108.214181269951,108.308262491448,108.402317130539,
108.496372674529,108.590519784193,108.684711144256,108.779067231775,108.869822561106,
108.965051660842,109.060149333012,109.155145150148,109.250072408718,109.344965092244,
109.439849765795,109.534752979965,109.62976052825,109.72482641713,109.820046463928,
109.868628272676,109.963857372412,110.058955044581,110.153950861717,110.248878120286,
110.343770803812,110.438655477363,110.533558691533,110.628566239817,110.723632128697,
110.818852175495,110.867433984245,110.962663083981,111.05776075615,111.152756573287,
111.247683831856,111.342576515382,111.437461188933,111.532364403104,111.627371951389,
111.722437840268,111.817657887066,111.866239695815,111.961468795551,112.056566467721,
112.151562284858,112.246489543427,112.341382226953,112.436266900505,112.531170114675,
112.62617766296,112.72124355184,112.816463598639,112.865045407385,112.960274507121,
113.05537217929,113.150367996427,113.245295254996,113.340187938522,113.435072612074,
113.529975826244,113.624983374529,113.720049263408,113.815269310207,113.863851118955,
113.973858328726,114.083374018364,114.192041198982,114.214635694482),
 .UNSPECIFIED.);
#850=B_SPLINE_CURVE_WITH_KNOTS('',3,(#100715,#100716,#100717,#100718,#100719,
#100720,#100721,#100722,#100723,#100724),.UNSPECIFIED.,.F.,.F.,(4,1,1,1,
1,1,1,4),(114.214635937601,114.862656830524,115.861462542094,116.860268253664,
117.859073965234,118.857879676803,119.856685388373,120.49782124478),
 .UNSPECIFIED.);
#851=B_SPLINE_CURVE_WITH_KNOTS('',3,(#100726,#100727,#100728,#100729,#100730,
#100731,#100732,#100733,#100734,#100735,#100736,#100737,#100738,#100739,
#100740,#100741,#100742,#100743,#100744,#100745,#100746,#100747,#100748,
#100749,#100750,#100751,#100752,#100753,#100754,#100755,#100756,#100757,
#100758,#100759,#100760,#100761,#100762,#100763,#100764,#100765,#100766,
#100767,#100768,#100769,#100770,#100771,#100772,#100773,#100774,#100775,
#100776,#100777,#100778,#100779,#100780,#100781,#100782,#100783,#100784,
#100785,#100786,#100787,#100788,#100789,#100790,#100791,#100792,#100793,
#100794,#100795,#100796,#100797,#100798,#100799,#100800,#100801,#100802,
#100803,#100804,#100805,#100806,#100807,#100808,#100809,#100810,#100811,
#100812,#100813,#100814,#100815,#100816,#100817,#100818,#100819,#100820,
#100821,#100822,#100823,#100824,#100825,#100826,#100827,#100828,#100829,
#100830,#100831,#100832,#100833,#100834,#100835,#100836,#100837,#100838,
#100839,#100840,#100841,#100842,#100843,#100844,#100845,#100846,#100847,
#100848,#100849,#100850,#100851,#100852,#100853,#100854,#100855,#100856,
#100857,#100858,#100859,#100860,#100861,#100862,#100863,#100864,#100865,
#100866,#100867,#100868,#100869,#100870,#100871,#100872,#100873,#100874,
#100875,#100876,#100877,#100878,#100879,#100880,#100881,#100882,#100883,
#100884,#100885,#100886,#100887,#100888,#100889,#100890,#100891,#100892,
#100893,#100894,#100895,#100896,#100897,#100898,#100899,#100900,#100901,
#100902,#100903,#100904,#100905,#100906,#100907,#100908,#100909,#100910,
#100911,#100912,#100913,#100914,#100915,#100916,#100917,#100918,#100919,
#100920,#100921,#100922,#100923,#100924,#100925,#100926,#100927,#100928,
#100929,#100930,#100931,#100932,#100933),.UNSPECIFIED.,.F.,.F.,(4,3,3,3,
3,3,3,3,3,3,3,3,3,3,3,3,3,3,3,3,3,3,3,3,3,3,3,3,3,3,3,3,3,3,3,3,3,3,3,3,
3,3,3,3,3,3,3,3,3,3,3,3,3,3,3,3,3,3,3,3,3,3,3,3,3,3,3,3,3,4),(120.497821489681,
120.606047186385,120.714828214309,120.824262399715,120.855491099943,120.950720199679,
121.045817871849,121.140813688985,121.235740947555,121.33063363108,121.425518304632,
121.520421518802,121.615429067087,121.710494955967,121.805715002765,121.854296811513,
121.949525911249,122.044623583418,122.139619400555,122.234546659124,122.32943934265,
122.424324016201,122.519227230372,122.614234778656,122.709300667536,122.804520714334,
122.853102523083,122.948331622818,123.043429294987,123.138425112122,123.233352370691,
123.328245054216,123.423129727767,123.518032941936,123.61304049022,123.708106379099,
123.803326425896,123.851908234652,123.94713733439,124.042235006561,124.137230823699,
124.232158082271,124.327050765798,124.421935439352,124.516838653524,124.61184620181,
124.706912090692,124.802132137492,124.850713946222,124.945943045957,125.041040718125,
125.13603653526,125.230963793828,125.325856477352,125.420741150902,125.515644365071,
125.610651913355,125.705717802233,125.80093784903,125.849519657792,125.943831432675,
126.038012641317,126.132086892519,126.226102626881,126.320087437328,126.414068880704,
126.508133752517,126.60223937965,126.696499648658,126.78100655196),
 .UNSPECIFIED.);
#852=B_SPLINE_CURVE_WITH_KNOTS('',3,(#100935,#100936,#100937,#100938,#100939,
#100940,#100941,#100942,#100943,#100944,#100945),.UNSPECIFIED.,.F.,.F.,
(4,1,1,1,1,1,1,1,4),(126.78100655196,126.848325369362,127.847131080932,
128.845936792501,129.844742504071,130.843548215641,131.842353927211,132.84115963878,
133.06419185914),.UNSPECIFIED.);
#853=B_SPLINE_CURVE_WITH_KNOTS('',3,(#100947,#100948,#100949,#100950,#100951,
#100952,#100953,#100954,#100955,#100956,#100957,#100958,#100959,#100960,
#100961,#100962,#100963,#100964,#100965,#100966,#100967,#100968,#100969,
#100970,#100971,#100972,#100973,#100974,#100975,#100976,#100977,#100978,
#100979,#100980,#100981,#100982,#100983,#100984,#100985,#100986,#100987,
#100988,#100989,#100990,#100991,#100992,#100993,#100994,#100995,#100996,
#100997,#100998,#100999,#101000,#101001,#101002,#101003,#101004,#101005,
#101006,#101007,#101008,#101009,#101010,#101011,#101012,#101013,#101014,
#101015,#101016,#101017,#101018,#101019,#101020,#101021,#101022,#101023,
#101024,#101025,#101026,#101027,#101028,#101029,#101030,#101031,#101032,
#101033,#101034,#101035,#101036,#101037,#101038,#101039,#101040,#101041,
#101042,#101043,#101044,#101045,#101046,#101047,#101048,#101049,#101050,
#101051,#101052,#101053,#101054,#101055,#101056,#101057,#101058,#101059,
#101060,#101061,#101062,#101063,#101064,#101065,#101066,#101067,#101068,
#101069,#101070,#101071,#101072,#101073,#101074,#101075,#101076,#101077,
#101078,#101079,#101080,#101081,#101082,#101083,#101084,#101085,#101086,
#101087,#101088,#101089,#101090,#101091,#101092,#101093,#101094,#101095,
#101096,#101097,#101098,#101099,#101100,#101101,#101102,#101103,#101104,
#101105,#101106,#101107,#101108,#101109,#101110,#101111,#101112,#101113,
#101114,#101115,#101116,#101117,#101118,#101119,#101120,#101121,#101122,
#101123,#101124,#101125,#101126,#101127,#101128,#101129,#101130,#101131,
#101132,#101133,#101134,#101135,#101136,#101137,#101138,#101139,#101140,
#101141,#101142,#101143,#101144,#101145,#101146,#101147,#101148,#101149,
#101150,#101151,#101152,#101153,#101154,#101155,#101156,#101157),
 .UNSPECIFIED.,.F.,.F.,(4,3,3,3,3,3,3,3,3,3,3,3,3,3,3,3,3,3,3,3,3,3,3,3,
3,3,3,3,3,3,3,3,3,3,3,3,3,3,3,3,3,3,3,3,3,3,3,3,3,3,3,3,3,3,3,3,3,3,3,3,
3,3,3,3,3,3,3,3,3,3,4),(133.06419185914,133.161163545541,133.254836014875,
133.348471030653,133.442096465485,133.535740176565,133.629484588454,133.723289562586,
133.817238172544,133.83996535035,133.93519444913,134.030292120345,134.125287936529,
134.220215194155,134.315107876743,134.409992549363,134.504895762609,134.599903309987,
134.694969197968,134.790189243889,134.83877106192,134.934000161428,135.02909783336,
135.124093650249,135.219020908559,135.313913591817,135.408798265093,135.503701478981,
135.598709026974,135.693774915557,135.788994962053,135.83757677349,135.932805877182,
136.027903553322,136.122899374438,136.217826636983,136.312719324482,136.407604001998,
136.502507220119,136.597514772312,136.69258066508,136.787800715699,136.836382485059,
136.931611577449,137.02670924228,137.121705052093,137.216632303392,137.311524979684,
137.406409646045,137.501312853078,137.596320394349,137.691386276274,137.786606316277,
137.835188196629,137.930417297129,138.025514969997,138.120510787766,138.21543804687,
138.310330730868,138.405215404831,138.500118619351,138.595126167891,138.690192056973,
138.785412103889,138.833993908199,138.933518394371,139.036983087358,139.136092611983,
139.235066506161,139.333886280039,139.347377166319),.UNSPECIFIED.);
#854=B_SPLINE_CURVE_WITH_KNOTS('',3,(#101159,#101160,#101161,#101162,#101163,
#101164,#101165,#101166,#101167,#101168),.UNSPECIFIED.,.F.,.F.,(4,1,1,1,
1,1,1,4),(139.347378254301,139.832799619769,140.831605331339,141.830411042908,
142.829216754478,143.828022466048,144.826828177618,145.630562473499),
 .UNSPECIFIED.);
#855=B_SPLINE_CURVE_WITH_KNOTS('',3,(#101170,#101171,#101172,#101173,#101174,
#101175,#101176,#101177,#101178,#101179),.UNSPECIFIED.,.F.,.F.,(4,1,1,1,
1,1,1,4),(145.630562473499,145.825633889187,146.824439600757,147.823245312327,
148.822051023897,149.820856735467,150.819662447036,151.160872120126),
 .UNSPECIFIED.);
#856=B_SPLINE_CURVE_WITH_KNOTS('',3,(#101183,#101184,#101185,#101186,#101187,
#101188,#101189,#101190,#101191,#101192,#101193,#101194,#101195,#101196,
#101197,#101198,#101199,#101200,#101201,#101202,#101203,#101204,#101205,
#101206,#101207,#101208,#101209,#101210,#101211,#101212,#101213,#101214,
#101215,#101216,#101217,#101218,#101219,#101220,#101221,#101222,#101223,
#101224,#101225,#101226,#101227,#101228,#101229,#101230,#101231,#101232,
#101233,#101234,#101235,#101236,#101237,#101238,#101239,#101240,#101241,
#101242,#101243,#101244,#101245,#101246,#101247,#101248,#101249,#101250,
#101251,#101252,#101253,#101254,#101255,#101256,#101257,#101258,#101259,
#101260,#101261,#101262,#101263,#101264,#101265,#101266,#101267,#101268,
#101269,#101270,#101271,#101272,#101273,#101274,#101275,#101276,#101277,
#101278,#101279,#101280,#101281,#101282,#101283,#101284,#101285,#101286,
#101287,#101288,#101289,#101290,#101291,#101292,#101293,#101294,#101295,
#101296,#101297,#101298,#101299,#101300,#101301,#101302,#101303,#101304,
#101305,#101306,#101307,#101308,#101309,#101310,#101311,#101312,#101313,
#101314,#101315,#101316,#101317,#101318,#101319,#101320,#101321,#101322,
#101323,#101324,#101325,#101326,#101327,#101328,#101329,#101330,#101331,
#101332,#101333),.UNSPECIFIED.,.F.,.F.,(4,3,3,3,3,3,3,3,3,3,3,3,3,3,3,3,
3,3,3,3,3,3,3,3,3,3,3,3,3,3,3,3,3,3,3,3,3,3,3,3,3,3,3,3,3,3,3,3,3,3,4),
(-153.229489605841,-153.13007506582,-153.030363631848,-152.930499334661,
-152.830341227169,-152.747163592623,-152.651787242391,-152.556542086082,
-152.461398768752,-152.366324659609,-152.271285582085,-152.176255164369,
-152.08120704973,-151.98605691229,-151.890849469052,-151.795491178329,-151.748816118161,
-151.653415212671,-151.558142356049,-151.462968244962,-151.367858839775,
-151.272781679139,-151.177710427419,-151.082618761718,-150.987421187822,
-150.892164024966,-150.796752931837,-150.750468643699,-150.655362433477,
-150.56038925176,-150.465519347467,-150.370719626968,-150.275955435646,
-150.181200054995,-150.086426781627,-149.991549499601,-149.896614184718,
-149.801524227629,-149.752121169238,-149.656859041422,-149.561728112202,
-149.466698857429,-149.371738058406,-149.27681177294,-149.181893478322,
-149.086956666316,-148.991915884423,-148.896816845217,-148.801564410731,
-148.753773694776,-148.606192485261),.UNSPECIFIED.);
#857=B_SPLINE_CURVE_WITH_KNOTS('',3,(#101335,#101336,#101337,#101338,#101339,
#101340,#101341,#101342,#101343,#101344),.UNSPECIFIED.,.F.,.F.,(4,1,1,1,
1,1,1,4),(-148.606185112125,-147.755426220315,-146.757078745853,-145.758731271391,
-144.76038379693,-143.762036322468,-142.763688848007,-142.323011718186),
 .UNSPECIFIED.);
#858=B_SPLINE_CURVE_WITH_KNOTS('',3,(#101346,#101347,#101348,#101349,#101350,
#101351,#101352,#101353,#101354,#101355,#101356,#101357,#101358,#101359,
#101360,#101361,#101362,#101363,#101364,#101365,#101366,#101367,#101368,
#101369,#101370,#101371,#101372,#101373,#101374,#101375,#101376,#101377,
#101378,#101379,#101380,#101381,#101382,#101383,#101384,#101385,#101386,
#101387,#101388,#101389,#101390,#101391,#101392,#101393,#101394,#101395,
#101396,#101397,#101398,#101399,#101400,#101401,#101402,#101403,#101404,
#101405,#101406,#101407,#101408,#101409,#101410,#101411,#101412,#101413,
#101414,#101415,#101416,#101417,#101418,#101419,#101420,#101421,#101422,
#101423,#101424,#101425,#101426,#101427,#101428,#101429,#101430,#101431,
#101432,#101433,#101434,#101435,#101436,#101437,#101438,#101439,#101440,
#101441,#101442,#101443,#101444,#101445,#101446,#101447,#101448,#101449,
#101450,#101451,#101452,#101453,#101454,#101455,#101456,#101457,#101458,
#101459,#101460,#101461,#101462,#101463,#101464,#101465,#101466,#101467,
#101468,#101469,#101470,#101471,#101472,#101473,#101474,#101475,#101476,
#101477,#101478,#101479,#101480,#101481,#101482,#101483,#101484,#101485,
#101486,#101487,#101488,#101489,#101490,#101491,#101492,#101493,#101494,
#101495,#101496,#101497,#101498,#101499,#101500,#101501,#101502,#101503,
#101504,#101505,#101506,#101507,#101508,#101509,#101510,#101511,#101512,
#101513,#101514,#101515,#101516,#101517,#101518,#101519,#101520,#101521,
#101522,#101523,#101524,#101525,#101526,#101527,#101528,#101529,#101530,
#101531,#101532,#101533,#101534,#101535,#101536,#101537,#101538,#101539,
#101540,#101541,#101542,#101543,#101544,#101545,#101546,#101547,#101548,
#101549,#101550,#101551,#101552,#101553),.UNSPECIFIED.,.F.,.F.,(4,3,3,3,
3,3,3,3,3,3,3,3,3,3,3,3,3,3,3,3,3,3,3,3,3,3,3,3,3,3,3,3,3,3,3,3,3,3,3,3,
3,3,3,3,3,3,3,3,3,3,3,3,3,3,3,3,3,3,3,3,3,3,3,3,3,3,3,3,3,4),(-142.323007178082,
-142.225700249726,-142.128324098792,-142.030775269004,-141.933134923198,
-141.835287450591,-141.765341373545,-141.670107095845,-141.575004137981,
-141.480002935616,-141.385070189996,-141.290171947565,-141.195281650218,
-141.10037275427,-141.005359593337,-140.910288048079,-140.815062640428,
-140.766993899084,-140.671759096531,-140.576655606462,-140.481653865323,
-140.386720573393,-140.291821780179,-140.196930928246,-140.102021474583,
-140.007007754557,-139.911935648591,-139.816709683177,-139.768646424622,
-139.673411759562,-139.57830840789,-139.48330680585,-139.388373653479,-139.293475000054,
-139.198584287968,-139.103674974034,-139.008661392702,-138.913589425047,
-138.818363595997,-138.77029895016,-138.675064351112,-138.579961066957,
-138.484959533839,-138.390026452196,-138.295127870597,-138.200237231348,
-138.105327991176,-138.010314484572,-137.915242592306,-137.820016838941,
-137.771951475699,-137.67671680145,-137.581613440991,-137.486611830579,
-137.391678670491,-137.296780009761,-137.201889290791,-137.106979970405,
-137.011966383323,-136.916894410309,-136.821668576563,-136.773604001237,
-136.679360684964,-136.585237144751,-136.491205576827,-136.397238279117,
-136.303283812116,-136.209340629697,-136.115332569317,-136.039821870902),
 .UNSPECIFIED.);
#859=B_SPLINE_CURVE_WITH_KNOTS('',3,(#101555,#101556,#101557,#101558,#101559,
#101560,#101561,#101562,#101563,#101564,#101565,#101566,#101567,#101568,
#101569,#101570,#101571,#101572,#101573,#101574,#101575,#101576,#101577,
#101578,#101579,#101580,#101581,#101582,#101583,#101584,#101585,#101586,
#101587,#101588,#101589,#101590,#101591,#101592,#101593,#101594,#101595,
#101596,#101597,#101598,#101599,#101600,#101601,#101602,#101603,#101604,
#101605,#101606,#101607,#101608,#101609,#101610,#101611,#101612,#101613,
#101614,#101615,#101616,#101617,#101618,#101619,#101620,#101621,#101622,
#101623,#101624,#101625,#101626,#101627,#101628,#101629,#101630,#101631,
#101632,#101633,#101634,#101635,#101636,#101637,#101638,#101639,#101640,
#101641,#101642,#101643,#101644,#101645,#101646,#101647,#101648,#101649,
#101650,#101651,#101652,#101653,#101654,#101655,#101656,#101657,#101658,
#101659,#101660,#101661,#101662,#101663,#101664,#101665,#101666,#101667,
#101668,#101669,#101670,#101671,#101672,#101673,#101674,#101675,#101676,
#101677,#101678,#101679,#101680,#101681,#101682,#101683,#101684,#101685,
#101686,#101687,#101688,#101689,#101690,#101691,#101692,#101693,#101694,
#101695,#101696,#101697,#101698,#101699,#101700,#101701,#101702,#101703,
#101704,#101705,#101706,#101707,#101708,#101709,#101710,#101711,#101712,
#101713,#101714,#101715,#101716,#101717,#101718,#101719,#101720,#101721,
#101722,#101723,#101724,#101725,#101726,#101727,#101728,#101729,#101730,
#101731,#101732,#101733,#101734,#101735,#101736,#101737,#101738,#101739,
#101740,#101741,#101742,#101743,#101744,#101745,#101746,#101747,#101748,
#101749,#101750,#101751,#101752,#101753,#101754,#101755,#101756,#101757,
#101758,#101759,#101760,#101761,#101762,#101763,#101764,#101765),
 .UNSPECIFIED.,.F.,.F.,(4,3,3,3,3,3,3,3,3,3,3,3,3,3,3,3,3,3,3,3,3,3,3,3,
3,3,3,3,3,3,3,3,3,3,3,3,3,3,3,3,3,3,3,3,3,3,3,3,3,3,3,3,3,3,3,3,3,3,3,3,
3,3,3,3,3,3,3,3,3,3,4),(-136.039821870719,-135.920529986285,-135.79889642772,
-135.775256526776,-135.680021883788,-135.584918554985,-135.489916976577,
-135.394983848877,-135.300085220761,-135.205194534592,-135.110285247153,
-135.015271693041,-134.920199753059,-134.824973952119,-134.776909052314,
-134.681674398784,-134.586571059276,-134.491569470019,-134.396636331297,
-134.301737692057,-134.206846994674,-134.111937695947,-134.016924130499,
-133.921852179138,-133.826626366862,-133.778561577852,-133.683326928468,
-133.588223593148,-133.493222008114,-133.398288873651,-133.303390238691,
-133.208499545602,-133.113590251179,-133.018576690024,-132.923504742956,
-132.82827893493,-132.780214103391,-132.684979454547,-132.589876119788,
-132.494874535335,-132.399941401479,-132.305042767143,-132.210152074695,
-132.115242780927,-132.020229220446,-131.925157274065,-131.829931466738,
-131.781866628929,-131.686631978641,-131.591528642414,-131.496527056472,
-131.401593921103,-131.306695285238,-131.211804591248,-131.116895295927,
-131.021881733886,-130.926809785936,-130.831583977046,-130.783519154468,
-130.688284504851,-130.593181169304,-130.498179584047,-130.403246449371,
-130.308347814202,-130.213457120912,-130.118547826292,-130.023534264952,
-129.928462317704,-129.83323650951,-129.785171680006,-129.756636563722),
 .UNSPECIFIED.);
#860=B_SPLINE_CURVE_WITH_KNOTS('',3,(#101767,#101768,#101769,#101770,#101771,
#101772,#101773,#101774,#101775,#101776,#101777,#101778,#101779,#101780,
#101781,#101782,#101783,#101784,#101785,#101786,#101787,#101788,#101789,
#101790,#101791,#101792,#101793,#101794,#101795,#101796,#101797,#101798,
#101799,#101800,#101801,#101802,#101803,#101804,#101805,#101806,#101807,
#101808,#101809,#101810,#101811,#101812,#101813,#101814,#101815,#101816,
#101817,#101818,#101819,#101820,#101821,#101822,#101823,#101824,#101825,
#101826,#101827,#101828,#101829,#101830,#101831,#101832,#101833,#101834,
#101835,#101836,#101837,#101838,#101839,#101840,#101841,#101842,#101843,
#101844,#101845,#101846,#101847,#101848,#101849,#101850,#101851,#101852,
#101853,#101854,#101855,#101856,#101857,#101858,#101859,#101860,#101861,
#101862,#101863,#101864,#101865,#101866,#101867,#101868,#101869,#101870,
#101871,#101872,#101873,#101874,#101875,#101876,#101877,#101878,#101879,
#101880,#101881,#101882,#101883,#101884,#101885,#101886,#101887,#101888,
#101889,#101890,#101891,#101892,#101893,#101894,#101895,#101896,#101897,
#101898,#101899,#101900,#101901,#101902,#101903,#101904,#101905,#101906,
#101907,#101908,#101909,#101910,#101911,#101912,#101913,#101914,#101915,
#101916,#101917,#101918,#101919,#101920,#101921,#101922,#101923,#101924,
#101925,#101926,#101927,#101928,#101929,#101930,#101931,#101932,#101933,
#101934,#101935,#101936,#101937,#101938,#101939,#101940,#101941,#101942,
#101943,#101944,#101945,#101946,#101947,#101948,#101949,#101950,#101951,
#101952,#101953,#101954,#101955,#101956,#101957,#101958,#101959,#101960,
#101961,#101962,#101963,#101964,#101965,#101966,#101967,#101968,#101969,
#101970,#101971,#101972,#101973,#101974),.UNSPECIFIED.,.F.,.F.,(4,3,3,3,
3,3,3,3,3,3,3,3,3,3,3,3,3,3,3,3,3,3,3,3,3,3,3,3,3,3,3,3,3,3,3,3,3,3,3,3,
3,3,3,3,3,3,3,3,3,3,3,3,3,3,3,3,3,3,3,3,3,3,3,3,3,3,3,3,3,4),(-129.756636563519,
-129.661856131417,-129.567205464658,-129.469657807268,-129.375173110179,
-129.280719043156,-129.186268524364,-129.091794482415,-128.997214655407,
-128.902571022647,-128.807782068836,-128.786824205545,-128.69158955575,
-128.596486220024,-128.501484634587,-128.40655149973,-128.311652864381,
-128.21676217091,-128.121852876109,-128.02683931459,-127.931767367163,-127.836541558792,
-127.788476731083,-127.693242081393,-127.598138745774,-127.503137160445,
-127.408204025697,-127.313305390457,-127.218414697095,-127.123505402406,
-127.028491840997,-126.93341989368,-126.83819408542,-126.790129256621,-126.694894606925,
-126.599791271299,-126.504789685965,-126.409856551211,-126.314957915965,
-126.220067222599,-126.125157927904,-126.03014436649,-125.93507241917,-125.839846610905,
-125.79178178216,-125.696547132439,-125.601443796787,-125.506442211426,
-125.411509076645,-125.316610441373,-125.221719747979,-125.126810453257,
-125.031796891815,-124.936724944467,-124.841499136174,-124.793434307698,
-124.698199657993,-124.603096322357,-124.508094737013,-124.413161602249,
-124.318262966993,-124.223372273616,-124.12846297891,-124.033449417486,
-123.938377470154,-123.843151661878,-123.795086833237,-123.681923502067,
-123.569966114734,-123.473451256749),.UNSPECIFIED.);
#861=B_SPLINE_CURVE_WITH_KNOTS('',3,(#101976,#101977,#101978,#101979,#101980,
#101981,#101982,#101983,#101984,#101985,#101986,#101987,#101988,#101989,
#101990,#101991,#101992,#101993,#101994,#101995,#101996,#101997,#101998,
#101999,#102000,#102001,#102002,#102003,#102004,#102005,#102006,#102007,
#102008,#102009,#102010,#102011,#102012,#102013,#102014,#102015,#102016,
#102017,#102018,#102019,#102020,#102021,#102022,#102023,#102024,#102025,
#102026,#102027,#102028,#102029,#102030,#102031,#102032,#102033,#102034,
#102035,#102036,#102037,#102038,#102039,#102040,#102041,#102042,#102043,
#102044,#102045,#102046,#102047,#102048,#102049,#102050,#102051,#102052,
#102053,#102054,#102055,#102056,#102057,#102058,#102059,#102060,#102061,
#102062,#102063,#102064,#102065,#102066,#102067,#102068,#102069,#102070,
#102071,#102072,#102073,#102074,#102075,#102076,#102077,#102078,#102079,
#102080,#102081,#102082,#102083,#102084,#102085,#102086,#102087,#102088,
#102089,#102090,#102091,#102092,#102093,#102094,#102095,#102096,#102097,
#102098,#102099,#102100,#102101,#102102,#102103,#102104,#102105,#102106,
#102107,#102108,#102109,#102110,#102111,#102112,#102113,#102114,#102115,
#102116,#102117,#102118,#102119,#102120,#102121,#102122,#102123,#102124,
#102125,#102126,#102127,#102128,#102129,#102130,#102131,#102132,#102133,
#102134,#102135,#102136,#102137,#102138,#102139,#102140,#102141,#102142,
#102143,#102144,#102145,#102146,#102147,#102148,#102149,#102150,#102151,
#102152,#102153,#102154,#102155,#102156,#102157,#102158,#102159,#102160,
#102161,#102162,#102163,#102164,#102165,#102166,#102167,#102168,#102169,
#102170,#102171,#102172,#102173,#102174,#102175,#102176,#102177,#102178,
#102179,#102180,#102181,#102182,#102183,#102184,#102185,#102186),
 .UNSPECIFIED.,.F.,.F.,(4,3,3,3,3,3,3,3,3,3,3,3,3,3,3,3,3,3,3,3,3,3,3,3,
3,3,3,3,3,3,3,3,3,3,3,3,3,3,3,3,3,3,3,3,3,3,3,3,3,3,3,3,3,3,3,3,3,3,3,3,
3,3,3,3,3,3,3,3,3,3,4),(-123.473451256543,-123.37878647411,-123.284143660694,
-123.189496038614,-123.091306868655,-122.996510725647,-122.901643366946,
-122.806627936808,-122.796739358775,-122.701504709064,-122.606401373423,
-122.511399788073,-122.416466653303,-122.321568018042,-122.226677324659,
-122.131768029948,-122.036754468518,-121.941682521181,-121.846456712899,
-121.798391884313,-121.703157234605,-121.608053898967,-121.51305231362,
-121.418119178853,-121.323220543594,-121.228329850215,-121.133420555507,
-121.038406994079,-120.943335046745,-120.848109238466,-120.800044409852,
-120.704809760143,-120.609706424505,-120.514704839156,-120.419771704389,
-120.32487306913,-120.229982375749,-120.13507308104,-120.040059519612,-119.944987572277,
-119.849761763998,-119.80169693539,-119.706462285681,-119.611358950042,
-119.516357364693,-119.421424229925,-119.326525594666,-119.231634901285,
-119.136725606576,-119.041712045147,-118.946640097812,-118.851414289532,
-118.803349460929,-118.708114811221,-118.613011475582,-118.518009890234,
-118.423076755466,-118.328178120207,-118.233287426827,-118.138378132118,
-118.04336457069,-117.948292623355,-117.853066815076,-117.805001986467,
-117.708768823806,-117.612674740797,-117.516694597092,-117.420813827615,
-117.324990934663,-117.229194871666,-117.190265949363),.UNSPECIFIED.);
#862=B_SPLINE_CURVE_WITH_KNOTS('',3,(#102188,#102189,#102190,#102191,#102192,
#102193,#102194,#102195,#102196,#102197),.UNSPECIFIED.,.F.,.F.,(4,1,1,1,
1,1,1,4),(-117.190258575718,-116.806654512005,-115.808307037544,-114.809959563082,
-113.811612088621,-112.813264614159,-111.814917139698,-110.907089376591),
 .UNSPECIFIED.);
#863=B_SPLINE_CURVE_WITH_KNOTS('',3,(#102199,#102200,#102201,#102202,#102203,
#102204,#102205,#102206,#102207,#102208,#102209,#102210,#102211,#102212,
#102213,#102214,#102215,#102216,#102217,#102218,#102219,#102220,#102221,
#102222,#102223,#102224,#102225,#102226,#102227,#102228,#102229,#102230,
#102231,#102232,#102233,#102234,#102235,#102236,#102237,#102238,#102239,
#102240,#102241,#102242,#102243,#102244,#102245,#102246,#102247,#102248,
#102249,#102250,#102251,#102252,#102253,#102254,#102255,#102256,#102257,
#102258,#102259,#102260,#102261,#102262,#102263,#102264,#102265,#102266,
#102267,#102268,#102269,#102270,#102271,#102272,#102273,#102274,#102275,
#102276,#102277,#102278,#102279,#102280,#102281,#102282,#102283,#102284,
#102285,#102286,#102287,#102288,#102289,#102290,#102291,#102292,#102293,
#102294,#102295,#102296,#102297,#102298,#102299,#102300,#102301,#102302,
#102303,#102304,#102305,#102306,#102307,#102308,#102309,#102310,#102311,
#102312,#102313,#102314,#102315,#102316,#102317,#102318,#102319,#102320,
#102321,#102322,#102323,#102324,#102325,#102326,#102327,#102328,#102329,
#102330,#102331,#102332,#102333,#102334,#102335,#102336,#102337,#102338,
#102339,#102340,#102341,#102342,#102343,#102344,#102345,#102346,#102347,
#102348,#102349,#102350,#102351,#102352,#102353,#102354,#102355,#102356,
#102357,#102358,#102359,#102360,#102361,#102362,#102363,#102364,#102365,
#102366,#102367,#102368,#102369,#102370,#102371,#102372,#102373,#102374,
#102375,#102376,#102377,#102378,#102379,#102380,#102381,#102382,#102383,
#102384,#102385,#102386,#102387,#102388,#102389,#102390,#102391,#102392,
#102393,#102394,#102395,#102396,#102397,#102398,#102399,#102400,#102401,
#102402,#102403,#102404,#102405,#102406),.UNSPECIFIED.,.F.,.F.,(4,3,3,3,
3,3,3,3,3,3,3,3,3,3,3,3,3,3,3,3,3,3,3,3,3,3,3,3,3,3,3,3,3,3,3,3,3,3,3,3,
3,3,3,3,3,3,3,3,3,3,3,3,3,3,3,3,3,3,3,3,3,3,3,3,3,3,3,3,3,4),(-110.907080642184,
-110.816569665236,-110.721335015528,-110.62623167989,-110.531230094543,
-110.436296959776,-110.341398324518,-110.246507631139,-110.151598336431,
-110.056584775004,-109.96151282767,-109.866287019391,-109.818222190774,
-109.722987541065,-109.627884205426,-109.532882620078,-109.43794948531,
-109.343050850051,-109.24816015667,-109.153250861961,-109.058237300533,
-108.963165353198,-108.867939544919,-108.819874716313,-108.724640066604,
-108.629536730965,-108.534535145616,-108.439602010848,-108.344703375589,
-108.249812682208,-108.154903387499,-108.05988982607,-107.964817878735,
-107.869592070455,-107.821527241851,-107.726292592142,-107.631189256504,
-107.536187671156,-107.441254536388,-107.346355901129,-107.251465207749,
-107.15655591304,-107.061542351612,-106.966470404277,-106.871244595998,
-106.82317976739,-106.727945117681,-106.632841782042,-106.537840196694,
-106.442907061927,-106.348008426667,-106.253117733287,-106.158208438578,
-106.06319487715,-105.968122929814,-105.872897121535,-105.824832292928,
-105.729597643219,-105.63449430758,-105.539492722231,-105.444559587463,
-105.349660952204,-105.254770258823,-105.159860964113,-105.064847402685,
-104.96977545535,-104.87454964707,-104.826484818466,-104.69097746786,-104.623895335004),
 .UNSPECIFIED.);
#864=B_SPLINE_CURVE_WITH_KNOTS('',3,(#102408,#102409,#102410,#102411,#102412,
#102413,#102414,#102415,#102416,#102417),.UNSPECIFIED.,.F.,.F.,(4,1,1,1,
1,1,1,4),(-104.623892444637,-103.828137344005,-102.829789869543,-101.831442395082,
-100.83309492062,-99.8347474461585,-98.8363999716969,-98.3407100278245),
 .UNSPECIFIED.);
#865=B_SPLINE_CURVE_WITH_KNOTS('',3,(#102419,#102420,#102421,#102422,#102423,
#102424,#102425,#102426,#102427,#102428),.UNSPECIFIED.,.F.,.F.,(4,1,1,1,
1,1,1,4),(-98.3407100278245,-97.8380524972354,-96.8397050227738,-95.8413575483122,
-94.8430100738506,-93.844662599389,-92.8463151249274,-92.0575269460171),
 .UNSPECIFIED.);
#866=B_SPLINE_CURVE_WITH_KNOTS('',3,(#102430,#102431,#102432,#102433,#102434,
#102435,#102436,#102437,#102438,#102439,#102440,#102441,#102442,#102443,
#102444,#102445,#102446,#102447,#102448,#102449,#102450,#102451,#102452,
#102453,#102454,#102455,#102456,#102457,#102458,#102459,#102460,#102461,
#102462,#102463,#102464,#102465,#102466,#102467,#102468,#102469,#102470,
#102471,#102472,#102473,#102474,#102475,#102476,#102477,#102478,#102479,
#102480,#102481,#102482,#102483,#102484,#102485,#102486,#102487,#102488,
#102489,#102490,#102491,#102492,#102493,#102494,#102495,#102496,#102497,
#102498,#102499,#102500,#102501,#102502,#102503,#102504,#102505,#102506,
#102507,#102508,#102509,#102510,#102511,#102512,#102513,#102514,#102515,
#102516,#102517,#102518,#102519,#102520,#102521,#102522,#102523,#102524,
#102525,#102526,#102527,#102528,#102529,#102530,#102531,#102532,#102533,
#102534,#102535,#102536,#102537,#102538,#102539,#102540,#102541,#102542,
#102543,#102544,#102545,#102546,#102547,#102548,#102549,#102550,#102551,
#102552,#102553,#102554,#102555,#102556,#102557,#102558,#102559,#102560,
#102561,#102562,#102563,#102564,#102565,#102566,#102567,#102568,#102569,
#102570,#102571,#102572,#102573,#102574,#102575,#102576,#102577,#102578,
#102579,#102580,#102581,#102582,#102583,#102584,#102585,#102586,#102587,
#102588,#102589,#102590,#102591,#102592,#102593,#102594,#102595,#102596,
#102597,#102598,#102599,#102600,#102601,#102602,#102603,#102604,#102605,
#102606,#102607,#102608,#102609,#102610,#102611,#102612,#102613,#102614,
#102615,#102616,#102617,#102618,#102619,#102620,#102621,#102622,#102623,
#102624,#102625,#102626,#102627,#102628,#102629,#102630,#102631,#102632,
#102633,#102634,#102635,#102636,#102637),.UNSPECIFIED.,.F.,.F.,(4,3,3,3,
3,3,3,3,3,3,3,3,3,3,3,3,3,3,3,3,3,3,3,3,3,3,3,3,3,3,3,3,3,3,3,3,3,3,3,3,
3,3,3,3,3,3,3,3,3,3,3,3,3,3,3,3,3,3,3,3,3,3,3,3,3,3,3,3,3,4),(-92.0575247206449,
-91.9242393989711,-91.8479676504659,-91.7527330007571,-91.6576296651182,
-91.5626280797698,-91.467694945002,-91.3727963097427,-91.277905616362,-91.182996321653,
-91.0879827602248,-90.9929108128895,-90.8976850046099,-90.8496201760043,
-90.7543855262956,-90.6592821906567,-90.5642806053084,-90.4693474705408,
-90.3744488352815,-90.2795581419008,-90.1846488471919,-90.0896352857637,
-89.9945633384285,-89.899337530149,-89.8512727015427,-89.756038051834,-89.6609347161951,
-89.5659331308468,-89.4709999960792,-89.3761013608199,-89.2812106674393,
-89.1863013727303,-89.0912878113021,-88.996215863967,-88.9009900556875,
-88.8529252270811,-88.7576905773724,-88.6625872417335,-88.5675856563851,
-88.4726525216175,-88.3777538863582,-88.2828631929775,-88.1879538982686,
-88.0929403368404,-87.9978683895053,-87.9026425812257,-87.8545777526195,
-87.7593431029108,-87.6642397672719,-87.5692381819235,-87.4743050471559,
-87.3794064118966,-87.2845157185159,-87.1896064238069,-87.0945928623787,
-86.9995209150436,-86.904295106764,-86.8562302781579,-86.7609956284492,
-86.6658922928102,-86.5708907074618,-86.4759575726941,-86.3810589374349,
-86.2861682440542,-86.1912589493452,-86.096245387917,-86.0011734405818,
-85.9059476323023,-85.8578828036963,-85.7743394134653),.UNSPECIFIED.);
#867=B_SPLINE_CURVE_WITH_KNOTS('',3,(#102639,#102640,#102641,#102642,#102643,
#102644,#102645,#102646,#102647,#102648),.UNSPECIFIED.,.F.,.F.,(4,1,1,1,
1,1,1,4),(-85.7743308767921,-84.8595353292348,-83.8611878547732,-82.8628403803116,
-81.86449290585,-80.8661454313884,-79.8677979569268,-79.4911616095461),
 .UNSPECIFIED.);
#868=B_SPLINE_CURVE_WITH_KNOTS('',3,(#102650,#102651,#102652,#102653,#102654,
#102655,#102656,#102657,#102658,#102659,#102660,#102661,#102662,#102663,
#102664,#102665,#102666,#102667,#102668,#102669,#102670,#102671,#102672,
#102673,#102674,#102675,#102676,#102677,#102678,#102679,#102680,#102681,
#102682,#102683,#102684,#102685,#102686,#102687,#102688,#102689,#102690,
#102691,#102692,#102693,#102694,#102695,#102696,#102697,#102698,#102699,
#102700,#102701,#102702,#102703,#102704,#102705,#102706,#102707,#102708,
#102709,#102710,#102711,#102712,#102713,#102714,#102715,#102716,#102717,
#102718,#102719,#102720,#102721,#102722,#102723,#102724,#102725,#102726,
#102727,#102728,#102729,#102730,#102731,#102732,#102733,#102734,#102735,
#102736,#102737,#102738,#102739,#102740,#102741,#102742,#102743,#102744,
#102745,#102746,#102747,#102748,#102749,#102750,#102751,#102752,#102753,
#102754,#102755,#102756,#102757,#102758,#102759,#102760,#102761,#102762,
#102763,#102764,#102765,#102766,#102767,#102768,#102769,#102770,#102771,
#102772,#102773,#102774,#102775,#102776,#102777,#102778,#102779,#102780,
#102781,#102782,#102783,#102784,#102785,#102786,#102787,#102788,#102789,
#102790,#102791,#102792,#102793,#102794,#102795,#102796,#102797,#102798,
#102799,#102800,#102801,#102802,#102803,#102804,#102805,#102806,#102807,
#102808,#102809,#102810,#102811,#102812,#102813,#102814,#102815,#102816,
#102817,#102818,#102819,#102820,#102821,#102822,#102823,#102824,#102825,
#102826,#102827,#102828,#102829,#102830,#102831,#102832,#102833,#102834,
#102835,#102836,#102837,#102838,#102839,#102840,#102841,#102842,#102843,
#102844,#102845,#102846,#102847,#102848,#102849,#102850,#102851,#102852,
#102853,#102854,#102855,#102856,#102857),.UNSPECIFIED.,.F.,.F.,(4,3,3,3,
3,3,3,3,3,3,3,3,3,3,3,3,3,3,3,3,3,3,3,3,3,3,3,3,3,3,3,3,3,3,3,3,3,3,3,3,
3,3,3,3,3,3,3,3,3,3,3,3,3,3,3,3,3,3,3,3,3,3,3,3,3,3,3,3,3,4),(-79.4911541062857,
-79.3955028226438,-79.2998389542877,-79.2041373614416,-79.108306823325,
-79.012403860413,-78.9163300256675,-78.8694504824652,-78.7742158327565,
-78.6791124971176,-78.5841109117691,-78.4891777770015,-78.3942791417422,
-78.2993884483615,-78.2044791536523,-78.1094655922242,-78.014393644889,
-77.9191678366095,-77.8711030080037,-77.7758683582949,-77.680765022656,
-77.5857634373076,-77.4908303025399,-77.3959316672807,-77.3010409739002,
-77.2061316791911,-77.111118117763,-77.0160461704278,-76.9208203621483,
-76.8727555335421,-76.7775208838335,-76.6824175481943,-76.5874159628459,
-76.4924828280783,-76.397584192819,-76.3026934994381,-76.2077842047291,
-76.1127706433009,-76.0176986959657,-75.9224728876861,-75.8744080590805,
-75.7791734093716,-75.684070073733,-75.5890684883847,-75.4941353536171,
-75.3992367183578,-75.3043460249771,-75.2094367302681,-75.1144231688399,
-75.0193512215048,-74.9241254132253,-74.8760605846189,-74.78082593491,-74.6857225992712,
-74.5907210139224,-74.4957878791548,-74.4008892438955,-74.3059985505149,
-74.2110892558056,-74.1160756943774,-74.0210037470425,-73.925777938763,
-73.8777131101573,-73.7826130999192,-73.6876406133148,-73.5927687779015,
-73.4965687832027,-73.4018105821085,-73.3048896906073,-73.2079687991061),
 .UNSPECIFIED.);
#869=B_SPLINE_CURVE_WITH_KNOTS('',3,(#102859,#102860,#102861,#102862,#102863,
#102864,#102865,#102866,#102867,#102868),.UNSPECIFIED.,.F.,.F.,(4,1,1,1,
1,1,1,4),(-73.2079617521312,-72.8793656356957,-71.8810181612341,-70.8826706867726,
-69.884323212311,-68.8859757378494,-67.8876282633878,-66.9247882546445),
 .UNSPECIFIED.);
#870=B_SPLINE_CURVE_WITH_KNOTS('',3,(#102870,#102871,#102872,#102873,#102874,
#102875,#102876,#102877,#102878,#102879,#102880,#102881,#102882,#102883,
#102884,#102885,#102886,#102887,#102888,#102889,#102890,#102891,#102892,
#102893,#102894,#102895,#102896,#102897,#102898,#102899,#102900,#102901,
#102902,#102903,#102904,#102905,#102906,#102907,#102908,#102909,#102910,
#102911,#102912,#102913,#102914,#102915,#102916,#102917,#102918,#102919,
#102920,#102921,#102922,#102923,#102924,#102925,#102926,#102927,#102928,
#102929,#102930,#102931,#102932,#102933,#102934,#102935,#102936,#102937,
#102938,#102939,#102940,#102941,#102942,#102943,#102944,#102945,#102946,
#102947,#102948,#102949,#102950,#102951,#102952,#102953,#102954,#102955,
#102956,#102957,#102958,#102959,#102960,#102961,#102962,#102963,#102964,
#102965,#102966,#102967,#102968,#102969,#102970,#102971,#102972,#102973,
#102974,#102975,#102976,#102977,#102978,#102979,#102980,#102981,#102982,
#102983,#102984,#102985,#102986,#102987,#102988,#102989,#102990,#102991,
#102992,#102993,#102994,#102995,#102996,#102997,#102998,#102999,#103000,
#103001,#103002,#103003,#103004,#103005,#103006,#103007,#103008,#103009,
#103010,#103011,#103012,#103013,#103014,#103015,#103016,#103017,#103018,
#103019,#103020,#103021,#103022,#103023,#103024,#103025,#103026,#103027,
#103028,#103029,#103030,#103031,#103032,#103033,#103034,#103035,#103036,
#103037,#103038,#103039,#103040,#103041,#103042,#103043,#103044,#103045,
#103046,#103047,#103048,#103049,#103050,#103051,#103052,#103053,#103054,
#103055,#103056,#103057,#103058,#103059,#103060,#103061,#103062,#103063,
#103064,#103065,#103066,#103067,#103068,#103069,#103070,#103071,#103072,
#103073,#103074,#103075,#103076,#103077,#103078,#103079,#103080),
 .UNSPECIFIED.,.F.,.F.,(4,3,3,3,3,3,3,3,3,3,3,3,3,3,3,3,3,3,3,3,3,3,3,3,
3,3,3,3,3,3,3,3,3,3,3,3,3,3,3,3,3,3,3,3,3,3,3,3,3,3,3,3,3,3,3,3,3,3,3,3,
3,3,3,3,3,3,3,3,3,3,4),(-66.9247834919265,-66.8892807889262,-66.7940461392173,
-66.6989428035783,-66.6039412182297,-66.5090080834618,-66.4141094482023,
-66.3192187548215,-66.2243094601123,-66.1292958986839,-66.0342239513486,
-65.9389981430689,-65.8909333144646,-65.7956986647559,-65.700595329117,
-65.6055937437686,-65.510660609001,-65.4157619737417,-65.3208712803611,
-65.2259619856521,-65.1309484242239,-65.0358764768888,-64.9406506686093,
-64.892585840003,-64.7973511902943,-64.7022478546555,-64.6072462693071,
-64.5123131345395,-64.4174144992803,-64.3225238058997,-64.2276145111908,
-64.1326009497626,-64.0375290024275,-63.942303194148,-63.8942383655415,
-63.7990037158327,-63.7039003801939,-63.6088987948455,-63.5139656600778,
-63.4190670248185,-63.3241763314379,-63.2292670367289,-63.1342534753007,
-63.0391815279656,-62.943955719686,-62.8958908910799,-62.8006562413711,
-62.7055529057322,-62.6105513203839,-62.5156181856163,-62.420719550357,
-62.3258288569763,-62.2309195622674,-62.1359060008392,-62.0408340535041,
-61.9456082452245,-61.8975434166183,-61.8023087669095,-61.7072054312706,
-61.6122038459222,-61.5172707111546,-61.4223720758953,-61.3274813825147,
-61.2325720878058,-61.1375585263776,-61.0424865790424,-60.9472607707629,
-60.8991959421567,-60.7703971397938,-60.6499426268912,-60.641598337431),
 .UNSPECIFIED.);
#871=B_SPLINE_CURVE_WITH_KNOTS('',3,(#103082,#103083,#103084,#103085,#103086,
#103087,#103088,#103089,#103090,#103091),.UNSPECIFIED.,.F.,.F.,(4,1,1,1,
1,1,1,4),(-60.6415981847469,-59.9008484676951,-58.9025009932335,-57.9041535187719,
-56.9058060443104,-55.9074585698488,-54.9091110953872,-54.3584128775673),
 .UNSPECIFIED.);
#872=B_SPLINE_CURVE_WITH_KNOTS('',3,(#103093,#103094,#103095,#103096,#103097,
#103098,#103099,#103100,#103101,#103102),.UNSPECIFIED.,.F.,.F.,(4,1,1,1,
1,1,1,4),(-54.3584128775673,-53.9107636209256,-52.912416146464,-51.9140686720024,
-50.9157211975409,-49.9173737230793,-48.9190262486177,-48.0752346473835),
 .UNSPECIFIED.);
#873=B_SPLINE_CURVE_WITH_KNOTS('',3,(#103104,#103105,#103106,#103107,#103108,
#103109,#103110,#103111,#103112,#103113,#103114,#103115,#103116,#103117,
#103118,#103119,#103120,#103121,#103122,#103123,#103124,#103125,#103126,
#103127,#103128,#103129,#103130,#103131,#103132,#103133,#103134,#103135,
#103136,#103137,#103138,#103139,#103140,#103141,#103142,#103143,#103144,
#103145,#103146,#103147,#103148,#103149,#103150,#103151,#103152,#103153,
#103154,#103155,#103156,#103157,#103158,#103159,#103160,#103161,#103162,
#103163,#103164,#103165,#103166,#103167,#103168,#103169,#103170,#103171,
#103172,#103173,#103174,#103175,#103176,#103177,#103178,#103179,#103180,
#103181,#103182,#103183,#103184,#103185,#103186,#103187,#103188,#103189,
#103190,#103191,#103192,#103193,#103194,#103195,#103196,#103197,#103198,
#103199,#103200,#103201,#103202,#103203,#103204,#103205,#103206,#103207,
#103208,#103209,#103210,#103211,#103212,#103213,#103214,#103215,#103216,
#103217,#103218,#103219,#103220,#103221,#103222,#103223,#103224,#103225,
#103226,#103227,#103228,#103229,#103230,#103231,#103232,#103233,#103234,
#103235,#103236,#103237,#103238,#103239,#103240,#103241,#103242,#103243,
#103244,#103245,#103246,#103247,#103248,#103249,#103250,#103251,#103252,
#103253,#103254,#103255,#103256,#103257,#103258,#103259,#103260,#103261,
#103262,#103263,#103264,#103265,#103266,#103267,#103268,#103269,#103270,
#103271,#103272,#103273,#103274,#103275,#103276,#103277,#103278,#103279,
#103280,#103281,#103282,#103283,#103284,#103285,#103286,#103287,#103288,
#103289,#103290,#103291,#103292,#103293,#103294,#103295,#103296,#103297,
#103298,#103299,#103300,#103301,#103302,#103303,#103304,#103305,#103306,
#103307,#103308),.UNSPECIFIED.,.F.,.F.,(4,3,3,3,3,3,3,3,3,3,3,3,3,3,3,3,
3,3,3,3,3,3,3,3,3,3,3,3,3,3,3,3,3,3,3,3,3,3,3,3,3,3,3,3,3,3,3,3,3,3,3,3,
3,3,3,3,3,3,3,3,3,3,3,3,3,3,3,3,4),(-48.0752275703878,-47.9206787741561,
-47.8254441244474,-47.7303407888087,-47.6353392034605,-47.540406068693,
-47.4455074334337,-47.3506167400531,-47.2557074453443,-47.1606938839162,
-47.0656219365811,-46.9703961283017,-46.9223312996945,-46.8270966499857,
-46.7319933143469,-46.6369917289985,-46.5420585942308,-46.4471599589715,
-46.3522692655909,-46.257359970882,-46.1623464094538,-46.0672744621186,
-45.9720486538391,-45.9239838252329,-45.8287491755241,-45.7336458398853,
-45.6386442545369,-45.5437111197692,-45.4488124845099,-45.3539217911292,
-45.2590124964203,-45.163998934992,-45.0689269876569,-44.9737011793773,
-44.9256363507713,-44.8304017010626,-44.7352983654238,-44.6402967800754,
-44.5453636453078,-44.4504650100485,-44.3555743166679,-44.260665021959,
-44.1656514605309,-44.0705795131957,-43.9753537049162,-43.9272888763098,
-43.832054226601,-43.7369508909622,-43.6419493056139,-43.5470161708462,
-43.4521175355869,-43.3572268422062,-43.2623175474973,-43.1673039860691,
-43.072232038734,-42.9770062304545,-42.9289414018482,-42.8337067521394,
-42.7386034165005,-42.6436018311521,-42.5486686963844,-42.4537700611251,
-42.3588793677445,-42.2639700730357,-42.1689565116075,-42.0738845642722,
-41.9786587559927,-41.9305939273866,-41.7920422632082),.UNSPECIFIED.);
#874=B_SPLINE_CURVE_WITH_KNOTS('',3,(#103310,#103311,#103312,#103313,#103314,
#103315,#103316,#103317,#103318,#103319),.UNSPECIFIED.,.F.,.F.,(4,1,1,1,
1,1,1,4),(-41.7920342547179,-40.932246452925,-39.9338989784634,-38.9355515040018,
-37.9372040295402,-36.9388565550787,-35.9405090806171,-35.5088620686574),
 .UNSPECIFIED.);
#875=B_SPLINE_CURVE_WITH_KNOTS('',3,(#103321,#103322,#103323,#103324,#103325,
#103326,#103327,#103328,#103329,#103330,#103331,#103332,#103333,#103334,
#103335,#103336,#103337,#103338,#103339,#103340,#103341,#103342,#103343,
#103344,#103345,#103346,#103347,#103348,#103349,#103350,#103351,#103352,
#103353,#103354,#103355,#103356,#103357,#103358,#103359,#103360,#103361,
#103362,#103363,#103364,#103365,#103366,#103367,#103368,#103369,#103370,
#103371,#103372,#103373,#103374,#103375,#103376,#103377,#103378,#103379,
#103380,#103381,#103382,#103383,#103384,#103385,#103386,#103387,#103388,
#103389,#103390,#103391,#103392,#103393,#103394,#103395,#103396,#103397,
#103398,#103399,#103400,#103401,#103402,#103403,#103404,#103405,#103406,
#103407,#103408,#103409,#103410,#103411,#103412,#103413,#103414,#103415,
#103416,#103417,#103418,#103419,#103420,#103421,#103422,#103423,#103424,
#103425,#103426,#103427,#103428,#103429,#103430,#103431,#103432,#103433,
#103434,#103435,#103436,#103437,#103438,#103439,#103440,#103441,#103442,
#103443,#103444,#103445,#103446,#103447,#103448,#103449,#103450,#103451,
#103452,#103453,#103454,#103455,#103456,#103457,#103458,#103459,#103460,
#103461,#103462,#103463,#103464,#103465,#103466,#103467,#103468,#103469,
#103470,#103471,#103472,#103473,#103474,#103475,#103476,#103477,#103478,
#103479,#103480,#103481,#103482,#103483,#103484,#103485,#103486,#103487,
#103488,#103489,#103490,#103491,#103492,#103493,#103494,#103495,#103496,
#103497,#103498,#103499,#103500,#103501,#103502,#103503,#103504,#103505,
#103506,#103507,#103508,#103509,#103510,#103511,#103512,#103513,#103514,
#103515,#103516,#103517,#103518,#103519,#103520,#103521,#103522,#103523,
#103524,#103525,#103526,#103527,#103528),.UNSPECIFIED.,.F.,.F.,(4,3,3,3,
3,3,3,3,3,3,3,3,3,3,3,3,3,3,3,3,3,3,3,3,3,3,3,3,3,3,3,3,3,3,3,3,3,3,3,3,
3,3,3,3,3,3,3,3,3,3,3,3,3,3,3,3,3,3,3,3,3,3,3,3,3,3,3,3,3,4),(-35.5088569560286,
-35.4118208844685,-35.3147250894648,-35.2174658762113,-35.1201218755024,
-35.0225716951327,-34.9421616061555,-34.8469269564469,-34.751823620808,
-34.6568220354598,-34.5618889006923,-34.4669902654331,-34.3720995720527,
-34.277190277344,-34.182176715916,-34.0871047685808,-33.9918789603015,-33.9438141316939,
-33.8485794819858,-33.7534761463474,-33.6584745609995,-33.5635414262326,
-33.468642790974,-33.373752097594,-33.2788428028856,-33.1838292414581,-33.0887572941236,
-32.9935314858447,-32.9454666572323,-32.8502320075217,-32.7551286718808,
-32.6601270865306,-32.5651939517611,-32.4702953164998,-32.3754046231173,
-32.280495328406,-32.185481766976,-32.0904098196392,-31.995184011358,-31.9471191827707,
-31.8518845330635,-31.756781197426,-31.6617796120795,-31.5668464773133,
-31.4719478420554,-31.3770571486762,-31.282147853969,-31.1871342925423,
-31.0920623452084,-30.9968365369302,-30.9487717083091,-30.853537058604,
-30.7584337229687,-30.6634321376237,-30.5684990028597,-30.4736003676041,
-30.378709674227,-30.2838003795219,-30.1887868180976,-30.0937148707661,
-29.9984890624903,-29.9504242338476,-29.8560879209494,-29.7618722070048,
-29.6677493757309,-29.5736918118656,-29.4796504770907,-29.3856213085643,
-29.291533789037,-29.225671648849),.UNSPECIFIED.);
#876=B_SPLINE_CURVE_WITH_KNOTS('',3,(#103530,#103531,#103532,#103533,#103534,
#103535,#103536,#103537,#103538,#103539,#103540),.UNSPECIFIED.,.F.,.F.,
(4,1,1,1,1,1,1,1,4),(-29.2256678766635,-28.952076759386,-27.9537292849244,
-26.9553818104628,-25.9570343360012,-24.9586868615396,-23.960339387078,
-22.9619919126165,-22.9424863416694),.UNSPECIFIED.);
#877=B_SPLINE_CURVE_WITH_KNOTS('',3,(#103542,#103543,#103544,#103545,#103546,
#103547,#103548,#103549,#103550,#103551,#103552,#103553,#103554,#103555,
#103556,#103557,#103558,#103559,#103560,#103561,#103562,#103563,#103564,
#103565,#103566,#103567,#103568,#103569,#103570,#103571,#103572,#103573,
#103574,#103575,#103576,#103577,#103578,#103579,#103580,#103581,#103582,
#103583,#103584,#103585,#103586,#103587,#103588,#103589,#103590,#103591,
#103592,#103593,#103594,#103595,#103596,#103597,#103598,#103599,#103600,
#103601,#103602,#103603,#103604,#103605,#103606,#103607,#103608,#103609,
#103610,#103611,#103612,#103613,#103614,#103615,#103616,#103617,#103618,
#103619,#103620,#103621,#103622,#103623,#103624,#103625,#103626,#103627,
#103628,#103629,#103630,#103631,#103632,#103633,#103634,#103635,#103636,
#103637,#103638,#103639,#103640,#103641,#103642,#103643,#103644,#103645,
#103646,#103647,#103648,#103649,#103650,#103651,#103652,#103653,#103654,
#103655,#103656,#103657,#103658,#103659,#103660,#103661,#103662,#103663,
#103664,#103665,#103666,#103667,#103668,#103669,#103670,#103671,#103672,
#103673,#103674,#103675,#103676,#103677,#103678,#103679,#103680,#103681,
#103682,#103683,#103684,#103685,#103686,#103687,#103688,#103689,#103690,
#103691,#103692,#103693,#103694,#103695,#103696,#103697,#103698,#103699,
#103700,#103701,#103702,#103703,#103704,#103705,#103706,#103707,#103708,
#103709,#103710,#103711,#103712,#103713,#103714,#103715,#103716,#103717,
#103718,#103719,#103720,#103721,#103722,#103723,#103724,#103725,#103726,
#103727,#103728,#103729,#103730,#103731,#103732,#103733,#103734,#103735,
#103736,#103737,#103738,#103739,#103740,#103741,#103742,#103743,#103744,
#103745,#103746,#103747,#103748,#103749),.UNSPECIFIED.,.F.,.F.,(4,3,3,3,
3,3,3,3,3,3,3,3,3,3,3,3,3,3,3,3,3,3,3,3,3,3,3,3,3,3,3,3,3,3,3,3,3,3,3,3,
3,3,3,3,3,3,3,3,3,3,3,3,3,3,3,3,3,3,3,3,3,3,3,3,3,3,3,3,3,4),(-22.9424863416694,
-22.8475708151219,-22.7527857967021,-22.6541431268837,-22.5595268545539,
-22.4649420606623,-22.3703618097769,-22.2757591778819,-22.1810510326589,
-22.0862803854588,-21.9913622734999,-21.9636444381549,-21.8684097886978,
-21.7733064533207,-21.6783048682431,-21.5833717337592,-21.4884730987915,
-21.3935824057097,-21.2986731113068,-21.203659550193,-21.1085876031777,
-21.013361795223,-20.9652969636933,-20.8700623100051,-20.7749589703722,
-20.6799573810214,-20.5850242422547,-20.4901256029999,-20.3952349056325,
-20.3003256069498,-20.2053120415923,-20.110240090347,-20.0150142782255,
-19.9669494892317,-19.8717148468358,-19.7766115185031,-19.6816099404442,
-19.5866768129127,-19.4917781848538,-19.3968874986289,-19.301978211023,
-19.2069646565748,-19.1118927161601,-19.0166669146419,-18.9686020147701,
-18.8733673644384,-18.7782640282422,-18.683262442402,-18.588329307241,-18.4934306716492,
-18.3985399779968,-18.3036306830774,-18.2086171215313,-18.1135451741308,
-18.0183193658673,-17.9702545403085,-17.8750198652429,-17.7799165041353,
-17.684914893242,-17.5899817329218,-17.4950830721146,-17.4001923532219,
-17.3052830330679,-17.2102694464511,-17.115197474035,-17.019971641087,-16.9719070658469,
-16.8576236664657,-16.7446612540388,-16.6593012388575),.UNSPECIFIED.);
#878=B_SPLINE_CURVE_WITH_KNOTS('',3,(#103751,#103752,#103753,#103754,#103755,
#103756,#103757,#103758,#103759,#103760),.UNSPECIFIED.,.F.,.F.,(4,1,1,1,
1,1,1,4),(-16.6593010344898,-15.9735595913854,-14.9752121169238,-13.9768646424622,
-12.9785171680006,-11.980169693539,-10.9818222190774,-10.3761157273102),
 .UNSPECIFIED.);
#879=B_SPLINE_CURVE_WITH_KNOTS('',3,(#103761,#103762,#103763,#103764,#103765,
#103766,#103767,#103768,#103769,#103770),.UNSPECIFIED.,.F.,.F.,(4,1,1,1,
1,1,1,4),(-10.3761157273102,-9.98347474461585,-8.98512727015427,-7.98677979569268,
-6.9884323212311,-5.99008484676951,-4.99173737230793,-4.09293042013064),
 .UNSPECIFIED.);
#880=B_SPLINE_CURVE_WITH_KNOTS('',3,(#103773,#103774,#103775,#103776),
 .UNSPECIFIED.,.F.,.F.,(4,4),(-0.0182935576830915,-0.000735173289463335),
 .UNSPECIFIED.);
#881=B_SPLINE_CURVE_WITH_KNOTS('',3,(#103778,#103779,#103780,#103781,#103782,
#103783,#103784,#103785,#103786,#103787,#103788,#103789,#103790,#103791,
#103792,#103793,#103794,#103795,#103796,#103797,#103798,#103799,#103800,
#103801,#103802,#103803,#103804,#103805,#103806,#103807,#103808,#103809,
#103810,#103811,#103812,#103813,#103814,#103815,#103816,#103817,#103818,
#103819,#103820,#103821,#103822,#103823,#103824,#103825,#103826,#103827,
#103828,#103829,#103830,#103831,#103832,#103833,#103834,#103835,#103836,
#103837,#103838,#103839,#103840,#103841,#103842,#103843,#103844,#103845,
#103846,#103847,#103848,#103849,#103850,#103851,#103852,#103853,#103854,
#103855,#103856,#103857,#103858,#103859,#103860,#103861,#103862,#103863,
#103864,#103865,#103866,#103867,#103868,#103869,#103870,#103871,#103872,
#103873,#103874,#103875,#103876,#103877,#103878,#103879,#103880,#103881,
#103882,#103883,#103884,#103885,#103886,#103887,#103888,#103889,#103890,
#103891,#103892,#103893,#103894,#103895,#103896,#103897,#103898,#103899,
#103900,#103901,#103902,#103903,#103904,#103905,#103906,#103907,#103908,
#103909,#103910,#103911,#103912,#103913,#103914,#103915,#103916,#103917,
#103918,#103919,#103920,#103921,#103922,#103923,#103924,#103925,#103926,
#103927,#103928,#103929,#103930,#103931,#103932,#103933,#103934,#103935,
#103936,#103937,#103938,#103939,#103940,#103941,#103942,#103943,#103944,
#103945,#103946,#103947,#103948,#103949,#103950,#103951,#103952,#103953,
#103954,#103955,#103956,#103957,#103958,#103959,#103960,#103961),
 .UNSPECIFIED.,.F.,.F.,(4,3,3,3,3,3,3,3,3,3,3,3,3,3,3,3,3,3,3,3,3,3,3,3,
3,3,3,3,3,3,3,3,3,3,3,3,3,3,3,3,3,3,3,3,3,3,3,3,3,3,3,3,3,3,3,3,3,3,3,3,
3,4),(160.221225333079,160.368806542595,160.469339670852,160.569727809779,
160.669999441629,160.770207358655,160.870382770703,160.970556846841,161.070830871274,
161.171152974707,161.27165768423,161.367154017056,161.467516405285,161.567733113192,
161.66783306709,161.767869225672,161.867873027848,161.967875871739,162.067980449723,
162.168133797921,162.268472935545,162.365501491518,162.466201520456,162.56675562374,
162.667191045365,162.767561354686,162.867897546487,162.968230573328,163.068659575677,
163.169134733737,163.269787443802,163.363848965979,163.464493158123,163.564994418424,
163.665381690691,163.76570671933,163.866000534004,163.966294124919,164.066688533638,
164.167131688191,164.267757109287,164.362196440441,164.461610403654,164.560878328294,
164.66083652662,164.759929309251,164.858993337879,164.958061073645,165.05868178396,
165.157920089979,165.259232002441,165.360543914903,165.463867173735,165.567024747684,
165.670017169689,165.772912391584,165.875735823741,165.978512792525,166.081298147787,
166.184082570356,166.286939951846,166.358891389364),.UNSPECIFIED.);
#882=B_SPLINE_CURVE_WITH_KNOTS('',3,(#103965,#103966,#103967,#103968,#103969,
#103970,#103971,#103972,#103973,#103974,#103975,#103976,#103977,#103978,
#103979,#103980,#103981,#103982,#103983,#103984,#103985,#103986,#103987,
#103988,#103989,#103990,#103991,#103992,#103993,#103994,#103995,#103996,
#103997,#103998,#103999,#104000,#104001,#104002,#104003,#104004,#104005,
#104006,#104007,#104008,#104009,#104010,#104011,#104012,#104013,#104014,
#104015,#104016,#104017,#104018,#104019,#104020,#104021,#104022,#104023,
#104024,#104025,#104026,#104027,#104028,#104029,#104030,#104031,#104032,
#104033,#104034,#104035,#104036,#104037,#104038,#104039,#104040,#104041,
#104042,#104043,#104044,#104045,#104046,#104047,#104048,#104049,#104050,
#104051,#104052,#104053,#104054,#104055,#104056,#104057,#104058,#104059,
#104060,#104061,#104062,#104063,#104064,#104065,#104066,#104067,#104068,
#104069,#104070,#104071,#104072,#104073,#104074,#104075,#104076,#104077,
#104078,#104079,#104080,#104081,#104082,#104083,#104084,#104085,#104086,
#104087,#104088,#104089,#104090,#104091,#104092,#104093,#104094,#104095,
#104096,#104097,#104098,#104099,#104100,#104101,#104102,#104103,#104104,
#104105,#104106,#104107,#104108,#104109,#104110,#104111,#104112),
 .UNSPECIFIED.,.F.,.F.,(4,3,3,3,3,3,3,3,3,3,3,3,3,3,3,3,3,3,3,3,3,3,3,3,
3,3,3,3,3,3,3,3,3,3,3,3,3,3,3,3,3,3,3,3,3,3,3,3,3,4),(160.221225333356,
160.320301206291,160.420857483327,160.519706082362,160.618507137317,160.717293427671,
160.819157926397,160.918073596558,161.021412509567,161.124751422577,161.225446048277,
161.325994622524,161.426424373396,161.526788920669,161.627119267854,161.727446376164,
161.827869516093,161.928338756658,162.028985881907,162.123557134147,162.224194799688,
162.32468940722,162.425069890594,162.525388042217,162.625674901913,162.725961469978,
162.826348931459,162.926785091202,163.027403880915,163.122362845717,163.221770660997,
163.321032315316,163.421049345562,163.520135597098,163.619193029126,163.718254109008,
163.818982721077,163.918214476708,164.019691516997,164.121168557286,164.224488491831,
164.327642572721,164.430631285823,164.533522676262,164.636342167034,164.739115097018,
164.841896378103,164.944676659303,165.047530054968,165.119974268856),
 .UNSPECIFIED.);
#883=B_SPLINE_CURVE_WITH_KNOTS('',3,(#104113,#104114,#104115,#104116,#104117,
#104118),.UNSPECIFIED.,.F.,.F.,(4,2,4),(-2.98959515967248,-2.97760081308363,
-2.9723526798557),.UNSPECIFIED.);
#884=B_SPLINE_CURVE_WITH_KNOTS('',3,(#104121,#104122,#104123,#104124,#104125,
#104126,#104127,#104128,#104129,#104130,#104131,#104132,#104133,#104134,
#104135,#104136,#104137,#104138,#104139,#104140,#104141,#104142,#104143,
#104144,#104145,#104146,#104147,#104148,#104149,#104150,#104151,#104152),
 .UNSPECIFIED.,.F.,.F.,(4,2,2,2,2,2,2,2,2,2,2,2,2,2,2,4),(-1.69880658936105,
-1.64118631745314,-1.58114877567363,-1.48716057166322,-1.37259659624477,
-1.23655075175843,-1.07630244975344,-0.917316760995069,-0.841499276240901,
-0.674438906112136,-0.53603761134625,-0.366273268631182,-0.24012056206555,
-0.139018770734191,-0.0749773698883539,-0.000229398401183072),
 .UNSPECIFIED.);
#885=B_SPLINE_CURVE_WITH_KNOTS('',3,(#104153,#104154,#104155,#104156,#104157,
#104158,#104159,#104160,#104161,#104162,#104163,#104164,#104165,#104166,
#104167,#104168,#104169,#104170,#104171,#104172,#104173,#104174,#104175,
#104176,#104177,#104178,#104179,#104180,#104181,#104182,#104183,#104184,
#104185,#104186,#104187,#104188,#104189,#104190,#104191,#104192,#104193,
#104194,#104195,#104196,#104197,#104198,#104199,#104200,#104201,#104202,
#104203,#104204,#104205,#104206,#104207,#104208,#104209,#104210,#104211,
#104212,#104213,#104214,#104215,#104216),.UNSPECIFIED.,.F.,.F.,(4,3,3,3,
3,3,3,3,3,3,3,3,3,3,3,3,3,3,3,3,3,4),(-0.410648750432886,-0.38129858226722,
-0.351337992790239,-0.323268054558464,-0.314071396249984,-0.306968635230723,
-0.302737007688542,-0.275182991632929,-0.261456224359294,-0.23321386673853,
-0.204062133396214,-0.199389510033103,-0.195719588682917,-0.168524343679287,
-0.141432694273413,-0.114802283736653,-0.100451998269572,-0.0961034389970428,
-0.0703282844310466,-0.0449344423665578,-0.0202868318695185,0.),
 .UNSPECIFIED.);
#886=B_SPLINE_CURVE_WITH_KNOTS('',3,(#104218,#104219,#104220,#104221,#104222,
#104223,#104224,#104225,#104226,#104227,#104228,#104229,#104230,#104231,
#104232,#104233,#104234,#104235,#104236,#104237,#104238,#104239,#104240,
#104241,#104242,#104243,#104244,#104245,#104246,#104247,#104248),
 .UNSPECIFIED.,.F.,.F.,(4,3,3,3,3,3,3,3,3,3,4),(-0.219677966287973,-0.192200047075235,
-0.164960141568471,-0.163244232429979,-0.133734144811955,-0.116159664156593,
-0.111352235849027,-0.0817226425906419,-0.0517048216881644,-0.0217334754545278,
-7.02415695071034E-6),.UNSPECIFIED.);
#887=B_SPLINE_CURVE_WITH_KNOTS('',3,(#104249,#104250,#104251,#104252),
 .UNSPECIFIED.,.F.,.F.,(4,4),(-0.000229398401183072,-6.51013309275102E-5),
 .UNSPECIFIED.);
#888=B_SPLINE_CURVE_WITH_KNOTS('',3,(#104888,#104889,#104890,#104891,#104892,
#104893,#104894,#104895,#104896,#104897,#104898,#104899,#104900,#104901,
#104902,#104903,#104904,#104905,#104906,#104907,#104908,#104909,#104910,
#104911,#104912,#104913,#104914,#104915,#104916,#104917,#104918,#104919,
#104920,#104921,#104922,#104923,#104924,#104925,#104926,#104927,#104928,
#104929,#104930,#104931,#104932,#104933,#104934,#104935,#104936,#104937,
#104938,#104939,#104940,#104941,#104942,#104943,#104944,#104945,#104946,
#104947,#104948,#104949,#104950,#104951,#104952,#104953,#104954,#104955,
#104956,#104957,#104958,#104959,#104960,#104961,#104962,#104963,#104964,
#104965,#104966,#104967,#104968,#104969,#104970,#104971,#104972,#104973,
#104974,#104975,#104976,#104977,#104978),.UNSPECIFIED.,.F.,.F.,(4,3,3,3,
3,3,3,3,3,3,3,3,3,3,3,3,3,3,3,3,3,3,3,3,3,3,3,3,3,3,4),(-0.55274537837504,
-0.531622029508336,-0.502168749051018,-0.486643707191791,-0.477816865703623,
-0.472110472955742,-0.443081444772573,-0.414132449696304,-0.402724598745165,
-0.39668011484503,-0.368410079973193,-0.34044453265584,-0.313301444273823,
-0.297447725699577,-0.291428269583587,-0.264625124759166,-0.252536542129385,
-0.224781440291452,-0.197026338453519,-0.192163335093477,-0.188174560077401,
-0.161544510496889,-0.134901746785557,-0.108748508340938,-0.0997156910642904,
-0.0945974717680295,-0.0905458946870925,-0.0649973519765065,-0.0398488838857292,
-0.0154859190233527,-2.23248444130412E-15),.UNSPECIFIED.);
#889=B_SPLINE_CURVE_WITH_KNOTS('',3,(#105620,#105621,#105622,#105623,#105624,
#105625,#105626,#105627,#105628,#105629,#105630,#105631,#105632,#105633,
#105634,#105635,#105636,#105637,#105638,#105639,#105640,#105641,#105642,
#105643,#105644,#105645,#105646,#105647,#105648,#105649,#105650,#105651,
#105652,#105653,#105654,#105655,#105656,#105657,#105658,#105659,#105660,
#105661,#105662,#105663,#105664,#105665,#105666,#105667,#105668,#105669,
#105670,#105671,#105672,#105673,#105674,#105675,#105676,#105677,#105678,
#105679,#105680,#105681,#105682,#105683,#105684,#105685,#105686,#105687,
#105688,#105689,#105690,#105691,#105692,#105693,#105694,#105695,#105696,
#105697,#105698,#105699,#105700,#105701,#105702,#105703,#105704,#105705,
#105706,#105707),.UNSPECIFIED.,.F.,.F.,(4,3,3,3,3,3,3,3,3,3,3,3,3,3,3,3,
3,3,3,3,3,3,3,3,3,3,3,3,3,4),(-0.555272788399368,-0.538161110412913,-0.513269663833761,
-0.491669801821604,-0.486294250181284,-0.460760853903715,-0.434570412970994,
-0.426707251754789,-0.422174147549878,-0.395448584781258,-0.368380105141822,
-0.341395216874052,-0.330298718755938,-0.32518015111859,-0.321082990951348,
-0.293166557766596,-0.28265706582854,-0.255451682715235,-0.22824629960193,
-0.222182340122818,-0.217930129258396,-0.190046398040851,-0.161669107568982,
-0.132937855371596,-0.116194762555652,-0.111789614273972,-0.0823323644615424,
-0.0527795159223115,-0.0237791283446704,0.),.UNSPECIFIED.);
#890=B_SPLINE_CURVE_WITH_KNOTS('',3,(#105708,#105709,#105710,#105711),
 .UNSPECIFIED.,.F.,.F.,(4,4),(-0.0132953779643571,0.),.UNSPECIFIED.);
#902=SHAPE_REPRESENTATION_RELATIONSHIP('SRR','None',#105870,#914);
#914=ADVANCED_BREP_SHAPE_REPRESENTATION('',(#938),#105805);
#926=STYLED_ITEM('',(#105932),#938);
#938=MANIFOLD_SOLID_BREP('Body1',#7213);
#996=FACE_BOUND('',#1663,.T.);
#997=FACE_BOUND('',#1666,.T.);
#1055=PLANE('',#7709);
#1056=PLANE('',#7710);
#1057=PLANE('',#7711);
#1058=PLANE('',#7712);
#1059=PLANE('',#7713);
#1060=PLANE('',#7714);
#1061=PLANE('',#7715);
#1062=PLANE('',#7716);
#1063=PLANE('',#7720);
#1064=PLANE('',#7721);
#1297=FACE_OUTER_BOUND('',#1626,.T.);
#1298=FACE_OUTER_BOUND('',#1627,.T.);
#1299=FACE_OUTER_BOUND('',#1628,.T.);
#1300=FACE_OUTER_BOUND('',#1629,.T.);
#1301=FACE_OUTER_BOUND('',#1630,.T.);
#1302=FACE_OUTER_BOUND('',#1631,.T.);
#1303=FACE_OUTER_BOUND('',#1632,.T.);
#1304=FACE_OUTER_BOUND('',#1633,.T.);
#1305=FACE_OUTER_BOUND('',#1634,.T.);
#1306=FACE_OUTER_BOUND('',#1635,.T.);
#1307=FACE_OUTER_BOUND('',#1636,.T.);
#1308=FACE_OUTER_BOUND('',#1637,.T.);
#1309=FACE_OUTER_BOUND('',#1638,.T.);
#1310=FACE_OUTER_BOUND('',#1639,.T.);
#1311=FACE_OUTER_BOUND('',#1640,.T.);
#1312=FACE_OUTER_BOUND('',#1641,.T.);
#1313=FACE_OUTER_BOUND('',#1642,.T.);
#1314=FACE_OUTER_BOUND('',#1643,.T.);
#1315=FACE_OUTER_BOUND('',#1644,.T.);
#1316=FACE_OUTER_BOUND('',#1645,.T.);
#1317=FACE_OUTER_BOUND('',#1646,.T.);
#1318=FACE_OUTER_BOUND('',#1647,.T.);
#1319=FACE_OUTER_BOUND('',#1648,.T.);
#1320=FACE_OUTER_BOUND('',#1649,.T.);
#1321=FACE_OUTER_BOUND('',#1650,.T.);
#1322=FACE_OUTER_BOUND('',#1651,.T.);
#1323=FACE_OUTER_BOUND('',#1652,.T.);
#1324=FACE_OUTER_BOUND('',#1653,.T.);
#1325=FACE_OUTER_BOUND('',#1654,.T.);
#1326=FACE_OUTER_BOUND('',#1655,.T.);
#1327=FACE_OUTER_BOUND('',#1656,.T.);
#1328=FACE_OUTER_BOUND('',#1657,.T.);
#1329=FACE_OUTER_BOUND('',#1658,.T.);
#1330=FACE_OUTER_BOUND('',#1659,.T.);
#1331=FACE_OUTER_BOUND('',#1660,.T.);
#1332=FACE_OUTER_BOUND('',#1661,.T.);
#1333=FACE_OUTER_BOUND('',#1662,.T.);
#1334=FACE_OUTER_BOUND('',#1664,.T.);
#1335=FACE_OUTER_BOUND('',#1665,.T.);
#1336=FACE_OUTER_BOUND('',#1667,.T.);
#1626=EDGE_LOOP('',(#6365,#6366,#6367,#6368));
#1627=EDGE_LOOP('',(#6369,#6370,#6371,#6372,#6373));
#1628=EDGE_LOOP('',(#6374,#6375,#6376,#6377,#6378));
#1629=EDGE_LOOP('',(#6379,#6380,#6381,#6382,#6383));
#1630=EDGE_LOOP('',(#6384,#6385,#6386,#6387,#6388,#6389));
#1631=EDGE_LOOP('',(#6390,#6391,#6392,#6393,#6394));
#1632=EDGE_LOOP('',(#6395,#6396,#6397,#6398,#6399,#6400));
#1633=EDGE_LOOP('',(#6401,#6402,#6403,#6404));
#1634=EDGE_LOOP('',(#6405,#6406,#6407,#6408,#6409,#6410));
#1635=EDGE_LOOP('',(#6411,#6412,#6413,#6414));
#1636=EDGE_LOOP('',(#6415,#6416,#6417,#6418,#6419,#6420));
#1637=EDGE_LOOP('',(#6421,#6422,#6423,#6424,#6425,#6426));
#1638=EDGE_LOOP('',(#6427,#6428,#6429,#6430,#6431));
#1639=EDGE_LOOP('',(#6432,#6433,#6434,#6435,#6436));
#1640=EDGE_LOOP('',(#6437,#6438,#6439,#6440,#6441));
#1641=EDGE_LOOP('',(#6442,#6443,#6444,#6445,#6446));
#1642=EDGE_LOOP('',(#6447,#6448,#6449,#6450,#6451));
#1643=EDGE_LOOP('',(#6452,#6453,#6454,#6455,#6456));
#1644=EDGE_LOOP('',(#6457,#6458,#6459,#6460,#6461,#6462));
#1645=EDGE_LOOP('',(#6463,#6464,#6465,#6466));
#1646=EDGE_LOOP('',(#6467,#6468,#6469,#6470,#6471,#6472));
#1647=EDGE_LOOP('',(#6473,#6474,#6475,#6476));
#1648=EDGE_LOOP('',(#6477,#6478,#6479,#6480,#6481,#6482));
#1649=EDGE_LOOP('',(#6483,#6484,#6485,#6486));
#1650=EDGE_LOOP('',(#6487,#6488,#6489,#6490,#6491,#6492,#6493,#6494,#6495,
#6496,#6497,#6498,#6499,#6500,#6501,#6502,#6503,#6504,#6505,#6506,#6507,
#6508,#6509,#6510,#6511,#6512,#6513,#6514,#6515,#6516,#6517,#6518,#6519,
#6520,#6521,#6522,#6523,#6524,#6525,#6526,#6527,#6528,#6529,#6530,#6531,
#6532,#6533,#6534,#6535,#6536,#6537,#6538));
#1651=EDGE_LOOP('',(#6539,#6540,#6541,#6542,#6543,#6544));
#1652=EDGE_LOOP('',(#6545,#6546,#6547,#6548,#6549,#6550,#6551,#6552,#6553));
#1653=EDGE_LOOP('',(#6554,#6555,#6556,#6557,#6558,#6559,#6560,#6561,#6562,
#6563,#6564,#6565,#6566,#6567,#6568,#6569,#6570,#6571,#6572,#6573,#6574,
#6575,#6576,#6577,#6578,#6579,#6580,#6581,#6582,#6583,#6584,#6585,#6586,
#6587,#6588,#6589,#6590,#6591,#6592,#6593,#6594,#6595,#6596,#6597,#6598,
#6599,#6600,#6601,#6602,#6603,#6604,#6605,#6606,#6607,#6608,#6609,#6610,
#6611,#6612,#6613,#6614,#6615,#6616,#6617,#6618,#6619));
#1654=EDGE_LOOP('',(#6620,#6621,#6622,#6623,#6624,#6625,#6626,#6627,#6628,
#6629,#6630,#6631,#6632,#6633,#6634,#6635,#6636,#6637,#6638,#6639,#6640,
#6641,#6642,#6643,#6644,#6645,#6646,#6647,#6648,#6649,#6650,#6651,#6652,
#6653,#6654,#6655,#6656,#6657,#6658,#6659,#6660,#6661,#6662,#6663,#6664,
#6665,#6666,#6667,#6668,#6669,#6670,#6671,#6672,#6673,#6674,#6675,#6676,
#6677,#6678,#6679,#6680,#6681,#6682,#6683,#6684,#6685,#6686,#6687,#6688));
#1655=EDGE_LOOP('',(#6689,#6690,#6691,#6692));
#1656=EDGE_LOOP('',(#6693,#6694,#6695,#6696));
#1657=EDGE_LOOP('',(#6697,#6698,#6699,#6700));
#1658=EDGE_LOOP('',(#6701,#6702,#6703,#6704));
#1659=EDGE_LOOP('',(#6705,#6706,#6707,#6708));
#1660=EDGE_LOOP('',(#6709,#6710,#6711,#6712));
#1661=EDGE_LOOP('',(#6713,#6714,#6715,#6716,#6717,#6718));
#1662=EDGE_LOOP('',(#6719));
#1663=EDGE_LOOP('',(#6720,#6721,#6722,#6723,#6724));
#1664=EDGE_LOOP('',(#6725,#6726,#6727,#6728));
#1665=EDGE_LOOP('',(#6729));
#1666=EDGE_LOOP('',(#6730,#6731,#6732,#6733,#6734,#6735));
#1667=EDGE_LOOP('',(#6736));
#1904=LINE('',#88856,#2184);
#1905=LINE('',#89157,#2185);
#1906=LINE('',#89622,#2186);
#1907=LINE('',#90045,#2187);
#1908=LINE('',#90288,#2188);
#1909=LINE('',#90528,#2189);
#1910=LINE('',#90932,#2190);
#1911=LINE('',#91462,#2191);
#1912=LINE('',#91980,#2192);
#1913=LINE('',#92426,#2193);
#1914=LINE('',#92868,#2194);
#1915=LINE('',#92914,#2195);
#1916=LINE('',#93379,#2196);
#1917=LINE('',#93854,#2197);
#1918=LINE('',#94301,#2198);
#1919=LINE('',#94750,#2199);
#1920=LINE('',#95201,#2200);
#1921=LINE('',#95630,#2201);
#1922=LINE('',#95902,#2202);
#1923=LINE('',#96346,#2203);
#1924=LINE('',#96814,#2204);
#1925=LINE('',#97260,#2205);
#1926=LINE('',#97686,#2206);
#1927=LINE('',#98152,#2207);
#1928=LINE('',#104254,#2208);
#1929=LINE('',#105715,#2209);
#1930=LINE('',#105717,#2210);
#1931=LINE('',#105719,#2211);
#1932=LINE('',#105720,#2212);
#1933=LINE('',#105723,#2213);
#1934=LINE('',#105725,#2214);
#1935=LINE('',#105726,#2215);
#1936=LINE('',#105729,#2216);
#1937=LINE('',#105731,#2217);
#1938=LINE('',#105732,#2218);
#1939=LINE('',#105735,#2219);
#1940=LINE('',#105737,#2220);
#1941=LINE('',#105738,#2221);
#1942=LINE('',#105741,#2222);
#1943=LINE('',#105743,#2223);
#1944=LINE('',#105744,#2224);
#1945=LINE('',#105746,#2225);
#1946=LINE('',#105747,#2226);
#1947=LINE('',#105754,#2227);
#2184=VECTOR('',#8641,2.37175);
#2185=VECTOR('',#8646,2.37175);
#2186=VECTOR('',#8649,2.37175);
#2187=VECTOR('',#8652,2.37175);
#2188=VECTOR('',#8655,2.37175);
#2189=VECTOR('',#8658,2.37175);
#2190=VECTOR('',#8661,2.37175);
#2191=VECTOR('',#8664,2.37175);
#2192=VECTOR('',#8667,2.37175);
#2193=VECTOR('',#8670,2.37175);
#2194=VECTOR('',#8673,2.37175);
#2195=VECTOR('',#8676,2.37175);
#2196=VECTOR('',#8679,2.37175);
#2197=VECTOR('',#8682,2.37175);
#2198=VECTOR('',#8685,2.37175);
#2199=VECTOR('',#8688,2.37175);
#2200=VECTOR('',#8691,2.37175);
#2201=VECTOR('',#8694,2.37175);
#2202=VECTOR('',#8697,2.37175);
#2203=VECTOR('',#8700,2.37175);
#2204=VECTOR('',#8703,2.37175);
#2205=VECTOR('',#8706,2.37175);
#2206=VECTOR('',#8709,2.37175);
#2207=VECTOR('',#8712,2.37175);
#2208=VECTOR('',#8725,2.5);
#2209=VECTOR('',#8730,10.);
#2210=VECTOR('',#8731,10.);
#2211=VECTOR('',#8732,10.);
#2212=VECTOR('',#8733,10.);
#2213=VECTOR('',#8736,10.);
#2214=VECTOR('',#8737,10.);
#2215=VECTOR('',#8738,10.);
#2216=VECTOR('',#8741,9.99999999999999);
#2217=VECTOR('',#8742,10.);
#2218=VECTOR('',#8743,10.);
#2219=VECTOR('',#8746,10.);
#2220=VECTOR('',#8747,10.);
#2221=VECTOR('',#8748,10.);
#2222=VECTOR('',#8751,10.);
#2223=VECTOR('',#8752,10.);
#2224=VECTOR('',#8753,10.);
#2225=VECTOR('',#8756,10.);
#2226=VECTOR('',#8757,10.);
#2227=VECTOR('',#8766,5.);
#2319=CIRCLE('',#7678,2.37175);
#2320=CIRCLE('',#7703,2.942);
#2321=CIRCLE('',#7704,2.942);
#2322=CIRCLE('',#7706,2.37175);
#2323=CIRCLE('',#7708,2.);
#2324=CIRCLE('',#7717,5.);
#2325=CIRCLE('',#7719,5.);
#3101=VERTEX_POINT('',#88854);
#3102=VERTEX_POINT('',#88855);
#3103=VERTEX_POINT('',#88857);
#3104=VERTEX_POINT('',#89028);
#3105=VERTEX_POINT('',#89155);
#3106=VERTEX_POINT('',#89156);
#3107=VERTEX_POINT('',#89410);
#3108=VERTEX_POINT('',#89620);
#3109=VERTEX_POINT('',#89621);
#3110=VERTEX_POINT('',#89623);
#3111=VERTEX_POINT('',#90043);
#3112=VERTEX_POINT('',#90044);
#3113=VERTEX_POINT('',#90270);
#3114=VERTEX_POINT('',#90286);
#3115=VERTEX_POINT('',#90287);
#3116=VERTEX_POINT('',#90289);
#3117=VERTEX_POINT('',#90304);
#3118=VERTEX_POINT('',#90526);
#3119=VERTEX_POINT('',#90527);
#3120=VERTEX_POINT('',#90529);
#3121=VERTEX_POINT('',#90930);
#3122=VERTEX_POINT('',#90931);
#3123=VERTEX_POINT('',#90933);
#3124=VERTEX_POINT('',#91214);
#3125=VERTEX_POINT('',#91460);
#3126=VERTEX_POINT('',#91461);
#3127=VERTEX_POINT('',#91978);
#3128=VERTEX_POINT('',#91979);
#3129=VERTEX_POINT('',#91981);
#3130=VERTEX_POINT('',#92198);
#3131=VERTEX_POINT('',#92424);
#3132=VERTEX_POINT('',#92425);
#3133=VERTEX_POINT('',#92866);
#3134=VERTEX_POINT('',#92867);
#3135=VERTEX_POINT('',#92869);
#3136=VERTEX_POINT('',#92896);
#3137=VERTEX_POINT('',#92912);
#3138=VERTEX_POINT('',#92913);
#3139=VERTEX_POINT('',#92915);
#3140=VERTEX_POINT('',#93110);
#3141=VERTEX_POINT('',#93377);
#3142=VERTEX_POINT('',#93378);
#3143=VERTEX_POINT('',#93380);
#3144=VERTEX_POINT('',#93852);
#3145=VERTEX_POINT('',#93853);
#3146=VERTEX_POINT('',#94085);
#3147=VERTEX_POINT('',#94299);
#3148=VERTEX_POINT('',#94300);
#3149=VERTEX_POINT('',#94302);
#3150=VERTEX_POINT('',#94748);
#3151=VERTEX_POINT('',#94749);
#3152=VERTEX_POINT('',#94979);
#3153=VERTEX_POINT('',#95199);
#3154=VERTEX_POINT('',#95200);
#3155=VERTEX_POINT('',#95202);
#3156=VERTEX_POINT('',#95628);
#3157=VERTEX_POINT('',#95629);
#3158=VERTEX_POINT('',#95883);
#3159=VERTEX_POINT('',#95900);
#3160=VERTEX_POINT('',#95901);
#3161=VERTEX_POINT('',#95903);
#3162=VERTEX_POINT('',#96130);
#3163=VERTEX_POINT('',#96344);
#3164=VERTEX_POINT('',#96345);
#3165=VERTEX_POINT('',#96812);
#3166=VERTEX_POINT('',#96813);
#3167=VERTEX_POINT('',#96815);
#3168=VERTEX_POINT('',#97034);
#3169=VERTEX_POINT('',#97258);
#3170=VERTEX_POINT('',#97259);
#3171=VERTEX_POINT('',#97684);
#3172=VERTEX_POINT('',#97685);
#3173=VERTEX_POINT('',#97687);
#3174=VERTEX_POINT('',#97934);
#3175=VERTEX_POINT('',#98150);
#3176=VERTEX_POINT('',#98151);
#3177=VERTEX_POINT('',#98676);
#3178=VERTEX_POINT('',#98677);
#3179=VERTEX_POINT('',#98684);
#3180=VERTEX_POINT('',#98686);
#3181=VERTEX_POINT('',#98724);
#3182=VERTEX_POINT('',#98933);
#3183=VERTEX_POINT('',#98944);
#3184=VERTEX_POINT('',#99153);
#3185=VERTEX_POINT('',#99166);
#3186=VERTEX_POINT('',#99375);
#3187=VERTEX_POINT('',#99386);
#3188=VERTEX_POINT('',#99398);
#3189=VERTEX_POINT('',#99409);
#3190=VERTEX_POINT('',#99618);
#3191=VERTEX_POINT('',#99830);
#3192=VERTEX_POINT('',#100039);
#3193=VERTEX_POINT('',#100050);
#3194=VERTEX_POINT('',#100061);
#3195=VERTEX_POINT('',#100270);
#3196=VERTEX_POINT('',#100281);
#3197=VERTEX_POINT('',#100493);
#3198=VERTEX_POINT('',#100505);
#3199=VERTEX_POINT('',#100714);
#3200=VERTEX_POINT('',#100725);
#3201=VERTEX_POINT('',#100934);
#3202=VERTEX_POINT('',#100946);
#3203=VERTEX_POINT('',#101158);
#3204=VERTEX_POINT('',#101169);
#3205=VERTEX_POINT('',#101180);
#3206=VERTEX_POINT('',#101182);
#3207=VERTEX_POINT('',#101334);
#3208=VERTEX_POINT('',#101345);
#3209=VERTEX_POINT('',#101554);
#3210=VERTEX_POINT('',#101766);
#3211=VERTEX_POINT('',#101975);
#3212=VERTEX_POINT('',#102187);
#3213=VERTEX_POINT('',#102198);
#3214=VERTEX_POINT('',#102407);
#3215=VERTEX_POINT('',#102418);
#3216=VERTEX_POINT('',#102429);
#3217=VERTEX_POINT('',#102638);
#3218=VERTEX_POINT('',#102649);
#3219=VERTEX_POINT('',#102858);
#3220=VERTEX_POINT('',#102869);
#3221=VERTEX_POINT('',#103081);
#3222=VERTEX_POINT('',#103092);
#3223=VERTEX_POINT('',#103103);
#3224=VERTEX_POINT('',#103309);
#3225=VERTEX_POINT('',#103320);
#3226=VERTEX_POINT('',#103529);
#3227=VERTEX_POINT('',#103541);
#3228=VERTEX_POINT('',#103750);
#3229=VERTEX_POINT('',#103772);
#3230=VERTEX_POINT('',#103777);
#3231=VERTEX_POINT('',#103962);
#3232=VERTEX_POINT('',#103964);
#3233=VERTEX_POINT('',#104120);
#3234=VERTEX_POINT('',#104217);
#3235=VERTEX_POINT('',#104253);
#3236=VERTEX_POINT('',#105619);
#3237=VERTEX_POINT('',#105713);
#3238=VERTEX_POINT('',#105714);
#3239=VERTEX_POINT('',#105716);
#3240=VERTEX_POINT('',#105718);
#3241=VERTEX_POINT('',#105722);
#3242=VERTEX_POINT('',#105724);
#3243=VERTEX_POINT('',#105728);
#3244=VERTEX_POINT('',#105730);
#3245=VERTEX_POINT('',#105734);
#3246=VERTEX_POINT('',#105736);
#3247=VERTEX_POINT('',#105740);
#3248=VERTEX_POINT('',#105742);
#3249=VERTEX_POINT('',#105750);
#3250=VERTEX_POINT('',#105753);
#4227=EDGE_CURVE('',#3101,#3102,#1904,.T.);
#4228=EDGE_CURVE('',#3103,#3101,#756,.F.);
#4229=EDGE_CURVE('',#3104,#3103,#2319,.T.);
#4230=EDGE_CURVE('',#3104,#3102,#757,.T.);
#4231=EDGE_CURVE('',#3105,#3106,#1905,.T.);
#4232=EDGE_CURVE('',#3101,#3105,#758,.F.);
#4233=EDGE_CURVE('',#3102,#3107,#759,.T.);
#4234=EDGE_CURVE('',#3107,#3106,#760,.T.);
#4235=EDGE_CURVE('',#3108,#3109,#1906,.T.);
#4236=EDGE_CURVE('',#3110,#3108,#761,.F.);
#4237=EDGE_CURVE('',#3105,#3110,#762,.F.);
#4238=EDGE_CURVE('',#3106,#3109,#763,.T.);
#4239=EDGE_CURVE('',#3111,#3112,#1907,.T.);
#4240=EDGE_CURVE('',#3108,#3111,#764,.F.);
#4241=EDGE_CURVE('',#3109,#3113,#765,.T.);
#4242=EDGE_CURVE('',#3113,#3112,#766,.T.);
#4243=EDGE_CURVE('',#3114,#3115,#1908,.T.);
#4244=EDGE_CURVE('',#3116,#3114,#767,.T.);
#4245=EDGE_CURVE('',#3111,#3116,#768,.F.);
#4246=EDGE_CURVE('',#3112,#3117,#769,.T.);
#4247=EDGE_CURVE('',#3117,#3115,#770,.T.);
#4248=EDGE_CURVE('',#3118,#3119,#1909,.T.);
#4249=EDGE_CURVE('',#3120,#3118,#771,.T.);
#4250=EDGE_CURVE('',#3114,#3120,#772,.T.);
#4251=EDGE_CURVE('',#3115,#3119,#773,.T.);
#4252=EDGE_CURVE('',#3121,#3122,#1910,.T.);
#4253=EDGE_CURVE('',#3123,#3121,#774,.F.);
#4254=EDGE_CURVE('',#3118,#3123,#775,.T.);
#4255=EDGE_CURVE('',#3119,#3124,#776,.T.);
#4256=EDGE_CURVE('',#3124,#3122,#777,.T.);
#4257=EDGE_CURVE('',#3125,#3126,#1911,.T.);
#4258=EDGE_CURVE('',#3121,#3125,#778,.F.);
#4259=EDGE_CURVE('',#3122,#3126,#779,.T.);
#4260=EDGE_CURVE('',#3127,#3128,#1912,.T.);
#4261=EDGE_CURVE('',#3129,#3127,#780,.F.);
#4262=EDGE_CURVE('',#3125,#3129,#781,.F.);
#4263=EDGE_CURVE('',#3126,#3130,#782,.T.);
#4264=EDGE_CURVE('',#3130,#3128,#783,.T.);
#4265=EDGE_CURVE('',#3131,#3132,#1913,.T.);
#4266=EDGE_CURVE('',#3127,#3131,#784,.F.);
#4267=EDGE_CURVE('',#3128,#3132,#785,.T.);
#4268=EDGE_CURVE('',#3133,#3134,#1914,.T.);
#4269=EDGE_CURVE('',#3135,#3133,#786,.T.);
#4270=EDGE_CURVE('',#3131,#3135,#787,.F.);
#4271=EDGE_CURVE('',#3132,#3136,#788,.T.);
#4272=EDGE_CURVE('',#3136,#3134,#789,.T.);
#4273=EDGE_CURVE('',#3137,#3138,#1915,.T.);
#4274=EDGE_CURVE('',#3139,#3137,#790,.T.);
#4275=EDGE_CURVE('',#3133,#3139,#791,.T.);
#4276=EDGE_CURVE('',#3134,#3140,#792,.T.);
#4277=EDGE_CURVE('',#3140,#3138,#793,.T.);
#4278=EDGE_CURVE('',#3141,#3142,#1916,.T.);
#4279=EDGE_CURVE('',#3143,#3141,#794,.F.);
#4280=EDGE_CURVE('',#3137,#3143,#795,.T.);
#4281=EDGE_CURVE('',#3138,#3142,#796,.T.);
#4282=EDGE_CURVE('',#3144,#3145,#1917,.T.);
#4283=EDGE_CURVE('',#3141,#3144,#797,.F.);
#4284=EDGE_CURVE('',#3142,#3146,#798,.T.);
#4285=EDGE_CURVE('',#3146,#3145,#799,.T.);
#4286=EDGE_CURVE('',#3147,#3148,#1918,.T.);
#4287=EDGE_CURVE('',#3149,#3147,#800,.F.);
#4288=EDGE_CURVE('',#3144,#3149,#801,.F.);
#4289=EDGE_CURVE('',#3145,#3148,#802,.T.);
#4290=EDGE_CURVE('',#3150,#3151,#1919,.T.);
#4291=EDGE_CURVE('',#3147,#3150,#803,.F.);
#4292=EDGE_CURVE('',#3148,#3152,#804,.T.);
#4293=EDGE_CURVE('',#3152,#3151,#805,.T.);
#4294=EDGE_CURVE('',#3153,#3154,#1920,.T.);
#4295=EDGE_CURVE('',#3155,#3153,#806,.F.);
#4296=EDGE_CURVE('',#3150,#3155,#807,.F.);
#4297=EDGE_CURVE('',#3151,#3154,#808,.T.);
#4298=EDGE_CURVE('',#3156,#3157,#1921,.T.);
#4299=EDGE_CURVE('',#3153,#3156,#809,.F.);
#4300=EDGE_CURVE('',#3154,#3158,#810,.T.);
#4301=EDGE_CURVE('',#3158,#3157,#811,.T.);
#4302=EDGE_CURVE('',#3159,#3160,#1922,.T.);
#4303=EDGE_CURVE('',#3161,#3159,#812,.F.);
#4304=EDGE_CURVE('',#3156,#3161,#813,.F.);
#4305=EDGE_CURVE('',#3157,#3162,#814,.T.);
#4306=EDGE_CURVE('',#3162,#3160,#815,.T.);
#4307=EDGE_CURVE('',#3163,#3164,#1923,.T.);
#4308=EDGE_CURVE('',#3159,#3163,#816,.F.);
#4309=EDGE_CURVE('',#3160,#3164,#817,.T.);
#4310=EDGE_CURVE('',#3165,#3166,#1924,.T.);
#4311=EDGE_CURVE('',#3167,#3165,#818,.F.);
#4312=EDGE_CURVE('',#3163,#3167,#819,.F.);
#4313=EDGE_CURVE('',#3164,#3168,#820,.T.);
#4314=EDGE_CURVE('',#3168,#3166,#821,.T.);
#4315=EDGE_CURVE('',#3169,#3170,#1925,.T.);
#4316=EDGE_CURVE('',#3165,#3169,#822,.F.);
#4317=EDGE_CURVE('',#3166,#3170,#823,.T.);
#4318=EDGE_CURVE('',#3171,#3172,#1926,.T.);
#4319=EDGE_CURVE('',#3173,#3171,#824,.F.);
#4320=EDGE_CURVE('',#3169,#3173,#825,.F.);
#4321=EDGE_CURVE('',#3170,#3174,#826,.T.);
#4322=EDGE_CURVE('',#3174,#3172,#827,.T.);
#4323=EDGE_CURVE('',#3175,#3176,#1927,.T.);
#4324=EDGE_CURVE('',#3171,#3175,#828,.F.);
#4325=EDGE_CURVE('',#3172,#3176,#829,.T.);
#4326=EDGE_CURVE('',#3177,#3178,#830,.T.);
#4327=EDGE_CURVE('',#3178,#3179,#2320,.F.);
#4328=EDGE_CURVE('',#3179,#3180,#831,.T.);
#4329=EDGE_CURVE('',#3180,#3181,#832,.T.);
#4330=EDGE_CURVE('',#3181,#3182,#833,.T.);
#4331=EDGE_CURVE('',#3182,#3183,#834,.T.);
#4332=EDGE_CURVE('',#3183,#3184,#835,.T.);
#4333=EDGE_CURVE('',#3184,#3185,#836,.T.);
#4334=EDGE_CURVE('',#3185,#3186,#837,.T.);
#4335=EDGE_CURVE('',#3186,#3187,#838,.T.);
#4336=EDGE_CURVE('',#3187,#3188,#839,.T.);
#4337=EDGE_CURVE('',#3188,#3189,#840,.T.);
#4338=EDGE_CURVE('',#3189,#3190,#841,.T.);
#4339=EDGE_CURVE('',#3190,#3191,#842,.T.);
#4340=EDGE_CURVE('',#3191,#3192,#843,.T.);
#4341=EDGE_CURVE('',#3192,#3193,#844,.T.);
#4342=EDGE_CURVE('',#3193,#3194,#845,.T.);
#4343=EDGE_CURVE('',#3194,#3195,#846,.T.);
#4344=EDGE_CURVE('',#3195,#3196,#847,.T.);
#4345=EDGE_CURVE('',#3196,#3197,#848,.T.);
#4346=EDGE_CURVE('',#3197,#3198,#849,.T.);
#4347=EDGE_CURVE('',#3198,#3199,#850,.T.);
#4348=EDGE_CURVE('',#3199,#3200,#851,.T.);
#4349=EDGE_CURVE('',#3200,#3201,#852,.T.);
#4350=EDGE_CURVE('',#3201,#3202,#853,.T.);
#4351=EDGE_CURVE('',#3202,#3203,#854,.T.);
#4352=EDGE_CURVE('',#3203,#3204,#855,.T.);
#4353=EDGE_CURVE('',#3204,#3205,#2321,.T.);
#4354=EDGE_CURVE('',#3205,#3206,#856,.T.);
#4355=EDGE_CURVE('',#3206,#3207,#857,.T.);
#4356=EDGE_CURVE('',#3207,#3208,#858,.T.);
#4357=EDGE_CURVE('',#3208,#3209,#859,.T.);
#4358=EDGE_CURVE('',#3209,#3210,#860,.T.);
#4359=EDGE_CURVE('',#3210,#3211,#861,.T.);
#4360=EDGE_CURVE('',#3211,#3212,#862,.T.);
#4361=EDGE_CURVE('',#3212,#3213,#863,.T.);
#4362=EDGE_CURVE('',#3213,#3214,#864,.T.);
#4363=EDGE_CURVE('',#3214,#3215,#865,.T.);
#4364=EDGE_CURVE('',#3215,#3216,#866,.T.);
#4365=EDGE_CURVE('',#3216,#3217,#867,.T.);
#4366=EDGE_CURVE('',#3217,#3218,#868,.T.);
#4367=EDGE_CURVE('',#3218,#3219,#869,.T.);
#4368=EDGE_CURVE('',#3219,#3220,#870,.T.);
#4369=EDGE_CURVE('',#3220,#3221,#871,.T.);
#4370=EDGE_CURVE('',#3221,#3222,#872,.T.);
#4371=EDGE_CURVE('',#3222,#3223,#873,.T.);
#4372=EDGE_CURVE('',#3223,#3224,#874,.T.);
#4373=EDGE_CURVE('',#3224,#3225,#875,.T.);
#4374=EDGE_CURVE('',#3225,#3226,#876,.T.);
#4375=EDGE_CURVE('',#3226,#3227,#877,.T.);
#4376=EDGE_CURVE('',#3227,#3228,#878,.T.);
#4377=EDGE_CURVE('',#3228,#3177,#879,.T.);
#4378=EDGE_CURVE('',#3176,#3229,#880,.T.);
#4379=EDGE_CURVE('',#3229,#3230,#881,.T.);
#4380=EDGE_CURVE('',#3230,#3231,#2322,.T.);
#4381=EDGE_CURVE('',#3232,#3231,#882,.T.);
#4382=EDGE_CURVE('',#3175,#3232,#883,.F.);
#4383=EDGE_CURVE('',#3231,#3233,#884,.T.);
#4384=EDGE_CURVE('',#3205,#3230,#885,.T.);
#4385=EDGE_CURVE('',#3234,#3204,#886,.T.);
#4386=EDGE_CURVE('',#3233,#3234,#887,.T.);
#4387=EDGE_CURVE('',#3233,#3235,#1928,.T.);
#4388=EDGE_CURVE('',#3235,#3235,#2323,.T.);
#4389=EDGE_CURVE('',#3178,#3104,#888,.T.);
#4390=EDGE_CURVE('',#3236,#3179,#889,.T.);
#4391=EDGE_CURVE('',#3236,#3103,#890,.T.);
#4392=EDGE_CURVE('',#3237,#3238,#1929,.T.);
#4393=EDGE_CURVE('',#3237,#3239,#1930,.T.);
#4394=EDGE_CURVE('',#3239,#3240,#1931,.T.);
#4395=EDGE_CURVE('',#3238,#3240,#1932,.T.);
#4396=EDGE_CURVE('',#3241,#3237,#1933,.T.);
#4397=EDGE_CURVE('',#3241,#3242,#1934,.T.);
#4398=EDGE_CURVE('',#3242,#3239,#1935,.T.);
#4399=EDGE_CURVE('',#3243,#3241,#1936,.T.);
#4400=EDGE_CURVE('',#3243,#3244,#1937,.T.);
#4401=EDGE_CURVE('',#3244,#3242,#1938,.T.);
#4402=EDGE_CURVE('',#3245,#3243,#1939,.T.);
#4403=EDGE_CURVE('',#3245,#3246,#1940,.T.);
#4404=EDGE_CURVE('',#3246,#3244,#1941,.T.);
#4405=EDGE_CURVE('',#3247,#3245,#1942,.T.);
#4406=EDGE_CURVE('',#3247,#3248,#1943,.T.);
#4407=EDGE_CURVE('',#3248,#3246,#1944,.T.);
#4408=EDGE_CURVE('',#3238,#3247,#1945,.T.);
#4409=EDGE_CURVE('',#3240,#3248,#1946,.T.);
#4410=EDGE_CURVE('',#3249,#3249,#2324,.T.);
#4411=EDGE_CURVE('',#3249,#3250,#1947,.T.);
#4412=EDGE_CURVE('',#3250,#3250,#2325,.T.);
#6365=ORIENTED_EDGE('',*,*,#4227,.F.);
#6366=ORIENTED_EDGE('',*,*,#4228,.F.);
#6367=ORIENTED_EDGE('',*,*,#4229,.F.);
#6368=ORIENTED_EDGE('',*,*,#4230,.T.);
#6369=ORIENTED_EDGE('',*,*,#4231,.F.);
#6370=ORIENTED_EDGE('',*,*,#4232,.F.);
#6371=ORIENTED_EDGE('',*,*,#4227,.T.);
#6372=ORIENTED_EDGE('',*,*,#4233,.T.);
#6373=ORIENTED_EDGE('',*,*,#4234,.T.);
#6374=ORIENTED_EDGE('',*,*,#4235,.F.);
#6375=ORIENTED_EDGE('',*,*,#4236,.F.);
#6376=ORIENTED_EDGE('',*,*,#4237,.F.);
#6377=ORIENTED_EDGE('',*,*,#4231,.T.);
#6378=ORIENTED_EDGE('',*,*,#4238,.T.);
#6379=ORIENTED_EDGE('',*,*,#4239,.F.);
#6380=ORIENTED_EDGE('',*,*,#4240,.F.);
#6381=ORIENTED_EDGE('',*,*,#4235,.T.);
#6382=ORIENTED_EDGE('',*,*,#4241,.T.);
#6383=ORIENTED_EDGE('',*,*,#4242,.T.);
#6384=ORIENTED_EDGE('',*,*,#4243,.F.);
#6385=ORIENTED_EDGE('',*,*,#4244,.F.);
#6386=ORIENTED_EDGE('',*,*,#4245,.F.);
#6387=ORIENTED_EDGE('',*,*,#4239,.T.);
#6388=ORIENTED_EDGE('',*,*,#4246,.T.);
#6389=ORIENTED_EDGE('',*,*,#4247,.T.);
#6390=ORIENTED_EDGE('',*,*,#4248,.F.);
#6391=ORIENTED_EDGE('',*,*,#4249,.F.);
#6392=ORIENTED_EDGE('',*,*,#4250,.F.);
#6393=ORIENTED_EDGE('',*,*,#4243,.T.);
#6394=ORIENTED_EDGE('',*,*,#4251,.T.);
#6395=ORIENTED_EDGE('',*,*,#4252,.F.);
#6396=ORIENTED_EDGE('',*,*,#4253,.F.);
#6397=ORIENTED_EDGE('',*,*,#4254,.F.);
#6398=ORIENTED_EDGE('',*,*,#4248,.T.);
#6399=ORIENTED_EDGE('',*,*,#4255,.T.);
#6400=ORIENTED_EDGE('',*,*,#4256,.T.);
#6401=ORIENTED_EDGE('',*,*,#4257,.F.);
#6402=ORIENTED_EDGE('',*,*,#4258,.F.);
#6403=ORIENTED_EDGE('',*,*,#4252,.T.);
#6404=ORIENTED_EDGE('',*,*,#4259,.T.);
#6405=ORIENTED_EDGE('',*,*,#4260,.F.);
#6406=ORIENTED_EDGE('',*,*,#4261,.F.);
#6407=ORIENTED_EDGE('',*,*,#4262,.F.);
#6408=ORIENTED_EDGE('',*,*,#4257,.T.);
#6409=ORIENTED_EDGE('',*,*,#4263,.T.);
#6410=ORIENTED_EDGE('',*,*,#4264,.T.);
#6411=ORIENTED_EDGE('',*,*,#4265,.F.);
#6412=ORIENTED_EDGE('',*,*,#4266,.F.);
#6413=ORIENTED_EDGE('',*,*,#4260,.T.);
#6414=ORIENTED_EDGE('',*,*,#4267,.T.);
#6415=ORIENTED_EDGE('',*,*,#4268,.F.);
#6416=ORIENTED_EDGE('',*,*,#4269,.F.);
#6417=ORIENTED_EDGE('',*,*,#4270,.F.);
#6418=ORIENTED_EDGE('',*,*,#4265,.T.);
#6419=ORIENTED_EDGE('',*,*,#4271,.T.);
#6420=ORIENTED_EDGE('',*,*,#4272,.T.);
#6421=ORIENTED_EDGE('',*,*,#4273,.F.);
#6422=ORIENTED_EDGE('',*,*,#4274,.F.);
#6423=ORIENTED_EDGE('',*,*,#4275,.F.);
#6424=ORIENTED_EDGE('',*,*,#4268,.T.);
#6425=ORIENTED_EDGE('',*,*,#4276,.T.);
#6426=ORIENTED_EDGE('',*,*,#4277,.T.);
#6427=ORIENTED_EDGE('',*,*,#4278,.F.);
#6428=ORIENTED_EDGE('',*,*,#4279,.F.);
#6429=ORIENTED_EDGE('',*,*,#4280,.F.);
#6430=ORIENTED_EDGE('',*,*,#4273,.T.);
#6431=ORIENTED_EDGE('',*,*,#4281,.T.);
#6432=ORIENTED_EDGE('',*,*,#4282,.F.);
#6433=ORIENTED_EDGE('',*,*,#4283,.F.);
#6434=ORIENTED_EDGE('',*,*,#4278,.T.);
#6435=ORIENTED_EDGE('',*,*,#4284,.T.);
#6436=ORIENTED_EDGE('',*,*,#4285,.T.);
#6437=ORIENTED_EDGE('',*,*,#4286,.F.);
#6438=ORIENTED_EDGE('',*,*,#4287,.F.);
#6439=ORIENTED_EDGE('',*,*,#4288,.F.);
#6440=ORIENTED_EDGE('',*,*,#4282,.T.);
#6441=ORIENTED_EDGE('',*,*,#4289,.T.);
#6442=ORIENTED_EDGE('',*,*,#4290,.F.);
#6443=ORIENTED_EDGE('',*,*,#4291,.F.);
#6444=ORIENTED_EDGE('',*,*,#4286,.T.);
#6445=ORIENTED_EDGE('',*,*,#4292,.T.);
#6446=ORIENTED_EDGE('',*,*,#4293,.T.);
#6447=ORIENTED_EDGE('',*,*,#4294,.F.);
#6448=ORIENTED_EDGE('',*,*,#4295,.F.);
#6449=ORIENTED_EDGE('',*,*,#4296,.F.);
#6450=ORIENTED_EDGE('',*,*,#4290,.T.);
#6451=ORIENTED_EDGE('',*,*,#4297,.T.);
#6452=ORIENTED_EDGE('',*,*,#4298,.F.);
#6453=ORIENTED_EDGE('',*,*,#4299,.F.);
#6454=ORIENTED_EDGE('',*,*,#4294,.T.);
#6455=ORIENTED_EDGE('',*,*,#4300,.T.);
#6456=ORIENTED_EDGE('',*,*,#4301,.T.);
#6457=ORIENTED_EDGE('',*,*,#4302,.F.);
#6458=ORIENTED_EDGE('',*,*,#4303,.F.);
#6459=ORIENTED_EDGE('',*,*,#4304,.F.);
#6460=ORIENTED_EDGE('',*,*,#4298,.T.);
#6461=ORIENTED_EDGE('',*,*,#4305,.T.);
#6462=ORIENTED_EDGE('',*,*,#4306,.T.);
#6463=ORIENTED_EDGE('',*,*,#4307,.F.);
#6464=ORIENTED_EDGE('',*,*,#4308,.F.);
#6465=ORIENTED_EDGE('',*,*,#4302,.T.);
#6466=ORIENTED_EDGE('',*,*,#4309,.T.);
#6467=ORIENTED_EDGE('',*,*,#4310,.F.);
#6468=ORIENTED_EDGE('',*,*,#4311,.F.);
#6469=ORIENTED_EDGE('',*,*,#4312,.F.);
#6470=ORIENTED_EDGE('',*,*,#4307,.T.);
#6471=ORIENTED_EDGE('',*,*,#4313,.T.);
#6472=ORIENTED_EDGE('',*,*,#4314,.T.);
#6473=ORIENTED_EDGE('',*,*,#4315,.F.);
#6474=ORIENTED_EDGE('',*,*,#4316,.F.);
#6475=ORIENTED_EDGE('',*,*,#4310,.T.);
#6476=ORIENTED_EDGE('',*,*,#4317,.T.);
#6477=ORIENTED_EDGE('',*,*,#4318,.F.);
#6478=ORIENTED_EDGE('',*,*,#4319,.F.);
#6479=ORIENTED_EDGE('',*,*,#4320,.F.);
#6480=ORIENTED_EDGE('',*,*,#4315,.T.);
#6481=ORIENTED_EDGE('',*,*,#4321,.T.);
#6482=ORIENTED_EDGE('',*,*,#4322,.T.);
#6483=ORIENTED_EDGE('',*,*,#4323,.F.);
#6484=ORIENTED_EDGE('',*,*,#4324,.F.);
#6485=ORIENTED_EDGE('',*,*,#4318,.T.);
#6486=ORIENTED_EDGE('',*,*,#4325,.T.);
#6487=ORIENTED_EDGE('',*,*,#4326,.T.);
#6488=ORIENTED_EDGE('',*,*,#4327,.T.);
#6489=ORIENTED_EDGE('',*,*,#4328,.T.);
#6490=ORIENTED_EDGE('',*,*,#4329,.T.);
#6491=ORIENTED_EDGE('',*,*,#4330,.T.);
#6492=ORIENTED_EDGE('',*,*,#4331,.T.);
#6493=ORIENTED_EDGE('',*,*,#4332,.T.);
#6494=ORIENTED_EDGE('',*,*,#4333,.T.);
#6495=ORIENTED_EDGE('',*,*,#4334,.T.);
#6496=ORIENTED_EDGE('',*,*,#4335,.T.);
#6497=ORIENTED_EDGE('',*,*,#4336,.T.);
#6498=ORIENTED_EDGE('',*,*,#4337,.T.);
#6499=ORIENTED_EDGE('',*,*,#4338,.T.);
#6500=ORIENTED_EDGE('',*,*,#4339,.T.);
#6501=ORIENTED_EDGE('',*,*,#4340,.T.);
#6502=ORIENTED_EDGE('',*,*,#4341,.T.);
#6503=ORIENTED_EDGE('',*,*,#4342,.T.);
#6504=ORIENTED_EDGE('',*,*,#4343,.T.);
#6505=ORIENTED_EDGE('',*,*,#4344,.T.);
#6506=ORIENTED_EDGE('',*,*,#4345,.T.);
#6507=ORIENTED_EDGE('',*,*,#4346,.T.);
#6508=ORIENTED_EDGE('',*,*,#4347,.T.);
#6509=ORIENTED_EDGE('',*,*,#4348,.T.);
#6510=ORIENTED_EDGE('',*,*,#4349,.T.);
#6511=ORIENTED_EDGE('',*,*,#4350,.T.);
#6512=ORIENTED_EDGE('',*,*,#4351,.T.);
#6513=ORIENTED_EDGE('',*,*,#4352,.T.);
#6514=ORIENTED_EDGE('',*,*,#4353,.T.);
#6515=ORIENTED_EDGE('',*,*,#4354,.T.);
#6516=ORIENTED_EDGE('',*,*,#4355,.T.);
#6517=ORIENTED_EDGE('',*,*,#4356,.T.);
#6518=ORIENTED_EDGE('',*,*,#4357,.T.);
#6519=ORIENTED_EDGE('',*,*,#4358,.T.);
#6520=ORIENTED_EDGE('',*,*,#4359,.T.);
#6521=ORIENTED_EDGE('',*,*,#4360,.T.);
#6522=ORIENTED_EDGE('',*,*,#4361,.T.);
#6523=ORIENTED_EDGE('',*,*,#4362,.T.);
#6524=ORIENTED_EDGE('',*,*,#4363,.T.);
#6525=ORIENTED_EDGE('',*,*,#4364,.T.);
#6526=ORIENTED_EDGE('',*,*,#4365,.T.);
#6527=ORIENTED_EDGE('',*,*,#4366,.T.);
#6528=ORIENTED_EDGE('',*,*,#4367,.T.);
#6529=ORIENTED_EDGE('',*,*,#4368,.T.);
#6530=ORIENTED_EDGE('',*,*,#4369,.T.);
#6531=ORIENTED_EDGE('',*,*,#4370,.T.);
#6532=ORIENTED_EDGE('',*,*,#4371,.T.);
#6533=ORIENTED_EDGE('',*,*,#4372,.T.);
#6534=ORIENTED_EDGE('',*,*,#4373,.T.);
#6535=ORIENTED_EDGE('',*,*,#4374,.T.);
#6536=ORIENTED_EDGE('',*,*,#4375,.T.);
#6537=ORIENTED_EDGE('',*,*,#4376,.T.);
#6538=ORIENTED_EDGE('',*,*,#4377,.T.);
#6539=ORIENTED_EDGE('',*,*,#4323,.T.);
#6540=ORIENTED_EDGE('',*,*,#4378,.T.);
#6541=ORIENTED_EDGE('',*,*,#4379,.T.);
#6542=ORIENTED_EDGE('',*,*,#4380,.T.);
#6543=ORIENTED_EDGE('',*,*,#4381,.F.);
#6544=ORIENTED_EDGE('',*,*,#4382,.F.);
#6545=ORIENTED_EDGE('',*,*,#4383,.F.);
#6546=ORIENTED_EDGE('',*,*,#4380,.F.);
#6547=ORIENTED_EDGE('',*,*,#4384,.F.);
#6548=ORIENTED_EDGE('',*,*,#4353,.F.);
#6549=ORIENTED_EDGE('',*,*,#4385,.F.);
#6550=ORIENTED_EDGE('',*,*,#4386,.F.);
#6551=ORIENTED_EDGE('',*,*,#4387,.T.);
#6552=ORIENTED_EDGE('',*,*,#4388,.F.);
#6553=ORIENTED_EDGE('',*,*,#4387,.F.);
#6554=ORIENTED_EDGE('',*,*,#4384,.T.);
#6555=ORIENTED_EDGE('',*,*,#4379,.F.);
#6556=ORIENTED_EDGE('',*,*,#4378,.F.);
#6557=ORIENTED_EDGE('',*,*,#4325,.F.);
#6558=ORIENTED_EDGE('',*,*,#4322,.F.);
#6559=ORIENTED_EDGE('',*,*,#4321,.F.);
#6560=ORIENTED_EDGE('',*,*,#4317,.F.);
#6561=ORIENTED_EDGE('',*,*,#4314,.F.);
#6562=ORIENTED_EDGE('',*,*,#4313,.F.);
#6563=ORIENTED_EDGE('',*,*,#4309,.F.);
#6564=ORIENTED_EDGE('',*,*,#4306,.F.);
#6565=ORIENTED_EDGE('',*,*,#4305,.F.);
#6566=ORIENTED_EDGE('',*,*,#4301,.F.);
#6567=ORIENTED_EDGE('',*,*,#4300,.F.);
#6568=ORIENTED_EDGE('',*,*,#4297,.F.);
#6569=ORIENTED_EDGE('',*,*,#4293,.F.);
#6570=ORIENTED_EDGE('',*,*,#4292,.F.);
#6571=ORIENTED_EDGE('',*,*,#4289,.F.);
#6572=ORIENTED_EDGE('',*,*,#4285,.F.);
#6573=ORIENTED_EDGE('',*,*,#4284,.F.);
#6574=ORIENTED_EDGE('',*,*,#4281,.F.);
#6575=ORIENTED_EDGE('',*,*,#4277,.F.);
#6576=ORIENTED_EDGE('',*,*,#4276,.F.);
#6577=ORIENTED_EDGE('',*,*,#4272,.F.);
#6578=ORIENTED_EDGE('',*,*,#4271,.F.);
#6579=ORIENTED_EDGE('',*,*,#4267,.F.);
#6580=ORIENTED_EDGE('',*,*,#4264,.F.);
#6581=ORIENTED_EDGE('',*,*,#4263,.F.);
#6582=ORIENTED_EDGE('',*,*,#4259,.F.);
#6583=ORIENTED_EDGE('',*,*,#4256,.F.);
#6584=ORIENTED_EDGE('',*,*,#4255,.F.);
#6585=ORIENTED_EDGE('',*,*,#4251,.F.);
#6586=ORIENTED_EDGE('',*,*,#4247,.F.);
#6587=ORIENTED_EDGE('',*,*,#4246,.F.);
#6588=ORIENTED_EDGE('',*,*,#4242,.F.);
#6589=ORIENTED_EDGE('',*,*,#4241,.F.);
#6590=ORIENTED_EDGE('',*,*,#4238,.F.);
#6591=ORIENTED_EDGE('',*,*,#4234,.F.);
#6592=ORIENTED_EDGE('',*,*,#4233,.F.);
#6593=ORIENTED_EDGE('',*,*,#4230,.F.);
#6594=ORIENTED_EDGE('',*,*,#4389,.F.);
#6595=ORIENTED_EDGE('',*,*,#4326,.F.);
#6596=ORIENTED_EDGE('',*,*,#4377,.F.);
#6597=ORIENTED_EDGE('',*,*,#4376,.F.);
#6598=ORIENTED_EDGE('',*,*,#4375,.F.);
#6599=ORIENTED_EDGE('',*,*,#4374,.F.);
#6600=ORIENTED_EDGE('',*,*,#4373,.F.);
#6601=ORIENTED_EDGE('',*,*,#4372,.F.);
#6602=ORIENTED_EDGE('',*,*,#4371,.F.);
#6603=ORIENTED_EDGE('',*,*,#4370,.F.);
#6604=ORIENTED_EDGE('',*,*,#4369,.F.);
#6605=ORIENTED_EDGE('',*,*,#4368,.F.);
#6606=ORIENTED_EDGE('',*,*,#4367,.F.);
#6607=ORIENTED_EDGE('',*,*,#4366,.F.);
#6608=ORIENTED_EDGE('',*,*,#4365,.F.);
#6609=ORIENTED_EDGE('',*,*,#4364,.F.);
#6610=ORIENTED_EDGE('',*,*,#4363,.F.);
#6611=ORIENTED_EDGE('',*,*,#4362,.F.);
#6612=ORIENTED_EDGE('',*,*,#4361,.F.);
#6613=ORIENTED_EDGE('',*,*,#4360,.F.);
#6614=ORIENTED_EDGE('',*,*,#4359,.F.);
#6615=ORIENTED_EDGE('',*,*,#4358,.F.);
#6616=ORIENTED_EDGE('',*,*,#4357,.F.);
#6617=ORIENTED_EDGE('',*,*,#4356,.F.);
#6618=ORIENTED_EDGE('',*,*,#4355,.F.);
#6619=ORIENTED_EDGE('',*,*,#4354,.F.);
#6620=ORIENTED_EDGE('',*,*,#4383,.T.);
#6621=ORIENTED_EDGE('',*,*,#4386,.T.);
#6622=ORIENTED_EDGE('',*,*,#4385,.T.);
#6623=ORIENTED_EDGE('',*,*,#4352,.F.);
#6624=ORIENTED_EDGE('',*,*,#4351,.F.);
#6625=ORIENTED_EDGE('',*,*,#4350,.F.);
#6626=ORIENTED_EDGE('',*,*,#4349,.F.);
#6627=ORIENTED_EDGE('',*,*,#4348,.F.);
#6628=ORIENTED_EDGE('',*,*,#4347,.F.);
#6629=ORIENTED_EDGE('',*,*,#4346,.F.);
#6630=ORIENTED_EDGE('',*,*,#4345,.F.);
#6631=ORIENTED_EDGE('',*,*,#4344,.F.);
#6632=ORIENTED_EDGE('',*,*,#4343,.F.);
#6633=ORIENTED_EDGE('',*,*,#4342,.F.);
#6634=ORIENTED_EDGE('',*,*,#4341,.F.);
#6635=ORIENTED_EDGE('',*,*,#4340,.F.);
#6636=ORIENTED_EDGE('',*,*,#4339,.F.);
#6637=ORIENTED_EDGE('',*,*,#4338,.F.);
#6638=ORIENTED_EDGE('',*,*,#4337,.F.);
#6639=ORIENTED_EDGE('',*,*,#4336,.F.);
#6640=ORIENTED_EDGE('',*,*,#4335,.F.);
#6641=ORIENTED_EDGE('',*,*,#4334,.F.);
#6642=ORIENTED_EDGE('',*,*,#4333,.F.);
#6643=ORIENTED_EDGE('',*,*,#4332,.F.);
#6644=ORIENTED_EDGE('',*,*,#4331,.F.);
#6645=ORIENTED_EDGE('',*,*,#4330,.F.);
#6646=ORIENTED_EDGE('',*,*,#4329,.F.);
#6647=ORIENTED_EDGE('',*,*,#4328,.F.);
#6648=ORIENTED_EDGE('',*,*,#4390,.F.);
#6649=ORIENTED_EDGE('',*,*,#4391,.T.);
#6650=ORIENTED_EDGE('',*,*,#4228,.T.);
#6651=ORIENTED_EDGE('',*,*,#4232,.T.);
#6652=ORIENTED_EDGE('',*,*,#4237,.T.);
#6653=ORIENTED_EDGE('',*,*,#4236,.T.);
#6654=ORIENTED_EDGE('',*,*,#4240,.T.);
#6655=ORIENTED_EDGE('',*,*,#4245,.T.);
#6656=ORIENTED_EDGE('',*,*,#4244,.T.);
#6657=ORIENTED_EDGE('',*,*,#4250,.T.);
#6658=ORIENTED_EDGE('',*,*,#4249,.T.);
#6659=ORIENTED_EDGE('',*,*,#4254,.T.);
#6660=ORIENTED_EDGE('',*,*,#4253,.T.);
#6661=ORIENTED_EDGE('',*,*,#4258,.T.);
#6662=ORIENTED_EDGE('',*,*,#4262,.T.);
#6663=ORIENTED_EDGE('',*,*,#4261,.T.);
#6664=ORIENTED_EDGE('',*,*,#4266,.T.);
#6665=ORIENTED_EDGE('',*,*,#4270,.T.);
#6666=ORIENTED_EDGE('',*,*,#4269,.T.);
#6667=ORIENTED_EDGE('',*,*,#4275,.T.);
#6668=ORIENTED_EDGE('',*,*,#4274,.T.);
#6669=ORIENTED_EDGE('',*,*,#4280,.T.);
#6670=ORIENTED_EDGE('',*,*,#4279,.T.);
#6671=ORIENTED_EDGE('',*,*,#4283,.T.);
#6672=ORIENTED_EDGE('',*,*,#4288,.T.);
#6673=ORIENTED_EDGE('',*,*,#4287,.T.);
#6674=ORIENTED_EDGE('',*,*,#4291,.T.);
#6675=ORIENTED_EDGE('',*,*,#4296,.T.);
#6676=ORIENTED_EDGE('',*,*,#4295,.T.);
#6677=ORIENTED_EDGE('',*,*,#4299,.T.);
#6678=ORIENTED_EDGE('',*,*,#4304,.T.);
#6679=ORIENTED_EDGE('',*,*,#4303,.T.);
#6680=ORIENTED_EDGE('',*,*,#4308,.T.);
#6681=ORIENTED_EDGE('',*,*,#4312,.T.);
#6682=ORIENTED_EDGE('',*,*,#4311,.T.);
#6683=ORIENTED_EDGE('',*,*,#4316,.T.);
#6684=ORIENTED_EDGE('',*,*,#4320,.T.);
#6685=ORIENTED_EDGE('',*,*,#4319,.T.);
#6686=ORIENTED_EDGE('',*,*,#4324,.T.);
#6687=ORIENTED_EDGE('',*,*,#4382,.T.);
#6688=ORIENTED_EDGE('',*,*,#4381,.T.);
#6689=ORIENTED_EDGE('',*,*,#4392,.F.);
#6690=ORIENTED_EDGE('',*,*,#4393,.T.);
#6691=ORIENTED_EDGE('',*,*,#4394,.T.);
#6692=ORIENTED_EDGE('',*,*,#4395,.F.);
#6693=ORIENTED_EDGE('',*,*,#4396,.F.);
#6694=ORIENTED_EDGE('',*,*,#4397,.T.);
#6695=ORIENTED_EDGE('',*,*,#4398,.T.);
#6696=ORIENTED_EDGE('',*,*,#4393,.F.);
#6697=ORIENTED_EDGE('',*,*,#4399,.F.);
#6698=ORIENTED_EDGE('',*,*,#4400,.T.);
#6699=ORIENTED_EDGE('',*,*,#4401,.T.);
#6700=ORIENTED_EDGE('',*,*,#4397,.F.);
#6701=ORIENTED_EDGE('',*,*,#4402,.F.);
#6702=ORIENTED_EDGE('',*,*,#4403,.T.);
#6703=ORIENTED_EDGE('',*,*,#4404,.T.);
#6704=ORIENTED_EDGE('',*,*,#4400,.F.);
#6705=ORIENTED_EDGE('',*,*,#4405,.F.);
#6706=ORIENTED_EDGE('',*,*,#4406,.T.);
#6707=ORIENTED_EDGE('',*,*,#4407,.T.);
#6708=ORIENTED_EDGE('',*,*,#4403,.F.);
#6709=ORIENTED_EDGE('',*,*,#4408,.F.);
#6710=ORIENTED_EDGE('',*,*,#4395,.T.);
#6711=ORIENTED_EDGE('',*,*,#4409,.T.);
#6712=ORIENTED_EDGE('',*,*,#4406,.F.);
#6713=ORIENTED_EDGE('',*,*,#4409,.F.);
#6714=ORIENTED_EDGE('',*,*,#4394,.F.);
#6715=ORIENTED_EDGE('',*,*,#4398,.F.);
#6716=ORIENTED_EDGE('',*,*,#4401,.F.);
#6717=ORIENTED_EDGE('',*,*,#4404,.F.);
#6718=ORIENTED_EDGE('',*,*,#4407,.F.);
#6719=ORIENTED_EDGE('',*,*,#4410,.T.);
#6720=ORIENTED_EDGE('',*,*,#4389,.T.);
#6721=ORIENTED_EDGE('',*,*,#4229,.T.);
#6722=ORIENTED_EDGE('',*,*,#4391,.F.);
#6723=ORIENTED_EDGE('',*,*,#4390,.T.);
#6724=ORIENTED_EDGE('',*,*,#4327,.F.);
#6725=ORIENTED_EDGE('',*,*,#4410,.F.);
#6726=ORIENTED_EDGE('',*,*,#4411,.T.);
#6727=ORIENTED_EDGE('',*,*,#4412,.T.);
#6728=ORIENTED_EDGE('',*,*,#4411,.F.);
#6729=ORIENTED_EDGE('',*,*,#4412,.F.);
#6730=ORIENTED_EDGE('',*,*,#4392,.T.);
#6731=ORIENTED_EDGE('',*,*,#4408,.T.);
#6732=ORIENTED_EDGE('',*,*,#4405,.T.);
#6733=ORIENTED_EDGE('',*,*,#4402,.T.);
#6734=ORIENTED_EDGE('',*,*,#4399,.T.);
#6735=ORIENTED_EDGE('',*,*,#4396,.T.);
#6736=ORIENTED_EDGE('',*,*,#4388,.T.);
#6903=CYLINDRICAL_SURFACE('',#7677,2.37175);
#6904=CYLINDRICAL_SURFACE('',#7679,2.37175);
#6905=CYLINDRICAL_SURFACE('',#7680,2.37175);
#6906=CYLINDRICAL_SURFACE('',#7681,2.37175);
#6907=CYLINDRICAL_SURFACE('',#7682,2.37175);
#6908=CYLINDRICAL_SURFACE('',#7683,2.37175);
#6909=CYLINDRICAL_SURFACE('',#7684,2.37175);
#6910=CYLINDRICAL_SURFACE('',#7685,2.37175);
#6911=CYLINDRICAL_SURFACE('',#7686,2.37175);
#6912=CYLINDRICAL_SURFACE('',#7687,2.37175);
#6913=CYLINDRICAL_SURFACE('',#7688,2.37175);
#6914=CYLINDRICAL_SURFACE('',#7689,2.37175);
#6915=CYLINDRICAL_SURFACE('',#7690,2.37175);
#6916=CYLINDRICAL_SURFACE('',#7691,2.37175);
#6917=CYLINDRICAL_SURFACE('',#7692,2.37175);
#6918=CYLINDRICAL_SURFACE('',#7693,2.37175);
#6919=CYLINDRICAL_SURFACE('',#7694,2.37175);
#6920=CYLINDRICAL_SURFACE('',#7695,2.37175);
#6921=CYLINDRICAL_SURFACE('',#7696,2.37175);
#6922=CYLINDRICAL_SURFACE('',#7697,2.37175);
#6923=CYLINDRICAL_SURFACE('',#7698,2.37175);
#6924=CYLINDRICAL_SURFACE('',#7699,2.37175);
#6925=CYLINDRICAL_SURFACE('',#7700,2.37175);
#6926=CYLINDRICAL_SURFACE('',#7701,2.37175);
#6927=CYLINDRICAL_SURFACE('',#7702,2.942);
#6928=CYLINDRICAL_SURFACE('',#7705,2.37175);
#6929=CYLINDRICAL_SURFACE('',#7718,5.);
#7162=ADVANCED_FACE('',(#1297),#6903,.T.);
#7163=ADVANCED_FACE('',(#1298),#6904,.T.);
#7164=ADVANCED_FACE('',(#1299),#6905,.T.);
#7165=ADVANCED_FACE('',(#1300),#6906,.T.);
#7166=ADVANCED_FACE('',(#1301),#6907,.T.);
#7167=ADVANCED_FACE('',(#1302),#6908,.T.);
#7168=ADVANCED_FACE('',(#1303),#6909,.T.);
#7169=ADVANCED_FACE('',(#1304),#6910,.T.);
#7170=ADVANCED_FACE('',(#1305),#6911,.T.);
#7171=ADVANCED_FACE('',(#1306),#6912,.T.);
#7172=ADVANCED_FACE('',(#1307),#6913,.T.);
#7173=ADVANCED_FACE('',(#1308),#6914,.T.);
#7174=ADVANCED_FACE('',(#1309),#6915,.T.);
#7175=ADVANCED_FACE('',(#1310),#6916,.T.);
#7176=ADVANCED_FACE('',(#1311),#6917,.T.);
#7177=ADVANCED_FACE('',(#1312),#6918,.T.);
#7178=ADVANCED_FACE('',(#1313),#6919,.T.);
#7179=ADVANCED_FACE('',(#1314),#6920,.T.);
#7180=ADVANCED_FACE('',(#1315),#6921,.T.);
#7181=ADVANCED_FACE('',(#1316),#6922,.T.);
#7182=ADVANCED_FACE('',(#1317),#6923,.T.);
#7183=ADVANCED_FACE('',(#1318),#6924,.T.);
#7184=ADVANCED_FACE('',(#1319),#6925,.T.);
#7185=ADVANCED_FACE('',(#1320),#6926,.T.);
#7186=ADVANCED_FACE('',(#1321),#6927,.T.);
#7187=ADVANCED_FACE('',(#1322),#6928,.T.);
#7188=ADVANCED_FACE('',(#1323),#106,.T.);
#7189=ADVANCED_FACE('',(#1324),#103,.F.);
#7190=ADVANCED_FACE('',(#1325),#104,.F.);
#7191=ADVANCED_FACE('',(#1326),#1055,.F.);
#7192=ADVANCED_FACE('',(#1327),#1056,.F.);
#7193=ADVANCED_FACE('',(#1328),#1057,.F.);
#7194=ADVANCED_FACE('',(#1329),#1058,.F.);
#7195=ADVANCED_FACE('',(#1330),#1059,.F.);
#7196=ADVANCED_FACE('',(#1331),#1060,.F.);
#7197=ADVANCED_FACE('',(#1332),#1061,.F.);
#7198=ADVANCED_FACE('',(#1333,#996),#1062,.T.);
#7199=ADVANCED_FACE('',(#1334),#6929,.T.);
#7200=ADVANCED_FACE('',(#1335,#997),#1063,.F.);
#7201=ADVANCED_FACE('',(#1336),#1064,.T.);
#7213=CLOSED_SHELL('',(#7162,#7163,#7164,#7165,#7166,#7167,#7168,#7169,
#7170,#7171,#7172,#7173,#7174,#7175,#7176,#7177,#7178,#7179,#7180,#7181,
#7182,#7183,#7184,#7185,#7186,#7187,#7188,#7189,#7190,#7191,#7192,#7193,
#7194,#7195,#7196,#7197,#7198,#7199,#7200,#7201));
#7676=AXIS2_PLACEMENT_3D('',#88852,#8637,#8638);
#7677=AXIS2_PLACEMENT_3D('',#88853,#8639,#8640);
#7678=AXIS2_PLACEMENT_3D('',#89029,#8642,#8643);
#7679=AXIS2_PLACEMENT_3D('',#89154,#8644,#8645);
#7680=AXIS2_PLACEMENT_3D('',#89619,#8647,#8648);
#7681=AXIS2_PLACEMENT_3D('',#90042,#8650,#8651);
#7682=AXIS2_PLACEMENT_3D('',#90285,#8653,#8654);
#7683=AXIS2_PLACEMENT_3D('',#90525,#8656,#8657);
#7684=AXIS2_PLACEMENT_3D('',#90929,#8659,#8660);
#7685=AXIS2_PLACEMENT_3D('',#91459,#8662,#8663);
#7686=AXIS2_PLACEMENT_3D('',#91977,#8665,#8666);
#7687=AXIS2_PLACEMENT_3D('',#92423,#8668,#8669);
#7688=AXIS2_PLACEMENT_3D('',#92865,#8671,#8672);
#7689=AXIS2_PLACEMENT_3D('',#92911,#8674,#8675);
#7690=AXIS2_PLACEMENT_3D('',#93376,#8677,#8678);
#7691=AXIS2_PLACEMENT_3D('',#93851,#8680,#8681);
#7692=AXIS2_PLACEMENT_3D('',#94298,#8683,#8684);
#7693=AXIS2_PLACEMENT_3D('',#94747,#8686,#8687);
#7694=AXIS2_PLACEMENT_3D('',#95198,#8689,#8690);
#7695=AXIS2_PLACEMENT_3D('',#95627,#8692,#8693);
#7696=AXIS2_PLACEMENT_3D('',#95899,#8695,#8696);
#7697=AXIS2_PLACEMENT_3D('',#96343,#8698,#8699);
#7698=AXIS2_PLACEMENT_3D('',#96811,#8701,#8702);
#7699=AXIS2_PLACEMENT_3D('',#97257,#8704,#8705);
#7700=AXIS2_PLACEMENT_3D('',#97683,#8707,#8708);
#7701=AXIS2_PLACEMENT_3D('',#98149,#8710,#8711);
#7702=AXIS2_PLACEMENT_3D('',#98675,#8713,#8714);
#7703=AXIS2_PLACEMENT_3D('',#98685,#8715,#8716);
#7704=AXIS2_PLACEMENT_3D('',#101181,#8717,#8718);
#7705=AXIS2_PLACEMENT_3D('',#103771,#8719,#8720);
#7706=AXIS2_PLACEMENT_3D('',#103963,#8721,#8722);
#7707=AXIS2_PLACEMENT_3D('',#104119,#8723,#8724);
#7708=AXIS2_PLACEMENT_3D('',#104255,#8726,#8727);
#7709=AXIS2_PLACEMENT_3D('',#105712,#8728,#8729);
#7710=AXIS2_PLACEMENT_3D('',#105721,#8734,#8735);
#7711=AXIS2_PLACEMENT_3D('',#105727,#8739,#8740);
#7712=AXIS2_PLACEMENT_3D('',#105733,#8744,#8745);
#7713=AXIS2_PLACEMENT_3D('',#105739,#8749,#8750);
#7714=AXIS2_PLACEMENT_3D('',#105745,#8754,#8755);
#7715=AXIS2_PLACEMENT_3D('',#105748,#8758,#8759);
#7716=AXIS2_PLACEMENT_3D('',#105749,#8760,#8761);
#7717=AXIS2_PLACEMENT_3D('',#105751,#8762,#8763);
#7718=AXIS2_PLACEMENT_3D('',#105752,#8764,#8765);
#7719=AXIS2_PLACEMENT_3D('',#105755,#8767,#8768);
#7720=AXIS2_PLACEMENT_3D('',#105756,#8769,#8770);
#7721=AXIS2_PLACEMENT_3D('',#105757,#8771,#8772);
#8637=DIRECTION('axis',(0.,0.,1.));
#8638=DIRECTION('refdir',(1.,0.,0.));
#8639=DIRECTION('center_axis',(0.,0.,1.));
#8640=DIRECTION('ref_axis',(0.997333822932903,-0.0729742806339326,0.));
#8641=DIRECTION('',(0.,0.,-1.));
#8642=DIRECTION('center_axis',(0.,0.,-1.));
#8643=DIRECTION('ref_axis',(1.,-6.57997986587321E-14,0.));
#8644=DIRECTION('center_axis',(0.,0.,1.));
#8645=DIRECTION('ref_axis',(0.997333822932903,-0.0729742806339326,0.));
#8646=DIRECTION('',(0.,0.,-1.));
#8647=DIRECTION('center_axis',(0.,0.,1.));
#8648=DIRECTION('ref_axis',(0.997333822932903,-0.0729742806339326,0.));
#8649=DIRECTION('',(0.,0.,-1.));
#8650=DIRECTION('center_axis',(0.,0.,1.));
#8651=DIRECTION('ref_axis',(0.997333822932903,-0.0729742806339326,0.));
#8652=DIRECTION('',(0.,0.,-1.));
#8653=DIRECTION('center_axis',(0.,0.,1.));
#8654=DIRECTION('ref_axis',(0.997333822932903,-0.0729742806339326,0.));
#8655=DIRECTION('',(0.,0.,-1.));
#8656=DIRECTION('center_axis',(0.,0.,1.));
#8657=DIRECTION('ref_axis',(0.997333822932903,-0.0729742806339326,0.));
#8658=DIRECTION('',(0.,0.,-1.));
#8659=DIRECTION('center_axis',(0.,0.,1.));
#8660=DIRECTION('ref_axis',(0.997333822932903,-0.0729742806339326,0.));
#8661=DIRECTION('',(0.,0.,-1.));
#8662=DIRECTION('center_axis',(0.,0.,1.));
#8663=DIRECTION('ref_axis',(0.997333822932903,-0.0729742806339326,0.));
#8664=DIRECTION('',(0.,0.,-1.));
#8665=DIRECTION('center_axis',(0.,0.,1.));
#8666=DIRECTION('ref_axis',(0.997333822932903,-0.0729742806339326,0.));
#8667=DIRECTION('',(0.,0.,-1.));
#8668=DIRECTION('center_axis',(0.,0.,1.));
#8669=DIRECTION('ref_axis',(0.997333822932903,-0.0729742806339326,0.));
#8670=DIRECTION('',(0.,0.,-1.));
#8671=DIRECTION('center_axis',(0.,0.,1.));
#8672=DIRECTION('ref_axis',(0.997333822932903,-0.0729742806339326,0.));
#8673=DIRECTION('',(0.,0.,-1.));
#8674=DIRECTION('center_axis',(0.,0.,1.));
#8675=DIRECTION('ref_axis',(0.997333822932903,-0.0729742806339326,0.));
#8676=DIRECTION('',(0.,0.,-1.));
#8677=DIRECTION('center_axis',(0.,0.,1.));
#8678=DIRECTION('ref_axis',(0.997333822932903,-0.0729742806339326,0.));
#8679=DIRECTION('',(0.,0.,-1.));
#8680=DIRECTION('center_axis',(0.,0.,1.));
#8681=DIRECTION('ref_axis',(0.997333822932903,-0.0729742806339326,0.));
#8682=DIRECTION('',(0.,0.,-1.));
#8683=DIRECTION('center_axis',(0.,0.,1.));
#8684=DIRECTION('ref_axis',(0.997333822932903,-0.0729742806339326,0.));
#8685=DIRECTION('',(0.,0.,-1.));
#8686=DIRECTION('center_axis',(0.,0.,1.));
#8687=DIRECTION('ref_axis',(0.997333822932903,-0.0729742806339326,0.));
#8688=DIRECTION('',(0.,0.,-1.));
#8689=DIRECTION('center_axis',(0.,0.,1.));
#8690=DIRECTION('ref_axis',(0.997333822932903,-0.0729742806339326,0.));
#8691=DIRECTION('',(0.,0.,-1.));
#8692=DIRECTION('center_axis',(0.,0.,1.));
#8693=DIRECTION('ref_axis',(0.997333822932903,-0.0729742806339326,0.));
#8694=DIRECTION('',(0.,0.,-1.));
#8695=DIRECTION('center_axis',(0.,0.,1.));
#8696=DIRECTION('ref_axis',(0.997333822932903,-0.0729742806339326,0.));
#8697=DIRECTION('',(0.,0.,-1.));
#8698=DIRECTION('center_axis',(0.,0.,1.));
#8699=DIRECTION('ref_axis',(0.997333822932903,-0.0729742806339326,0.));
#8700=DIRECTION('',(0.,0.,-1.));
#8701=DIRECTION('center_axis',(0.,0.,1.));
#8702=DIRECTION('ref_axis',(0.997333822932903,-0.0729742806339326,0.));
#8703=DIRECTION('',(0.,0.,-1.));
#8704=DIRECTION('center_axis',(0.,0.,1.));
#8705=DIRECTION('ref_axis',(0.997333822932903,-0.0729742806339326,0.));
#8706=DIRECTION('',(0.,0.,-1.));
#8707=DIRECTION('center_axis',(0.,0.,1.));
#8708=DIRECTION('ref_axis',(0.997333822932903,-0.0729742806339326,0.));
#8709=DIRECTION('',(0.,0.,-1.));
#8710=DIRECTION('center_axis',(0.,0.,1.));
#8711=DIRECTION('ref_axis',(0.997333822932903,-0.0729742806339326,0.));
#8712=DIRECTION('',(0.,0.,-1.));
#8713=DIRECTION('center_axis',(0.,0.,1.));
#8714=DIRECTION('ref_axis',(1.,0.,0.));
#8715=DIRECTION('center_axis',(0.,0.,-1.));
#8716=DIRECTION('ref_axis',(1.,0.,0.));
#8717=DIRECTION('center_axis',(0.,0.,-1.));
#8718=DIRECTION('ref_axis',(1.,0.,0.));
#8719=DIRECTION('center_axis',(0.,0.,1.));
#8720=DIRECTION('ref_axis',(0.997333822932903,-0.0729742806339326,0.));
#8721=DIRECTION('center_axis',(0.,0.,-1.));
#8722=DIRECTION('ref_axis',(1.,-6.57997986587321E-14,0.));
#8723=DIRECTION('center_axis',(0.,0.,-1.));
#8724=DIRECTION('ref_axis',(1.,0.,0.));
#8725=DIRECTION('',(0.707106781186547,-8.65956056235493E-17,0.707106781186548));
#8726=DIRECTION('center_axis',(0.,0.,1.));
#8727=DIRECTION('ref_axis',(1.,0.,0.));
#8728=DIRECTION('center_axis',(-1.92296268638356E-16,-1.,0.));
#8729=DIRECTION('ref_axis',(1.,-1.92296268638356E-16,0.));
#8730=DIRECTION('',(1.,-1.92296268638356E-16,0.));
#8731=DIRECTION('',(0.,0.,1.));
#8732=DIRECTION('',(1.,-1.92296268638356E-16,0.));
#8733=DIRECTION('',(0.,0.,1.));
#8734=DIRECTION('center_axis',(-0.866025403784439,-0.5,0.));
#8735=DIRECTION('ref_axis',(0.5,-0.866025403784439,0.));
#8736=DIRECTION('',(0.5,-0.866025403784439,0.));
#8737=DIRECTION('',(0.,0.,1.));
#8738=DIRECTION('',(0.5,-0.866025403784439,0.));
#8739=DIRECTION('center_axis',(-0.866025403784439,0.5,0.));
#8740=DIRECTION('ref_axis',(-0.5,-0.866025403784439,0.));
#8741=DIRECTION('',(-0.5,-0.866025403784439,0.));
#8742=DIRECTION('',(0.,0.,1.));
#8743=DIRECTION('',(-0.5,-0.866025403784439,0.));
#8744=DIRECTION('center_axis',(1.92296268638356E-16,1.,0.));
#8745=DIRECTION('ref_axis',(-1.,1.92296268638356E-16,0.));
#8746=DIRECTION('',(-1.,1.92296268638356E-16,0.));
#8747=DIRECTION('',(0.,0.,1.));
#8748=DIRECTION('',(-1.,1.92296268638356E-16,0.));
#8749=DIRECTION('center_axis',(0.866025403784439,0.5,0.));
#8750=DIRECTION('ref_axis',(-0.5,0.866025403784439,0.));
#8751=DIRECTION('',(-0.5,0.866025403784439,0.));
#8752=DIRECTION('',(0.,0.,1.));
#8753=DIRECTION('',(-0.5,0.866025403784439,0.));
#8754=DIRECTION('center_axis',(0.866025403784439,-0.5,0.));
#8755=DIRECTION('ref_axis',(0.5,0.866025403784439,0.));
#8756=DIRECTION('',(0.5,0.866025403784439,0.));
#8757=DIRECTION('',(0.5,0.866025403784439,0.));
#8758=DIRECTION('center_axis',(0.,0.,1.));
#8759=DIRECTION('ref_axis',(1.,0.,0.));
#8760=DIRECTION('center_axis',(0.,0.,1.));
#8761=DIRECTION('ref_axis',(1.,0.,0.));
#8762=DIRECTION('center_axis',(0.,0.,1.));
#8763=DIRECTION('ref_axis',(1.,0.,0.));
#8764=DIRECTION('center_axis',(0.,0.,1.));
#8765=DIRECTION('ref_axis',(1.,0.,0.));
#8766=DIRECTION('',(0.,0.,-1.));
#8767=DIRECTION('center_axis',(0.,0.,1.));
#8768=DIRECTION('ref_axis',(1.,0.,0.));
#8769=DIRECTION('center_axis',(0.,0.,1.));
#8770=DIRECTION('ref_axis',(1.,0.,0.));
#8771=DIRECTION('center_axis',(0.,0.,1.));
#8772=DIRECTION('ref_axis',(1.,0.,0.));
#88852=CARTESIAN_POINT('',(0.,0.,0.));
#88853=CARTESIAN_POINT('Origin',(0.,0.,-1.84858989190503));
#88854=CARTESIAN_POINT('',(-2.36542648444351,0.173076888096584,0.838413605944557));
#88855=CARTESIAN_POINT('',(-2.36542649454111,0.173076750093528,0.639821592488593));
#88856=CARTESIAN_POINT('',(-2.36542649454111,0.173076750093529,-1.84858989190503));
#88857=CARTESIAN_POINT('',(-1.35150067398999,-1.94901102888224,-5.43618969284232E-15));
#88858=CARTESIAN_POINT('Ctrl Pts',(-2.36542648444351,0.173076888096584,
0.838413605944556));
#88859=CARTESIAN_POINT('Ctrl Pts',(-2.35882845273757,0.263251602433591,
0.831953464375971));
#88860=CARTESIAN_POINT('Ctrl Pts',(-2.34707785797561,0.352996265264053,
0.825376328096348));
#88861=CARTESIAN_POINT('Ctrl Pts',(-2.30344086365932,0.583117657947324,
0.808270841295367));
#88862=CARTESIAN_POINT('Ctrl Pts',(-2.26386739771479,0.721649711978628,
0.797725648659815));
#88863=CARTESIAN_POINT('Ctrl Pts',(-2.20518235143571,0.873340955132987,
0.786412943593282));
#88864=CARTESIAN_POINT('Ctrl Pts',(-2.19816898024188,0.8908461245749,0.78511146551529));
#88865=CARTESIAN_POINT('Ctrl Pts',(-2.18800275925427,0.91536938434873,0.783295708307795));
#88866=CARTESIAN_POINT('Ctrl Pts',(-2.18502363822882,0.922458068899643,
0.782771737102728));
#88867=CARTESIAN_POINT('Ctrl Pts',(-2.17995655497133,0.934352681901471,
0.781894180782981));
#88868=CARTESIAN_POINT('Ctrl Pts',(-2.17788706398935,0.939166361277973,
0.781539496599892));
#88869=CARTESIAN_POINT('Ctrl Pts',(-2.17363202058509,0.948973980764961,
0.780817837826489));
#88870=CARTESIAN_POINT('Ctrl Pts',(-2.17144517915015,0.953967301624584,
0.780450944257678));
#88871=CARTESIAN_POINT('Ctrl Pts',(-2.16583343935226,0.966661579005291,
0.779519429431435));
#88872=CARTESIAN_POINT('Ctrl Pts',(-2.16238463595257,0.974351983093089,
0.778956250237148));
#88873=CARTESIAN_POINT('Ctrl Pts',(-2.14823818374022,1.00545173545004,0.776682784415733));
#88874=CARTESIAN_POINT('Ctrl Pts',(-2.13720033304501,1.02870567134393,0.774992118228455));
#88875=CARTESIAN_POINT('Ctrl Pts',(-2.03678114929324,1.23166671347637,0.760277761846239));
#88876=CARTESIAN_POINT('Ctrl Pts',(-1.92529086506381,1.39955674033437,0.748342490018322));
#88877=CARTESIAN_POINT('Ctrl Pts',(-1.71647613141014,1.64101857339006,0.728609169452957));
#88878=CARTESIAN_POINT('Ctrl Pts',(-1.63239079233033,1.72468166692776,0.721161418709966));
#88879=CARTESIAN_POINT('Ctrl Pts',(-1.52835819326624,1.81374247090932,0.712216477780571));
#88880=CARTESIAN_POINT('Ctrl Pts',(-1.51416036452442,1.82561191830619,0.711001326633681));
#88881=CARTESIAN_POINT('Ctrl Pts',(-1.4908071680934,1.84467546574982,0.709010763794069));
#88882=CARTESIAN_POINT('Ctrl Pts',(-1.48173497720693,1.85197058170622,0.708239442578538));
#88883=CARTESIAN_POINT('Ctrl Pts',(-1.46543003483459,1.86488518675399,0.706856478940121));
#88884=CARTESIAN_POINT('Ctrl Pts',(-1.45821769512675,1.87053016450956,0.706245870875885));
#88885=CARTESIAN_POINT('Ctrl Pts',(-1.44288154591547,1.88239090967805,0.704949770501894));
#88886=CARTESIAN_POINT('Ctrl Pts',(-1.43474987976872,1.88859616360747,0.704263879562391));
#88887=CARTESIAN_POINT('Ctrl Pts',(-1.41293136818131,1.90502357734161,0.702426922128258));
#88888=CARTESIAN_POINT('Ctrl Pts',(-1.39917400904025,1.91515063302255,0.701272178138156));
#88889=CARTESIAN_POINT('Ctrl Pts',(-1.33085533810299,1.96431227585873,0.695553841641458));
#88890=CARTESIAN_POINT('Ctrl Pts',(-1.27476918107105,2.00116481582797,0.690908081597918));
#88891=CARTESIAN_POINT('Ctrl Pts',(-1.06467100998372,2.12679522624806,0.673664136910677));
#88892=CARTESIAN_POINT('Ctrl Pts',(-0.902386257657863,2.20056026983934,
0.660588977907503));
#88893=CARTESIAN_POINT('Ctrl Pts',(-0.640355477985702,2.2857645632085,0.640556214998197));
#88894=CARTESIAN_POINT('Ctrl Pts',(-0.545495406345934,2.31024116793884,
0.633521162604947));
#88895=CARTESIAN_POINT('Ctrl Pts',(-0.437029945150103,2.33117163427879,
0.625900456969698));
#88896=CARTESIAN_POINT('Ctrl Pts',(-0.424657044275813,2.33345725773121,
0.625037320823393));
#88897=CARTESIAN_POINT('Ctrl Pts',(-0.405925635001334,2.33676355173499,
0.623740524895043));
#88898=CARTESIAN_POINT('Ctrl Pts',(-0.399580439684234,2.33785692303564,
0.623302954475343));
#88899=CARTESIAN_POINT('Ctrl Pts',(-0.388175393850692,2.33977439198356,
0.622519624565479));
#88900=CARTESIAN_POINT('Ctrl Pts',(-0.383117296047,2.34060792971696,0.622173346695847));
#88901=CARTESIAN_POINT('Ctrl Pts',(-0.372030164872043,2.34239810469478,
0.621416781989657));
#88902=CARTESIAN_POINT('Ctrl Pts',(-0.366000136548875,2.34334786718063,
0.621006884778632));
#88903=CARTESIAN_POINT('Ctrl Pts',(-0.348772092038685,2.34599325616917,
0.619840126917685));
#88904=CARTESIAN_POINT('Ctrl Pts',(-0.337565315213134,2.34763199859982,
0.619086378997433));
#88905=CARTESIAN_POINT('Ctrl Pts',(-0.261233449977285,2.35823593739986,
0.613985286134159));
#88906=CARTESIAN_POINT('Ctrl Pts',(-0.195765000908738,2.36457132035811,
0.609772428655903));
#88907=CARTESIAN_POINT('Ctrl Pts',(0.110174716895957,2.38138012782496,0.590488052955399));
#88908=CARTESIAN_POINT('Ctrl Pts',(0.35106720268076,2.35793855776526,0.576305692927121));
#88909=CARTESIAN_POINT('Ctrl Pts',(0.624832421383487,2.28834645913277,0.558176642545399));
#88910=CARTESIAN_POINT('Ctrl Pts',(0.66505986667524,2.2769804787425,0.555464417224489));
#88911=CARTESIAN_POINT('Ctrl Pts',(0.719308968142765,2.26009256154776,0.551730696707469));
#88912=CARTESIAN_POINT('Ctrl Pts',(0.73361076822872,2.25549085606611,0.550739095864994));
#88913=CARTESIAN_POINT('Ctrl Pts',(0.756231382968104,2.24797460700757,0.549158722690731));
#88914=CARTESIAN_POINT('Ctrl Pts',(0.76457949868733,2.24514897611453,0.54857287809079));
#88915=CARTESIAN_POINT('Ctrl Pts',(0.781634695848507,2.23927005935689,0.547370549740896));
#88916=CARTESIAN_POINT('Ctrl Pts',(0.790340086659133,2.2362123646376,0.546753928949542));
#88917=CARTESIAN_POINT('Ctrl Pts',(0.810374353528146,2.22904390027971,0.545327993926065));
#88918=CARTESIAN_POINT('Ctrl Pts',(0.821690101297483,2.22489745164558,0.544517506736585));
#88919=CARTESIAN_POINT('Ctrl Pts',(0.857220114182346,2.21157010968876,0.541956310211719));
#88920=CARTESIAN_POINT('Ctrl Pts',(0.881315191753872,2.20207904360719,0.540195309000516));
#88921=CARTESIAN_POINT('Ctrl Pts',(1.0005066872654,2.15285989296877,0.531360078603607));
#88922=CARTESIAN_POINT('Ctrl Pts',(1.09308567096607,2.10736276147444,0.524093208452545));
#88923=CARTESIAN_POINT('Ctrl Pts',(1.30993455767744,1.98265305703226,0.506098161896216));
#88924=CARTESIAN_POINT('Ctrl Pts',(1.43036384860764,1.89760302833471,0.495243843136743));
#88925=CARTESIAN_POINT('Ctrl Pts',(1.56141150895823,1.78545130440902,0.482770085121858));
#88926=CARTESIAN_POINT('Ctrl Pts',(1.58042934154114,1.76863942826671,0.480942538592971));
#88927=CARTESIAN_POINT('Ctrl Pts',(1.63999568589212,1.7142542764494,0.475171133281602));
#88928=CARTESIAN_POINT('Ctrl Pts',(1.67950573937826,1.67556413927506,0.471271134091533));
#88929=CARTESIAN_POINT('Ctrl Pts',(1.7246894941321,1.62811209320835,0.466759933912571));
#88930=CARTESIAN_POINT('Ctrl Pts',(1.73170022601144,1.62065331763146,0.466058451112532));
#88931=CARTESIAN_POINT('Ctrl Pts',(1.74305505568855,1.60841500916403,0.464920146687879));
#88932=CARTESIAN_POINT('Ctrl Pts',(1.74742821756293,1.60366280615676,0.464481213599434));
#88933=CARTESIAN_POINT('Ctrl Pts',(1.7552192195573,1.59512681330722,0.463698375253306));
#88934=CARTESIAN_POINT('Ctrl Pts',(1.75864434363002,1.5913497836382,0.463353922941777));
#88935=CARTESIAN_POINT('Ctrl Pts',(1.76607254010742,1.58310512213734,0.46260628031285));
#88936=CARTESIAN_POINT('Ctrl Pts',(1.77007085835728,1.57863333396174,0.462203446979245));
#88937=CARTESIAN_POINT('Ctrl Pts',(1.7813879982382,1.56587899441908,0.461061914284783));
#88938=CARTESIAN_POINT('Ctrl Pts',(1.7886660715918,1.55756024659359,0.460326205678364));
#88939=CARTESIAN_POINT('Ctrl Pts',(1.83615320297324,1.50251120150658,0.455513021599716));
#88940=CARTESIAN_POINT('Ctrl Pts',(1.87458942508493,1.45427457315995,0.451555465202916));
#88941=CARTESIAN_POINT('Ctrl Pts',(2.02473002043905,1.24999109880192,0.435573844947295));
#88942=CARTESIAN_POINT('Ctrl Pts',(2.11918051815449,1.0821706007713,0.424169801814584));
#88943=CARTESIAN_POINT('Ctrl Pts',(2.20767374851595,0.867744834740668,0.40968795284765));
#88944=CARTESIAN_POINT('Ctrl Pts',(2.22202163645874,0.830315657834007,0.407165773223575));
#88945=CARTESIAN_POINT('Ctrl Pts',(2.25365109097284,0.741102847970854,0.401145749575422));
#88946=CARTESIAN_POINT('Ctrl Pts',(2.27010617083441,0.689052898042909,0.397626654700763));
#88947=CARTESIAN_POINT('Ctrl Pts',(2.2891817487847,0.620578464971442,0.392965623320821));
#88948=CARTESIAN_POINT('Ctrl Pts',(2.29344660808414,0.604626614392158,0.391877642763972));
#88949=CARTESIAN_POINT('Ctrl Pts',(2.30003944373639,0.578893496662921,0.39011852379195));
#88950=CARTESIAN_POINT('Ctrl Pts',(2.30247244349693,0.56913949503013,0.389450817251523));
#88951=CARTESIAN_POINT('Ctrl Pts',(2.30699117746388,0.550520395889349,0.388174365520821));
#88952=CARTESIAN_POINT('Ctrl Pts',(2.30908800998514,0.541658155390165,0.387565993651542));
#88953=CARTESIAN_POINT('Ctrl Pts',(2.31376685751924,0.521362052308742,0.386170753644772));
#88954=CARTESIAN_POINT('Ctrl Pts',(2.31631523547038,0.509920760324331,0.385382812076915));
#88955=CARTESIAN_POINT('Ctrl Pts',(2.32393240149492,0.474486666160826,0.382937883633644));
#88956=CARTESIAN_POINT('Ctrl Pts',(2.32871383644352,0.450434447535796,0.381271713575045));
#88957=CARTESIAN_POINT('Ctrl Pts',(2.34992725871791,0.334337903573334,0.37319502298379));
#88958=CARTESIAN_POINT('Ctrl Pts',(2.36127769125885,0.241461352893806,0.366625517186806));
#88959=CARTESIAN_POINT('Ctrl Pts',(2.37360181955217,0.0445715376189227,
0.352488068927495));
#88960=CARTESIAN_POINT('Ctrl Pts',(2.3732781772528,-0.0593322762628842,
0.344903769168617));
#88961=CARTESIAN_POINT('Ctrl Pts',(2.35770452936616,-0.285579165871283,
0.328331051913376));
#88962=CARTESIAN_POINT('Ctrl Pts',(2.33972489181835,-0.407455486345739,
0.31936501879041));
#88963=CARTESIAN_POINT('Ctrl Pts',(2.30811900222491,-0.546031135884901,
0.309473923804203));
#88964=CARTESIAN_POINT('Ctrl Pts',(2.30364389567164,-0.5646133106769,0.308154267159724));
#88965=CARTESIAN_POINT('Ctrl Pts',(2.29704910606919,-0.590612303618463,
0.306319206564952));
#88966=CARTESIAN_POINT('Ctrl Pts',(2.29511728484466,-0.598075364753959,
0.305793765318625));
#88967=CARTESIAN_POINT('Ctrl Pts',(2.29193500142203,-0.610126728461225,
0.304947560987187));
#88968=CARTESIAN_POINT('Ctrl Pts',(2.29070708362945,-0.614720858579664,
0.304625514646067));
#88969=CARTESIAN_POINT('Ctrl Pts',(2.28807190141162,-0.62446257965839,0.303943810009646));
#88970=CARTESIAN_POINT('Ctrl Pts',(2.28666106761748,-0.629609166638432,
0.303584362816388));
#88971=CARTESIAN_POINT('Ctrl Pts',(2.28312684153687,-0.642333099951298,
0.302697332886097));
#88972=CARTESIAN_POINT('Ctrl Pts',(2.28098306636702,-0.649904793966007,
0.302170920000501));
#88973=CARTESIAN_POINT('Ctrl Pts',(2.2728571536084,-0.678069517800896,0.300217675204858));
#88974=CARTESIAN_POINT('Ctrl Pts',(2.26663328099306,-0.698592557584431,
0.298804115327949));
#88975=CARTESIAN_POINT('Ctrl Pts',(2.22090970768154,-0.842315911662801,
0.28895511550237));
#88976=CARTESIAN_POINT('Ctrl Pts',(2.17166027737835,-0.962204067261257,
0.280993437826904));
#88977=CARTESIAN_POINT('Ctrl Pts',(2.02930351392623,-1.24135426858414,0.261780269272243));
#88978=CARTESIAN_POINT('Ctrl Pts',(1.92697114560946,-1.39492141482945,0.250579747106606));
#88979=CARTESIAN_POINT('Ctrl Pts',(1.78956967640727,-1.55674119882285,0.236813504223705));
#88980=CARTESIAN_POINT('Ctrl Pts',(1.77082288055304,-1.57803326969538,0.234959336828218));
#88981=CARTESIAN_POINT('Ctrl Pts',(1.74389545159007,-1.60753248998782,0.232326356996511));
#88982=CARTESIAN_POINT('Ctrl Pts',(1.73602919827401,-1.61602433991634,0.231560708771867));
#88983=CARTESIAN_POINT('Ctrl Pts',(1.72221465838979,-1.63072026991237,0.230221975230984));
#88984=CARTESIAN_POINT('Ctrl Pts',(1.71629417530401,-1.63695028292761,0.229650082047395));
#88985=CARTESIAN_POINT('Ctrl Pts',(1.70382807447056,-1.64992615144839,0.22844966545211));
#88986=CARTESIAN_POINT('Ctrl Pts',(1.69727596715171,-1.65666553641231,0.227820866844937));
#88987=CARTESIAN_POINT('Ctrl Pts',(1.6815714904615,-1.67262793607172,0.22631865812438));
#88988=CARTESIAN_POINT('Ctrl Pts',(1.67238313005619,-1.68181495554965,0.225443679232295));
#88989=CARTESIAN_POINT('Ctrl Pts',(1.64091038779628,-1.71277015315762,0.222459499243495));
#88990=CARTESIAN_POINT('Ctrl Pts',(1.61827362684124,-1.73417381100087,0.220334677545939));
#88991=CARTESIAN_POINT('Ctrl Pts',(1.56289211756675,-1.78450975125133,0.215184630203508));
#88992=CARTESIAN_POINT('Ctrl Pts',(1.52975757961476,-1.81299425027077,0.212142169107271));
#88993=CARTESIAN_POINT('Ctrl Pts',(1.295593761634,-2.0033049568681,0.190900568318592));
#88994=CARTESIAN_POINT('Ctrl Pts',(1.07015773753808,-2.13225727392394,0.171479134689879));
#88995=CARTESIAN_POINT('Ctrl Pts',(0.804987994816205,-2.23110228262024,
0.151681448966647));
#88996=CARTESIAN_POINT('Ctrl Pts',(0.781424686826433,-2.23946392045831,
0.149948750330738));
#88997=CARTESIAN_POINT('Ctrl Pts',(0.749661120413222,-2.25017306405519,
0.147652428160719));
#88998=CARTESIAN_POINT('Ctrl Pts',(0.74157506083843,-2.25285087131227,0.147071243707183));
#88999=CARTESIAN_POINT('Ctrl Pts',(0.728260020849596,-2.25718086823613,
0.146119989156702));
#89000=CARTESIAN_POINT('Ctrl Pts',(0.723039488203981,-2.2588585681277,0.145748474576035));
#89001=CARTESIAN_POINT('Ctrl Pts',(0.712766643234138,-2.26212064423224,
0.14502032287958));
#89002=CARTESIAN_POINT('Ctrl Pts',(0.707714805397492,-2.26370622042107,
0.144663612332407));
#89003=CARTESIAN_POINT('Ctrl Pts',(0.697498787849602,-2.26687509092163,
0.143944942793365));
#89004=CARTESIAN_POINT('Ctrl Pts',(0.692334423965896,-2.26845768831963,
0.14358302475386));
#89005=CARTESIAN_POINT('Ctrl Pts',(0.673757270738551,-2.27408122813314,
0.14228594615369));
#89006=CARTESIAN_POINT('Ctrl Pts',(0.660313820056548,-2.27802106529962,
0.141356294878642));
#89007=CARTESIAN_POINT('Ctrl Pts',(0.531945423148506,-2.31440977868095,
0.132557624836019));
#89008=CARTESIAN_POINT('Ctrl Pts',(0.414742458143056,-2.33825900818764,
0.125115973224835));
#89009=CARTESIAN_POINT('Ctrl Pts',(0.102061160892701,-2.37762055134687,
0.105654159096787));
#89010=CARTESIAN_POINT('Ctrl Pts',(-0.0943608051712325,-2.37793690014678,
0.0937590278414453));
#89011=CARTESIAN_POINT('Ctrl Pts',(-0.315165659561377,-2.35086916583635,
0.0793014817004178));
#89012=CARTESIAN_POINT('Ctrl Pts',(-0.341688623976874,-2.34716084218601,
0.0775482835218531));
#89013=CARTESIAN_POINT('Ctrl Pts',(-0.380179456179028,-2.3411130076066,
0.0749772556349703));
#89014=CARTESIAN_POINT('Ctrl Pts',(-0.39220169013825,-2.33912897428847,
0.074170410657453));
#89015=CARTESIAN_POINT('Ctrl Pts',(-0.413456569779718,-2.3354528091372,
0.0727369375012271));
#89016=CARTESIAN_POINT('Ctrl Pts',(-0.422695529542975,-2.33379832972636,
0.0721114937516175));
#89017=CARTESIAN_POINT('Ctrl Pts',(-0.441880640723978,-2.33024507093785,
0.0708077251933305));
#89018=CARTESIAN_POINT('Ctrl Pts',(-0.451824921733991,-2.32833735226487,
0.0701291322535876));
#89019=CARTESIAN_POINT('Ctrl Pts',(-0.477568297848316,-2.3232275920694,
0.0683649695055473));
#89020=CARTESIAN_POINT('Ctrl Pts',(-0.493347290089823,-2.31992809219195,
0.0672763598045879));
#89021=CARTESIAN_POINT('Ctrl Pts',(-0.562269321199218,-2.30478107048403,
0.0624884294285706));
#89022=CARTESIAN_POINT('Ctrl Pts',(-0.615025227240541,-2.29126727035618,
0.0587370028246758));
#89023=CARTESIAN_POINT('Ctrl Pts',(-0.757823346299244,-2.24940155808092,
0.0483345334727881));
#89024=CARTESIAN_POINT('Ctrl Pts',(-0.846705737141405,-2.21747367686783,
0.0415806383145637));
#89025=CARTESIAN_POINT('Ctrl Pts',(-1.08025369384199,-2.11748770243054,
0.0231531306418185));
#89026=CARTESIAN_POINT('Ctrl Pts',(-1.22031304748997,-2.03998032716046,
0.0113379304209554));
#89027=CARTESIAN_POINT('Ctrl Pts',(-1.35150067398999,-1.94901102888224,
-5.43618969284232E-15));
#89028=CARTESIAN_POINT('',(1.37702479013102,-1.93106208855765,0.));
#89029=CARTESIAN_POINT('Origin',(0.,0.,0.));
#89030=CARTESIAN_POINT('Ctrl Pts',(1.377024790131,-1.93106208855766,8.88178419700125E-16));
#89031=CARTESIAN_POINT('Ctrl Pts',(1.44323442930785,-1.88384852922553,0.00545688894094474));
#89032=CARTESIAN_POINT('Ctrl Pts',(1.50706076889383,-1.83319246581089,0.0109137778818887));
#89033=CARTESIAN_POINT('Ctrl Pts',(1.56814231099797,-1.77936161444434,0.0163706668228325));
#89034=CARTESIAN_POINT('Ctrl Pts',(1.62918664869343,-1.7255635511333,0.0218242320047606));
#89035=CARTESIAN_POINT('Ctrl Pts',(1.68748918816346,-1.66859483606143,0.0272777971866886));
#89036=CARTESIAN_POINT('Ctrl Pts',(1.74272158951512,-1.60876335237284,0.0327313623686167));
#89037=CARTESIAN_POINT('Ctrl Pts',(1.79794854973166,-1.54893776289089,0.0381843903009549));
#89038=CARTESIAN_POINT('Ctrl Pts',(1.85010566943635,-1.48625027976053,0.0436374182332935));
#89039=CARTESIAN_POINT('Ctrl Pts',(1.89890209573401,-1.42104500045459,0.0490904461656316));
#89040=CARTESIAN_POINT('Ctrl Pts',(1.94769763273321,-1.35584090949293,0.0545433747183692));
#89041=CARTESIAN_POINT('Ctrl Pts',(1.99313233564526,-1.28811946349422,0.0599963032711064));
#89042=CARTESIAN_POINT('Ctrl Pts',(2.03495704214576,-1.218256089302,0.065449231823844));
#89043=CARTESIAN_POINT('Ctrl Pts',(2.07679126035066,-1.14837682689872,0.0709034004724213));
#89044=CARTESIAN_POINT('Ctrl Pts',(2.11501362448989,-1.07635504271482,0.0763575691209986));
#89045=CARTESIAN_POINT('Ctrl Pts',(2.1494200941166,-1.00259230074232,0.081811737769576));
#89046=CARTESIAN_POINT('Ctrl Pts',(2.18384284291776,-0.928794658457252,
0.0872684870189499));
#89047=CARTESIAN_POINT('Ctrl Pts',(2.21444592129525,-0.853254816187775,
0.0927252362683234));
#89048=CARTESIAN_POINT('Ctrl Pts',(2.24107318383604,-0.776394904150594,
0.0981819855176973));
#89049=CARTESIAN_POINT('Ctrl Pts',(2.26774034407289,-0.699419826936176,
0.103646911038391));
#89050=CARTESIAN_POINT('Ctrl Pts',(2.29041964825811,-0.621121144024271,
0.109111836559085));
#89051=CARTESIAN_POINT('Ctrl Pts',(2.30900469105276,-0.541936711430734,
0.114576762079779));
#89052=CARTESIAN_POINT('Ctrl Pts',(2.32760431554601,-0.462690151268103,
0.120045975343995));
#89053=CARTESIAN_POINT('Ctrl Pts',(2.34210319909487,-0.382556886917718,
0.125515188608211));
#89054=CARTESIAN_POINT('Ctrl Pts',(2.35244643305339,-0.301983181840315,
0.130984401872427));
#89055=CARTESIAN_POINT('Ctrl Pts',(2.3628098942255,-0.221251906939983,0.136464310722315));
#89056=CARTESIAN_POINT('Ctrl Pts',(2.36900143325511,-0.140078906893982,
0.141944219572203));
#89057=CARTESIAN_POINT('Ctrl Pts',(2.3710181814828,-0.0589138827273241,
0.147424128422091));
#89058=CARTESIAN_POINT('Ctrl Pts',(2.37242499804373,-0.00229585842526928,
0.151246730776019));
#89059=CARTESIAN_POINT('Ctrl Pts',(2.37180146375247,0.0543182630853344,
0.155069333129946));
#89060=CARTESIAN_POINT('Ctrl Pts',(2.36916154938288,0.110777323607845,0.158891935483873));
#89061=CARTESIAN_POINT('Ctrl Pts',(2.36551681281839,0.188726216440715,0.164169522791762));
#89062=CARTESIAN_POINT('Ctrl Pts',(2.35801245769879,0.266674309576874,0.169447110099651));
#89063=CARTESIAN_POINT('Ctrl Pts',(2.34664078348069,0.344202114759797,0.17472469740754));
#89064=CARTESIAN_POINT('Ctrl Pts',(2.33528742825447,0.421605027934216,0.179993782882088));
#89065=CARTESIAN_POINT('Ctrl Pts',(2.32007918549393,0.498588527466604,0.185262868356636));
#89066=CARTESIAN_POINT('Ctrl Pts',(2.30106032801871,0.5747342249409,0.190531953831185));
#89067=CARTESIAN_POINT('Ctrl Pts',(2.28192207585617,0.651357942283229,0.195834117045208));
#89068=CARTESIAN_POINT('Ctrl Pts',(2.25892520061864,0.727132808352569,0.201136280259231));
#89069=CARTESIAN_POINT('Ctrl Pts',(2.23216780058896,0.801638929015961,0.206438443473254));
#89070=CARTESIAN_POINT('Ctrl Pts',(2.20563356521996,0.875523646511697,0.211696385071828));
#89071=CARTESIAN_POINT('Ctrl Pts',(2.17540145399492,0.948160240731734,0.216954326670403));
#89072=CARTESIAN_POINT('Ctrl Pts',(2.14161761336225,1.01915261891268,0.222212268268977));
#89073=CARTESIAN_POINT('Ctrl Pts',(2.10784804477187,1.09011500623988,0.227467988640969));
#89074=CARTESIAN_POINT('Ctrl Pts',(2.07052992972339,1.1594341230509,0.232723709012963));
#89075=CARTESIAN_POINT('Ctrl Pts',(2.02985724532268,1.22673453775094,0.237979429384955));
#89076=CARTESIAN_POINT('Ctrl Pts',(1.98918841914434,1.29402856831458,0.243234651197824));
#89077=CARTESIAN_POINT('Ctrl Pts',(1.94516590451668,1.35930386698306,0.248489873010692));
#89078=CARTESIAN_POINT('Ctrl Pts',(1.89802843584865,1.42221169985693,0.25374509482356));
#89079=CARTESIAN_POINT('Ctrl Pts',(1.8501613506344,1.48609325060424,0.259081659502242));
#89080=CARTESIAN_POINT('Ctrl Pts',(1.79908234605505,1.54753299939798,0.264418224180925));
#89081=CARTESIAN_POINT('Ctrl Pts',(1.74508434773943,1.60620007526299,0.269754788859607));
#89082=CARTESIAN_POINT('Ctrl Pts',(1.6918351201776,1.66405363596099,0.275017353321953));
#89083=CARTESIAN_POINT('Ctrl Pts',(1.63574774002439,1.719210645093,0.280279917784299));
#89084=CARTESIAN_POINT('Ctrl Pts',(1.57713928335961,1.77139203548619,0.285542482246645));
#89085=CARTESIAN_POINT('Ctrl Pts',(1.51729463134653,1.8246740587188,0.290916047033495));
#89086=CARTESIAN_POINT('Ctrl Pts',(1.45482174846241,1.87485317119378,0.296289611820345));
#89087=CARTESIAN_POINT('Ctrl Pts',(1.39009065932477,1.92167791821576,0.301663176607196));
#89088=CARTESIAN_POINT('Ctrl Pts',(1.32535957018712,1.96850266523773,0.307036741394046));
#89089=CARTESIAN_POINT('Ctrl Pts',(1.25837075515963,2.01197282475023,0.312410306180897));
#89090=CARTESIAN_POINT('Ctrl Pts',(1.18952013501392,2.05188691474371,0.317783870967748));
#89091=CARTESIAN_POINT('Ctrl Pts',(1.12110087339485,2.09155093751898,0.323123769638238));
#89092=CARTESIAN_POINT('Ctrl Pts',(1.05056820942786,2.12786295700445,0.328463668308728));
#89093=CARTESIAN_POINT('Ctrl Pts',(0.97828367652601,2.16059230553632,0.333803566979218));
#89094=CARTESIAN_POINT('Ctrl Pts',(0.906103429712095,2.19327443489721,0.339135761689816));
#89095=CARTESIAN_POINT('Ctrl Pts',(0.832176755690867,2.22238396760182,0.344467956400415));
#89096=CARTESIAN_POINT('Ctrl Pts',(0.756891277378829,2.2477352283416,0.349800151111013));
#89097=CARTESIAN_POINT('Ctrl Pts',(0.681693782616492,2.27305686193469,0.355126114269008));
#89098=CARTESIAN_POINT('Ctrl Pts',(0.605141080097607,2.29462880434646,0.360452077427004));
#89099=CARTESIAN_POINT('Ctrl Pts',(0.527640948372251,2.31231336373356,0.365778040584999));
#89100=CARTESIAN_POINT('Ctrl Pts',(0.45019049891151,2.32998658625014,0.371100589478978));
#89101=CARTESIAN_POINT('Ctrl Pts',(0.371794280151321,2.34377726891592,0.376423138372958));
#89102=CARTESIAN_POINT('Ctrl Pts',(0.292874274958876,2.35359782494107,0.381745687266938));
#89103=CARTESIAN_POINT('Ctrl Pts',(0.213980483290613,2.36341511903811,0.387066468259816));
#89104=CARTESIAN_POINT('Ctrl Pts',(0.134563713958973,2.36926484766798,0.392387249252693));
#89105=CARTESIAN_POINT('Ctrl Pts',(0.0550537088996654,2.37111095304214,
0.397708030245571));
#89106=CARTESIAN_POINT('Ctrl Pts',(-0.0244544470979098,2.37295701548381,
0.403028687499902));
#89107=CARTESIAN_POINT('Ctrl Pts',(-0.104055367419461,2.37079963020706,
0.408349344754232));
#89108=CARTESIAN_POINT('Ctrl Pts',(-0.183318127710723,2.36465484300619,
0.413670002008563));
#89109=CARTESIAN_POINT('Ctrl Pts',(-0.26265795540767,2.35850408121137,0.418995832552968));
#89110=CARTESIAN_POINT('Ctrl Pts',(-0.341658499354637,2.34835820866443,
0.424321663097373));
#89111=CARTESIAN_POINT('Ctrl Pts',(-0.419893374233965,2.33428524751677,
0.429647493641779));
#89112=CARTESIAN_POINT('Ctrl Pts',(-0.498164825645014,2.32020570694899,
0.434975814129578));
#89113=CARTESIAN_POINT('Ctrl Pts',(-0.575669438982421,2.30219552530526,
0.440304134617377));
#89114=CARTESIAN_POINT('Ctrl Pts',(-0.651992935900375,2.28037349441621,
0.445632455105176));
#89115=CARTESIAN_POINT('Ctrl Pts',(-0.728452664517911,2.25851251284387,
0.450970286244154));
#89116=CARTESIAN_POINT('Ctrl Pts',(-0.803726620498811,2.23282623700074,
0.456308117383132));
#89117=CARTESIAN_POINT('Ctrl Pts',(-0.877417743213549,2.20348273566961,
0.46164594852211));
#89118=CARTESIAN_POINT('Ctrl Pts',(-0.94658235809367,2.17594167110125,0.466655901165276));
#89119=CARTESIAN_POINT('Ctrl Pts',(-1.01435252431405,2.14517947154205,0.471665853808442));
#89120=CARTESIAN_POINT('Ctrl Pts',(-1.08042043865333,2.1113715301292,0.476675806451608));
#89121=CARTESIAN_POINT('Ctrl Pts',(-1.15085759099418,2.07532778418321,0.482017079913562));
#89122=CARTESIAN_POINT('Ctrl Pts',(-1.21961720760008,2.03568988249139,0.487358353375516));
#89123=CARTESIAN_POINT('Ctrl Pts',(-1.28630969075306,1.99263781003342,0.492699626837469));
#89124=CARTESIAN_POINT('Ctrl Pts',(-1.35290829972811,1.94964633627741,0.498033382095997));
#89125=CARTESIAN_POINT('Ctrl Pts',(-1.417445164947,1.90325048760995,0.503367137354524));
#89126=CARTESIAN_POINT('Ctrl Pts',(-1.47955450671666,1.85367648853688,0.508700892613051));
#89127=CARTESIAN_POINT('Ctrl Pts',(-1.54159448650848,1.8041578523211,0.514028691282705));
#89128=CARTESIAN_POINT('Ctrl Pts',(-1.60121196736101,1.75146840916292,0.519356489952359));
#89129=CARTESIAN_POINT('Ctrl Pts',(-1.6580706854012,1.69587725520251,0.524684288622014));
#89130=CARTESIAN_POINT('Ctrl Pts',(-1.71489474473583,1.6403199872934,0.530008839687576));
#89131=CARTESIAN_POINT('Ctrl Pts',(-1.76896304640341,1.58186484532476,0.535333390753139));
#89132=CARTESIAN_POINT('Ctrl Pts',(-1.81997385675543,1.52081991807931,0.540657941818702));
#89133=CARTESIAN_POINT('Ctrl Pts',(-1.8709693038848,1.4597933760899,0.54598088925823));
#89134=CARTESIAN_POINT('Ctrl Pts',(-1.9189087892869,1.39617895589138,0.551303836697758));
#89135=CARTESIAN_POINT('Ctrl Pts',(-1.96352978159866,1.33031908175261,0.556626784137286));
#89136=CARTESIAN_POINT('Ctrl Pts',(-2.00815109504782,1.26445873362016,0.56194976988608));
#89137=CARTESIAN_POINT('Ctrl Pts',(-2.04945360726806,1.19635328678691,0.567272755634874));
#89138=CARTESIAN_POINT('Ctrl Pts',(-2.08721801761038,1.12637427592368,0.572595741383668));
#89139=CARTESIAN_POINT('Ctrl Pts',(-2.12502084240226,1.0563240815001,0.577924141742823));
#89140=CARTESIAN_POINT('Ctrl Pts',(-2.15927815392128,0.984396927969013,
0.583252542101979));
#89141=CARTESIAN_POINT('Ctrl Pts',(-2.18981685108996,0.910988595528203,
0.588580942461134));
#89142=CARTESIAN_POINT('Ctrl Pts',(-2.22037059747506,0.837544088070657,
0.593911968611746));
#89143=CARTESIAN_POINT('Ctrl Pts',(-2.24720192115811,0.762617387700967,
0.599242994762358));
#89144=CARTESIAN_POINT('Ctrl Pts',(-2.27018699839248,0.686621478567161,
0.60457402091297));
#89145=CARTESIAN_POINT('Ctrl Pts',(-2.293213949893,0.610487119912694,0.609914759139188));
#89146=CARTESIAN_POINT('Ctrl Pts',(-2.31238054031918,0.533280114454326,
0.615255497365405));
#89147=CARTESIAN_POINT('Ctrl Pts',(-2.32761371816615,0.455425560882073,
0.620596235591622));
#89148=CARTESIAN_POINT('Ctrl Pts',(-2.34184793131004,0.38267657042831,0.625586737706242));
#89149=CARTESIAN_POINT('Ctrl Pts',(-2.35264818505678,0.309362574879414,
0.630577239820862));
#89150=CARTESIAN_POINT('Ctrl Pts',(-2.35999596812134,0.235832764795321,
0.635567741935482));
#89151=CARTESIAN_POINT('Ctrl Pts',(-2.36208369198396,0.214940757263645,
0.636985692119852));
#89152=CARTESIAN_POINT('Ctrl Pts',(-2.36389406907271,0.194020289892537,
0.638403642304223));
#89153=CARTESIAN_POINT('Ctrl Pts',(-2.36542649454111,0.173076750093528,
0.639821592488593));
#89154=CARTESIAN_POINT('Origin',(0.,0.,-1.84858989190503));
#89155=CARTESIAN_POINT('',(-2.36542648301433,0.173076907629062,1.83854786047046));
#89156=CARTESIAN_POINT('',(-2.36542650134106,0.173076657159213,1.63877486397391));
#89157=CARTESIAN_POINT('',(-2.36542649454111,0.173076750093529,-1.84858989190503));
#89158=CARTESIAN_POINT('Ctrl Pts',(-2.36542648301433,0.173076907629062,
1.83854786047046));
#89159=CARTESIAN_POINT('Ctrl Pts',(-2.36078946920551,0.236450557041656,
1.8345366875538));
#89160=CARTESIAN_POINT('Ctrl Pts',(-2.35360599959298,0.29963333287273,1.83046499197252));
#89161=CARTESIAN_POINT('Ctrl Pts',(-2.34163874790418,0.377018108149751,
1.82535131063931));
#89162=CARTESIAN_POINT('Ctrl Pts',(-2.33925412049139,0.391541598455056,
1.82438608712068));
#89163=CARTESIAN_POINT('Ctrl Pts',(-2.33499820758016,0.416034006121167,
1.82274857644167));
#89164=CARTESIAN_POINT('Ctrl Pts',(-2.33319784448188,0.426014949010509,
1.82207852454145));
#89165=CARTESIAN_POINT('Ctrl Pts',(-2.32975839799822,0.444406675857587,
1.82083860890605));
#89166=CARTESIAN_POINT('Ctrl Pts',(-2.32813763609304,0.452820748977882,
1.82026933439943));
#89167=CARTESIAN_POINT('Ctrl Pts',(-2.32469467624383,0.470187401195334,
1.81909007778314));
#89168=CARTESIAN_POINT('Ctrl Pts',(-2.32286627614208,0.479138590730262,
1.81847990664027));
#89169=CARTESIAN_POINT('Ctrl Pts',(-2.31862843843171,0.499290994858359,
1.81710076874745));
#89170=CARTESIAN_POINT('Ctrl Pts',(-2.31618947377455,0.51048569676617,1.81633086850144));
#89171=CARTESIAN_POINT('Ctrl Pts',(-2.30973066525293,0.539131726326424,
1.81435084913924));
#89172=CARTESIAN_POINT('Ctrl Pts',(-2.30559416500161,0.556555729359762,
1.81313701525027));
#89173=CARTESIAN_POINT('Ctrl Pts',(-2.27703296145798,0.671076118074422,
1.80509474436746));
#89174=CARTESIAN_POINT('Ctrl Pts',(-2.24668163386356,0.766576103238891,
1.7980760022881));
#89175=CARTESIAN_POINT('Ctrl Pts',(-2.17711251585113,0.945412934733576,
1.78433365041024));
#89176=CARTESIAN_POINT('Ctrl Pts',(-2.13889589125223,1.02895429625545,1.77764627994544));
#89177=CARTESIAN_POINT('Ctrl Pts',(-2.05640439074153,1.18470813939627,1.76477140616635));
#89178=CARTESIAN_POINT('Ctrl Pts',(-2.01291108543624,1.2571883049359,1.7585962317565));
#89179=CARTESIAN_POINT('Ctrl Pts',(-1.93002190020279,1.37995125326647,1.74795549229346));
#89180=CARTESIAN_POINT('Ctrl Pts',(-1.89228839017556,1.431256898583,1.74344846149813));
#89181=CARTESIAN_POINT('Ctrl Pts',(-1.84546732484836,1.48982429587284,1.73828626527198));
#89182=CARTESIAN_POINT('Ctrl Pts',(-1.83833892869344,1.49861138251134,1.73751130188896));
#89183=CARTESIAN_POINT('Ctrl Pts',(-1.82728026725469,1.51204560728817,1.73632621798991));
#89184=CARTESIAN_POINT('Ctrl Pts',(-1.82339466620307,1.51672904205132,1.73591302280914));
#89185=CARTESIAN_POINT('Ctrl Pts',(-1.81621265750569,1.52531825037258,1.73515522855756));
#89186=CARTESIAN_POINT('Ctrl Pts',(-1.8129216648719,1.52922830873908,1.73481026226366));
#89187=CARTESIAN_POINT('Ctrl Pts',(-1.80547096310068,1.53802269854776,1.73403435786301));
#89188=CARTESIAN_POINT('Ctrl Pts',(-1.8013040663673,1.54290080134626,1.73360395471793));
#89189=CARTESIAN_POINT('Ctrl Pts',(-1.78896062672022,1.55723285602097,1.7323391399935));
#89190=CARTESIAN_POINT('Ctrl Pts',(-1.78072892657754,1.56663933272245,1.73150865772511));
#89191=CARTESIAN_POINT('Ctrl Pts',(-1.71086348463299,1.64521334697599,1.7245640790034));
#89192=CARTESIAN_POINT('Ctrl Pts',(-1.64529200704371,1.71078913814569,1.71871835763982));
#89193=CARTESIAN_POINT('Ctrl Pts',(-1.41156096440522,1.91862999146322,1.69931285419988));
#89194=CARTESIAN_POINT('Ctrl Pts',(-1.22753265730542,2.04127618589842,1.68619121536536));
#89195=CARTESIAN_POINT('Ctrl Pts',(-1.00671123389437,2.14763948570874,1.6704010962321));
#89196=CARTESIAN_POINT('Ctrl Pts',(-0.984021977492536,2.15812963990116,
1.66877980845074));
#89197=CARTESIAN_POINT('Ctrl Pts',(-0.942982730400442,2.17632200945155,
1.66584648732082));
#89198=CARTESIAN_POINT('Ctrl Pts',(-0.924693377660703,2.18415568037977,
1.66453895848046));
#89199=CARTESIAN_POINT('Ctrl Pts',(-0.896338233776443,2.19588074060702,
1.66251036777533));
#89200=CARTESIAN_POINT('Ctrl Pts',(-0.886340513137628,2.19993521371126,
1.66179483627105));
#89201=CARTESIAN_POINT('Ctrl Pts',(-0.876224236830244,2.203957612787,1.66107045510289));
#89202=CARTESIAN_POINT('Ctrl Pts',(-0.876132854440562,2.20399394135745,
1.66106391159001));
#89203=CARTESIAN_POINT('Ctrl Pts',(-0.875948293566478,2.20406729923371,
1.6610506958929));
#89204=CARTESIAN_POINT('Ctrl Pts',(-0.875855114987727,2.20410432831643,
1.66104402370074));
#89205=CARTESIAN_POINT('Ctrl Pts',(-0.875666914997403,2.20417910500324,
1.66103054729461));
#89206=CARTESIAN_POINT('Ctrl Pts',(-0.875571893499305,2.20421685236911,
1.6610237430732));
#89207=CARTESIAN_POINT('Ctrl Pts',(-0.875379959564238,2.20429308390839,
1.66100999915995));
#89208=CARTESIAN_POINT('Ctrl Pts',(-0.875283047018924,2.20433156783963,
1.66100305945903));
#89209=CARTESIAN_POINT('Ctrl Pts',(-0.875087281387327,2.20440929134447,
1.66098904103077));
#89210=CARTESIAN_POINT('Ctrl Pts',(-0.874988428197988,2.20444853066051,
1.66098196229468));
#89211=CARTESIAN_POINT('Ctrl Pts',(-0.874788730188428,2.20452778431258,
1.66096766213328));
#89212=CARTESIAN_POINT('Ctrl Pts',(-0.874687885262558,2.20456779837812,
1.66096044069897));
#89213=CARTESIAN_POINT('Ctrl Pts',(-0.874516479199353,2.20463579665004,
1.66094816636857));
#89214=CARTESIAN_POINT('Ctrl Pts',(-0.874445919459017,2.2046637843906,1.66094311359132));
#89215=CARTESIAN_POINT('Ctrl Pts',(-0.874298124993661,2.20472239931375,
1.66093253000387));
#89216=CARTESIAN_POINT('Ctrl Pts',(-0.874220890016408,2.20475302581993,
1.66092699917204));
#89217=CARTESIAN_POINT('Ctrl Pts',(-0.87405909559096,2.20481717341567,1.66091541295426));
#89218=CARTESIAN_POINT('Ctrl Pts',(-0.873974535816569,2.204850693702,1.66090935754066));
#89219=CARTESIAN_POINT('Ctrl Pts',(-0.873797376069789,2.20492090969152,
1.66089667089196));
#89220=CARTESIAN_POINT('Ctrl Pts',(-0.873704775706758,2.20495760442883,
1.6608900396237));
#89221=CARTESIAN_POINT('Ctrl Pts',(-0.873510745645776,2.20503447856122,
1.66087614473807));
#89222=CARTESIAN_POINT('Ctrl Pts',(-0.873409315489886,2.20507465679007,
1.66086888108166));
#89223=CARTESIAN_POINT('Ctrl Pts',(-0.873196755344978,2.20515883855136,
1.66085365906175));
#89224=CARTESIAN_POINT('Ctrl Pts',(-0.873085624804296,2.20520284068071,
1.6608457006512));
#89225=CARTESIAN_POINT('Ctrl Pts',(-0.872852703142428,2.20529504562849,
1.66082902029729));
#89226=CARTESIAN_POINT('Ctrl Pts',(-0.872730911358362,2.20534324675688,
1.66082029829735));
#89227=CARTESIAN_POINT('Ctrl Pts',(-0.872475606378897,2.20544426349637,
1.6608020147658));
#89228=CARTESIAN_POINT('Ctrl Pts',(-0.872342092385068,2.20549707707095,
1.66079245316602));
#89229=CARTESIAN_POINT('Ctrl Pts',(-0.872062171201412,2.20560777493306,
1.66077240648304));
#89230=CARTESIAN_POINT('Ctrl Pts',(-0.871915763045639,2.20566565676627,
1.66076192131738));
#89231=CARTESIAN_POINT('Ctrl Pts',(-0.871608758801001,2.20578699422658,
1.66073993473703));
#89232=CARTESIAN_POINT('Ctrl Pts',(-0.871448161551489,2.20585044689032,
1.66072843322314));
#89233=CARTESIAN_POINT('Ctrl Pts',(-0.871111346273246,2.20598348153119,
1.66070431127949));
#89234=CARTESIAN_POINT('Ctrl Pts',(-0.870935126838851,2.20605305993026,
1.66069169072928));
#89235=CARTESIAN_POINT('Ctrl Pts',(-0.870565498262388,2.20619895271629,
1.66066521828813));
#89236=CARTESIAN_POINT('Ctrl Pts',(-0.870372081269755,2.20627526521112,
1.66065136581131));
#89237=CARTESIAN_POINT('Ctrl Pts',(-0.861654597737763,2.2097134154118,1.66002701550167));
#89238=CARTESIAN_POINT('Ctrl Pts',(-0.853111241095542,2.21302580877359,
1.65941486439869));
#89239=CARTESIAN_POINT('Ctrl Pts',(-0.833602346320865,2.22045995697617,
1.6580162805502));
#89240=CARTESIAN_POINT('Ctrl Pts',(-0.82262510588512,2.2245501160716,1.65722880643304));
#89241=CARTESIAN_POINT('Ctrl Pts',(-0.793991863493191,2.2349780486938,1.65517316846091));
#89242=CARTESIAN_POINT('Ctrl Pts',(-0.776290462273415,2.24118786366923,
1.65390079528855));
#89243=CARTESIAN_POINT('Ctrl Pts',(-0.610447408566426,2.29716669274774,
1.6419630319133));
#89244=CARTESIAN_POINT('Ctrl Pts',(-0.457829257236879,2.3323798346759,1.63081220241945));
#89245=CARTESIAN_POINT('Ctrl Pts',(-0.190713177547464,2.36677375944278,
1.61120713032582));
#89246=CARTESIAN_POINT('Ctrl Pts',(-0.0776495612631143,2.37317526241946,
1.60289350109526));
#89247=CARTESIAN_POINT('Ctrl Pts',(0.104411712666428,2.37045446012087,1.58978273650796));
#89248=CARTESIAN_POINT('Ctrl Pts',(0.173312923810354,2.36641518660472,1.58488721040152));
#89249=CARTESIAN_POINT('Ctrl Pts',(0.253306797740341,2.35821206335886,1.57935022432202));
#89250=CARTESIAN_POINT('Ctrl Pts',(0.264658543276269,2.35696506937642,1.5785679660727));
#89251=CARTESIAN_POINT('Ctrl Pts',(0.282067453334594,2.35492533211052,1.57737410250882));
#89252=CARTESIAN_POINT('Ctrl Pts',(0.28813110208817,2.35419112185069,1.57695935292082));
#89253=CARTESIAN_POINT('Ctrl Pts',(0.299262419565145,2.35279964687085,1.57620004898276));
#89254=CARTESIAN_POINT('Ctrl Pts',(0.304330783839253,2.35214943171765,1.57585511726128));
#89255=CARTESIAN_POINT('Ctrl Pts',(0.315732224892021,2.3506492831538,1.57508095693518));
#89256=CARTESIAN_POINT('Ctrl Pts',(0.322063981448061,2.34979013626968,1.57465225185626));
#89257=CARTESIAN_POINT('Ctrl Pts',(0.338309633588639,2.34751888822697,1.57355526580704));
#89258=CARTESIAN_POINT('Ctrl Pts',(0.348218321895944,2.34606955307509,1.57288901637182));
#89259=CARTESIAN_POINT('Ctrl Pts',(0.408757211352561,2.3368225838086,1.56883414380662));
#89260=CARTESIAN_POINT('Ctrl Pts',(0.459137310044456,2.32744840920093,1.56552686046377));
#89261=CARTESIAN_POINT('Ctrl Pts',(0.539307523466072,2.30982620105871,1.56031487896943));
#89262=CARTESIAN_POINT('Ctrl Pts',(0.569305596630838,2.30261611072903,1.55837627227424));
#89263=CARTESIAN_POINT('Ctrl Pts',(0.806769121196318,2.24061673541437,1.54306315222918));
#89264=CARTESIAN_POINT('Ctrl Pts',(1.00606045543149,2.15849173842311,1.53031226461131));
#89265=CARTESIAN_POINT('Ctrl Pts',(1.23636181296534,2.02466989643282,1.51332260638178));
#89266=CARTESIAN_POINT('Ctrl Pts',(1.28026129344819,1.99720031575992,1.50997648385924));
#89267=CARTESIAN_POINT('Ctrl Pts',(1.33623241912281,1.95957308264996,1.50554833987802));
#89268=CARTESIAN_POINT('Ctrl Pts',(1.34915320767797,1.95069970693627,1.50451451250084));
#89269=CARTESIAN_POINT('Ctrl Pts',(1.37010328722942,1.93600448926739,1.50281867490047));
#89270=CARTESIAN_POINT('Ctrl Pts',(1.37818583151874,1.9302591040672,1.50215959124514));
#89271=CARTESIAN_POINT('Ctrl Pts',(1.39372866385759,1.91906326993115,1.50088266602632));
#89272=CARTESIAN_POINT('Ctrl Pts',(1.40119361331933,1.91361957459484,1.50026509325537));
#89273=CARTESIAN_POINT('Ctrl Pts',(1.41832747823791,1.90097096861113,1.49883757703691));
#89274=CARTESIAN_POINT('Ctrl Pts',(1.42797356639931,1.89373571105629,1.49802645876315));
#89275=CARTESIAN_POINT('Ctrl Pts',(1.45883677398842,1.87021620795255,1.49540683272591));
#89276=CARTESIAN_POINT('Ctrl Pts',(1.47983310342644,1.85364702176488,1.49358713373708));
#89277=CARTESIAN_POINT('Ctrl Pts',(1.65962779041565,1.70676081712812,1.47766829828814));
#89278=CARTESIAN_POINT('Ctrl Pts',(1.80112210429016,1.55670177420236,1.46270789923479));
#89279=CARTESIAN_POINT('Ctrl Pts',(1.99182340855291,1.2931479144705,1.43896385083393));
#89280=CARTESIAN_POINT('Ctrl Pts',(2.05468641772583,1.19074043538516,1.43025887009652));
#89281=CARTESIAN_POINT('Ctrl Pts',(2.11583771251502,1.07173646831121,1.42101465012874));
#89282=CARTESIAN_POINT('Ctrl Pts',(2.12203441110386,1.05941411364828,1.4200674690894));
#89283=CARTESIAN_POINT('Ctrl Pts',(2.13103254406417,1.04112524826161,1.41867716107195));
#89284=CARTESIAN_POINT('Ctrl Pts',(2.13391703052254,1.03520026852153,1.4182291317618));
#89285=CARTESIAN_POINT('Ctrl Pts',(2.13897989649594,1.02468962931504,1.41743866117201));
#89286=CARTESIAN_POINT('Ctrl Pts',(2.14116828377551,1.02010892378651,1.4170956091862));
#89287=CARTESIAN_POINT('Ctrl Pts',(2.14588324857263,1.01015759706576,1.41635350112827));
#89288=CARTESIAN_POINT('Ctrl Pts',(2.1484043787382,1.00478451162321,1.41595478125966));
#89289=CARTESIAN_POINT('Ctrl Pts',(2.15526194882771,0.990025700850975,1.41486481842168));
#89290=CARTESIAN_POINT('Ctrl Pts',(2.15955729328035,0.980620856009067,1.41417604623083));
#89291=CARTESIAN_POINT('Ctrl Pts',(2.18107486487989,0.932680056254436,1.41069289709984));
#89292=CARTESIAN_POINT('Ctrl Pts',(2.19732891832583,0.893714618238608,1.40795284046196));
#89293=CARTESIAN_POINT('Ctrl Pts',(2.29901066351523,0.63038123066438,1.3899025210155));
#89294=CARTESIAN_POINT('Ctrl Pts',(2.35099110175549,0.394584735383903,1.3758382498165));
#89295=CARTESIAN_POINT('Ctrl Pts',(2.37092947700188,0.0901015995568576,
1.35652774570403));
#89296=CARTESIAN_POINT('Ctrl Pts',(2.37250804637827,0.0250845980826749,
1.35234969097489));
#89297=CARTESIAN_POINT('Ctrl Pts',(2.37112964660744,-0.0568168608126222,
1.3469792015065));
#89298=CARTESIAN_POINT('Ctrl Pts',(2.37066434685687,-0.0737189700969752,
1.34586518855255));
#89299=CARTESIAN_POINT('Ctrl Pts',(2.36962920091126,-0.100793227308003,
1.34407097712792));
#89300=CARTESIAN_POINT('Ctrl Pts',(2.36917445765771,-0.110969401803757,
1.3433943926132));
#89301=CARTESIAN_POINT('Ctrl Pts',(2.36818631869682,-0.130290163147333,
1.34210547398921));
#89302=CARTESIAN_POINT('Ctrl Pts',(2.36766547034975,-0.139435229124785,
1.34149354507675));
#89303=CARTESIAN_POINT('Ctrl Pts',(2.36635893524258,-0.160250628796372,
1.34009639716961));
#89304=CARTESIAN_POINT('Ctrl Pts',(2.3655398701337,-0.171918552513906,1.33931014376602));
#89305=CARTESIAN_POINT('Ctrl Pts',(2.36318695089678,-0.202225782935935,
1.33725960078347));
#89306=CARTESIAN_POINT('Ctrl Pts',(2.36151889844341,-0.220853547448027,
1.33599113472671));
#89307=CARTESIAN_POINT('Ctrl Pts',(2.3434832057252,-0.398577263587962,1.32380854990065));
#89308=CARTESIAN_POINT('Ctrl Pts',(2.31128595077761,-0.555622095833425,
1.31238418157411));
#89309=CARTESIAN_POINT('Ctrl Pts',(2.22568147377741,-0.82922891150625,1.29150236552574));
#89310=CARTESIAN_POINT('Ctrl Pts',(2.1781704149492,-0.947023880515805,1.28217169300353));
#89311=CARTESIAN_POINT('Ctrl Pts',(2.09775985342188,-1.10788681887603,1.2693257546231));
#89312=CARTESIAN_POINT('Ctrl Pts',(2.07246563938949,-1.1545115019453,1.26559126242188));
#89313=CARTESIAN_POINT('Ctrl Pts',(2.04022070762839,-1.20946751382153,1.2612089611619));
#89314=CARTESIAN_POINT('Ctrl Pts',(2.0347517882203,-1.21864571310415,1.26047775507982));
#89315=CARTESIAN_POINT('Ctrl Pts',(2.02614118893451,-1.23287685423037,1.25934543186852));
#89316=CARTESIAN_POINT('Ctrl Pts',(2.0230422877164,-1.23795531393218,1.25894164405185));
#89317=CARTESIAN_POINT('Ctrl Pts',(2.01723926112892,-1.24738529425189,1.25819248220313));
#89318=CARTESIAN_POINT('Ctrl Pts',(2.01454016861473,-1.25173967691547,1.25784680447665));
#89319=CARTESIAN_POINT('Ctrl Pts',(2.00833414714447,-1.2616796386663,1.25705825432367));
#89320=CARTESIAN_POINT('Ctrl Pts',(2.00481801740971,-1.26725935662109,1.25661599498647));
#89321=CARTESIAN_POINT('Ctrl Pts',(1.99553869541549,-1.28184935684369,1.25546037829484));
#89322=CARTESIAN_POINT('Ctrl Pts',(1.9897376692077,-1.2908355731592,1.25474943525184));
#89323=CARTESIAN_POINT('Ctrl Pts',(1.94833654444581,-1.35402668219223,1.24975357531829));
#89324=CARTESIAN_POINT('Ctrl Pts',(1.91058357049398,-1.40679625713357,1.24559968142671));
#89325=CARTESIAN_POINT('Ctrl Pts',(1.76734723253114,-1.59058344953836,1.23094002278382));
#89326=CARTESIAN_POINT('Ctrl Pts',(1.65016865711554,-1.71184752180714,1.22086508850055));
#89327=CARTESIAN_POINT('Ctrl Pts',(1.4461511635487,-1.88239169538279,1.20435936797207));
#89328=CARTESIAN_POINT('Ctrl Pts',(1.36736387498747,-1.94037736599113,1.19819308032981));
#89329=CARTESIAN_POINT('Ctrl Pts',(1.26407760998354,-2.00697267912134,1.19020050705911));
#89330=CARTESIAN_POINT('Ctrl Pts',(1.24270933223078,-2.02027349011524,1.18855192986346));
#89331=CARTESIAN_POINT('Ctrl Pts',(1.2109357731743,-2.03935630449554,1.18610573772215));
#89332=CARTESIAN_POINT('Ctrl Pts',(1.20069168525949,-2.04540437362625,1.18531784267427));
#89333=CARTESIAN_POINT('Ctrl Pts',(1.18245774542269,-2.05598543787751,1.18391658698031));
#89334=CARTESIAN_POINT('Ctrl Pts',(1.17448618471124,-2.06054959617885,1.18330437004523));
#89335=CARTESIAN_POINT('Ctrl Pts',(1.15770870808564,-2.07002663946857,1.18201656193481));
#89336=CARTESIAN_POINT('Ctrl Pts',(1.14889759114437,-2.07492989291094,1.18134064005603));
#89337=CARTESIAN_POINT('Ctrl Pts',(1.12564259485237,-2.08767740949748,1.17955759492487));
#89338=CARTESIAN_POINT('Ctrl Pts',(1.11114818601917,-2.09542785664514,1.17844716024833));
#89339=CARTESIAN_POINT('Ctrl Pts',(1.049360698672,-2.12764551254143,1.17371647218485));
#89340=CARTESIAN_POINT('Ctrl Pts',(1.00133464037768,-2.15066535028755,1.17004613274108));
#89341=CARTESIAN_POINT('Ctrl Pts',(0.743327201315127,-2.26381761734797,
1.15034802259969));
#89342=CARTESIAN_POINT('Ctrl Pts',(0.521925415414737,-2.32485798124351,
1.13335238799741));
#89343=CARTESIAN_POINT('Ctrl Pts',(0.230791534347974,-2.36138916194391,
1.11226318756905));
#89344=CARTESIAN_POINT('Ctrl Pts',(0.165981409199571,-2.36682813887218,
1.10765836584278));
#89345=CARTESIAN_POINT('Ctrl Pts',(0.0897706055122537,-2.37007724721254,
1.10240729187704));
#89346=CARTESIAN_POINT('Ctrl Pts',(0.078514193344609,-2.37047684095977,
1.10163590066085));
#89347=CARTESIAN_POINT('Ctrl Pts',(0.0611824109264023,-2.37096851141382,
1.10045506284741));
#89348=CARTESIAN_POINT('Ctrl Pts',(0.0551090122691025,-2.37111745141414,
1.10004257632034));
#89349=CARTESIAN_POINT('Ctrl Pts',(0.0439220309175732,-2.37134878741136,
1.09928527165299));
#89350=CARTESIAN_POINT('Ctrl Pts',(0.0388087791932072,-2.37143798062947,
1.09894009233226));
#89351=CARTESIAN_POINT('Ctrl Pts',(0.0272613420224132,-2.37160204999804,
1.09816270906982));
#89352=CARTESIAN_POINT('Ctrl Pts',(0.0208271249187241,-2.37166728224456,
1.0977310472707));
#89353=CARTESIAN_POINT('Ctrl Pts',(0.00181701753952309,-2.37178264448879,
1.09645989411048));
#89354=CARTESIAN_POINT('Ctrl Pts',(-0.0107593420243934,-2.37175893970204,
1.09562438529971));
#89355=CARTESIAN_POINT('Ctrl Pts',(-0.121277569906074,-2.37067151636503,
1.08832521448204));
#89356=CARTESIAN_POINT('Ctrl Pts',(-0.219079821903782,-2.3636414361208,
1.08216168954137));
#89357=CARTESIAN_POINT('Ctrl Pts',(-0.483043320752052,-2.32813548884667,
1.06566907232984));
#89358=CARTESIAN_POINT('Ctrl Pts',(-0.647038750826236,-2.28798749469019,
1.05554603311277));
#89359=CARTESIAN_POINT('Ctrl Pts',(-0.876155866956401,-2.20526814717473,
1.04021323313317));
#89360=CARTESIAN_POINT('Ctrl Pts',(-0.945647848826268,-2.1763742870372,
1.03539900093213));
#89361=CARTESIAN_POINT('Ctrl Pts',(-1.02963222535785,-2.13667224048885,
1.02931351886025));
#89362=CARTESIAN_POINT('Ctrl Pts',(-1.0455343238144,-2.12893605642434,1.02814913830386));
#89363=CARTESIAN_POINT('Ctrl Pts',(-1.0706132522976,-2.11638670019131,1.02629277940939));
#89364=CARTESIAN_POINT('Ctrl Pts',(-1.07984782311123,-2.11168986213796,
1.0256048711188));
#89365=CARTESIAN_POINT('Ctrl Pts',(-1.09716813447094,-2.1027371767555,1.02430625645085));
#89366=CARTESIAN_POINT('Ctrl Pts',(-1.1052606555503,-2.09849480081972,1.02369603413449));
#89367=CARTESIAN_POINT('Ctrl Pts',(-1.12341901413624,-2.08884139642988,
1.02231884017649));
#89368=CARTESIAN_POINT('Ctrl Pts',(-1.13347060393941,-2.0834041957356,1.02155094916313));
#89369=CARTESIAN_POINT('Ctrl Pts',(-1.15907935536975,-2.0693114911521,1.01958012934961));
#89370=CARTESIAN_POINT('Ctrl Pts',(-1.17457883687511,-2.06055320853583,
1.01837354805827));
#89371=CARTESIAN_POINT('Ctrl Pts',(-1.27414616094219,-2.00280234377696,
1.01053150551717));
#89372=CARTESIAN_POINT('Ctrl Pts',(-1.35521890737835,-1.9488567920097,1.0037167884491));
#89373=CARTESIAN_POINT('Ctrl Pts',(-1.57855936091099,-1.77955863673795,
0.983669897191608));
#89374=CARTESIAN_POINT('Ctrl Pts',(-1.71108144236095,-1.65253458391559,
0.970092985407875));
#89375=CARTESIAN_POINT('Ctrl Pts',(-1.86630449524888,-1.46484758807362,
0.952624710264361));
#89376=CARTESIAN_POINT('Ctrl Pts',(-1.90312816625077,-1.41667765377752,
0.948340471879313));
#89377=CARTESIAN_POINT('Ctrl Pts',(-1.94445010363024,-1.3580995539869,0.94340711967876));
#89378=CARTESIAN_POINT('Ctrl Pts',(-1.95076783510353,-1.34900906952627,
0.94264913413746));
#89379=CARTESIAN_POINT('Ctrl Pts',(-1.96043036731073,-1.33489596632093,
0.941484449330477));
#89380=CARTESIAN_POINT('Ctrl Pts',(-1.96381993225245,-1.32990441074984,
0.941074835692234));
#89381=CARTESIAN_POINT('Ctrl Pts',(-1.97004587104733,-1.32066023512288,
0.9403205921403));
#89382=CARTESIAN_POINT('Ctrl Pts',(-1.97288753236756,-1.31641140084742,
0.939975617425657));
#89383=CARTESIAN_POINT('Ctrl Pts',(-1.97929720234882,-1.30676032981454,
0.939195822797598));
#89384=CARTESIAN_POINT('Ctrl Pts',(-1.98285683729383,-1.30135265786273,
0.938761564612629));
#89385=CARTESIAN_POINT('Ctrl Pts',(-1.992024799152,-1.28730006092161,0.937639809005604));
#89386=CARTESIAN_POINT('Ctrl Pts',(-1.99759908221054,-1.27863292762991,
0.936954507167876));
#89387=CARTESIAN_POINT('Ctrl Pts',(-2.0335349882673,-1.22194961132857,0.93251322097085));
#89388=CARTESIAN_POINT('Ctrl Pts',(-2.06222240129705,-1.1728876292401,0.928857675183559));
#89389=CARTESIAN_POINT('Ctrl Pts',(-2.09539630956863,-1.11116514935026,
0.924426345993814));
#89390=CARTESIAN_POINT('Ctrl Pts',(-2.10157234166695,-1.09943957850797,
0.923591766862014));
#89391=CARTESIAN_POINT('Ctrl Pts',(-2.15892055163134,-0.988311423760099,
0.915744570409303));
#89392=CARTESIAN_POINT('Ctrl Pts',(-2.20310484075919,-0.885454186833194,
0.908944597628195));
#89393=CARTESIAN_POINT('Ctrl Pts',(-2.29138478011646,-0.63190122933475,
0.892478253612548));
#89394=CARTESIAN_POINT('Ctrl Pts',(-2.32810564990069,-0.479225872352841,
0.882776773069896));
#89395=CARTESIAN_POINT('Ctrl Pts',(-2.35206623302021,-0.305504894988578,
0.871326184600345));
#89396=CARTESIAN_POINT('Ctrl Pts',(-2.3544052013262,-0.28692319567133,0.870096731533758));
#89397=CARTESIAN_POINT('Ctrl Pts',(-2.35784734632995,-0.256692082399001,
0.868088023005161));
#89398=CARTESIAN_POINT('Ctrl Pts',(-2.35908483082418,-0.245058536702408,
0.867313000083297));
#89399=CARTESIAN_POINT('Ctrl Pts',(-2.36113700084134,-0.224307620635848,
0.865926754975572));
#89400=CARTESIAN_POINT('Ctrl Pts',(-2.36198507628958,-0.21519372843047,
0.865316597329193));
#89401=CARTESIAN_POINT('Ctrl Pts',(-2.36366401397413,-0.195943669444697,
0.864024967808889));
#89402=CARTESIAN_POINT('Ctrl Pts',(-2.36448247638349,-0.185806635575639,
0.86334311835523));
#89403=CARTESIAN_POINT('Ctrl Pts',(-2.36648445926961,-0.158850969118815,
0.861525369690516));
#89404=CARTESIAN_POINT('Ctrl Pts',(-2.36755386077973,-0.142024705494687,
0.860385911937931));
#89405=CARTESIAN_POINT('Ctrl Pts',(-2.37185064482659,-0.0607339844925643,
0.854856836730944));
#89406=CARTESIAN_POINT('Ctrl Pts',(-2.37262471810026,0.00382708308958538,
0.850391297016508));
#89407=CARTESIAN_POINT('Ctrl Pts',(-2.36975766244938,0.103295683469262,
0.843391208767397));
#89408=CARTESIAN_POINT('Ctrl Pts',(-2.36797705995664,0.138218398695283,
0.840910877802362));
#89409=CARTESIAN_POINT('Ctrl Pts',(-2.36542648444351,0.173076888096584,
0.838413605944556));
#89410=CARTESIAN_POINT('',(-2.37174952154217,0.00150650738259589,0.651410108094974));
#89411=CARTESIAN_POINT('Ctrl Pts',(-2.36542649454111,0.173076750093528,
0.639821592488593));
#89412=CARTESIAN_POINT('Ctrl Pts',(-2.36960119137977,0.116021492795841,
0.643684431024054));
#89413=CARTESIAN_POINT('Ctrl Pts',(-2.37171313261937,0.0587949158190506,
0.647547269559515));
#89414=CARTESIAN_POINT('Ctrl Pts',(-2.37174952154217,0.00150650738259589,
0.651410108094975));
#89415=CARTESIAN_POINT('Ctrl Pts',(-2.37174945202138,0.00161224572303678,
0.653084671769645));
#89416=CARTESIAN_POINT('Ctrl Pts',(-2.37190019934435,-0.220149781945233,
0.667087663185996));
#89417=CARTESIAN_POINT('Ctrl Pts',(-2.34095033112989,-0.440855449603671,
0.680174251846229));
#89418=CARTESIAN_POINT('Ctrl Pts',(-2.26803542871565,-0.695000945652463,
0.696904420974021));
#89419=CARTESIAN_POINT('Ctrl Pts',(-2.25519376496381,-0.735602998464327,
0.699626122806353));
#89420=CARTESIAN_POINT('Ctrl Pts',(-2.23126906427678,-0.804717684726376,
0.704359803829371));
#89421=CARTESIAN_POINT('Ctrl Pts',(-2.22071433456381,-0.833402599367388,
0.706354868725316));
#89422=CARTESIAN_POINT('Ctrl Pts',(-2.20491777535979,-0.873900622561888,
0.709218881062143));
#89423=CARTESIAN_POINT('Ctrl Pts',(-2.20012887739718,-0.885888032356933,
0.710072601531635));
#89424=CARTESIAN_POINT('Ctrl Pts',(-2.19168555197582,-0.906532287564808,
0.711553480751627));
#89425=CARTESIAN_POINT('Ctrl Pts',(-2.18807705833341,-0.915207697490257,
0.712179067489534));
#89426=CARTESIAN_POINT('Ctrl Pts',(-2.1810549556744,-0.931811056687275,
0.713382739602757));
#89427=CARTESIAN_POINT('Ctrl Pts',(-2.17764942411063,-0.93974227704877,
0.713960540291353));
#89428=CARTESIAN_POINT('Ctrl Pts',(-2.16953133285275,-0.958367585308325,
0.715324167136951));
#89429=CARTESIAN_POINT('Ctrl Pts',(-2.164782911702,-0.969045700377584,0.716111218095771));
#89430=CARTESIAN_POINT('Ctrl Pts',(-2.14795354818637,-1.00615004130597,
0.718864773368497));
#89431=CARTESIAN_POINT('Ctrl Pts',(-2.13546647825305,-1.03238807584507,
0.720845254770805));
#89432=CARTESIAN_POINT('Ctrl Pts',(-2.04878050945216,-1.2062287334226,0.734197410158997));
#89433=CARTESIAN_POINT('Ctrl Pts',(-1.95982950152917,-1.34593395505048,
0.74609990990669));
#89434=CARTESIAN_POINT('Ctrl Pts',(-1.79132296328342,-1.55805861808975,
0.765890965173791));
#89435=CARTESIAN_POINT('Ctrl Pts',(-1.72006701784822,-1.63638501540437,
0.77364993904509));
#89436=CARTESIAN_POINT('Ctrl Pts',(-1.61682357753721,-1.73565028426971,
0.783902046849395));
#89437=CARTESIAN_POINT('Ctrl Pts',(-1.58921656430365,-1.76096321164395,
0.786557065683813));
#89438=CARTESIAN_POINT('Ctrl Pts',(-1.54897649959918,-1.79614191254435,
0.790292824397852));
#89439=CARTESIAN_POINT('Ctrl Pts',(-1.5368262808448,-1.80654891481901,0.791404002870828));
#89440=CARTESIAN_POINT('Ctrl Pts',(-1.51783483534004,-1.82248533867831,
0.793113786790275));
#89441=CARTESIAN_POINT('Ctrl Pts',(-1.51106684033085,-1.82810076502783,
0.793717874523316));
#89442=CARTESIAN_POINT('Ctrl Pts',(-1.49850413807854,-1.83840664264008,
0.794829312550551));
#89443=CARTESIAN_POINT('Ctrl Pts',(-1.49271827740694,-1.84310764299804,
0.795337375969917));
#89444=CARTESIAN_POINT('Ctrl Pts',(-1.48280103164723,-1.85108805379323,
0.796201584216745));
#89445=CARTESIAN_POINT('Ctrl Pts',(-1.4786807259983,-1.85438108143118,0.796558696021009));
#89446=CARTESIAN_POINT('Ctrl Pts',(-1.47075912240844,-1.86066898825736,
0.797241513427998));
#89447=CARTESIAN_POINT('Ctrl Pts',(-1.46695963052574,-1.86366599032622,
0.797567379194729));
#89448=CARTESIAN_POINT('Ctrl Pts',(-1.45700536702365,-1.87146851321087,
0.798416919920881));
#89449=CARTESIAN_POINT('Ctrl Pts',(-1.45083592425455,-1.87625535594329,
0.798939280585641));
#89450=CARTESIAN_POINT('Ctrl Pts',(-1.42945187967792,-1.89267859590599,
0.800735954687388));
#89451=CARTESIAN_POINT('Ctrl Pts',(-1.41411954130577,-1.90416147541205,
0.802000054202724));
#89452=CARTESIAN_POINT('Ctrl Pts',(-1.28904322366006,-1.99549102025476,
0.812134204340709));
#89453=CARTESIAN_POINT('Ctrl Pts',(-1.17275377297891,-2.06598059179946,
0.820469858355212));
#89454=CARTESIAN_POINT('Ctrl Pts',(-0.935135019537183,-2.1834474356548,
0.836719936389383));
#89455=CARTESIAN_POINT('Ctrl Pts',(-0.81472756750881,-2.23117374801227,
0.844611975351883));
#89456=CARTESIAN_POINT('Ctrl Pts',(-0.626287275787845,-2.28856798794186,
0.857060353877867));
#89457=CARTESIAN_POINT('Ctrl Pts',(-0.560730850375216,-2.30550618002345,
0.861405122693557));
#89458=CARTESIAN_POINT('Ctrl Pts',(-0.477612661246062,-2.32322704923897,
0.86697526467404));
#89459=CARTESIAN_POINT('Ctrl Pts',(-0.460642315188279,-2.32665132917977,
0.868115618744511));
#89460=CARTESIAN_POINT('Ctrl Pts',(-0.433432762114011,-2.33183232493086,
0.869949616303167));
#89461=CARTESIAN_POINT('Ctrl Pts',(-0.42321664310937,-2.33370812614228,
0.870639466603019));
#89462=CARTESIAN_POINT('Ctrl Pts',(-0.40381592610359,-2.33713874865389,
0.871952040370887));
#89463=CARTESIAN_POINT('Ctrl Pts',(-0.394633821963965,-2.33870668852129,
0.872574334551565));
#89464=CARTESIAN_POINT('Ctrl Pts',(-0.373738321697926,-2.34214825347425,
0.873993018764612));
#89465=CARTESIAN_POINT('Ctrl Pts',(-0.362019703088027,-2.34398816124571,
0.874790458893769));
#89466=CARTESIAN_POINT('Ctrl Pts',(-0.331587823052923,-2.34853253566632,
0.876866245566565));
#89467=CARTESIAN_POINT('Ctrl Pts',(-0.312855452614087,-2.35110122819033,
0.8781488246241));
#89468=CARTESIAN_POINT('Ctrl Pts',(-0.14081865159366,-2.37259955144097,
0.889974655290919));
#89469=CARTESIAN_POINT('Ctrl Pts',(0.01393223192626,-2.37673044150717,0.900989036229827));
#89470=CARTESIAN_POINT('Ctrl Pts',(0.278971995363583,-2.35791408269947,
0.92031441702774));
#89471=CARTESIAN_POINT('Ctrl Pts',(0.389293736889757,-2.34222868082347,
0.928487732465121));
#89472=CARTESIAN_POINT('Ctrl Pts',(0.566921254213198,-2.30407296062881,
0.941572026516472));
#89473=CARTESIAN_POINT('Ctrl Pts',(0.635050844897255,-2.28623368806033,
0.946569421408522));
#89474=CARTESIAN_POINT('Ctrl Pts',(0.713393317430371,-2.26194675144873,
0.952217861868752));
#89475=CARTESIAN_POINT('Ctrl Pts',(0.724468899589216,-2.25842377757426,
0.953014056132335));
#89476=CARTESIAN_POINT('Ctrl Pts',(0.741431981247928,-2.25289044805436,
0.954229401872169));
#89477=CARTESIAN_POINT('Ctrl Pts',(0.747338019425586,-2.25093816901379,
0.954651784849289));
#89478=CARTESIAN_POINT('Ctrl Pts',(0.758167016164119,-2.24731125486395,
0.955424751406431));
#89479=CARTESIAN_POINT('Ctrl Pts',(0.763092151157998,-2.24564366513496,
0.955775727035633));
#89480=CARTESIAN_POINT('Ctrl Pts',(0.77416779464427,-2.24185294388493,0.956563714468716));
#89481=CARTESIAN_POINT('Ctrl Pts',(0.780315064556629,-2.23972069661643,
0.95700018466537));
#89482=CARTESIAN_POINT('Ctrl Pts',(0.798386795140658,-2.233368886105,0.958280932031745));
#89483=CARTESIAN_POINT('Ctrl Pts',(0.810286598367615,-2.2290791152583,0.959121205456315));
#89484=CARTESIAN_POINT('Ctrl Pts',(0.909203606115786,-2.1925236199448,0.96608484339345));
#89485=CARTESIAN_POINT('Ctrl Pts',(0.994303796470286,-2.15526690220199,
0.971940235128547));
#89486=CARTESIAN_POINT('Ctrl Pts',(1.24714665948801,-2.02639802979163,0.989548746400151));
#89487=CARTESIAN_POINT('Ctrl Pts',(1.40618086426479,-1.91945816567038,1.00098286634381));
#89488=CARTESIAN_POINT('Ctrl Pts',(1.58051329611421,-1.76882192714282,1.01560935133936));
#89489=CARTESIAN_POINT('Ctrl Pts',(1.60970406700244,-1.74229900959039,1.018137045335));
#89490=CARTESIAN_POINT('Ctrl Pts',(1.65908363214104,-1.69513188391543,1.02256446757721));
#89491=CARTESIAN_POINT('Ctrl Pts',(1.67958218262384,-1.67482362527024,1.02445031393656));
#89492=CARTESIAN_POINT('Ctrl Pts',(1.70854439430026,-1.64506375809287,1.02718815613796));
#89493=CARTESIAN_POINT('Ctrl Pts',(1.71731123647221,-1.63590978420207,1.02802691111613));
#89494=CARTESIAN_POINT('Ctrl Pts',(1.73245994703098,-1.61983616266004,1.02949409910292));
#89495=CARTESIAN_POINT('Ctrl Pts',(1.73887483423045,-1.61294791249619,1.03012109510505));
#89496=CARTESIAN_POINT('Ctrl Pts',(1.75119421061471,-1.59956056399419,1.03133639233605));
#89497=CARTESIAN_POINT('Ctrl Pts',(1.75710395476042,-1.59306649257013,1.0319244556718));
#89498=CARTESIAN_POINT('Ctrl Pts',(1.77107018243296,-1.57754709383758,1.03332642563169));
#89499=CARTESIAN_POINT('Ctrl Pts',(1.779093872831,-1.56849271805066,1.03414168943855));
#89500=CARTESIAN_POINT('Ctrl Pts',(1.80749742536801,-1.53594222495514,1.03706338754893));
#89501=CARTESIAN_POINT('Ctrl Pts',(1.82748317151552,-1.51210798508983,1.03918590478852));
#89502=CARTESIAN_POINT('Ctrl Pts',(2.00726799425765,-1.28893171373883,1.05891737124993));
#89503=CARTESIAN_POINT('Ctrl Pts',(2.13432091598966,-1.06540269509682,1.07791407339119));
#89504=CARTESIAN_POINT('Ctrl Pts',(2.24652140572883,-0.763414152816783,
1.10108988173988));
#89505=CARTESIAN_POINT('Ctrl Pts',(2.26713165456713,-0.699839653650499,
1.10582608471784));
#89506=CARTESIAN_POINT('Ctrl Pts',(2.28809913041615,-0.624444929267538,
1.11121472490217));
#89507=CARTESIAN_POINT('Ctrl Pts',(2.29108641721762,-0.613393953721566,
1.11199889659272));
#89508=CARTESIAN_POINT('Ctrl Pts',(2.29555942119889,-0.596358130423177,
1.11319859336554));
#89509=CARTESIAN_POINT('Ctrl Pts',(2.29710195584187,-0.590388586143888,
1.11361725757825));
#89510=CARTESIAN_POINT('Ctrl Pts',(2.29989826776665,-0.579390093938672,
1.11438536481693));
#89511=CARTESIAN_POINT('Ctrl Pts',(2.30115883630344,-0.574363068285223,
1.11473518284833));
#89512=CARTESIAN_POINT('Ctrl Pts',(2.30396753918112,-0.563004549516923,
1.11552278262396));
#89513=CARTESIAN_POINT('Ctrl Pts',(2.30550605654453,-0.556670791572006,
1.11596000904311));
#89514=CARTESIAN_POINT('Ctrl Pts',(2.30940601757654,-0.54032192621445,1.11708374140538));
#89515=CARTESIAN_POINT('Ctrl Pts',(2.31172846324525,-0.530297520000732,
1.11776808399291));
#89516=CARTESIAN_POINT('Ctrl Pts',(2.32597930071005,-0.466913146234204,
1.12206752539788));
#89517=CARTESIAN_POINT('Ctrl Pts',(2.33612582332861,-0.413164409637929,
1.12558995646478));
#89518=CARTESIAN_POINT('Ctrl Pts',(2.37566296653211,-0.155049719209109,
1.14212772190332));
#89519=CARTESIAN_POINT('Ctrl Pts',(2.38014721162845,0.052225095872193,1.1543618853275));
#89520=CARTESIAN_POINT('Ctrl Pts',(2.34886528777714,0.338677239461878,1.17243915997578));
#89521=CARTESIAN_POINT('Ctrl Pts',(2.33580962194246,0.419358512665458,1.17765242157147));
#89522=CARTESIAN_POINT('Ctrl Pts',(2.31477686546005,0.517048826088778,1.18419451420769));
#89523=CARTESIAN_POINT('Ctrl Pts',(2.31072803220957,0.534852648535692,1.18539614662353));
#89524=CARTESIAN_POINT('Ctrl Pts',(2.30401136974957,0.562886663600749,1.18730383391873));
#89525=CARTESIAN_POINT('Ctrl Pts',(2.30147994542172,0.573149057969203,1.18800549655524));
#89526=CARTESIAN_POINT('Ctrl Pts',(2.29660534685727,0.592357545578668,1.18932520790242));
#89527=CARTESIAN_POINT('Ctrl Pts',(2.29427827567475,0.601307550761481,1.18994272527489));
#89528=CARTESIAN_POINT('Ctrl Pts',(2.28894762795982,0.621327925757816,1.19133002635045));
#89529=CARTESIAN_POINT('Ctrl Pts',(2.2859159797053,0.632390512696399,1.19210070835192));
#89530=CARTESIAN_POINT('Ctrl Pts',(2.27800522657661,0.660456792871386,1.19406663020587));
#89531=CARTESIAN_POINT('Ctrl Pts',(2.27301598474208,0.677428439775392,1.19526542502308));
#89532=CARTESIAN_POINT('Ctrl Pts',(2.24118225912961,0.781402685033221,1.20267280526242));
#89533=CARTESIAN_POINT('Ctrl Pts',(2.20953944962569,0.86684468595643,1.20903741614421));
#89534=CARTESIAN_POINT('Ctrl Pts',(2.08956404200462,1.14120970025995,1.23040210042115));
#89535=CARTESIAN_POINT('Ctrl Pts',(1.98126506448331,1.3203083178078,1.24594997852642));
#89536=CARTESIAN_POINT('Ctrl Pts',(1.83292444535077,1.50546297717635,1.26279472511943));
#89537=CARTESIAN_POINT('Ctrl Pts',(1.81447101068959,1.52765372860108,1.26482590178007));
#89538=CARTESIAN_POINT('Ctrl Pts',(1.78284419706529,1.56430394082163,1.26819413674651));
#89539=CARTESIAN_POINT('Ctrl Pts',(1.76988906733138,1.57894680160847,1.26954360469841));
#89540=CARTESIAN_POINT('Ctrl Pts',(1.75161927047042,1.59908924169789,1.27140317389021));
#89541=CARTESIAN_POINT('Ctrl Pts',(1.74645728007169,1.60472534864904,1.27192386700856));
#89542=CARTESIAN_POINT('Ctrl Pts',(1.73764415443683,1.61425504260885,1.27280473822091));
#89543=CARTESIAN_POINT('Ctrl Pts',(1.73400698250907,1.61816140631649,1.27316595449202));
#89544=CARTESIAN_POINT('Ctrl Pts',(1.72699344772756,1.6256432191736,1.27385799371603));
#89545=CARTESIAN_POINT('Ctrl Pts',(1.72361913166181,1.62922046839549,1.27418897268696));
#89546=CARTESIAN_POINT('Ctrl Pts',(1.71550618610293,1.63776791525224,1.2749801205559));
#89547=CARTESIAN_POINT('Ctrl Pts',(1.7107570146786,1.64272811459033,1.27543948715198));
#89548=CARTESIAN_POINT('Ctrl Pts',(1.69350193061568,1.66059393607221,1.27709528267932));
#89549=CARTESIAN_POINT('Ctrl Pts',(1.68087059228491,1.67337835221554,1.27828247997792));
#89550=CARTESIAN_POINT('Ctrl Pts',(1.55151292539915,1.8013608426658,1.29020707135639));
#89551=CARTESIAN_POINT('Ctrl Pts',(1.42326367688259,1.90431886829479,1.30015100712979));
#89552=CARTESIAN_POINT('Ctrl Pts',(1.15016341902545,2.08043646260925,1.3200744672154));
#89553=CARTESIAN_POINT('Ctrl Pts',(1.00642616440537,2.15364530483014,1.33000947438913));
#89554=CARTESIAN_POINT('Ctrl Pts',(0.835369327703635,2.21987940513822,1.34196775509124));
#89555=CARTESIAN_POINT('Ctrl Pts',(0.814227880787186,2.22772067092529,1.34344717641525));
#89556=CARTESIAN_POINT('Ctrl Pts',(0.782154198812306,2.23909910039529,1.34569528351832));
#89557=CARTESIAN_POINT('Ctrl Pts',(0.771302379492129,2.24286036204504,1.34645653451253));
#89558=CARTESIAN_POINT('Ctrl Pts',(0.7516516964297,2.24951184848982,1.34783634828496));
#89559=CARTESIAN_POINT('Ctrl Pts',(0.742862356425267,2.25242965361046,1.34845398598422));
#89560=CARTESIAN_POINT('Ctrl Pts',(0.723988858100967,2.25857262125769,1.34978137707116));
#89561=CARTESIAN_POINT('Ctrl Pts',(0.713899773765236,2.26178187694073,1.35049163825368));
#89562=CARTESIAN_POINT('Ctrl Pts',(0.686763633164498,2.27021400999783,1.35240401233554));
#89563=CARTESIAN_POINT('Ctrl Pts',(0.669678889897915,2.2753123067269,1.35361016286553));
#89564=CARTESIAN_POINT('Ctrl Pts',(0.587382568876115,2.2988633654662,1.35943155263109));
#89565=CARTESIAN_POINT('Ctrl Pts',(0.521463526818901,2.31470629694618,1.36413005784406));
#89566=CARTESIAN_POINT('Ctrl Pts',(0.267800401144007,2.36428609419862,1.38235710521474));
#89567=CARTESIAN_POINT('Ctrl Pts',(0.0769230484837968,2.37815697464309,
1.39644633071298));
#89568=CARTESIAN_POINT('Ctrl Pts',(-0.170214055682804,2.36631516694071,
1.41435916701414));
#89569=CARTESIAN_POINT('Ctrl Pts',(-0.226802027086609,2.36156347236873,
1.41843164725273));
#89570=CARTESIAN_POINT('Ctrl Pts',(-0.304292437948064,2.35224506487116,
1.42392533183133));
#89571=CARTESIAN_POINT('Ctrl Pts',(-0.325382024273615,2.34942063989615,
1.42541190361973));
#89572=CARTESIAN_POINT('Ctrl Pts',(-0.361760298662337,2.3440494110431,1.42795816395798));
#89573=CARTESIAN_POINT('Ctrl Pts',(-0.377067004165928,2.34163589429986,
1.42902400952776));
#89574=CARTESIAN_POINT('Ctrl Pts',(-0.399222753271042,2.33791955104351,
1.43055768759882));
#89575=CARTESIAN_POINT('Ctrl Pts',(-0.406091044918971,2.33673633520323,
1.43103185873806));
#89576=CARTESIAN_POINT('Ctrl Pts',(-0.418105702324698,2.33461197044672,
1.4318589811803));
#89577=CARTESIAN_POINT('Ctrl Pts',(-0.423254303472963,2.33368404623458,
1.43221266720454));
#89578=CARTESIAN_POINT('Ctrl Pts',(-0.434180675578784,2.33167745354801,
1.43296161530433));
#89579=CARTESIAN_POINT('Ctrl Pts',(-0.439957525235858,2.33059434143513,
1.43335662325605));
#89580=CARTESIAN_POINT('Ctrl Pts',(-0.455664815203087,2.32758886946662,
1.43442816983229));
#89581=CARTESIAN_POINT('Ctrl Pts',(-0.465587223293734,2.32562441416782,
1.4351023696552));
#89582=CARTESIAN_POINT('Ctrl Pts',(-0.512023495830056,2.31612177139858,
1.43824619974959));
#89583=CARTESIAN_POINT('Ctrl Pts',(-0.548371213900686,2.3077862799206,1.44067397929807));
#89584=CARTESIAN_POINT('Ctrl Pts',(-0.820004876912631,2.23871260792112,
1.4586716819596));
#89585=CARTESIAN_POINT('Ctrl Pts',(-1.04491825131775,2.14299262869263,1.47288826058656));
#89586=CARTESIAN_POINT('Ctrl Pts',(-1.30821181642694,1.97945826629906,1.49248231528067));
#89587=CARTESIAN_POINT('Ctrl Pts',(-1.36351544968512,1.94177689001353,1.49677766855442));
#89588=CARTESIAN_POINT('Ctrl Pts',(-1.43095670604976,1.89152252922257,1.50229038128703));
#89589=CARTESIAN_POINT('Ctrl Pts',(-1.44465154991784,1.88108384886257,1.50342465932356));
#89590=CARTESIAN_POINT('Ctrl Pts',(-1.46639317180412,1.86413417801869,1.50525003912168));
#89591=CARTESIAN_POINT('Ctrl Pts',(-1.47451327519083,1.85771789124956,1.5059373877947));
#89592=CARTESIAN_POINT('Ctrl Pts',(-1.4898439540602,1.84544016425115,1.50724592915649));
#89593=CARTESIAN_POINT('Ctrl Pts',(-1.49706260214114,1.83958907593791,1.50786669876694));
#89594=CARTESIAN_POINT('Ctrl Pts',(-1.51340658001697,1.82618152318832,1.50928289069435));
#89595=CARTESIAN_POINT('Ctrl Pts',(-1.52250998605765,1.81859884679442,1.51007936756823));
#89596=CARTESIAN_POINT('Ctrl Pts',(-1.54599657544538,1.79873575837169,1.51215453977213));
#89597=CARTESIAN_POINT('Ctrl Pts',(-1.56029012488012,1.7863511496179,1.51343749040584));
#89598=CARTESIAN_POINT('Ctrl Pts',(-1.69096482546408,1.67036345598563,1.52535607241086));
#89599=CARTESIAN_POINT('Ctrl Pts',(-1.79699694451576,1.55571872582698,1.5364732521844));
#89600=CARTESIAN_POINT('Ctrl Pts',(-1.95912979380173,1.34154624215709,1.55602500011903));
#89601=CARTESIAN_POINT('Ctrl Pts',(-2.02074112783512,1.24681268843549,1.56432013105911));
#89602=CARTESIAN_POINT('Ctrl Pts',(-2.10880660932832,1.08761354906334,1.57742079317095));
#89603=CARTESIAN_POINT('Ctrl Pts',(-2.13958722590301,1.02573734574186,1.5823232036035));
#89604=CARTESIAN_POINT('Ctrl Pts',(-2.17230802171485,0.952055160998176,
1.58787530815811));
#89605=CARTESIAN_POINT('Ctrl Pts',(-2.17691365760954,0.941476559308161,
1.58866571460658));
#89606=CARTESIAN_POINT('Ctrl Pts',(-2.18386957156493,0.925175665865188,
1.58987293352133));
#89607=CARTESIAN_POINT('Ctrl Pts',(-2.1862748838328,0.919477271531227,1.59029294423025));
#89608=CARTESIAN_POINT('Ctrl Pts',(-2.19065525371491,0.908985422420414,
1.59106250204987));
#89609=CARTESIAN_POINT('Ctrl Pts',(-2.19263688087375,0.904194917318299,
1.59141243187071));
#89610=CARTESIAN_POINT('Ctrl Pts',(-2.19706796319036,0.893382720664257,
1.59219899774017));
#89611=CARTESIAN_POINT('Ctrl Pts',(-2.19950837527459,0.887357442133621,
1.59263508730703));
#89612=CARTESIAN_POINT('Ctrl Pts',(-2.20662459883719,0.869578036253152,
1.59391553795137));
#89613=CARTESIAN_POINT('Ctrl Pts',(-2.21123127437524,0.857796217109768,
1.59475588428019));
#89614=CARTESIAN_POINT('Ctrl Pts',(-2.24963888490191,0.757200884133428,
1.60186625241047));
#89615=CARTESIAN_POINT('Ctrl Pts',(-2.27817269073683,0.666454957687184,
1.60785450222644));
#89616=CARTESIAN_POINT('Ctrl Pts',(-2.33405985860222,0.442491303857375,
1.62216303430729));
#89617=CARTESIAN_POINT('Ctrl Pts',(-2.35553379466809,0.308279583528868,
1.63036049649394));
#89618=CARTESIAN_POINT('Ctrl Pts',(-2.36542650134105,0.173076657159373,
1.6387748639739));
#89619=CARTESIAN_POINT('Origin',(0.,0.,-1.84858989190503));
#89620=CARTESIAN_POINT('',(-2.36542649402054,0.173076757208175,2.83502806412758));
#89621=CARTESIAN_POINT('',(-2.36542650247982,0.173076641595803,2.63790316127816));
#89622=CARTESIAN_POINT('',(-2.36542649454111,0.173076750093529,-1.84858989190503));
#89623=CARTESIAN_POINT('',(-2.37174916735844,-0.00198736875130605,1.84947704601095));
#89624=CARTESIAN_POINT('Ctrl Pts',(-2.36542649402054,0.173076757208175,
2.83502806412758));
#89625=CARTESIAN_POINT('Ctrl Pts',(-2.35062081331563,0.375424836559319,
2.82209801839282));
#89626=CARTESIAN_POINT('Ctrl Pts',(-2.30990985923019,0.57508075576675,2.81006493442228));
#89627=CARTESIAN_POINT('Ctrl Pts',(-2.21435099249438,0.854630846330757,
2.7916303956933));
#89628=CARTESIAN_POINT('Ctrl Pts',(-2.17936365792477,0.940273970300902,
2.78575936514911));
#89629=CARTESIAN_POINT('Ctrl Pts',(-2.13187396907725,1.03952936624924,2.77856555361437));
#89630=CARTESIAN_POINT('Ctrl Pts',(-2.12410018256202,1.05532284642277,2.77740884225984));
#89631=CARTESIAN_POINT('Ctrl Pts',(-2.11101960895563,1.08116761947343,2.77549531335063));
#89632=CARTESIAN_POINT('Ctrl Pts',(-2.10581499890869,1.09127008276156,2.77474207227732));
#89633=CARTESIAN_POINT('Ctrl Pts',(-2.09629936250158,1.10941893269071,2.77337917708499));
#89634=CARTESIAN_POINT('Ctrl Pts',(-2.09201407875898,1.11747862426932,2.77277044258954));
#89635=CARTESIAN_POINT('Ctrl Pts',(-2.08274928435277,1.13466362669319,2.77146490022835));
#89636=CARTESIAN_POINT('Ctrl Pts',(-2.07775610554488,1.143781310873,2.77076761449222));
#89637=CARTESIAN_POINT('Ctrl Pts',(-2.06402338411574,1.16847096434277,2.76886668025715));
#89638=CARTESIAN_POINT('Ctrl Pts',(-2.0551678075032,1.18397727055729,2.76765888766045));
#89639=CARTESIAN_POINT('Ctrl Pts',(-2.00676312582322,1.26655537258809,2.76115041054048));
#89640=CARTESIAN_POINT('Ctrl Pts',(-1.96410850220163,1.33174176550113,2.75573742120935));
#89641=CARTESIAN_POINT('Ctrl Pts',(-1.81115241140593,1.54212307468216,2.73730964331619));
#89642=CARTESIAN_POINT('Ctrl Pts',(-1.68734476134249,1.67668428328827,2.72384076927719));
#89643=CARTESIAN_POINT('Ctrl Pts',(-1.48747566683035,1.849134708769,2.70473155581573));
#89644=CARTESIAN_POINT('Ctrl Pts',(-1.4228433826762,1.89931641364159,2.69889204304126));
#89645=CARTESIAN_POINT('Ctrl Pts',(-1.34563152556959,1.95310666895128,2.69240238160787));
#89646=CARTESIAN_POINT('Ctrl Pts',(-1.3354671407645,1.96007076283614,2.6915573427475));
#89647=CARTESIAN_POINT('Ctrl Pts',(-1.31995994152628,1.970518836045,2.69028268012245));
#89648=CARTESIAN_POINT('Ctrl Pts',(-1.31465677815963,1.97406086241314,2.68984932718709));
#89649=CARTESIAN_POINT('Ctrl Pts',(-1.30507933980531,1.98040200006651,2.68907138424483));
#89650=CARTESIAN_POINT('Ctrl Pts',(-1.30081027544932,1.98320871162198,2.68872629486574));
#89651=CARTESIAN_POINT('Ctrl Pts',(-1.29140929748524,1.98934600201504,2.68797003593557));
#89652=CARTESIAN_POINT('Ctrl Pts',(-1.28627356241031,1.99267052323071,2.68755926929789));
#89653=CARTESIAN_POINT('Ctrl Pts',(-1.27147493704341,2.00216908228728,2.68638228085509));
#89654=CARTESIAN_POINT('Ctrl Pts',(-1.26177989149606,2.00829307329571,2.68561928890724));
#89655=CARTESIAN_POINT('Ctrl Pts',(-1.19237782366946,2.05143073482997,2.6802119084379));
#89656=CARTESIAN_POINT('Ctrl Pts',(-1.1310901639791,2.085849983014,2.67572216380749));
#89657=CARTESIAN_POINT('Ctrl Pts',(-0.968736177501661,2.16776364535339,
2.66431135084394));
#89658=CARTESIAN_POINT('Ctrl Pts',(-0.865686114569203,2.21093626346685,
2.65752338993734));
#89659=CARTESIAN_POINT('Ctrl Pts',(-0.611756271118086,2.29683145976531,
2.64107986378301));
#89660=CARTESIAN_POINT('Ctrl Pts',(-0.458962915100539,2.33217142389709,
2.63138910592421));
#89661=CARTESIAN_POINT('Ctrl Pts',(-0.285229359811498,2.35461110655365,
2.61995046272885));
#89662=CARTESIAN_POINT('Ctrl Pts',(-0.266616384671434,2.35679123408781,
2.61872019165903));
#89663=CARTESIAN_POINT('Ctrl Pts',(-0.236335264165208,2.35997474627779,
2.61671000396813));
#89664=CARTESIAN_POINT('Ctrl Pts',(-0.224681844158692,2.36111270817905,
2.61593431964769));
#89665=CARTESIAN_POINT('Ctrl Pts',(-0.203895270850146,2.36298724727675,
2.61454679027975));
#89666=CARTESIAN_POINT('Ctrl Pts',(-0.194765311181239,2.36375728063889,
2.61393600986113));
#89667=CARTESIAN_POINT('Ctrl Pts',(-0.175480590673122,2.36527129422841,
2.61264294912869));
#89668=CARTESIAN_POINT('Ctrl Pts',(-0.16532506705863,2.36600282112872,2.61196029022927));
#89669=CARTESIAN_POINT('Ctrl Pts',(-0.13831748613817,2.36777351195848,2.6101400969242));
#89670=CARTESIAN_POINT('Ctrl Pts',(-0.121458766433615,2.36869813889126,
2.60899899669715));
#89671=CARTESIAN_POINT('Ctrl Pts',(-0.03995370405994,2.37229593697193,2.60345751955741));
#89672=CARTESIAN_POINT('Ctrl Pts',(0.0247682367854278,2.37250277940886,
2.59898092228217));
#89673=CARTESIAN_POINT('Ctrl Pts',(0.215265930670928,2.36531609832025,2.58556982924745));
#89674=CARTESIAN_POINT('Ctrl Pts',(0.340526931628984,2.3505518795912,2.57643685893082));
#89675=CARTESIAN_POINT('Ctrl Pts',(0.604265445461789,2.29793735776597,2.55679686752159));
#89676=CARTESIAN_POINT('Ctrl Pts',(0.741716841050238,2.25732514175687,2.54630939780244));
#89677=CARTESIAN_POINT('Ctrl Pts',(0.892238477155408,2.19760445527891,2.53504622392181));
#89678=CARTESIAN_POINT('Ctrl Pts',(0.909712530380675,2.19042872758904,2.53374253691056));
#89679=CARTESIAN_POINT('Ctrl Pts',(0.934185709619427,2.18003541035256,2.53192395898065));
#89680=CARTESIAN_POINT('Ctrl Pts',(0.941257182833415,2.17699155956425,2.53139935011336));
#89681=CARTESIAN_POINT('Ctrl Pts',(0.953120984368067,2.17181628084528,2.53052082432183));
#89682=CARTESIAN_POINT('Ctrl Pts',(0.957921244220867,2.16970331158631,2.5301658060735));
#89683=CARTESIAN_POINT('Ctrl Pts',(0.967697065993907,2.16536144182146,2.52944377180796));
#89684=CARTESIAN_POINT('Ctrl Pts',(0.97267201264778,2.1631312818722,2.52907683547195));
#89685=CARTESIAN_POINT('Ctrl Pts',(0.985318148235508,2.15740984599261,2.52814528409324));
#89686=CARTESIAN_POINT('Ctrl Pts',(0.992978580523133,2.15389476086213,2.52758211071458));
#89687=CARTESIAN_POINT('Ctrl Pts',(1.02394872638793,2.13948337850417,2.52530915710261));
#89688=CARTESIAN_POINT('Ctrl Pts',(1.04710019543511,2.12824844347747,2.52361898167136));
#89689=CARTESIAN_POINT('Ctrl Pts',(1.24937448612338,2.02598878461525,2.50889115926759));
#89690=CARTESIAN_POINT('Ctrl Pts',(1.41646280776033,1.91290981479908,2.49694374947774));
#89691=CARTESIAN_POINT('Ctrl Pts',(1.65580116804072,1.70218177847199,2.47722798843879));
#89692=CARTESIAN_POINT('Ctrl Pts',(1.73835111036047,1.61778554900491,2.46981392460874));
#89693=CARTESIAN_POINT('Ctrl Pts',(1.8261812897705,1.51347331686101,2.46090714208561));
#89694=CARTESIAN_POINT('Ctrl Pts',(1.83791826507087,1.49919845352564,2.45969366402645));
#89695=CARTESIAN_POINT('Ctrl Pts',(1.85676816633963,1.4757185752457,2.45770551259056));
#89696=CARTESIAN_POINT('Ctrl Pts',(1.8639824473826,1.46659563770402,2.45693491744183));
#89697=CARTESIAN_POINT('Ctrl Pts',(1.87675406868395,1.4501986131215,2.45555304184385));
#89698=CARTESIAN_POINT('Ctrl Pts',(1.88233698611168,1.44294466924186,2.45494279309596));
#89699=CARTESIAN_POINT('Ctrl Pts',(1.89406793249607,1.42751858466975,2.45364723152288));
#89700=CARTESIAN_POINT('Ctrl Pts',(1.90020536178318,1.41933865579932,2.45296151895348));
#89701=CARTESIAN_POINT('Ctrl Pts',(1.91645555549108,1.39738617219141,2.45112450922611));
#89702=CARTESIAN_POINT('Ctrl Pts',(1.926472554029,1.38354381291824,2.44996952880264));
#89703=CARTESIAN_POINT('Ctrl Pts',(1.97514433440288,1.31473144210644,2.44424328049535));
#89704=CARTESIAN_POINT('Ctrl Pts',(2.01159681321878,1.25824901956538,2.43958948434016));
#89705=CARTESIAN_POINT('Ctrl Pts',(2.1284803081641,1.0590514697767,2.42331889086194));
#89706=CARTESIAN_POINT('Ctrl Pts',(2.19649950927833,0.909612717007057,2.41131412795717));
#89707=CARTESIAN_POINT('Ctrl Pts',(2.284130618943,0.648413228828248,2.391228778403));
#89708=CARTESIAN_POINT('Ctrl Pts',(2.31215262685408,0.5400452827606,2.3831486763035));
#89709=CARTESIAN_POINT('Ctrl Pts',(2.33472179274567,0.417650904454418,2.37456136314503));
#89710=CARTESIAN_POINT('Ctrl Pts',(2.3369165204411,0.405190475947076,2.37369331304474));
#89711=CARTESIAN_POINT('Ctrl Pts',(2.34007915481195,0.386353709549208,2.372390983812));
#89712=CARTESIAN_POINT('Ctrl Pts',(2.34112089563768,0.379990255382738,2.37195273511217));
#89713=CARTESIAN_POINT('Ctrl Pts',(2.34294207326737,0.368573794852299,2.37116963887605));
#89714=CARTESIAN_POINT('Ctrl Pts',(2.34373113217126,0.363522465128319,2.37082426045647));
#89715=CARTESIAN_POINT('Ctrl Pts',(2.34541965613234,0.352478952600832,2.37007160591892));
#89716=CARTESIAN_POINT('Ctrl Pts',(2.34631249411381,0.346485869046732,2.36966470594815));
#89717=CARTESIAN_POINT('Ctrl Pts',(2.34878900711256,0.329413887988917,2.36850984522781));
#89718=CARTESIAN_POINT('Ctrl Pts',(2.35031727441194,0.318326925452593,2.36776492818652));
#89719=CARTESIAN_POINT('Ctrl Pts',(2.35997274440637,0.244416601982731,2.3628302789541));
#89720=CARTESIAN_POINT('Ctrl Pts',(2.36565953936341,0.181293752952874,2.35876597869869));
#89721=CARTESIAN_POINT('Ctrl Pts',(2.37918314435107,-0.0901588441511683,
2.34164038455785));
#89722=CARTESIAN_POINT('Ctrl Pts',(2.36206988193449,-0.298793572045404,
2.32928465013728));
#89723=CARTESIAN_POINT('Ctrl Pts',(2.30271240836311,-0.572585419331684,
2.31163056069565));
#89724=CARTESIAN_POINT('Ctrl Pts',(2.28435356803838,-0.641923431926614,
2.30703919982841));
#89725=CARTESIAN_POINT('Ctrl Pts',(2.25750139053517,-0.727467235907128,
2.30116901131475));
#89726=CARTESIAN_POINT('Ctrl Pts',(2.25192386609037,-0.744553543674305,
2.29998612991807));
#89727=CARTESIAN_POINT('Ctrl Pts',(2.24277310909129,-0.77154236815718,2.29810042182438));
#89728=CARTESIAN_POINT('Ctrl Pts',(2.2393271379669,-0.781487560874939,2.29740180172756));
#89729=CARTESIAN_POINT('Ctrl Pts',(2.2330776115169,-0.799143134136172,2.29615471620873));
#89730=CARTESIAN_POINT('Ctrl Pts',(2.2303000134326,-0.806862575076773,2.29560712167823));
#89731=CARTESIAN_POINT('Ctrl Pts',(2.22377733787605,-0.824699215634724,
2.29433633777904));
#89732=CARTESIAN_POINT('Ctrl Pts',(2.22000319464273,-0.834805518552139,
2.29361218701013));
#89733=CARTESIAN_POINT('Ctrl Pts',(2.20915229016338,-0.863267767433512,
2.29156091095236));
#89734=CARTESIAN_POINT('Ctrl Pts',(2.20191604539839,-0.881561550692104,
2.29022846541761));
#89735=CARTESIAN_POINT('Ctrl Pts',(2.15071883403685,-1.00642767758,2.28103487349744));
#89736=CARTESIAN_POINT('Ctrl Pts',(2.09927293223996,-1.10974495264606,2.27291904803231));
#89737=CARTESIAN_POINT('Ctrl Pts',(1.97749088074027,-1.31530350736038,2.25571784087368));
#89738=CARTESIAN_POINT('Ctrl Pts',(1.90622855021484,-1.41660987756806,2.24662961200988));
#89739=CARTESIAN_POINT('Ctrl Pts',(1.76418956046454,-1.58829007632479,2.23042270751757));
#89740=CARTESIAN_POINT('Ctrl Pts',(1.69624396525468,-1.66065994285745,2.22329002653166));
#89741=CARTESIAN_POINT('Ctrl Pts',(1.61478580231013,-1.73718832831345,2.21557902892978));
#89742=CARTESIAN_POINT('Ctrl Pts',(1.60554405013478,-1.74573331181411,2.21471553119767));
#89743=CARTESIAN_POINT('Ctrl Pts',(1.59147566477693,-1.75853480720565,2.21341867076947));
#89744=CARTESIAN_POINT('Ctrl Pts',(1.58669919720094,-1.76284574476228,2.21298138657661));
#89745=CARTESIAN_POINT('Ctrl Pts',(1.57809650949775,-1.77054669506712,2.21219931310642));
#89746=CARTESIAN_POINT('Ctrl Pts',(1.57427683625649,-1.77394380889891,2.21185399913475));
#89747=CARTESIAN_POINT('Ctrl Pts',(1.56589717107805,-1.78134807393061,2.21110066730268));
#89748=CARTESIAN_POINT('Ctrl Pts',(1.56133277452735,-1.78535007216217,2.21069303072267));
#89749=CARTESIAN_POINT('Ctrl Pts',(1.54827034845832,-1.79671461595299,2.20953396468365));
#89750=CARTESIAN_POINT('Ctrl Pts',(1.53973511612032,-1.80403444196131,2.20878561392358));
#89751=CARTESIAN_POINT('Ctrl Pts',(1.481832939209,-1.85298112029766,2.20376665137196));
#89752=CARTESIAN_POINT('Ctrl Pts',(1.43083071762854,-1.89264182771465,2.19962644643547));
#89753=CARTESIAN_POINT('Ctrl Pts',(1.1969838308649,-2.05962342461504,2.18153456650361));
#89754=CARTESIAN_POINT('Ctrl Pts',(0.998367222239815,-2.16289007118117,
2.168372080254));
#89755=CARTESIAN_POINT('Ctrl Pts',(0.733203815247222,-2.25632804369121,
2.150522682491));
#89756=CARTESIAN_POINT('Ctrl Pts',(0.677467091254764,-2.27368456931606,
2.14676435216336));
#89757=CARTESIAN_POINT('Ctrl Pts',(0.604762121050798,-2.29341430949082,
2.1418255507741));
#89758=CARTESIAN_POINT('Ctrl Pts',(0.588326865706808,-2.29768533357595,
2.14070681513311));
#89759=CARTESIAN_POINT('Ctrl Pts',(0.561945301404778,-2.30423949417779,
2.13890674021568));
#89760=CARTESIAN_POINT('Ctrl Pts',(0.552027451498906,-2.30663561394877,
2.13822905617417));
#89761=CARTESIAN_POINT('Ctrl Pts',(0.533178927643971,-2.31106083086407,
2.13693917022092));
#89762=CARTESIAN_POINT('Ctrl Pts',(0.524251336081692,-2.31310234650119,
2.13632738093875));
#89763=CARTESIAN_POINT('Ctrl Pts',(0.503920125714679,-2.3176278346579,2.1349321189594));
#89764=CARTESIAN_POINT('Ctrl Pts',(0.492509619106658,-2.32007942529672,
2.13414762321001));
#89765=CARTESIAN_POINT('Ctrl Pts',(0.457583893943007,-2.32731409124368,
2.13174177912825));
#89766=CARTESIAN_POINT('Ctrl Pts',(0.434014400223242,-2.33182446288757,
2.13011179381475));
#89767=CARTESIAN_POINT('Ctrl Pts',(0.247163100869148,-2.36465025509908,
2.11713495678288));
#89768=CARTESIAN_POINT('Ctrl Pts',(0.081421367215168,-2.37613357769856,
2.10524532297555));
#89769=CARTESIAN_POINT('Ctrl Pts',(-0.24078672014201,-2.36469696014912,
2.08172600016612));
#89770=CARTESIAN_POINT('Ctrl Pts',(-0.396517831685705,-2.34361942114607,
2.07018478833533));
#89771=CARTESIAN_POINT('Ctrl Pts',(-0.566813667614349,-2.30309663461945,
2.05801790885964));
#89772=CARTESIAN_POINT('Ctrl Pts',(-0.584538278609191,-2.29866197916364,
2.05675757471618));
#89773=CARTESIAN_POINT('Ctrl Pts',(-0.60883021444775,-2.29228503294966,
2.05504017565372));
#89774=CARTESIAN_POINT('Ctrl Pts',(-0.615442436888273,-2.29051861204719,
2.05457371798211));
#89775=CARTESIAN_POINT('Ctrl Pts',(-0.626743874510441,-2.28744701976707,
2.05377830879206));
#89776=CARTESIAN_POINT('Ctrl Pts',(-0.631436839247676,-2.28615600334246,
2.05344855895873));
#89777=CARTESIAN_POINT('Ctrl Pts',(-0.641181736044021,-2.28344292400903,
2.0527650218046));
#89778=CARTESIAN_POINT('Ctrl Pts',(-0.646232952666576,-2.28201853133619,
2.0524113840728));
#89779=CARTESIAN_POINT('Ctrl Pts',(-0.658437109372578,-2.27853331025056,
2.05155850187604));
#89780=CARTESIAN_POINT('Ctrl Pts',(-0.665585237920955,-2.27645552729718,
2.05106023482164));
#89781=CARTESIAN_POINT('Ctrl Pts',(-0.690615007887174,-2.2690520228246,
2.04931960577326));
#89782=CARTESIAN_POINT('Ctrl Pts',(-0.708444054436159,-2.2635488170332,
2.04808707765989));
#89783=CARTESIAN_POINT('Ctrl Pts',(-0.752117415395505,-2.24950178005459,
2.04508176292201));
#89784=CARTESIAN_POINT('Ctrl Pts',(-0.77788369401656,-2.24072219656346,
2.04332071290167));
#89785=CARTESIAN_POINT('Ctrl Pts',(-0.979353671698342,-2.16817909300825,
2.02960367271257));
#89786=CARTESIAN_POINT('Ctrl Pts',(-1.14712811172788,-2.08428559385173,
2.01845457026305));
#89787=CARTESIAN_POINT('Ctrl Pts',(-1.39866341320645,-1.91884358646531,
1.99981857520511));
#89788=CARTESIAN_POINT('Ctrl Pts',(-1.48934132143161,-1.84934508542921,
1.99263234211975));
#89789=CARTESIAN_POINT('Ctrl Pts',(-1.58839601014194,-1.76140104583153,
1.98397943805746));
#89790=CARTESIAN_POINT('Ctrl Pts',(-1.60199082627184,-1.74904570854021,
1.98277307534447));
#89791=CARTESIAN_POINT('Ctrl Pts',(-1.62393190348548,-1.72863464610982,
1.9807942629888));
#89792=CARTESIAN_POINT('Ctrl Pts',(-1.63236518286793,-1.72067326025132,
1.98002582700524));
#89793=CARTESIAN_POINT('Ctrl Pts',(-1.64734697982213,-1.70632051974592,
1.97864633423306));
#89794=CARTESIAN_POINT('Ctrl Pts',(-1.65391758477715,-1.69995247191225,
1.97803629515263));
#89795=CARTESIAN_POINT('Ctrl Pts',(-1.66656174174637,-1.68755540894127,
1.97685247814919));
#89796=CARTESIAN_POINT('Ctrl Pts',(-1.67263984433204,-1.68153122038186,
1.97627891777883));
#89797=CARTESIAN_POINT('Ctrl Pts',(-1.68882848120876,-1.66531156031195,
1.97473908075235));
#89798=CARTESIAN_POINT('Ctrl Pts',(-1.69887912232864,-1.65505708171102,
1.97377018700507));
#89799=CARTESIAN_POINT('Ctrl Pts',(-1.7395503242715,-1.61280019994762,1.9697957019647));
#89800=CARTESIAN_POINT('Ctrl Pts',(-1.76936292228399,-1.58003614038908,
1.96675575715211));
#89801=CARTESIAN_POINT('Ctrl Pts',(-1.84435648524047,-1.49283279205689,
1.95876454216031));
#89802=CARTESIAN_POINT('Ctrl Pts',(-1.88804782304586,-1.43717583196341,
1.95375879449328));
#89803=CARTESIAN_POINT('Ctrl Pts',(-1.97607022494181,-1.31409326855003,
1.94289981546531));
#89804=CARTESIAN_POINT('Ctrl Pts',(-2.0195814065101,-1.24618790615456,1.93703226972127));
#89805=CARTESIAN_POINT('Ctrl Pts',(-2.12991662313723,-1.05298929952,1.92078355393102));
#89806=CARTESIAN_POINT('Ctrl Pts',(-2.18909162317828,-0.923697420941236,
1.91038241703514));
#89807=CARTESIAN_POINT('Ctrl Pts',(-2.24265835185452,-0.772036079430949,
1.89919481253991));
#89808=CARTESIAN_POINT('Ctrl Pts',(-2.24874729671578,-0.75411659808541,
1.89788862536016));
#89809=CARTESIAN_POINT('Ctrl Pts',(-2.25701261235393,-0.72880140648472,
1.89606717479653));
#89810=CARTESIAN_POINT('Ctrl Pts',(-2.25936822820612,-0.72146561664592,
1.89554215352828));
#89811=CARTESIAN_POINT('Ctrl Pts',(-2.26326757594523,-0.709115971272732,
1.89466313509022));
#89812=CARTESIAN_POINT('Ctrl Pts',(-2.26483048032696,-0.704108285893273,
1.89430803391391));
#89813=CARTESIAN_POINT('Ctrl Pts',(-2.26798326299849,-0.693887372182228,
1.89358603075452));
#89814=CARTESIAN_POINT('Ctrl Pts',(-2.26957180670773,-0.688673785077757,
1.89321920737618));
#89815=CARTESIAN_POINT('Ctrl Pts',(-2.27356891667768,-0.675391257562155,
1.89228827019927));
#89816=CARTESIAN_POINT('Ctrl Pts',(-2.27595253453937,-0.667314794982954,
1.89172559438466));
#89817=CARTESIAN_POINT('Ctrl Pts',(-2.2854279574098,-0.634567600332631,
1.88945716464447));
#89818=CARTESIAN_POINT('Ctrl Pts',(-2.29216236482781,-0.609794076340319,
1.88777091797322));
#89819=CARTESIAN_POINT('Ctrl Pts',(-2.34697257601765,-0.394410731675212,
1.87332845728201));
#89820=CARTESIAN_POINT('Ctrl Pts',(-2.37158441769536,-0.198601548167095,
1.86161808344996));
#89821=CARTESIAN_POINT('Ctrl Pts',(-2.37174916735844,-0.00198736875130605,
1.84947704601095));
#89822=CARTESIAN_POINT('Ctrl Pts',(-2.37174916921441,-0.00198515257602363,
1.84947690916085));
#89823=CARTESIAN_POINT('Ctrl Pts',(-2.37179808021083,0.056450967917035,
1.84586844475866));
#89824=CARTESIAN_POINT('Ctrl Pts',(-2.36968731411222,0.114844513390865,
1.84223362268876));
#89825=CARTESIAN_POINT('Ctrl Pts',(-2.36542648301433,0.173076907629062,
1.83854786047046));
#89826=CARTESIAN_POINT('Ctrl Pts',(-2.36542650134104,0.173076657159373,
1.6387748639739));
#89827=CARTESIAN_POINT('Ctrl Pts',(-2.36960866311417,0.115919346327277,
1.64233205486039));
#89828=CARTESIAN_POINT('Ctrl Pts',(-2.3717210489944,0.0585847397316989,
1.64592561797024));
#89829=CARTESIAN_POINT('Ctrl Pts',(-2.37177718696143,-0.0538671038640167,
1.65307890001155));
#89830=CARTESIAN_POINT('Ctrl Pts',(-2.36988797458106,-0.108898665586173,
1.65662887810539));
#89831=CARTESIAN_POINT('Ctrl Pts',(-2.36492762284214,-0.180545786629185,
1.661338529028));
#89832=CARTESIAN_POINT('Ctrl Pts',(-2.36359158010639,-0.197266978274198,
1.66244389580054));
#89833=CARTESIAN_POINT('Ctrl Pts',(-2.36115356912776,-0.224180622973592,
1.6642336739387));
#89834=CARTESIAN_POINT('Ctrl Pts',(-2.36016267298024,-0.234382764222406,
1.66491458962881));
#89835=CARTESIAN_POINT('Ctrl Pts',(-2.35814538825979,-0.253840717673803,
1.66621811164116));
#89836=CARTESIAN_POINT('Ctrl Pts',(-2.35713055506391,-0.263097556494081,
1.66684034261606));
#89837=CARTESIAN_POINT('Ctrl Pts',(-2.35468027003334,-0.284294775500551,
1.66827011588567));
#89838=CARTESIAN_POINT('Ctrl Pts',(-2.35320847105944,-0.296230612731584,
1.66907878953395));
#89839=CARTESIAN_POINT('Ctrl Pts',(-2.34835554719776,-0.333265142479105,
1.67159938964166));
#89840=CARTESIAN_POINT('Ctrl Pts',(-2.34466324693694,-0.358320530915857,
1.67332106147969));
#89841=CARTESIAN_POINT('Ctrl Pts',(-2.32475587553721,-0.479878710264843,
1.68175676352726));
#89842=CARTESIAN_POINT('Ctrl Pts',(-2.30298229721019,-0.575362019405487,
1.68864375829141));
#89843=CARTESIAN_POINT('Ctrl Pts',(-2.22805682500464,-0.830112927903093,
1.70770542951043));
#89844=CARTESIAN_POINT('Ctrl Pts',(-2.16380798862314,-0.985522392842536,
1.72012008919406));
#89845=CARTESIAN_POINT('Ctrl Pts',(-2.05290309707372,-1.18951539834122,
1.73681252166438));
#89846=CARTESIAN_POINT('Ctrl Pts',(-2.01979431203779,-1.24490587947179,
1.74138379174626));
#89847=CARTESIAN_POINT('Ctrl Pts',(-1.97856176638615,-1.30790198260453,
1.74657210707806));
#89848=CARTESIAN_POINT('Ctrl Pts',(-1.97259685623466,-1.31688113104749,
1.74731134604191));
#89849=CARTESIAN_POINT('Ctrl Pts',(-1.96284318392614,-1.33134862602584,
1.74850158332934));
#89850=CARTESIAN_POINT('Ctrl Pts',(-1.95909221363581,-1.33686208336675,
1.74895497253596));
#89851=CARTESIAN_POINT('Ctrl Pts',(-1.95237735076523,-1.3466431366851,1.74975883545705));
#89852=CARTESIAN_POINT('Ctrl Pts',(-1.94942264367262,-1.35091687958915,
1.75010991136192));
#89853=CARTESIAN_POINT('Ctrl Pts',(-1.9429926839962,-1.36015226547633,1.75086819954687));
#89854=CARTESIAN_POINT('Ctrl Pts',(-1.93951246334868,-1.36511031127238,
1.75127506757081));
#89855=CARTESIAN_POINT('Ctrl Pts',(-1.92969355646658,-1.37898532588265,
1.75241322610954));
#89856=CARTESIAN_POINT('Ctrl Pts',(-1.92331201055418,-1.38787199426419,
1.75314166310371));
#89857=CARTESIAN_POINT('Ctrl Pts',(-1.88400681211253,-1.44181496092983,
1.75756224076753));
#89858=CARTESIAN_POINT('Ctrl Pts',(-1.84955995273617,-1.48574600793919,
1.7611577073597));
#89859=CARTESIAN_POINT('Ctrl Pts',(-1.71758436786876,-1.64234507337006,
1.77412607853238));
#89860=CARTESIAN_POINT('Ctrl Pts',(-1.61104992035398,-1.74697402619156,
1.78311157905132));
#89861=CARTESIAN_POINT('Ctrl Pts',(-1.39149335244066,-1.92532163242049,
1.80052847758672));
#89862=CARTESIAN_POINT('Ctrl Pts',(-1.28064751275175,-2.00076276880269,
1.80889252556014));
#89863=CARTESIAN_POINT('Ctrl Pts',(-1.14753597617226,-2.0757451907461,1.81886663680873));
#89864=CARTESIAN_POINT('Ctrl Pts',(-1.13092069824292,-2.08484417969762,
1.8201100759378));
#89865=CARTESIAN_POINT('Ctrl Pts',(-1.10373114491279,-2.09931327301803,
1.82214330128084));
#89866=CARTESIAN_POINT('Ctrl Pts',(-1.09322223253599,-2.10480493161774,
1.8229287781269));
#89867=CARTESIAN_POINT('Ctrl Pts',(-1.07440395123258,-2.11445987972742,
1.82433487949348));
#89868=CARTESIAN_POINT('Ctrl Pts',(-1.06611039875946,-2.11865359292916,
1.8249544187976));
#89869=CARTESIAN_POINT('Ctrl Pts',(-1.04853385295497,-2.12741200283253,
1.82626719428472));
#89870=CARTESIAN_POINT('Ctrl Pts',(-1.03924523799089,-2.13196491528773,
1.82696082617108));
#89871=CARTESIAN_POINT('Ctrl Pts',(-1.01443641358905,-2.14392456919899,
1.82881327156069));
#89872=CARTESIAN_POINT('Ctrl Pts',(-0.998865171384125,-2.15122340490828,
1.8299757898895));
#89873=CARTESIAN_POINT('Ctrl Pts',(-0.922597474088439,-2.18596641186419,
1.83567011632628));
#89874=CARTESIAN_POINT('Ctrl Pts',(-0.860848042614488,-2.2110120693348,
1.84028272111396));
#89875=CARTESIAN_POINT('Ctrl Pts',(-0.55161147521398,-2.32152016902032,
1.86341125685316));
#89876=CARTESIAN_POINT('Ctrl Pts',(-0.292265328172684,-2.3681796462979,
1.88315671105829));
#89877=CARTESIAN_POINT('Ctrl Pts',(-0.00805945332513304,-2.37184314805694,
1.90300287202571));
#89878=CARTESIAN_POINT('Ctrl Pts',(0.0144551904437281,-2.37181281189842,
1.904561106136));
#89879=CARTESIAN_POINT('Ctrl Pts',(0.0453074398984561,-2.3713318785506,
1.90667422344017));
#89880=CARTESIAN_POINT('Ctrl Pts',(0.0536472955290461,-2.37115786385569,
1.90724321209398));
#89881=CARTESIAN_POINT('Ctrl Pts',(0.0669243505919645,-2.3708107464807,
1.90814532348815));
#89882=CARTESIAN_POINT('Ctrl Pts',(0.0718621270061494,-2.37066621441762,
1.90848000221215));
#89883=CARTESIAN_POINT('Ctrl Pts',(0.0821216854233761,-2.37033382605763,
1.90917363489297));
#89884=CARTESIAN_POINT('Ctrl Pts',(0.0874433193823489,-2.3701434734459,
1.90953243528803));
#89885=CARTESIAN_POINT('Ctrl Pts',(0.100315498453076,-2.36963962894656,
1.91039801822529));
#89886=CARTESIAN_POINT('Ctrl Pts',(0.107865361284689,-2.36930796607062,
1.91090379380933));
#89887=CARTESIAN_POINT('Ctrl Pts',(0.134361159951856,-2.36801710336895,
1.91267248061633));
#89888=CARTESIAN_POINT('Ctrl Pts',(0.153297668416236,-2.36686666386296,
1.91392524257181));
#89889=CARTESIAN_POINT('Ctrl Pts',(0.270708846490515,-2.35831856107061,
1.92163378137981));
#89890=CARTESIAN_POINT('Ctrl Pts',(0.368667254409959,-2.34500296920853,
1.92780970694033));
#89891=CARTESIAN_POINT('Ctrl Pts',(0.623485683637577,-2.29399575005869,
1.94385026179236));
#89892=CARTESIAN_POINT('Ctrl Pts',(0.77781166374246,-2.24636568389503,1.95356615447729));
#89893=CARTESIAN_POINT('Ctrl Pts',(0.991785427209705,-2.15560843666167,
1.96821505579086));
#89894=CARTESIAN_POINT('Ctrl Pts',(1.05615719325343,-2.1248097545131,1.97278325831184));
#89895=CARTESIAN_POINT('Ctrl Pts',(1.13499087013338,-2.08262361320781,1.97863674111826));
#89896=CARTESIAN_POINT('Ctrl Pts',(1.15084407995003,-2.07390531682452,1.97982736881521));
#89897=CARTESIAN_POINT('Ctrl Pts',(1.17586370069562,-2.0597708443004,1.98172878532738));
#89898=CARTESIAN_POINT('Ctrl Pts',(1.18509627619574,-2.05447272639503,1.98243533726153));
#89899=CARTESIAN_POINT('Ctrl Pts',(1.2022852473987,-2.04445440795957,1.9837601368272));
#89900=CARTESIAN_POINT('Ctrl Pts',(1.21025032576496,-2.03974944224587,1.98437782339233));
#89901=CARTESIAN_POINT('Ctrl Pts',(1.22796466447456,-2.02914531055221,1.98576017204667));
#89902=CARTESIAN_POINT('Ctrl Pts',(1.23769929297568,-2.02322227172872,1.9865256962754));
#89903=CARTESIAN_POINT('Ctrl Pts',(1.26620401986214,-2.00559585223416,1.9887848843073));
#89904=CARTESIAN_POINT('Ctrl Pts',(1.28485307724654,-1.99370004123265,1.99028560297049));
#89905=CARTESIAN_POINT('Ctrl Pts',(1.42704076453219,-1.90017817445824,2.00190693758804));
#89906=CARTESIAN_POINT('Ctrl Pts',(1.54283433512278,-1.80742073632707,2.01245598405812));
#89907=CARTESIAN_POINT('Ctrl Pts',(1.76550242867467,-1.59197487330605,2.03498243151264));
#89908=CARTESIAN_POINT('Ctrl Pts',(1.86997795541834,-1.4678453320116,2.04694403924147));
#89909=CARTESIAN_POINT('Ctrl Pts',(1.9778778492428,-1.30923539062315,2.06043308706646));
#89910=CARTESIAN_POINT('Ctrl Pts',(1.99428112798441,-1.28411101093527,2.0625203676908));
#89911=CARTESIAN_POINT('Ctrl Pts',(2.01515941361527,-1.25076687813245,2.06521975799979));
#89912=CARTESIAN_POINT('Ctrl Pts',(2.02006796429726,-1.24282366918957,2.06585763806313));
#89913=CARTESIAN_POINT('Ctrl Pts',(2.02789948908344,-1.22998140756852,2.06688038601462));
#89914=CARTESIAN_POINT('Ctrl Pts',(2.03085185959194,-1.22510053748358,2.06726712099598));
#89915=CARTESIAN_POINT('Ctrl Pts',(2.03650595413957,-1.21567656017414,2.06800996259131));
#89916=CARTESIAN_POINT('Ctrl Pts',(2.03921011884692,-1.21113504281481,2.06836621867915));
#89917=CARTESIAN_POINT('Ctrl Pts',(2.04563202130727,-1.2002672775886,2.06921469604775));
#89918=CARTESIAN_POINT('Ctrl Pts',(2.0493356654387,-1.19393267742906,2.06970600890315));
#89919=CARTESIAN_POINT('Ctrl Pts',(2.06183417112514,-1.17232610189998,2.07137116293955));
#89920=CARTESIAN_POINT('Ctrl Pts',(2.0704884552349,-1.15697287819407,2.07253636998755));
#89921=CARTESIAN_POINT('Ctrl Pts',(2.11986367385172,-1.06704954035079,2.07926526456413));
#89922=CARTESIAN_POINT('Ctrl Pts',(2.15672970114372,-0.99042263836784,2.08462047719697));
#89923=CARTESIAN_POINT('Ctrl Pts',(2.22726789245448,-0.821079263496044,
2.09600422192559));
#89924=CARTESIAN_POINT('Ctrl Pts',(2.25943296622754,-0.727912820277594,
2.1019954441008));
#89925=CARTESIAN_POINT('Ctrl Pts',(2.32431094794245,-0.493648901755764,
2.11693155945737));
#89926=CARTESIAN_POINT('Ctrl Pts',(2.35007550830609,-0.351065642441476,
2.12592863611524));
#89927=CARTESIAN_POINT('Ctrl Pts',(2.36436023085634,-0.18804802703086,2.13661065817768));
#89928=CARTESIAN_POINT('Ctrl Pts',(2.36579506824295,-0.169041480099765,
2.13786165827944));
#89929=CARTESIAN_POINT('Ctrl Pts',(2.3677528348711,-0.138152063751828,2.13990476592596));
#89930=CARTESIAN_POINT('Ctrl Pts',(2.36841575047315,-0.126278675743689,
2.14069249265964));
#89931=CARTESIAN_POINT('Ctrl Pts',(2.3694377699601,-0.105114930825181,2.14210105298806));
#89932=CARTESIAN_POINT('Ctrl Pts',(2.36983159409495,-0.0958264357804435,
2.14272078625121));
#89933=CARTESIAN_POINT('Ctrl Pts',(2.37054746237549,-0.0762192142190349,
2.14403233757156));
#89934=CARTESIAN_POINT('Ctrl Pts',(2.37085676323617,-0.0659002455208639,
2.14472454165748));
#89935=CARTESIAN_POINT('Ctrl Pts',(2.37149951559256,-0.0384796487041291,
2.14656929693222));
#89936=CARTESIAN_POINT('Ctrl Pts',(2.37171534331981,-0.0213761388779025,
2.14772549964854));
#89937=CARTESIAN_POINT('Ctrl Pts',(2.37186413371387,0.0612265397337218,
2.15333734299061));
#89938=CARTESIAN_POINT('Ctrl Pts',(2.36926884517759,0.126695860115009,2.15787097884521));
#89939=CARTESIAN_POINT('Ctrl Pts',(2.34412911014829,0.436275167414346,2.17973302915143));
#89940=CARTESIAN_POINT('Ctrl Pts',(2.28654803409132,0.675974835079976,2.19811804365447));
#89941=CARTESIAN_POINT('Ctrl Pts',(2.17923234400931,0.936755134417593,2.21805908819881));
#89942=CARTESIAN_POINT('Ctrl Pts',(2.16437082333313,0.970599355541919,2.22064125488903));
#89943=CARTESIAN_POINT('Ctrl Pts',(2.14445520943913,1.01321841682862,2.22387331363644));
#89944=CARTESIAN_POINT('Ctrl Pts',(2.14012876240169,1.02232509263733,2.22456276599095));
#89945=CARTESIAN_POINT('Ctrl Pts',(2.13319184158391,1.03668948080599,2.22564810929301));
#89946=CARTESIAN_POINT('Ctrl Pts',(2.13061975664414,1.04196543470679,2.22604628475393));
#89947=CARTESIAN_POINT('Ctrl Pts',(2.12571867051075,1.0519246894908,2.22679695187334));
#89948=CARTESIAN_POINT('Ctrl Pts',(2.1233937899295,1.05660978226665,2.22714967323411));
#89949=CARTESIAN_POINT('Ctrl Pts',(2.11793147937511,1.06752657395764,2.22797065054157));
#89950=CARTESIAN_POINT('Ctrl Pts',(2.11478203029549,1.07375216176969,2.22843815152538));
#89951=CARTESIAN_POINT('Ctrl Pts',(2.10452396727163,1.09380929425726,2.22994239552722));
#89952=CARTESIAN_POINT('Ctrl Pts',(2.09730659357699,1.10758520460344,2.23097260674337));
#89953=CARTESIAN_POINT('Ctrl Pts',(2.03090970681291,1.23134131729201,2.24020983144616));
#89954=CARTESIAN_POINT('Ctrl Pts',(1.96325598583339,1.33657421394242,2.24794287603437));
#89955=CARTESIAN_POINT('Ctrl Pts',(1.76903805169605,1.59187311075522,2.26764663079275));
#89956=CARTESIAN_POINT('Ctrl Pts',(1.63162442350609,1.73243996059345,2.27951338710829));
#89957=CARTESIAN_POINT('Ctrl Pts',(1.45672768822789,1.87187554817997,2.29402701187766));
#89958=CARTESIAN_POINT('Ctrl Pts',(1.4346488056877,1.88885052957419,2.29584816668067));
#89959=CARTESIAN_POINT('Ctrl Pts',(1.40234856569355,1.91279096742626,2.29849951871082));
#89960=CARTESIAN_POINT('Ctrl Pts',(1.39236304498143,1.9200718543782,2.2993174331287));
#89961=CARTESIAN_POINT('Ctrl Pts',(1.37468846992077,1.93274879455816,2.30076235588069));
#89962=CARTESIAN_POINT('Ctrl Pts',(1.36702334408375,1.93817787227381,2.30138807618843));
#89963=CARTESIAN_POINT('Ctrl Pts',(1.35112354801326,1.94929818600801,2.30268424053735));
#89964=CARTESIAN_POINT('Ctrl Pts',(1.34288470595795,1.95498309996488,2.30335490899979));
#89965=CARTESIAN_POINT('Ctrl Pts',(1.32165372898751,1.96943523371533,2.30508085482682));
#89966=CARTESIAN_POINT('Ctrl Pts',(1.30861039832795,1.97812601316198,2.30613898681733));
#89967=CARTESIAN_POINT('Ctrl Pts',(1.25319502978267,2.01426136415358,2.31062604048716));
#89968=CARTESIAN_POINT('Ctrl Pts',(1.21004134444709,2.04047687902,2.31409992764073));
#89969=CARTESIAN_POINT('Ctrl Pts',(1.09238945039114,2.1069043838649,2.32352501594766));
#89970=CARTESIAN_POINT('Ctrl Pts',(1.01652511643256,2.14453604655934,2.32955733007252));
#89971=CARTESIAN_POINT('Ctrl Pts',(0.819760225371631,2.22934965965042,2.34504151968247));
#89972=CARTESIAN_POINT('Ctrl Pts',(0.69669892548546,2.27081829646661,2.35458844850216));
#89973=CARTESIAN_POINT('Ctrl Pts',(0.537286379423254,2.31035029855108,2.36647375759433));
#89974=CARTESIAN_POINT('Ctrl Pts',(0.503525002569843,2.31794260275288,2.3689633315658));
#89975=CARTESIAN_POINT('Ctrl Pts',(0.421715986099231,2.33446802564574,2.37491317167566));
#89976=CARTESIAN_POINT('Ctrl Pts',(0.373531839123247,2.34266090513998,2.3783494841183));
#89977=CARTESIAN_POINT('Ctrl Pts',(0.314304128349166,2.35085735705827,2.38246405929072));
#89978=CARTESIAN_POINT('Ctrl Pts',(0.303472679759252,2.3522801156695,2.38321207156198));
#89979=CARTESIAN_POINT('Ctrl Pts',(0.286557972724072,2.35438315680863,2.38437284754635));
#89980=CARTESIAN_POINT('Ctrl Pts',(0.280481430386411,2.35511479341488,2.38478837612026));
#89981=CARTESIAN_POINT('Ctrl Pts',(0.269247261819074,2.35642332926689,2.38555378563432));
#89982=CARTESIAN_POINT('Ctrl Pts',(0.264090603257937,2.3570068198735,2.38590401845155));
#89983=CARTESIAN_POINT('Ctrl Pts',(0.25238769815482,2.35829214805742,2.3866963951548));
#89984=CARTESIAN_POINT('Ctrl Pts',(0.245840425121376,2.35898365695781,2.38713795626461));
#89985=CARTESIAN_POINT('Ctrl Pts',(0.225881602952458,2.36100766727362,2.38847895365899));
#89986=CARTESIAN_POINT('Ctrl Pts',(0.212461211775942,2.36225315283245,2.38937368273893));
#89987=CARTESIAN_POINT('Ctrl Pts',(0.0670993162521076,2.37449469074952,
2.39899667922873));
#89988=CARTESIAN_POINT('Ctrl Pts',(-0.0655520068355683,2.37454017721609,
2.40717757634515));
#89989=CARTESIAN_POINT('Ctrl Pts',(-0.387716209696517,2.34761524772513,
2.42702233789465));
#89990=CARTESIAN_POINT('Ctrl Pts',(-0.575263906429226,2.30882726396974,
2.43860850260362));
#89991=CARTESIAN_POINT('Ctrl Pts',(-0.780276063690914,2.23986970219647,
2.45263828936978));
#89992=CARTESIAN_POINT('Ctrl Pts',(-0.804288192889097,2.23135999779909,
2.45430245736106));
#89993=CARTESIAN_POINT('Ctrl Pts',(-0.841002332520498,2.2176791985312,2.45688162814132));
#89994=CARTESIAN_POINT('Ctrl Pts',(-0.853804833542295,2.21278178857598,
2.45778756799049));
#89995=CARTESIAN_POINT('Ctrl Pts',(-0.874604653098438,2.2046177393872,2.45927047383288));
#89996=CARTESIAN_POINT('Ctrl Pts',(-0.882627970853697,2.20141784714506,
2.45984519114634));
#89997=CARTESIAN_POINT('Ctrl Pts',(-0.899454174854711,2.19460037953907,
2.461056248504));
#89998=CARTESIAN_POINT('Ctrl Pts',(-0.908253105723912,2.19097351191484,
2.4616928938984));
#89999=CARTESIAN_POINT('Ctrl Pts',(-0.929040267897562,2.18225842839452,
2.46320501506593));
#90000=CARTESIAN_POINT('Ctrl Pts',(-0.94100878454581,2.17712427832885,2.46408203803548));
#90001=CARTESIAN_POINT('Ctrl Pts',(-0.981558555028009,2.15933275601394,
2.46707563419829));
#90002=CARTESIAN_POINT('Ctrl Pts',(-1.00993056256718,2.14620950610422,2.46920802572197));
#90003=CARTESIAN_POINT('Ctrl Pts',(-1.07767154971281,2.11323579100419,2.47439374838691));
#90004=CARTESIAN_POINT('Ctrl Pts',(-1.11676128292594,2.092841436974,2.47746495517489));
#90005=CARTESIAN_POINT('Ctrl Pts',(-1.27098798403305,2.00682515200285,2.48990337888791));
#90006=CARTESIAN_POINT('Ctrl Pts',(-1.38109234372028,1.9327011873576,2.49953657173183));
#90007=CARTESIAN_POINT('Ctrl Pts',(-1.5882657024881,1.76644810497361,2.51893916695932));
#90008=CARTESIAN_POINT('Ctrl Pts',(-1.68492071811759,1.67450774250247,2.52867240873933));
#90009=CARTESIAN_POINT('Ctrl Pts',(-1.78609983330084,1.56058124554427,2.53927389283346));
#90010=CARTESIAN_POINT('Ctrl Pts',(-1.7986706465424,1.54607580761492,2.54059895501348));
#90011=CARTESIAN_POINT('Ctrl Pts',(-1.81610960099893,1.52545240199469,2.54244650263615));
#90012=CARTESIAN_POINT('Ctrl Pts',(-1.82112530082274,1.51946100860762,2.5429790002577));
#90013=CARTESIAN_POINT('Ctrl Pts',(-1.82950673886376,1.50934802717908,2.54387055359561));
#90014=CARTESIAN_POINT('Ctrl Pts',(-1.83288834822098,1.50523974156532,2.54423074264525));
#90015=CARTESIAN_POINT('Ctrl Pts',(-1.8397582844834,1.49683604134153,2.54496340982437));
#90016=CARTESIAN_POINT('Ctrl Pts',(-1.84324544983761,1.49253974595222,2.5453358052255));
#90017=CARTESIAN_POINT('Ctrl Pts',(-1.85209113095659,1.48156330988285,2.54628182071857));
#90018=CARTESIAN_POINT('Ctrl Pts',(-1.85742861932592,1.47486620692848,2.54685395242977));
#90019=CARTESIAN_POINT('Ctrl Pts',(-1.87896812733793,1.44753756110674,2.54916882430191));
#90020=CARTESIAN_POINT('Ctrl Pts',(-1.89486435107056,1.4266658501725,2.55089122107487));
#90021=CARTESIAN_POINT('Ctrl Pts',(-2.01761659093699,1.25982008788307,2.56434300730369));
#90022=CARTESIAN_POINT('Ctrl Pts',(-2.10781327456002,1.10229981245227,2.57519302598397));
#90023=CARTESIAN_POINT('Ctrl Pts',(-2.20487199990845,0.876333053352151,
2.59032852451187));
#90024=CARTESIAN_POINT('Ctrl Pts',(-2.22805070696789,0.815603780212274,
2.59435328726515));
#90025=CARTESIAN_POINT('Ctrl Pts',(-2.27263976342893,0.682623132077742,
2.60317515425029));
#90026=CARTESIAN_POINT('Ctrl Pts',(-2.29315914998258,0.610151739996926,
2.6079888559906));
#90027=CARTESIAN_POINT('Ctrl Pts',(-2.31435896754865,0.518920793631756,
2.61411862348711));
#90028=CARTESIAN_POINT('Ctrl Pts',(-2.31831267809239,0.500961591130818,
2.61532850041726));
#90029=CARTESIAN_POINT('Ctrl Pts',(-2.3242384920234,0.472470376827446,2.61725376837726));
#90030=CARTESIAN_POINT('Ctrl Pts',(-2.3263488025736,0.461967603992343,2.6179647378172));
#90031=CARTESIAN_POINT('Ctrl Pts',(-2.33014774546769,0.442374310960973,
2.61929357177407));
#90032=CARTESIAN_POINT('Ctrl Pts',(-2.33185451964203,0.433287481653748,
2.61991084460867));
#90033=CARTESIAN_POINT('Ctrl Pts',(-2.33509298476828,0.415472430566613,
2.62112307619704));
#90034=CARTESIAN_POINT('Ctrl Pts',(-2.33662897736577,0.406745137039638,
2.62171788683566));
#90035=CARTESIAN_POINT('Ctrl Pts',(-2.33997165757585,0.3871084869775,2.62305846729474));
#90036=CARTESIAN_POINT('Ctrl Pts',(-2.34175102017584,0.376194751720824,
2.62380509119799));
#90037=CARTESIAN_POINT('Ctrl Pts',(-2.34604114327896,0.348670646471449,
2.62569211847097));
#90038=CARTESIAN_POINT('Ctrl Pts',(-2.34845183229614,0.332045526566707,
2.62683564431836));
#90039=CARTESIAN_POINT('Ctrl Pts',(-2.35703167715799,0.268098989516441,
2.63124902139752));
#90040=CARTESIAN_POINT('Ctrl Pts',(-2.3619465149035,0.220637391362148,2.63455631919237));
#90041=CARTESIAN_POINT('Ctrl Pts',(-2.36542650247982,0.173076641595803,
2.63790316127816));
#90042=CARTESIAN_POINT('Origin',(0.,0.,-1.84858989190503));
#90043=CARTESIAN_POINT('',(-2.36542646296203,0.17307718168185,3.83677864400945));
#90044=CARTESIAN_POINT('',(-2.36847158556395,0.173320321679478,3.63969887294137));
#90045=CARTESIAN_POINT('',(-2.36542649454111,0.173076750093529,-1.84858989190503));
#90046=CARTESIAN_POINT('Ctrl Pts',(-2.36542646296204,0.173077181681802,
3.83677864400945));
#90047=CARTESIAN_POINT('Ctrl Pts',(-2.35656887892582,0.29413279093999,3.82791154518428));
#90048=CARTESIAN_POINT('Ctrl Pts',(-2.33842529469647,0.414417477642174,
3.81903475289074));
#90049=CARTESIAN_POINT('Ctrl Pts',(-2.30685655361473,0.551334760411727,
3.80917456728547));
#90050=CARTESIAN_POINT('Ctrl Pts',(-2.30237760527083,0.569749587144351,
3.80785386742358));
#90051=CARTESIAN_POINT('Ctrl Pts',(-2.29522651061167,0.597688121299326,
3.805860428478));
#90052=CARTESIAN_POINT('Ctrl Pts',(-2.29271483377461,0.607251615593695,
3.80517991262023));
#90053=CARTESIAN_POINT('Ctrl Pts',(-2.2879480781524,0.624950327913153,3.80392429428456));
#90054=CARTESIAN_POINT('Ctrl Pts',(-2.28570924283121,0.633089711975873,
3.80334834234869));
#90055=CARTESIAN_POINT('Ctrl Pts',(-2.28195222982755,0.646468744496542,
3.80240427745691));
#90056=CARTESIAN_POINT('Ctrl Pts',(-2.28045937203958,0.65171532961237,3.80203473584951));
#90057=CARTESIAN_POINT('Ctrl Pts',(-2.27749625386085,0.661994230146577,
3.80131212978613));
#90058=CARTESIAN_POINT('Ctrl Pts',(-2.27602739088326,0.667026883975227,
3.80095899142415));
#90059=CARTESIAN_POINT('Ctrl Pts',(-2.27236340333756,0.679427501577436,
3.80009037572077));
#90060=CARTESIAN_POINT('Ctrl Pts',(-2.27014909308326,0.686789826694812,
3.79957600631263));
#90061=CARTESIAN_POINT('Ctrl Pts',(-2.26238952534064,0.712141889283573,
3.79780896609926));
#90062=CARTESIAN_POINT('Ctrl Pts',(-2.25666573966031,0.730076865422134,
3.79656618069694));
#90063=CARTESIAN_POINT('Ctrl Pts',(-2.20506092858362,0.885367462522205,
3.78585346629572));
#90064=CARTESIAN_POINT('Ctrl Pts',(-2.14689565500221,1.01834203679391,3.77699668770544));
#90065=CARTESIAN_POINT('Ctrl Pts',(-2.03403167844092,1.22303501917587,3.76267448642867));
#90066=CARTESIAN_POINT('Ctrl Pts',(-1.98677025343337,1.29840002093787,3.75723492263853));
#90067=CARTESIAN_POINT('Ctrl Pts',(-1.8823928743076,1.44575318359468,3.74597893702903));
#90068=CARTESIAN_POINT('Ctrl Pts',(-1.82510503389702,1.51743000952789,3.74016516949508));
#90069=CARTESIAN_POINT('Ctrl Pts',(-1.74970440788952,1.60130515005882,3.73280617770581));
#90070=CARTESIAN_POINT('Ctrl Pts',(-1.73538291934173,1.61681470011158,3.73142044335896));
#90071=CARTESIAN_POINT('Ctrl Pts',(-1.71456293996811,1.63876649756727,3.72942174838033));
#90072=CARTESIAN_POINT('Ctrl Pts',(-1.70823094212641,1.64536584170514,3.72881592934065));
#90073=CARTESIAN_POINT('Ctrl Pts',(-1.69539080688644,1.65859409454865,3.72759142424398));
#90074=CARTESIAN_POINT('Ctrl Pts',(-1.6888815803483,1.66522171553472,3.72697269666013));
#90075=CARTESIAN_POINT('Ctrl Pts',(-1.67625406469718,1.67792871210869,3.72577618594853));
#90076=CARTESIAN_POINT('Ctrl Pts',(-1.67014120874367,1.68401329916968,3.72519864863319));
#90077=CARTESIAN_POINT('Ctrl Pts',(-1.65393497670828,1.69996955269224,3.72367180830487));
#90078=CARTESIAN_POINT('Ctrl Pts',(-1.64378653537458,1.70978454734174,3.72272004649197));
#90079=CARTESIAN_POINT('Ctrl Pts',(-1.60747956938144,1.74427655561821,3.71932984637613));
#90080=CARTESIAN_POINT('Ctrl Pts',(-1.58084926410761,1.76844751834255,3.71686998597352));
#90081=CARTESIAN_POINT('Ctrl Pts',(-1.41759214870149,1.90999277741035,3.70193893214385));
#90082=CARTESIAN_POINT('Ctrl Pts',(-1.26852862893191,2.01207654313201,3.68885038268129));
#90083=CARTESIAN_POINT('Ctrl Pts',(-1.00216819019323,2.15303799366413,3.66683807474532));
#90084=CARTESIAN_POINT('Ctrl Pts',(-0.890742161834415,2.20147635933036,
3.65799911947042));
#90085=CARTESIAN_POINT('Ctrl Pts',(-0.756677877038248,2.24790093655933,
3.64811483551695));
#90086=CARTESIAN_POINT('Ctrl Pts',(-0.737179557286774,2.2543705113912,3.64669541061935));
#90087=CARTESIAN_POINT('Ctrl Pts',(-0.710086085275302,2.26297104328652,
3.6447504037421));
#90088=CARTESIAN_POINT('Ctrl Pts',(-0.70256136451534,2.26531845991792,3.6442131087879));
#90089=CARTESIAN_POINT('Ctrl Pts',(-0.689924408600538,2.26919166936752,
3.64331579021148));
#90090=CARTESIAN_POINT('Ctrl Pts',(-0.684818533596174,2.27073778752834,
3.64295460143326));
#90091=CARTESIAN_POINT('Ctrl Pts',(-0.675130587241533,2.27363576113205,
3.64227192246454));
#90092=CARTESIAN_POINT('Ctrl Pts',(-0.670549590521043,2.27499101796484,
3.64195022994878));
#90093=CARTESIAN_POINT('Ctrl Pts',(-0.658539022661996,2.27850483317734,
3.64110965250314));
#90094=CARTESIAN_POINT('Ctrl Pts',(-0.651102851013865,2.28064091886693,
3.64059206567495));
#90095=CARTESIAN_POINT('Ctrl Pts',(-0.625256367238367,2.28792875970234,
3.63880247710767));
#90096=CARTESIAN_POINT('Ctrl Pts',(-0.606793722784177,2.29289445240452,
3.63754070039832));
#90097=CARTESIAN_POINT('Ctrl Pts',(-0.461076736284444,2.33020290816188,
3.62769721174357));
#90098=CARTESIAN_POINT('Ctrl Pts',(-0.33137783749447,2.35215553918783,3.61961639691837));
#90099=CARTESIAN_POINT('Ctrl Pts',(-0.0680890373155831,2.37449453399542,
3.60341336567613));
#90100=CARTESIAN_POINT('Ctrl Pts',(0.0650362530732931,2.37457950498845,
3.59531504719973));
#90101=CARTESIAN_POINT('Ctrl Pts',(0.242549305730111,2.359748881488,3.58406372648677));
#90102=CARTESIAN_POINT('Ctrl Pts',(0.287515412286639,2.35469306867313,3.58117599946213));
#90103=CARTESIAN_POINT('Ctrl Pts',(0.363967415982026,2.34387461484409,3.57618248303863));
#90104=CARTESIAN_POINT('Ctrl Pts',(0.395532273510814,2.33875491460261,3.57409625264696));
#90105=CARTESIAN_POINT('Ctrl Pts',(0.439855407764579,2.33064294503791,3.57112779887556));
#90106=CARTESIAN_POINT('Ctrl Pts',(0.45270807554578,2.32818055651806,3.57026237543125));
#90107=CARTESIAN_POINT('Ctrl Pts',(0.474735912751121,2.32377103837879,3.56877087926951));
#90108=CARTESIAN_POINT('Ctrl Pts',(0.483921216123206,2.32187559483966,3.56814646768479));
#90109=CARTESIAN_POINT('Ctrl Pts',(0.501424639372227,2.31815528216538,3.56695175617748));
#90110=CARTESIAN_POINT('Ctrl Pts',(0.509744663805219,2.31633999137526,3.56638177208391));
#90111=CARTESIAN_POINT('Ctrl Pts',(0.531246865472527,2.31152711092782,3.56490319177167));
#90112=CARTESIAN_POINT('Ctrl Pts',(0.544413360712654,2.30846158644601,3.56399242662124));
#90113=CARTESIAN_POINT('Ctrl Pts',(0.581976703452959,2.29937656894219,3.56137828508119));
#90114=CARTESIAN_POINT('Ctrl Pts',(0.606304433679942,2.29308184285837,3.55966612363967));
#90115=CARTESIAN_POINT('Ctrl Pts',(0.81797356332401,2.2347093202272,3.54459642125485));
#90116=CARTESIAN_POINT('Ctrl Pts',(0.998316528553454,2.16017133425058,3.53047671027753));
#90117=CARTESIAN_POINT('Ctrl Pts',(1.18874885762807,2.0524789858063,3.51449816613163));
#90118=CARTESIAN_POINT('Ctrl Pts',(1.20980862417159,2.04013650115321,3.51271656952236));
#90119=CARTESIAN_POINT('Ctrl Pts',(1.31407415198159,1.97684736065122,3.50383236829042));
#90120=CARTESIAN_POINT('Ctrl Pts',(1.39428058270697,1.92112003507617,3.49678906957557));
#90121=CARTESIAN_POINT('Ctrl Pts',(1.48554773892454,1.84897209317764,3.48870178608658));
#90122=CARTESIAN_POINT('Ctrl Pts',(1.5001243895938,1.83716541372752,3.48740790681232));
#90123=CARTESIAN_POINT('Ctrl Pts',(1.52030046454166,1.82042308376525,3.48561565096546));
#90124=CARTESIAN_POINT('Ctrl Pts',(1.52601852448462,1.81563244439876,3.48510755759805));
#90125=CARTESIAN_POINT('Ctrl Pts',(1.53572306853161,1.80742366146491,3.48424511151257));
#90126=CARTESIAN_POINT('Ctrl Pts',(1.53972094846687,1.80401913466382,3.48388978357505));
#90127=CARTESIAN_POINT('Ctrl Pts',(1.54739980197971,1.7974358313931,3.48320727652981));
#90128=CARTESIAN_POINT('Ctrl Pts',(1.55108232729112,1.79425899195246,3.48287995526891));
#90129=CARTESIAN_POINT('Ctrl Pts',(1.55991262760528,1.78659377048854,3.48209496754698));
#90130=CARTESIAN_POINT('Ctrl Pts',(1.56505087620746,1.78209440386842,3.48163810479394));
#90131=CARTESIAN_POINT('Ctrl Pts',(1.58378223970907,1.76554857306769,3.47997198748051));
#90132=CARTESIAN_POINT('Ctrl Pts',(1.59725672555464,1.75336788755086,3.47877222681043));
#90133=CARTESIAN_POINT('Ctrl Pts',(1.7277773004169,1.63262625133592,3.46712281047167));
#90134=CARTESIAN_POINT('Ctrl Pts',(1.83373822845497,1.51264753172426,3.4574248484245));
#90135=CARTESIAN_POINT('Ctrl Pts',(2.02494378528427,1.24623601691947,3.43732824743916));
#90136=CARTESIAN_POINT('Ctrl Pts',(2.10820379873936,1.09953045784547,3.42695877263075));
#90137=CARTESIAN_POINT('Ctrl Pts',(2.18350817719913,0.926239887498326,3.41462019402099));
#90138=CARTESIAN_POINT('Ctrl Pts',(2.19152475239492,0.907109422104458,3.41325762701685));
#90139=CARTESIAN_POINT('Ctrl Pts',(2.20341226479273,0.877663807018112,3.4111585331563));
#90140=CARTESIAN_POINT('Ctrl Pts',(2.20746409568505,0.867422403498191,3.41042811981367));
#90141=CARTESIAN_POINT('Ctrl Pts',(2.21441559590764,0.849487623037795,3.40914827010957));
#90142=CARTESIAN_POINT('Ctrl Pts',(2.21734689078835,0.841806638172909,3.40859990726908));
#90143=CARTESIAN_POINT('Ctrl Pts',(2.22387542189401,0.824428975056821,3.40735866074647));
#90144=CARTESIAN_POINT('Ctrl Pts',(2.2274492667578,0.81472374775033,3.40666500753011));
#90145=CARTESIAN_POINT('Ctrl Pts',(2.23693798535761,0.788426775510335,3.40478417454047));
#90146=CARTESIAN_POINT('Ctrl Pts',(2.24273158882932,0.771792278964785,3.403592998043));
#90147=CARTESIAN_POINT('Ctrl Pts',(2.26885293220143,0.694014479618448,3.39801562237932));
#90148=CARTESIAN_POINT('Ctrl Pts',(2.28686716492283,0.632128870352567,3.39355446507987));
#90149=CARTESIAN_POINT('Ctrl Pts',(2.35423213896257,0.359833805519979,3.37381027869488));
#90150=CARTESIAN_POINT('Ctrl Pts',(2.37721148295844,0.143977061040169,3.35774185953928));
#90151=CARTESIAN_POINT('Ctrl Pts',(2.36935363813576,-0.114942583988793,
3.33913191624066));
#90152=CARTESIAN_POINT('Ctrl Pts',(2.36687917453508,-0.157898383368767,
3.33607131716526));
#90153=CARTESIAN_POINT('Ctrl Pts',(2.36102481389732,-0.226810794523148,
3.3312273486414));
#90154=CARTESIAN_POINT('Ctrl Pts',(2.35838165075067,-0.252818990104549,
3.32941441903419));
#90155=CARTESIAN_POINT('Ctrl Pts',(2.35431242776139,-0.287198408725764,
3.32704271485801));
#90156=CARTESIAN_POINT('Ctrl Pts',(2.35327079589853,-0.295612077256806,
3.3264642585685));
#90157=CARTESIAN_POINT('Ctrl Pts',(2.35148382452944,-0.309437758480717,
3.32551715608932));
#90158=CARTESIAN_POINT('Ctrl Pts',(2.35076487259093,-0.314853011332579,
3.32514706354511));
#90159=CARTESIAN_POINT('Ctrl Pts',(2.34932004066704,-0.3254548124308,3.32442427578435));
#90160=CARTESIAN_POINT('Ctrl Pts',(2.34859568372984,-0.330641503205517,
3.32407150190324));
#90161=CARTESIAN_POINT('Ctrl Pts',(2.34676963400772,-0.343407938821845,
3.32320515132843));
#90162=CARTESIAN_POINT('Ctrl Pts',(2.34564837960225,-0.350984915519029,
3.32269266936383));
#90163=CARTESIAN_POINT('Ctrl Pts',(2.34167050153528,-0.376995036843662,
3.32093887204118));
#90164=CARTESIAN_POINT('Ctrl Pts',(2.33863305326271,-0.395400419141881,
3.31970724499628));
#90165=CARTESIAN_POINT('Ctrl Pts',(2.30924274821025,-0.561284117958674,
3.30867620028092));
#90166=CARTESIAN_POINT('Ctrl Pts',(2.26918470437125,-0.706014158090181,
3.29953470311035));
#90167=CARTESIAN_POINT('Ctrl Pts',(2.17251748492362,-0.959188039062189,
3.28293068048594));
#90168=CARTESIAN_POINT('Ctrl Pts',(2.12070087630864,-1.06887728099209,3.27550706518723));
#90169=CARTESIAN_POINT('Ctrl Pts',(2.04004690504821,-1.21043511997938,3.26518619782473));
#90170=CARTESIAN_POINT('Ctrl Pts',(2.01840334388994,-1.24619106956255,3.26251221719427));
#90171=CARTESIAN_POINT('Ctrl Pts',(1.97957029422061,-1.30667708803672,3.25785676284712));
#90172=CARTESIAN_POINT('Ctrl Pts',(1.9628333342493,-1.33168642331388,3.25589142400215));
#90173=CARTESIAN_POINT('Ctrl Pts',(1.93831935632939,-1.36685015952646,3.25306623588185));
#90174=CARTESIAN_POINT('Ctrl Pts',(1.93092857231915,-1.37727125996728,3.25222103930754));
#90175=CARTESIAN_POINT('Ctrl Pts',(1.91799974163037,-1.39519244699974,3.25075349610613));
#90176=CARTESIAN_POINT('Ctrl Pts',(1.91250094725718,-1.40272060494509,3.25013267256989));
#90177=CARTESIAN_POINT('Ctrl Pts',(1.90185650287572,-1.41711450440887,3.2489371565414));
#90178=CARTESIAN_POINT('Ctrl Pts',(1.89671769023006,-1.4239851390905,3.2483627373792));
#90179=CARTESIAN_POINT('Ctrl Pts',(1.88451959377135,-1.44011091689343,3.24700554836889));
#90180=CARTESIAN_POINT('Ctrl Pts',(1.87742928520924,-1.44934220350858,3.24622156446382));
#90181=CARTESIAN_POINT('Ctrl Pts',(1.85246456520938,-1.48135463892201,3.24347783010588));
#90182=CARTESIAN_POINT('Ctrl Pts',(1.83424176619718,-1.50385954963592,3.24150427973066));
#90183=CARTESIAN_POINT('Ctrl Pts',(1.7125492387606,-1.64864520560762,3.22850575714423));
#90184=CARTESIAN_POINT('Ctrl Pts',(1.59734837507036,-1.76048753739628,3.21698770460297));
#90185=CARTESIAN_POINT('Ctrl Pts',(1.38002655112039,-1.93246380846643,3.19676496389404));
#90186=CARTESIAN_POINT('Ctrl Pts',(1.28301869734184,-1.9981879664131,3.18817689086393));
#90187=CARTESIAN_POINT('Ctrl Pts',(1.15296112781332,-2.07291244164711,3.17748587302104));
#90188=CARTESIAN_POINT('Ctrl Pts',(1.12402906074737,-2.08874226728799,3.17515704205183));
#90189=CARTESIAN_POINT('Ctrl Pts',(1.07566590984934,-2.11390750204913,3.17135580629137));
#90190=CARTESIAN_POINT('Ctrl Pts',(1.05642159343243,-2.12359025629358,3.16986665403269));
#90191=CARTESIAN_POINT('Ctrl Pts',(1.02996336632331,-2.13645397065153,3.16785367011867));
#90192=CARTESIAN_POINT('Ctrl Pts',(1.02286230506093,-2.13986280262467,3.16731675476663));
#90193=CARTESIAN_POINT('Ctrl Pts',(1.01092455167749,-2.14552046379537,3.16641989280561));
#90194=CARTESIAN_POINT('Ctrl Pts',(1.00609707233937,-2.14778844222199,3.16605878354222));
#90195=CARTESIAN_POINT('Ctrl Pts',(0.996930428107869,-2.15205729817039,
3.16537612223321));
#90196=CARTESIAN_POINT('Ctrl Pts',(0.992592813292142,-2.1540613735774,3.16505436859447));
#90197=CARTESIAN_POINT('Ctrl Pts',(0.98121133816629,-2.15927819162227,3.16421338766116));
#90198=CARTESIAN_POINT('Ctrl Pts',(0.974157677210408,-2.16246961207071,
3.1636954608976));
#90199=CARTESIAN_POINT('Ctrl Pts',(0.949604311915052,-2.1734342334525,3.16190349122837));
#90200=CARTESIAN_POINT('Ctrl Pts',(0.932025628427168,-2.18103026164378,
3.16063970951804));
#90201=CARTESIAN_POINT('Ctrl Pts',(0.800822280802883,-2.23584925648303,
3.15133464740293));
#90202=CARTESIAN_POINT('Ctrl Pts',(0.683752834467941,-2.27438529626563,
3.14373194742638));
#90203=CARTESIAN_POINT('Ctrl Pts',(0.463161426831023,-2.3284119710937,3.12979157711026));
#90204=CARTESIAN_POINT('Ctrl Pts',(0.360597779832508,-2.34648446148754,
3.12345509000767));
#90205=CARTESIAN_POINT('Ctrl Pts',(0.164582677678252,-2.36786555890214,
3.1111921124064));
#90206=CARTESIAN_POINT('Ctrl Pts',(0.071478311598831,-2.37250133709471,
3.10530347247293));
#90207=CARTESIAN_POINT('Ctrl Pts',(-0.0461983933535427,-2.37142708612143,
3.0976457388164));
#90208=CARTESIAN_POINT('Ctrl Pts',(-0.070740632490637,-2.37082188393347,
3.09603715276356));
#90209=CARTESIAN_POINT('Ctrl Pts',(-0.107036589293985,-2.36936277233319,
3.0936392259401));
#90210=CARTESIAN_POINT('Ctrl Pts',(-0.118800982850021,-2.36880203823712,
3.09285905303097));
#90211=CARTESIAN_POINT('Ctrl Pts',(-0.139717212163434,-2.36764888923943,
3.09146650648274));
#90212=CARTESIAN_POINT('Ctrl Pts',(-0.148870772264499,-2.36709096808548,
3.09085522654525));
#90213=CARTESIAN_POINT('Ctrl Pts',(-0.168142499546943,-2.36580410618132,
3.08956422448299));
#90214=CARTESIAN_POINT('Ctrl Pts',(-0.178259662493634,-2.36506330912125,
3.08888414184679));
#90215=CARTESIAN_POINT('Ctrl Pts',(-0.205032001228322,-2.36293022983492,
3.08707813150628));
#90216=CARTESIAN_POINT('Ctrl Pts',(-0.221677495004204,-2.36142678391804,
3.08594873585244));
#90217=CARTESIAN_POINT('Ctrl Pts',(-0.29381504072408,-2.3541417832623,3.081024943442));
#90218=CARTESIAN_POINT('Ctrl Pts',(-0.349105209863459,-2.3465795229204,
3.07717523007461));
#90219=CARTESIAN_POINT('Ctrl Pts',(-0.626428686081089,-2.29863110387524,
3.05746655688346));
#90220=CARTESIAN_POINT('Ctrl Pts',(-0.842145272190765,-2.22864907360465,
3.04068218685984));
#90221=CARTESIAN_POINT('Ctrl Pts',(-1.10283636837371,-2.10074944757143,
3.01981333034785));
#90222=CARTESIAN_POINT('Ctrl Pts',(-1.15981875370415,-2.06983538036067,
3.01522376274076));
#90223=CARTESIAN_POINT('Ctrl Pts',(-1.22513166740634,-2.03085624505323,
3.00998786710767));
#90224=CARTESIAN_POINT('Ctrl Pts',(-1.23475362993853,-2.02502053732562,
3.00921717592305));
#90225=CARTESIAN_POINT('Ctrl Pts',(-1.249503371715,-2.0159306186073,3.00803722566984));
#90226=CARTESIAN_POINT('Ctrl Pts',(-1.25466063264682,-2.0127249275449,3.00762493256777));
#90227=CARTESIAN_POINT('Ctrl Pts',(-1.26413655749831,-2.00678423253315,
3.00686798184273));
#90228=CARTESIAN_POINT('Ctrl Pts',(-1.2684586720845,-2.00405508660435,3.00652296308584));
#90229=CARTESIAN_POINT('Ctrl Pts',(-1.27819918946859,-1.99786042078286,
3.00574592554362));
#90230=CARTESIAN_POINT('Ctrl Pts',(-1.283612331824,-1.99438682630894,3.00531444876674));
#90231=CARTESIAN_POINT('Ctrl Pts',(-1.29956699145617,-1.98405691101932,
3.00404354235361));
#90232=CARTESIAN_POINT('Ctrl Pts',(-1.31006839351826,-1.97713859226048,
3.0032080985197));
#90233=CARTESIAN_POINT('Ctrl Pts',(-1.40208920424571,-1.91546022824193,
2.99589211255175));
#90234=CARTESIAN_POINT('Ctrl Pts',(-1.48020063201021,-1.85576218044727,
2.9897135449707));
#90235=CARTESIAN_POINT('Ctrl Pts',(-1.63708275543549,-1.71963472855321,
2.97685381711691));
#90236=CARTESIAN_POINT('Ctrl Pts',(-1.71470560885042,-1.64224512723675,
2.97020875888437));
#90237=CARTESIAN_POINT('Ctrl Pts',(-1.84376628626021,-1.49440692543913,
2.95811091692015));
#90238=CARTESIAN_POINT('Ctrl Pts',(-1.89719264454364,-1.42596785963892,
2.95270740581405));
#90239=CARTESIAN_POINT('Ctrl Pts',(-1.97599425139401,-1.31273245209263,
2.94390474504922));
#90240=CARTESIAN_POINT('Ctrl Pts',(-2.0038710099289,-1.26977168280228,2.94059479357627));
#90241=CARTESIAN_POINT('Ctrl Pts',(-2.03840440031615,-1.21257961467826,
2.93620795143912));
#90242=CARTESIAN_POINT('Ctrl Pts',(-2.04634222440281,-1.19913523102338,
2.93517812215102));
#90243=CARTESIAN_POINT('Ctrl Pts',(-2.05909681324737,-1.17703714413883,
2.93348721633614));
#90244=CARTESIAN_POINT('Ctrl Pts',(-2.0639932201703,-1.16842976126621,2.93282903407027));
#90245=CARTESIAN_POINT('Ctrl Pts',(-2.07335558941737,-1.15172917984353,
2.93155270441238));
#90246=CARTESIAN_POINT('Ctrl Pts',(-2.07782843087107,-1.14364002708499,
2.9309348187649));
#90247=CARTESIAN_POINT('Ctrl Pts',(-2.08804154648656,-1.12491186313096,
2.92950490658579));
#90248=CARTESIAN_POINT('Ctrl Pts',(-2.0937479524662,-1.11425477417677,2.92869169213439));
#90249=CARTESIAN_POINT('Ctrl Pts',(-2.11189784904858,-1.07972690279284,
2.92605815058622));
#90250=CARTESIAN_POINT('Ctrl Pts',(-2.12401610371344,-1.05568849394934,
2.9242264636216));
#90251=CARTESIAN_POINT('Ctrl Pts',(-2.22441002246677,-0.847812645576312,
2.90839568709296));
#90252=CARTESIAN_POINT('Ctrl Pts',(-2.28902577512322,-0.653538321798643,
2.89354965260473));
#90253=CARTESIAN_POINT('Ctrl Pts',(-2.35073967197113,-0.33670268620984,
2.86998697049575));
#90254=CARTESIAN_POINT('Ctrl Pts',(-2.36466843310237,-0.21839321420602,
2.86135210729747));
#90255=CARTESIAN_POINT('Ctrl Pts',(-2.37030206316532,-0.0842595329870371,
2.85205830356647));
#90256=CARTESIAN_POINT('Ctrl Pts',(-2.37079573292328,-0.0689866878830017,
2.85100743750445));
#90257=CARTESIAN_POINT('Ctrl Pts',(-2.37129733476559,-0.046842264251883,
2.84949543001245));
#90258=CARTESIAN_POINT('Ctrl Pts',(-2.37142305786338,-0.0399741320860062,
2.84902810423781));
#90259=CARTESIAN_POINT('Ctrl Pts',(-2.37159088964592,-0.027951448455367,
2.84821300782077));
#90260=CARTESIAN_POINT('Ctrl Pts',(-2.37164603641732,-0.02279717871641,
2.84786452135961));
#90261=CARTESIAN_POINT('Ctrl Pts',(-2.37172741255881,-0.0118578461686369,
2.84712695927788));
#90262=CARTESIAN_POINT('Ctrl Pts',(-2.37174928065598,-0.00607285206230565,
2.8467381283931));
#90263=CARTESIAN_POINT('Ctrl Pts',(-2.3717511875859,0.00964443574313672,
2.84568485882211));
#90264=CARTESIAN_POINT('Ctrl Pts',(-2.37169000297992,0.0195767578266909,
2.84502267455331));
#90265=CARTESIAN_POINT('Ctrl Pts',(-2.37105122836884,0.070914175783284,
2.84161631971275));
#90266=CARTESIAN_POINT('Ctrl Pts',(-2.36945172122315,0.112302292666018,
2.83892488329156));
#90267=CARTESIAN_POINT('Ctrl Pts',(-2.36634812415,0.160115107416461,2.83585712621301));
#90268=CARTESIAN_POINT('Ctrl Pts',(-2.36590059103696,0.166597310392362,
2.83544210089004));
#90269=CARTESIAN_POINT('Ctrl Pts',(-2.36542649402054,0.173076757208175,
2.83502806412758));
#90270=CARTESIAN_POINT('',(-2.36993516591118,-0.00198226883289276,2.65141112235218));
#90271=CARTESIAN_POINT('Ctrl Pts',(-2.36542650247982,0.173076641595803,
2.63790316127816));
#90272=CARTESIAN_POINT('Ctrl Pts',(-2.36968965435484,0.114812439469591,
2.6420032035342));
#90273=CARTESIAN_POINT('Ctrl Pts',(-2.371799477955,0.0563994550688975,2.64616284491173));
#90274=CARTESIAN_POINT('Ctrl Pts',(-2.37174911952633,-0.00204365507856347,
2.65036731141953));
#90275=CARTESIAN_POINT('Ctrl Pts',(-2.36993516591118,-0.00198226883289275,
2.65141112235218));
#90276=CARTESIAN_POINT('Ctrl Pts',(-2.37186914624274,-0.249525648545458,
2.66799504931007));
#90277=CARTESIAN_POINT('Ctrl Pts',(-2.22218144459194,-1.28536352789007,
2.73754295476256));
#90278=CARTESIAN_POINT('Ctrl Pts',(-0.720433887694406,-2.70989311549094,
2.86005483870968));
#90279=CARTESIAN_POINT('Ctrl Pts',(1.88762043170213,-2.07350795749998,3.01894677419355));
#90280=CARTESIAN_POINT('Ctrl Pts',(2.76545213444046,0.463487386787571,3.17783870967742));
#90281=CARTESIAN_POINT('Ctrl Pts',(1.10842681518721,2.57564282834349,3.33673064516129));
#90282=CARTESIAN_POINT('Ctrl Pts',(-1.48151917809488,2.33465397998857,3.49068403291595));
#90283=CARTESIAN_POINT('Ctrl Pts',(-2.31143607334521,0.884136787947507,
3.59167344217597));
#90284=CARTESIAN_POINT('Ctrl Pts',(-2.36847158556395,0.173320321679478,
3.63969887294137));
#90285=CARTESIAN_POINT('Origin',(0.,0.,-1.84858989190503));
#90286=CARTESIAN_POINT('',(-2.36152614656945,0.172792042906829,4.83696616984731));
#90287=CARTESIAN_POINT('',(-2.36542650810962,0.173076564653691,4.64035944112689));
#90288=CARTESIAN_POINT('',(-2.36542649454111,0.173076750093529,-1.84858989190503));
#90289=CARTESIAN_POINT('',(-2.37061499902234,0.00211578448275317,3.84858989190501));
#90290=CARTESIAN_POINT('Ctrl Pts',(-2.37061499902234,0.00211578448275317,
3.84858989190501));
#90291=CARTESIAN_POINT('Ctrl Pts',(-2.36573802108978,-0.565818237034438,
3.88666572659761));
#90292=CARTESIAN_POINT('Ctrl Pts',(-1.87624458737536,-1.93166428036642,
3.97772985001846));
#90293=CARTESIAN_POINT('Ctrl Pts',(0.40722627036569,-2.77473424763259,4.12178226216756));
#90294=CARTESIAN_POINT('Ctrl Pts',(2.55350060517878,-1.1595766637486,4.2807471283523));
#90295=CARTESIAN_POINT('Ctrl Pts',(2.35722861767805,1.51936059698208,4.43971199453706));
#90296=CARTESIAN_POINT('Ctrl Pts',(-0.00153247116466099,2.80445735060936,
4.5986768607218));
#90297=CARTESIAN_POINT('Ctrl Pts',(-1.96521418831998,1.73182241497003,4.73109491915855));
#90298=CARTESIAN_POINT('Ctrl Pts',(-2.33268167915334,0.567299710385224,
4.81052468886706));
#90299=CARTESIAN_POINT('Ctrl Pts',(-2.36152614656945,0.172792042906829,
4.83696616984731));
#90300=CARTESIAN_POINT('Ctrl Pts',(-2.37174901274681,0.00216403200924694,
3.8492415291672));
#90301=CARTESIAN_POINT('Ctrl Pts',(-2.37169694361488,0.0592310771005431,
3.84510489340989));
#90302=CARTESIAN_POINT('Ctrl Pts',(-2.36958528398647,0.116239040395148,
3.84094193242637));
#90303=CARTESIAN_POINT('Ctrl Pts',(-2.36542646296204,0.1730771816818,3.83677864400945));
#90304=CARTESIAN_POINT('',(-2.37532752442066,-0.000269425568870816,3.65157275994242));
#90305=CARTESIAN_POINT('Ctrl Pts',(-2.36847158556395,0.173320321679478,
3.63969887294137));
#90306=CARTESIAN_POINT('Ctrl Pts',(-2.37310753894245,0.115543826473337,
3.64360247000484));
#90307=CARTESIAN_POINT('Ctrl Pts',(-2.37551285241125,0.0576284297436606,
3.64750606706831));
#90308=CARTESIAN_POINT('Ctrl Pts',(-2.37561175167707,-0.000280201698186815,
3.65140966413178));
#90309=CARTESIAN_POINT('Ctrl Pts',(-2.37174999622658,-0.000133787956428912,
3.65362562379593));
#90310=CARTESIAN_POINT('Ctrl Pts',(-2.37174970721966,-0.00525720993116726,
3.65397696200977));
#90311=CARTESIAN_POINT('Ctrl Pts',(-2.37173281688968,-0.0103806823582881,
3.65432745743365));
#90312=CARTESIAN_POINT('Ctrl Pts',(-2.37165813786147,-0.0218044944275061,
3.65510701147203));
#90313=CARTESIAN_POINT('Ctrl Pts',(-2.37159184582707,-0.0281047681602935,
3.65553561857383));
#90314=CARTESIAN_POINT('Ctrl Pts',(-2.37142817895413,-0.0393862208450815,
3.65630064254654));
#90315=CARTESIAN_POINT('Ctrl Pts',(-2.37134021411968,-0.0443674787193265,
3.65663757609617));
#90316=CARTESIAN_POINT('Ctrl Pts',(-2.37113220301038,-0.0543625767235476,
3.65731188805149));
#90317=CARTESIAN_POINT('Ctrl Pts',(-2.37101195003731,-0.0593763242050389,
3.6576492561793));
#90318=CARTESIAN_POINT('Ctrl Pts',(-2.37063889617656,-0.0731124373295902,
3.65857121978151));
#90319=CARTESIAN_POINT('Ctrl Pts',(-2.37035385828226,-0.0818339603874946,
3.65915404171882));
#90320=CARTESIAN_POINT('Ctrl Pts',(-2.36905857400245,-0.115734776685101,
3.66141021118516));
#90321=CARTESIAN_POINT('Ctrl Pts',(-2.36769516245422,-0.140899999641985,
3.66306510932193));
#90322=CARTESIAN_POINT('Ctrl Pts',(-2.3554783169029,-0.314979866878836,
3.67440461141037));
#90323=CARTESIAN_POINT('Ctrl Pts',(-2.33098360872185,-0.462620410842606,
3.68348708673121));
#90324=CARTESIAN_POINT('Ctrl Pts',(-2.26534192715558,-0.710565442903368,
3.69920747378263));
#90325=CARTESIAN_POINT('Ctrl Pts',(-2.23093644588801,-0.812156119878761,
3.70579008512994));
#90326=CARTESIAN_POINT('Ctrl Pts',(-2.16373862707967,-0.973668583495306,
3.71684337424294));
#90327=CARTESIAN_POINT('Ctrl Pts',(-2.1350228904034,-1.03511895541834,3.72119531228255));
#90328=CARTESIAN_POINT('Ctrl Pts',(-2.09573142586352,-1.11058851939073,
3.72677172255028));
#90329=CARTESIAN_POINT('Ctrl Pts',(-2.08757893011206,-1.12583802252723,
3.72791068993445));
#90330=CARTESIAN_POINT('Ctrl Pts',(-2.07427427723968,-1.15008335178748,
3.72974181874075));
#90331=CARTESIAN_POINT('Ctrl Pts',(-2.06922851821134,-1.15913710443726,
3.73043018412476));
#90332=CARTESIAN_POINT('Ctrl Pts',(-2.05954863937798,-1.17624136389318,
3.73173950145989));
#90333=CARTESIAN_POINT('Ctrl Pts',(-2.05492624086863,-1.1842983088943,3.73236002262995));
#90334=CARTESIAN_POINT('Ctrl Pts',(-2.0443148118103,-1.20254509765448,3.73377403941285));
#90335=CARTESIAN_POINT('Ctrl Pts',(-2.03829673734783,-1.21271767670587,
3.73456857763485));
#90336=CARTESIAN_POINT('Ctrl Pts',(-2.02250023213568,-1.23896933817815,
3.73663542108274));
#90337=CARTESIAN_POINT('Ctrl Pts',(-2.01260617453459,-1.25497751394195,
3.73791192567507));
#90338=CARTESIAN_POINT('Ctrl Pts',(-1.91658393600196,-1.40628123413224,
3.75013453113387));
#90339=CARTESIAN_POINT('Ctrl Pts',(-1.8171485330118,-1.53260343623574,3.76159306645173));
#90340=CARTESIAN_POINT('Ctrl Pts',(-1.65596131908237,-1.69944869451329,
3.77849059041007));
#90341=CARTESIAN_POINT('Ctrl Pts',(-1.60385871365316,-1.74870550438995,
3.78373875413573));
#90342=CARTESIAN_POINT('Ctrl Pts',(-1.47383411763604,-1.86092149620778,
3.79624160657363));
#90343=CARTESIAN_POINT('Ctrl Pts',(-1.39398922261316,-1.92146157633635,
3.80345633987108));
#90344=CARTESIAN_POINT('Ctrl Pts',(-1.30175906154513,-1.98260753120884,
3.81111537666522));
#90345=CARTESIAN_POINT('Ctrl Pts',(-1.29293046844369,-1.98837624479221,
3.81184199963821));
#90346=CARTESIAN_POINT('Ctrl Pts',(-1.27847826439515,-1.99768253729463,
3.81302050070138));
#90347=CARTESIAN_POINT('Ctrl Pts',(-1.27287786345306,-2.00125564077075,
3.81347452637887));
#90348=CARTESIAN_POINT('Ctrl Pts',(-1.26209889716921,-2.00806916010153,
3.8143431808272));
#90349=CARTESIAN_POINT('Ctrl Pts',(-1.25692268889739,-2.01131318651841,
3.81475803685688));
#90350=CARTESIAN_POINT('Ctrl Pts',(-1.24741519546511,-2.01722067335192,
3.81551577334873));
#90351=CARTESIAN_POINT('Ctrl Pts',(-1.24308788368918,-2.01989020232532,
3.81585904124444));
#90352=CARTESIAN_POINT('Ctrl Pts',(-1.23330739220442,-2.0258804754581,3.81663127023021));
#90353=CARTESIAN_POINT('Ctrl Pts',(-1.22784937818766,-2.02919312324305,
3.81705970142194));
#90354=CARTESIAN_POINT('Ctrl Pts',(-1.21221740224743,-2.03859451853526,
3.81827978580032));
#90355=CARTESIAN_POINT('Ctrl Pts',(-1.20201088927664,-2.04462917857802,
3.81906802919313));
#90356=CARTESIAN_POINT('Ctrl Pts',(-1.13319605022371,-2.08462295384708,
3.82432955625535));
#90357=CARTESIAN_POINT('Ctrl Pts',(-1.0731952255722,-2.11613801691913,3.82866089188509));
#90358=CARTESIAN_POINT('Ctrl Pts',(-0.87749173029746,-2.20846085825506,
3.84225084888042));
#90359=CARTESIAN_POINT('Ctrl Pts',(-0.737392594625412,-2.25910336498024,
3.85120452778059));
#90360=CARTESIAN_POINT('Ctrl Pts',(-0.486138510151893,-2.32403884228448,
3.86723646039136));
#90361=CARTESIAN_POINT('Ctrl Pts',(-0.377008688596753,-2.34421567352434,
3.87418864379667));
#90362=CARTESIAN_POINT('Ctrl Pts',(-0.240053621195826,-2.3597247765954,
3.88313845344956));
#90363=CARTESIAN_POINT('Ctrl Pts',(-0.213181660280136,-2.36230401188295,
3.88490461927424));
#90364=CARTESIAN_POINT('Ctrl Pts',(-0.173972016574562,-2.36539299873769,
3.88749897039356));
#90365=CARTESIAN_POINT('Ctrl Pts',(-0.161664457301236,-2.36626602362212,
3.88831578416466));
#90366=CARTESIAN_POINT('Ctrl Pts',(-0.140012976307824,-2.3676321445277,
3.88975730960645));
#90367=CARTESIAN_POINT('Ctrl Pts',(-0.130671824713955,-2.36816605736437,
3.89038072895759));
#90368=CARTESIAN_POINT('Ctrl Pts',(-0.111235292656852,-2.36916164488277,
3.89168113167471));
#90369=CARTESIAN_POINT('Ctrl Pts',(-0.101139650100711,-2.36961409423794,
3.89235839118452));
#90370=CARTESIAN_POINT('Ctrl Pts',(-0.0749404867581275,-2.37062051222863,
3.89412079326294));
#90371=CARTESIAN_POINT('Ctrl Pts',(-0.0588338876249706,-2.37107491253462,
3.89520902722751));
#90372=CARTESIAN_POINT('Ctrl Pts',(0.00656013330813427,-2.37225309905478,
3.89964742863056));
#90373=CARTESIAN_POINT('Ctrl Pts',(0.0558567489632089,-2.37160435045954,
3.90303993479772));
#90374=CARTESIAN_POINT('Ctrl Pts',(0.313039499773506,-2.3601971519408,3.92099558090533));
#90375=CARTESIAN_POINT('Ctrl Pts',(0.518842729267534,-2.32363885097875,
3.9363542566605));
#90376=CARTESIAN_POINT('Ctrl Pts',(0.774593047005348,-2.24250562374867,
3.9558100149284));
#90377=CARTESIAN_POINT('Ctrl Pts',(0.83129421337533,-2.22211089278136,3.96013938341992));
#90378=CARTESIAN_POINT('Ctrl Pts',(0.907677217471089,-2.19130315578729,
3.96594300835406));
#90379=CARTESIAN_POINT('Ctrl Pts',(0.928077527837284,-2.18274131177302,
3.96749011255936));
#90380=CARTESIAN_POINT('Ctrl Pts',(0.962990958682624,-2.16751042073987,
3.9701292799859));
#90381=CARTESIAN_POINT('Ctrl Pts',(0.97756171174331,-2.16097805291686,3.97122809751967));
#90382=CARTESIAN_POINT('Ctrl Pts',(0.998471007213169,-2.15134921296674,
3.97279999535397));
#90383=CARTESIAN_POINT('Ctrl Pts',(1.00486306061145,-2.14837101568828,3.97327986106315));
#90384=CARTESIAN_POINT('Ctrl Pts',(1.01598218928636,-2.14312988805785,3.97411330804923));
#90385=CARTESIAN_POINT('Ctrl Pts',(1.02071517915136,-2.14087973770407,3.97446766159697));
#90386=CARTESIAN_POINT('Ctrl Pts',(1.03069868576416,-2.13609276083518,3.97521420372924));
#90387=CARTESIAN_POINT('Ctrl Pts',(1.03594732396635,-2.13355225095705,3.97560616081146));
#90388=CARTESIAN_POINT('Ctrl Pts',(1.0500889258642,-2.12664277219426,3.97666095431636));
#90389=CARTESIAN_POINT('Ctrl Pts',(1.05896409323906,-2.12223733136424,3.97732157308264));
#90390=CARTESIAN_POINT('Ctrl Pts',(1.09924754701406,-2.10192586663983,3.9803150210401));
#90391=CARTESIAN_POINT('Ctrl Pts',(1.13032876996793,-2.08537639662299,3.98261067152649));
#90392=CARTESIAN_POINT('Ctrl Pts',(1.3763727253247,-1.94724991389,4.00076351122985));
#90393=CARTESIAN_POINT('Ctrl Pts',(1.57153143205635,-1.79346176049961,4.01518883974709));
#90394=CARTESIAN_POINT('Ctrl Pts',(1.78407782115422,-1.56415271190667,4.03496813084));
#90395=CARTESIAN_POINT('Ctrl Pts',(1.82668133820411,-1.51418011505167,4.0391853151012));
#90396=CARTESIAN_POINT('Ctrl Pts',(1.87770989534227,-1.44903299048138,4.04460994046612));
#90397=CARTESIAN_POINT('Ctrl Pts',(1.88811852017685,-1.4354440033568,4.04573756855323));
#90398=CARTESIAN_POINT('Ctrl Pts',(1.9045691203276,-1.41347839193573,4.04755476162712));
#90399=CARTESIAN_POINT('Ctrl Pts',(1.91070518600005,-1.40517272426412,4.04824063335782));
#90400=CARTESIAN_POINT('Ctrl Pts',(1.92226184314132,-1.38931418102175,4.04954799872266));
#90401=CARTESIAN_POINT('Ctrl Pts',(1.92769266202909,-1.38176896900196,4.05016908013848));
#90402=CARTESIAN_POINT('Ctrl Pts',(1.93996643793719,-1.36450342282666,4.05158826890566));
#90403=CARTESIAN_POINT('Ctrl Pts',(1.94678091135795,-1.35476324331788,4.05238744777883));
#90404=CARTESIAN_POINT('Ctrl Pts',(1.96432171480763,-1.32928588676958,4.05447436016386));
#90405=CARTESIAN_POINT('Ctrl Pts',(1.97493204283517,-1.31347027269504,4.05576642902));
#90406=CARTESIAN_POINT('Ctrl Pts',(2.06418426941142,-1.17690534560364,4.06689653573882));
#90407=CARTESIAN_POINT('Ctrl Pts',(2.13184646092771,-1.04937106700619,4.07714202908675));
#90408=CARTESIAN_POINT('Ctrl Pts',(2.22531539093317,-0.826280684265977,
4.09470715444235));
#90409=CARTESIAN_POINT('Ctrl Pts',(2.25749946991448,-0.733801162490264,
4.10188676800893));
#90410=CARTESIAN_POINT('Ctrl Pts',(2.30707275097781,-0.556784957029317,
4.11523832822761));
#90411=CARTESIAN_POINT('Ctrl Pts',(2.3257459865696,-0.472760990867566,4.12141632063393));
#90412=CARTESIAN_POINT('Ctrl Pts',(2.34271409477077,-0.37040932640452,4.12861986573909));
#90413=CARTESIAN_POINT('Ctrl Pts',(2.34541765901632,-0.352885889433598,
4.12984185161993));
#90414=CARTESIAN_POINT('Ctrl Pts',(2.34896453195006,-0.328051510826,4.13155613976685));
#90415=CARTESIAN_POINT('Ctrl Pts',(2.34997064001308,-0.320764962033692,
4.13205699365888));
#90416=CARTESIAN_POINT('Ctrl Pts',(2.35164185178808,-0.30823146073051,4.13291471475521));
#90417=CARTESIAN_POINT('Ctrl Pts',(2.35232332882057,-0.302986784280395,
4.13327248919099));
#90418=CARTESIAN_POINT('Ctrl Pts',(2.35370250739067,-0.292087367266539,
4.13401359199907));
#90419=CARTESIAN_POINT('Ctrl Pts',(2.35439738158168,-0.28643235634986,4.13439676152469));
#90420=CARTESIAN_POINT('Ctrl Pts',(2.35617359165118,-0.271533932111144,
4.13540284167518));
#90421=CARTESIAN_POINT('Ctrl Pts',(2.35722092668861,-0.262286447004037,
4.13602387464888));
#90422=CARTESIAN_POINT('Ctrl Pts',(2.36138660080207,-0.223463225092625,
4.13861759530537));
#90423=CARTESIAN_POINT('Ctrl Pts',(2.36400311925361,-0.19383484212269,4.14056412220954));
#90424=CARTESIAN_POINT('Ctrl Pts',(2.37727587942528,-0.00253661920322199,
4.15296567751372));
#90425=CARTESIAN_POINT('Ctrl Pts',(2.37190077141875,0.159834311433769,4.16274909999971));
#90426=CARTESIAN_POINT('Ctrl Pts',(2.3299939034092,0.467199987332939,4.18179507010532));
#90427=CARTESIAN_POINT('Ctrl Pts',(2.29627290561349,0.611775510969299,4.19099229690927));
#90428=CARTESIAN_POINT('Ctrl Pts',(2.24227577712706,0.773231415345579,4.20209525420844));
#90429=CARTESIAN_POINT('Ctrl Pts',(2.23496604832748,0.794112202902458,4.20354716516677));
#90430=CARTESIAN_POINT('Ctrl Pts',(2.22345016727089,0.825589048674656,4.20576159249658));
#90431=CARTESIAN_POINT('Ctrl Pts',(2.21945781941435,0.836262461060113,4.2065170052569));
#90432=CARTESIAN_POINT('Ctrl Pts',(2.2120854129001,0.855547643021267,4.20789033620728));
#90433=CARTESIAN_POINT('Ctrl Pts',(2.20873157129023,0.864169245725234,4.20850736584027));
#90434=CARTESIAN_POINT('Ctrl Pts',(2.2014104586864,0.882668316094854,4.20983803203578));
#90435=CARTESIAN_POINT('Ctrl Pts',(2.19742697308093,0.892539105816755,4.21055220421699));
#90436=CARTESIAN_POINT('Ctrl Pts',(2.18649446015358,0.919112229826322,4.21248624441324));
#90437=CARTESIAN_POINT('Ctrl Pts',(2.17942068038512,0.935762139399023,4.21371031221542));
#90438=CARTESIAN_POINT('Ctrl Pts',(2.14352697951076,1.01763169874518,4.21979136196593));
#90439=CARTESIAN_POINT('Ctrl Pts',(2.1119693588624,1.08160332434039,4.22474105442175));
#90440=CARTESIAN_POINT('Ctrl Pts',(1.98659147178823,1.30928787170186,4.24310617993216));
#90441=CARTESIAN_POINT('Ctrl Pts',(1.87621844088715,1.46306805842334,4.25704940759086));
#90442=CARTESIAN_POINT('Ctrl Pts',(1.6983172782291,1.65725898757842,4.27610689809782));
#90443=CARTESIAN_POINT('Ctrl Pts',(1.6452239886398,1.70997931759794,4.28145071638405));
#90444=CARTESIAN_POINT('Ctrl Pts',(1.57745429425221,1.77118867700159,4.28778227455734));
#90445=CARTESIAN_POINT('Ctrl Pts',(1.56506947489374,1.7821416771336,4.28892056505657));
#90446=CARTESIAN_POINT('Ctrl Pts',(1.54716442525568,1.79764608512422,4.29053828484874));
#90447=CARTESIAN_POINT('Ctrl Pts',(1.54173690806009,1.80230311431043,4.29102504503779));
#90448=CARTESIAN_POINT('Ctrl Pts',(1.53228447625674,1.81033973752036,4.29186640057855));
#90449=CARTESIAN_POINT('Ctrl Pts',(1.52826927262454,1.81373060680081,4.29222181245014));
#90450=CARTESIAN_POINT('Ctrl Pts',(1.51981173577431,1.82082503246241,4.29296625663399));
#90451=CARTESIAN_POINT('Ctrl Pts',(1.51536710822465,1.82452570279928,4.29335508263167));
#90452=CARTESIAN_POINT('Ctrl Pts',(1.50343691370139,1.83438531200724,4.29439250841883));
#90453=CARTESIAN_POINT('Ctrl Pts',(1.49592695059528,1.84051476304724,4.29503901437206));
#90454=CARTESIAN_POINT('Ctrl Pts',(1.46256386823337,1.86740579342634,4.29788341417074));
#90455=CARTESIAN_POINT('Ctrl Pts',(1.43631315030701,1.88767112475779,4.30004847965507));
#90456=CARTESIAN_POINT('Ctrl Pts',(1.21022240811456,2.05476288348075,4.31816976352286));
#90457=CARTESIAN_POINT('Ctrl Pts',(0.98890396331218,2.16997499662157,4.33264607965647));
#90458=CARTESIAN_POINT('Ctrl Pts',(0.690299094513248,2.27005713786344,4.352555097169));
#90459=CARTESIAN_POINT('Ctrl Pts',(0.626011687492244,2.2886197377138,4.35684998799354));
#90460=CARTESIAN_POINT('Ctrl Pts',(0.544300200113707,2.30851290578193,4.36236216618868));
#90461=CARTESIAN_POINT('Ctrl Pts',(0.527526746175417,2.31240352232557,4.36349638439595));
#90462=CARTESIAN_POINT('Ctrl Pts',(0.500606753032239,2.31833950035922,4.36532167646026));
#90463=CARTESIAN_POINT('Ctrl Pts',(0.490486390575309,2.32050172483876,4.3660089974678));
#90464=CARTESIAN_POINT('Ctrl Pts',(0.471252975983677,2.32447951917007,4.36731749144728));
#90465=CARTESIAN_POINT('Ctrl Pts',(0.462142748437205,2.32630790701498,4.36793824138728));
#90466=CARTESIAN_POINT('Ctrl Pts',(0.44139270999305,2.33034566155726,4.36935439581084));
#90467=CARTESIAN_POINT('Ctrl Pts',(0.429746691947089,2.33252142512537,4.37015085486697));
#90468=CARTESIAN_POINT('Ctrl Pts',(0.399468940107325,2.33794360536491,4.37222599795063));
#90469=CARTESIAN_POINT('Ctrl Pts',(0.380814115402512,2.3410545293295,4.37350893733382));
#90470=CARTESIAN_POINT('Ctrl Pts',(0.20820792657668,2.36772111865761,4.38542259099948));
#90471=CARTESIAN_POINT('Ctrl Pts',(0.0523537403355777,2.3762776780993,4.39653437377631));
#90472=CARTESIAN_POINT('Ctrl Pts',(-0.215849127161198,2.36459812494689,
4.41607365872699));
#90473=CARTESIAN_POINT('Ctrl Pts',(-0.328019740197203,2.35166300702794,
4.42436178304244));
#90474=CARTESIAN_POINT('Ctrl Pts',(-0.506807421998396,2.31800061285028,
4.43746241782096));
#90475=CARTESIAN_POINT('Ctrl Pts',(-0.57418470303871,2.30223686642559,4.44237116962679));
#90476=CARTESIAN_POINT('Ctrl Pts',(-0.651895147882249,2.28043065614961,
4.44792955360047));
#90477=CARTESIAN_POINT('Ctrl Pts',(-0.662984510624347,2.27723139220565,
4.44872022832433));
#90478=CARTESIAN_POINT('Ctrl Pts',(-0.679981547461973,2.2721930876725,4.44992779074919));
#90479=CARTESIAN_POINT('Ctrl Pts',(-0.685905921867381,2.27041172502435,
4.45034787880452));
#90480=CARTESIAN_POINT('Ctrl Pts',(-0.696782684413773,2.26709480073911,
4.45111755228678));
#90481=CARTESIAN_POINT('Ctrl Pts',(-0.70173699109438,2.26556618557821,4.45146752064036));
#90482=CARTESIAN_POINT('Ctrl Pts',(-0.712892019460722,2.26208428064445,
4.45225414322988));
#90483=CARTESIAN_POINT('Ctrl Pts',(-0.719089737897296,2.26012173910042,
4.45269025114568));
#90484=CARTESIAN_POINT('Ctrl Pts',(-0.73732221794135,2.25426573413145,4.45397064475268));
#90485=CARTESIAN_POINT('Ctrl Pts',(-0.749334228816196,2.25030137630539,
4.45481091742305));
#90486=CARTESIAN_POINT('Ctrl Pts',(-0.847354753326082,2.21707946262185,
4.46164523619786));
#90487=CARTESIAN_POINT('Ctrl Pts',(-0.931660081245402,2.18299453085569,
4.46738231061973));
#90488=CARTESIAN_POINT('Ctrl Pts',(-1.04143131933049,2.13109181013205,4.47492116658288));
#90489=CARTESIAN_POINT('Ctrl Pts',(-1.06879719188339,2.11749949828943,4.4768064350546));
#90490=CARTESIAN_POINT('Ctrl Pts',(-1.22661806832913,2.03527247854872,4.48775326911671));
#90491=CARTESIAN_POINT('Ctrl Pts',(-1.35070217210204,1.95512851108792,4.4966831924423));
#90492=CARTESIAN_POINT('Ctrl Pts',(-1.52363056909719,1.8190723751601,4.51055047610442));
#90493=CARTESIAN_POINT('Ctrl Pts',(-1.57861943795132,1.77156242950967,4.51520355521581));
#90494=CARTESIAN_POINT('Ctrl Pts',(-1.64415699757484,1.70946122985096,4.52111848714565));
#90495=CARTESIAN_POINT('Ctrl Pts',(-1.65683950576998,1.69717198690424,4.52228133551876));
#90496=CARTESIAN_POINT('Ctrl Pts',(-1.67680328580924,1.67739020976055,4.52414181436475));
#90497=CARTESIAN_POINT('Ctrl Pts',(-1.68417449882976,1.66998904985739,4.52483542853047));
#90498=CARTESIAN_POINT('Ctrl Pts',(-1.69799786760767,1.65592491537452,4.5261490029716));
#90499=CARTESIAN_POINT('Ctrl Pts',(-1.70446031702403,1.64927229626655,4.52676849402255));
#90500=CARTESIAN_POINT('Ctrl Pts',(-1.71897606798874,1.63415295459913,4.52817234722268));
#90501=CARTESIAN_POINT('Ctrl Pts',(-1.72700610338463,1.62566432934718,4.52895769479941));
#90502=CARTESIAN_POINT('Ctrl Pts',(-1.74750055129954,1.60367623792859,4.53098496474995));
#90503=CARTESIAN_POINT('Ctrl Pts',(-1.75987121619112,1.59009085341708,4.53223082426789));
#90504=CARTESIAN_POINT('Ctrl Pts',(-1.8444552732108,1.49500495954231,4.54090670219134));
#90505=CARTESIAN_POINT('Ctrl Pts',(-1.91112838304458,1.40877147700662,4.54856291767247));
#90506=CARTESIAN_POINT('Ctrl Pts',(-2.05758873578597,1.189722786498,4.56749876885224));
#90507=CARTESIAN_POINT('Ctrl Pts',(-2.13075707555524,1.0530819957587,4.57891935235387));
#90508=CARTESIAN_POINT('Ctrl Pts',(-2.21881323658195,0.841225920122657,
4.59547880856323));
#90509=CARTESIAN_POINT('Ctrl Pts',(-2.24424210985445,0.770826238065321,
4.60080184167317));
#90510=CARTESIAN_POINT('Ctrl Pts',(-2.26976558264185,0.688113489908777,
4.60676488655015));
#90511=CARTESIAN_POINT('Ctrl Pts',(-2.2731450094232,0.676866128282533,4.60756961799544));
#90512=CARTESIAN_POINT('Ctrl Pts',(-2.27818895136523,0.659615013952774,
4.60879406222779));
#90513=CARTESIAN_POINT('Ctrl Pts',(-2.27991352656112,0.653629236209919,
4.60921711278326));
#90514=CARTESIAN_POINT('Ctrl Pts',(-2.2830297419906,0.642650854391736,4.60998962721873));
#90515=CARTESIAN_POINT('Ctrl Pts',(-2.28442859851994,0.637660491857268,
4.61033949400754));
#90516=CARTESIAN_POINT('Ctrl Pts',(-2.28753190277648,0.626448297927628,
4.61112269280696));
#90517=CARTESIAN_POINT('Ctrl Pts',(-2.28922732873539,0.620224085363706,
4.61155550068257));
#90518=CARTESIAN_POINT('Ctrl Pts',(-2.29350161224627,0.60427610910025,4.61265961374422));
#90519=CARTESIAN_POINT('Ctrl Pts',(-2.29604407064238,0.594542593925732,
4.61332888508663));
#90520=CARTESIAN_POINT('Ctrl Pts',(-2.31095562919788,0.535932821222687,
4.61733289063216));
#90521=CARTESIAN_POINT('Ctrl Pts',(-2.3218266685692,0.486684404389039,4.62058910258438));
#90522=CARTESIAN_POINT('Ctrl Pts',(-2.34749859101888,0.349779301689913,
4.62943829620707));
#90523=CARTESIAN_POINT('Ctrl Pts',(-2.35894752791029,0.261624378967379,
4.63491166268408));
#90524=CARTESIAN_POINT('Ctrl Pts',(-2.36542650810962,0.173076564653691,
4.64035944112689));
#90525=CARTESIAN_POINT('Origin',(0.,0.,-1.84858989190503));
#90526=CARTESIAN_POINT('',(-2.36542649454111,0.173076750093528,5.83682189647116));
#90527=CARTESIAN_POINT('',(-2.36542649454144,0.173076750089109,5.63753449772567));
#90528=CARTESIAN_POINT('',(-2.36542649454111,0.173076750093529,-1.84858989190503));
#90529=CARTESIAN_POINT('',(-2.37152864642643,-0.000916510297551713,4.84858989190502));
#90530=CARTESIAN_POINT('Ctrl Pts',(-2.3717498228844,-0.000916595774276441,
4.84858989190502));
#90531=CARTESIAN_POINT('Ctrl Pts',(-2.37171639157236,-0.0874222405099675,
4.85436572821342));
#90532=CARTESIAN_POINT('Ctrl Pts',(-2.36694602552388,-0.17378123686453,
4.86014156452181));
#90533=CARTESIAN_POINT('Ctrl Pts',(-2.3575118136592,-0.2594920248434,4.8659174008302));
#90534=CARTESIAN_POINT('Ctrl Pts',(-2.34805218476827,-0.345433729127539,
4.87170879801269));
#90535=CARTESIAN_POINT('Ctrl Pts',(-2.33390367225374,-0.430723412740602,
4.87750019519518));
#90536=CARTESIAN_POINT('Ctrl Pts',(-2.31519033196285,-0.514870652966122,
4.88329159237767));
#90537=CARTESIAN_POINT('Ctrl Pts',(-2.29639624105013,-0.599381000037756,
4.88910798023079));
#90538=CARTESIAN_POINT('Ctrl Pts',(-2.2729979807044,-0.682738715538656,
4.89492436808392));
#90539=CARTESIAN_POINT('Ctrl Pts',(-2.24516998327953,-0.764467009543649,
4.90074075593704));
#90540=CARTESIAN_POINT('Ctrl Pts',(-2.21986708128255,-0.838779328249715,
4.9060293683218));
#90541=CARTESIAN_POINT('Ctrl Pts',(-2.19090256384451,-0.911744606802647,
4.91131798070655));
#90542=CARTESIAN_POINT('Ctrl Pts',(-2.15844069284499,-0.983021789163822,
4.9166065930913));
#90543=CARTESIAN_POINT('Ctrl Pts',(-2.12571462659243,-1.05487907035018,
4.92193824755109));
#90544=CARTESIAN_POINT('Ctrl Pts',(-2.08933423057337,-1.12523662812698,
4.92726990201087));
#90545=CARTESIAN_POINT('Ctrl Pts',(-2.0494593632955,-1.19369777611438,4.93260155647066));
#90546=CARTESIAN_POINT('Ctrl Pts',(-2.00964221368882,-1.26205982864896,
4.93792549352096));
#90547=CARTESIAN_POINT('Ctrl Pts',(-1.96634087154654,-1.32853052080258,
4.94324943057125));
#90548=CARTESIAN_POINT('Ctrl Pts',(-1.9197625697357,-1.39273462595779,4.94857336762155));
#90549=CARTESIAN_POINT('Ctrl Pts',(-1.87323859286367,-1.45686384894796,
4.95389109528801));
#90550=CARTESIAN_POINT('Ctrl Pts',(-1.82344552529404,-1.51873136068186,
4.95920882295447));
#90551=CARTESIAN_POINT('Ctrl Pts',(-1.77063487472742,-1.57798929112305,
4.96452655062093));
#90552=CARTESIAN_POINT('Ctrl Pts',(-1.71785796100039,-1.63720936603182,
4.96984088118239));
#90553=CARTESIAN_POINT('Ctrl Pts',(-1.66206760155225,-1.69382281937187,
4.97515521174384));
#90554=CARTESIAN_POINT('Ctrl Pts',(-1.60355594992264,-1.74751434270729,
4.9804695423053));
#90555=CARTESIAN_POINT('Ctrl Pts',(-1.54506344174328,-1.80118829960976,
4.98578213415968));
#90556=CARTESIAN_POINT('Ctrl Pts',(-1.48385175452992,-1.85194190800883,
4.99109472601406));
#90557=CARTESIAN_POINT('Ctrl Pts',(-1.42024924886854,-1.89949733708377,
4.99640731786844));
#90558=CARTESIAN_POINT('Ctrl Pts',(-1.35664773074818,-1.94705202777685,
5.00171982723546));
#90559=CARTESIAN_POINT('Ctrl Pts',(-1.29065584428519,-1.99140835813315,
5.00703233660249));
#90560=CARTESIAN_POINT('Ctrl Pts',(-1.22263311438146,-2.03233027092495,
5.01234484596951));
#90561=CARTESIAN_POINT('Ctrl Pts',(-1.15454246275261,-2.0732930448659,5.01766265995753));
#90562=CARTESIAN_POINT('Ctrl Pts',(-1.08441731954588,-2.11081430839001,
5.02298047394555));
#90563=CARTESIAN_POINT('Ctrl Pts',(-1.01264363412979,-2.14470299406617,
5.02829828793356));
#90564=CARTESIAN_POINT('Ctrl Pts',(-0.940835604055967,-2.17860789592664,
5.03361864656591));
#90565=CARTESIAN_POINT('Ctrl Pts',(-0.867377894386582,-2.20887657821286,
5.03893900519825));
#90566=CARTESIAN_POINT('Ctrl Pts',(-0.792675972084069,-2.23536638289578,
5.04425936383059));
#90567=CARTESIAN_POINT('Ctrl Pts',(-0.717837583701502,-2.26190457936965,
5.04958944173741));
#90568=CARTESIAN_POINT('Ctrl Pts',(-0.641750891206771,-2.28464996903973,
5.05491951964424));
#90569=CARTESIAN_POINT('Ctrl Pts',(-0.564835856817695,-2.30351004281575,
5.06024959755106));
#90570=CARTESIAN_POINT('Ctrl Pts',(-0.491135775750442,-2.32158178883092,
5.06535688479273));
#90571=CARTESIAN_POINT('Ctrl Pts',(-0.416675591263177,-2.33608653528661,
5.07046417203439));
#90572=CARTESIAN_POINT('Ctrl Pts',(-0.34182939364102,-2.34698758585192,
5.07557145927605));
#90573=CARTESIAN_POINT('Ctrl Pts',(-0.26369514262485,-2.35836752829748,
5.08090311373587));
#90574=CARTESIAN_POINT('Ctrl Pts',(-0.184843782864509,-2.36586300792345,
5.08623476819567));
#90575=CARTESIAN_POINT('Ctrl Pts',(-0.105695390738131,-2.36939370871046,
5.09156642265548));
#90576=CARTESIAN_POINT('Ctrl Pts',(-0.0266615635290246,-2.37291929891427,
5.09689035970581));
#90577=CARTESIAN_POINT('Ctrl Pts',(0.0526679777719226,-2.3724914861672,
5.10221429675613));
#90578=CARTESIAN_POINT('Ctrl Pts',(0.131865556626997,-2.36808140431773,
5.10753823380646));
#90579=CARTESIAN_POINT('Ctrl Pts',(0.210970766214455,-2.36367646600973,
5.11285596147295));
#90580=CARTESIAN_POINT('Ctrl Pts',(0.289943853474334,-2.35529851430046,
5.11817368913943));
#90581=CARTESIAN_POINT('Ctrl Pts',(0.368356177697091,-2.3429707187356,5.12349141680592));
#90582=CARTESIAN_POINT('Ctrl Pts',(0.446718410054345,-2.33065079849242,
5.1288057473674));
#90583=CARTESIAN_POINT('Ctrl Pts',(0.524520128448813,-2.31438611523804,
5.13412007792888));
#90584=CARTESIAN_POINT('Ctrl Pts',(0.601338068909978,-2.29425164037854,
5.13943440849037));
#90585=CARTESIAN_POINT('Ctrl Pts',(0.678130876591922,-2.27412375298166,
5.14474700034477));
#90586=CARTESIAN_POINT('Ctrl Pts',(0.753940092245238,-2.25012870684461,
5.15005959219918));
#90587=CARTESIAN_POINT('Ctrl Pts',(0.828354364895945,-2.22239220405801,
5.15537218405358));
#90588=CARTESIAN_POINT('Ctrl Pts',(0.902767482133873,-2.19465613192952,
5.16068469342063));
#90589=CARTESIAN_POINT('Ctrl Pts',(0.975785260524075,-2.16317888362801,
5.16599720278768));
#90590=CARTESIAN_POINT('Ctrl Pts',(1.04701460391984,-2.12813497731666,5.17130971215473));
#90591=CARTESIAN_POINT('Ctrl Pts',(1.11831507089285,-2.09305607913456,5.17662752614277));
#90592=CARTESIAN_POINT('Ctrl Pts',(1.18782311378482,-2.05440361608756,5.18194534013082));
#90593=CARTESIAN_POINT('Ctrl Pts',(1.25516916125407,-2.01239867798027,5.18726315411886));
#90594=CARTESIAN_POINT('Ctrl Pts',(1.32254743469775,-1.97037363995454,5.19258351275123));
#90595=CARTESIAN_POINT('Ctrl Pts',(1.38776126633877,-1.92499319923414,5.1979038713836));
#90596=CARTESIAN_POINT('Ctrl Pts',(1.45047122366833,-1.87652106084906,5.20322423001597));
#90597=CARTESIAN_POINT('Ctrl Pts',(1.51329574005863,-1.82796037316684,5.20855430792282));
#90598=CARTESIAN_POINT('Ctrl Pts',(1.57360688486171,-1.77629700762958,5.21388438582967));
#90599=CARTESIAN_POINT('Ctrl Pts',(1.63109954567416,-1.7218340032075,5.21921446373652));
#90600=CARTESIAN_POINT('Ctrl Pts',(1.68618908435905,-1.66964748502227,5.22432175097794));
#90601=CARTESIAN_POINT('Ctrl Pts',(1.73869084946442,-1.61489101139677,5.22942903821936));
#90602=CARTESIAN_POINT('Ctrl Pts',(1.78837148814904,-1.557859262859,5.23453632546079));
#90603=CARTESIAN_POINT('Ctrl Pts',(1.84023463707511,-1.4983220639372,5.23986797992062));
#90604=CARTESIAN_POINT('Ctrl Pts',(1.88921980802755,-1.43607921553118,5.24519963438045));
#90605=CARTESIAN_POINT('Ctrl Pts',(1.93503207904738,-1.37144045279318,5.25053128884028));
#90606=CARTESIAN_POINT('Ctrl Pts',(1.9807780381827,-1.30689525272027,5.25585522589063));
#90607=CARTESIAN_POINT('Ctrl Pts',(2.02335994892682,-1.2399614045999,5.26117916294098));
#90608=CARTESIAN_POINT('Ctrl Pts',(2.06252203564278,-1.17098288415672,5.26650309999132));
#90609=CARTESIAN_POINT('Ctrl Pts',(2.10163844705754,-1.10208481434734,5.27182082765783));
#90610=CARTESIAN_POINT('Ctrl Pts',(2.13734273032496,-1.0311472168224,5.27713855532434));
#90611=CARTESIAN_POINT('Ctrl Pts',(2.16942234081596,-0.958543045287285,
5.28245628299085));
#90612=CARTESIAN_POINT('Ctrl Pts',(2.20148145800376,-0.8859852552162,5.28777061355236));
#90613=CARTESIAN_POINT('Ctrl Pts',(2.22992030934231,-0.811763432003007,
5.29308494411386));
#90614=CARTESIAN_POINT('Ctrl Pts',(2.25457281697321,-0.736274049159331,
5.29839927467537));
#90615=CARTESIAN_POINT('Ctrl Pts',(2.2792172589618,-0.660809364426271,5.30371186652979));
#90616=CARTESIAN_POINT('Ctrl Pts',(2.30007767165316,-0.584078388937312,
5.30902445838422));
#90617=CARTESIAN_POINT('Ctrl Pts',(2.31703708140918,-0.506495040326016,
5.31433705023865));
#90618=CARTESIAN_POINT('Ctrl Pts',(2.33399622784046,-0.428912896332979,
5.31964955960573));
#90619=CARTESIAN_POINT('Ctrl Pts',(2.34705439289442,-0.350478863877989,
5.3249620689728));
#90620=CARTESIAN_POINT('Ctrl Pts',(2.35614553017602,-0.271617935953395,
5.33027457833988));
#90621=CARTESIAN_POINT('Ctrl Pts',(2.36524574509576,-0.192678264198936,
5.33559239232794));
#90622=CARTESIAN_POINT('Ctrl Pts',(2.37037096546595,-0.113311312370886,
5.34091020631601));
#90623=CARTESIAN_POINT('Ctrl Pts',(2.37150703763578,-0.0339475027647511,
5.34622802030408));
#90624=CARTESIAN_POINT('Ctrl Pts',(2.37264365343118,0.0454542834739599,
5.35154837893648));
#90625=CARTESIAN_POINT('Ctrl Pts',(2.36978733515543,0.124852455261711,5.35686873756887));
#90626=CARTESIAN_POINT('Ctrl Pts',(2.36297607546678,0.203818863875749,5.36218909620127));
#90627=CARTESIAN_POINT('Ctrl Pts',(2.35615237291347,0.282929528968124,5.36751917410814));
#90628=CARTESIAN_POINT('Ctrl Pts',(2.34535935558681,0.36160638899144,5.37284925201501));
#90629=CARTESIAN_POINT('Ctrl Pts',(2.33068666681875,0.439428860696832,5.37817932992188));
#90630=CARTESIAN_POINT('Ctrl Pts',(2.31662727829782,0.513998449315545,5.3832866171631));
#90631=CARTESIAN_POINT('Ctrl Pts',(2.29900622707555,0.58778330749414,5.38839390440432));
#90632=CARTESIAN_POINT('Ctrl Pts',(2.27794497244047,0.660427713707715,5.39350119164554));
#90633=CARTESIAN_POINT('Ctrl Pts',(2.2559584800227,0.736263446862324,5.39883284610536));
#90634=CARTESIAN_POINT('Ctrl Pts',(2.23013914030922,0.81114389055524,5.40416450056517));
#90635=CARTESIAN_POINT('Ctrl Pts',(2.20058774310761,0.884653405229739,5.40949615502498));
#90636=CARTESIAN_POINT('Ctrl Pts',(2.17107912066471,0.958056517092479,5.41482009207531));
#90637=CARTESIAN_POINT('Ctrl Pts',(2.1378493418084,1.03009220924528,5.42014402912563));
#90638=CARTESIAN_POINT('Ctrl Pts',(2.10104917685267,1.10035922268446,5.42546796617596));
#90639=CARTESIAN_POINT('Ctrl Pts',(2.06429193245503,1.17054428270206,5.43078569384245));
#90640=CARTESIAN_POINT('Ctrl Pts',(2.02397279350614,1.23896435008457,5.43610342150894));
#90641=CARTESIAN_POINT('Ctrl Pts',(1.98029029697572,1.30523882956485,5.44142114917543));
#90642=CARTESIAN_POINT('Ctrl Pts',(1.93663570597882,1.3714709711557,5.44673547973692));
#90643=CARTESIAN_POINT('Ctrl Pts',(1.88962227932606,1.43555985490998,5.4520498102984));
#90644=CARTESIAN_POINT('Ctrl Pts',(1.83949348281343,1.49715122455512,5.45736414085989));
#90645=CARTESIAN_POINT('Ctrl Pts',(1.78938108710467,1.55872244314851,5.4626767327143));
#90646=CARTESIAN_POINT('Ctrl Pts',(1.73615564124393,1.61779740679662,5.46798932456871));
#90647=CARTESIAN_POINT('Ctrl Pts',(1.68010185893517,1.674053704665,5.47330191642312));
#90648=CARTESIAN_POINT('Ctrl Pts',(1.6240489469602,1.73030912905517,5.47861442579017));
#90649=CARTESIAN_POINT('Ctrl Pts',(1.56516811772133,1.78374564344214,5.48392693515723));
#90650=CARTESIAN_POINT('Ctrl Pts',(1.50378096462929,1.83407766272822,5.48923944452428));
#90651=CARTESIAN_POINT('Ctrl Pts',(1.44233251553598,1.88445993929718,5.49455725851233));
#90652=CARTESIAN_POINT('Ctrl Pts',(1.3783731067335,1.93173123028774,5.49987507250038));
#90653=CARTESIAN_POINT('Ctrl Pts',(1.31225698662644,1.97564664440534,5.50519288648842));
#90654=CARTESIAN_POINT('Ctrl Pts',(1.24610922908144,2.01958307262944,5.5105132451208));
#90655=CARTESIAN_POINT('Ctrl Pts',(1.177803107976,2.06016018510454,5.51583360375317));
#90656=CARTESIAN_POINT('Ctrl Pts',(1.10771918719346,2.09717816716259,5.52115396238555));
#90657=CARTESIAN_POINT('Ctrl Pts',(1.0375072365337,2.13426377397173,5.5264840402924));
#90658=CARTESIAN_POINT('Ctrl Pts',(0.965511422674827,2.16777705958948,5.53181411819925));
#90659=CARTESIAN_POINT('Ctrl Pts',(0.892133907124781,2.19756573377414,5.5371441961061));
#90660=CARTESIAN_POINT('Ctrl Pts',(0.821823480987807,2.22610927821386,5.5422514833475));
#90661=CARTESIAN_POINT('Ctrl Pts',(0.750244923385628,2.25123330724193,5.54735877058889));
#90662=CARTESIAN_POINT('Ctrl Pts',(0.67776308065634,2.27284739236915,5.55246605783029));
#90663=CARTESIAN_POINT('Ctrl Pts',(0.602097052532584,2.29541100156454,5.55779771229011));
#90664=CARTESIAN_POINT('Ctrl Pts',(0.525159509164951,2.31423475176091,5.56312936674993));
#90665=CARTESIAN_POINT('Ctrl Pts',(0.447354488944852,2.32917840100772,5.56846102120975));
#90666=CARTESIAN_POINT('Ctrl Pts',(0.369662089151608,2.34410041977167,5.57378495826008));
#90667=CARTESIAN_POINT('Ctrl Pts',(0.29110516261796,2.3551534030962,5.57910889531041));
#90668=CARTESIAN_POINT('Ctrl Pts',(0.212102710997206,2.36224691818777,5.58443283236075));
#90669=CARTESIAN_POINT('Ctrl Pts',(0.133192401064382,2.36933216001136,5.58975056002724));
#90670=CARTESIAN_POINT('Ctrl Pts',(0.0538380632305106,2.37246706880857,
5.59506828769373));
#90671=CARTESIAN_POINT('Ctrl Pts',(-0.0255328190202548,2.37161256061206,
5.60038601536023));
#90672=CARTESIAN_POINT('Ctrl Pts',(-0.104852997053299,2.37075859829797,
5.60570034592172));
#90673=CARTESIAN_POINT('Ctrl Pts',(-0.184189230931479,2.36592028241939,
5.61101467648321));
#90674=CARTESIAN_POINT('Ctrl Pts',(-0.263111863375871,2.35711056377313,
5.6163290070447));
#90675=CARTESIAN_POINT('Ctrl Pts',(-0.342008674442017,2.3483037274316,5.62164159889911));
#90676=CARTESIAN_POINT('Ctrl Pts',(-0.420491687137116,2.3355281203851,5.62695419075352));
#90677=CARTESIAN_POINT('Ctrl Pts',(-0.49813569284986,2.31884861386184,5.63226678260793));
#90678=CARTESIAN_POINT('Ctrl Pts',(-0.575778493002547,2.30216936631733,
5.63757929197499));
#90679=CARTESIAN_POINT('Ctrl Pts',(-0.652581853916395,2.28158643955674,
5.64289180134205));
#90680=CARTESIAN_POINT('Ctrl Pts',(-0.728131567745196,2.25721564821639,
5.64820431070911));
#90681=CARTESIAN_POINT('Ctrl Pts',(-0.803756719106482,2.2328205222721,5.65352212469716));
#90682=CARTESIAN_POINT('Ctrl Pts',(-0.878125275447008,2.20463012046381,
5.65883993868521));
#90683=CARTESIAN_POINT('Ctrl Pts',(-0.95083956891916,2.17280974240213,5.66415775267327));
#90684=CARTESIAN_POINT('Ctrl Pts',(-1.02358865714246,2.1409741378687,5.66947811130564));
#90685=CARTESIAN_POINT('Ctrl Pts',(-1.09468148538153,2.10550530633641,5.67479846993803));
#90686=CARTESIAN_POINT('Ctrl Pts',(-1.16374404259843,2.0666150744192,5.6801188285704));
#90687=CARTESIAN_POINT('Ctrl Pts',(-1.23293276385728,2.0276537975096,5.68544890647726));
#90688=CARTESIAN_POINT('Ctrl Pts',(-1.30008340518587,1.98525888159663,5.69077898438412));
#90689=CARTESIAN_POINT('Ctrl Pts',(-1.3648502243344,1.93968603841816,5.69610906229097));
#90690=CARTESIAN_POINT('Ctrl Pts',(-1.42690987053112,1.89601808373062,5.70121634953233));
#90691=CARTESIAN_POINT('Ctrl Pts',(-1.4867807505984,1.84943284505042,5.70632363677368));
#90692=CARTESIAN_POINT('Ctrl Pts',(-1.54418933615934,1.80018814477593,5.71143092401504));
#90693=CARTESIAN_POINT('Ctrl Pts',(-1.60323464352845,1.7495394754942,5.71668382028555));
#90694=CARTESIAN_POINT('Ctrl Pts',(-1.65991290861986,1.69587307641002,5.72193671655606));
#90695=CARTESIAN_POINT('Ctrl Pts',(-1.71389270879525,1.63944193103583,5.72718961282656));
#90696=CARTESIAN_POINT('Ctrl Pts',(-1.76780249533153,1.58308397877895,5.73243569591172));
#90697=CARTESIAN_POINT('Ctrl Pts',(-1.81902042514459,1.52396873529004,5.73768177899688));
#90698=CARTESIAN_POINT('Ctrl Pts',(-1.86724818186334,1.46238924019156,5.74292786208204));
#90699=CARTESIAN_POINT('Ctrl Pts',(-1.91542944584182,1.40086910923661,5.74816888781444));
#90700=CARTESIAN_POINT('Ctrl Pts',(-1.96062595724657,1.33688981662153,5.75340991354684));
#90701=CARTESIAN_POINT('Ctrl Pts',(-2.00257751185276,1.27077982810619,5.75865093927924));
#90702=CARTESIAN_POINT('Ctrl Pts',(-2.04450258508999,1.20471157065457,5.76388865668285));
#90703=CARTESIAN_POINT('Ctrl Pts',(-2.0831865077308,1.13651569351908,5.76912637408646));
#90704=CARTESIAN_POINT('Ctrl Pts',(-2.11841152831787,1.06655082353818,5.77436409149006));
#90705=CARTESIAN_POINT('Ctrl Pts',(-2.15364020563546,0.99657869046214,5.77960235262425));
#90706=CARTESIAN_POINT('Ctrl Pts',(-2.18540902907395,0.924837621173666,
5.78484061375845));
#90707=CARTESIAN_POINT('Ctrl Pts',(-2.21354609619333,0.851711067514837,
5.79007887489264));
#90708=CARTESIAN_POINT('Ctrl Pts',(-2.24168272106826,0.778585663222877,
5.79531705369444));
#90709=CARTESIAN_POINT('Ctrl Pts',(-2.26618753750677,0.704075272927715,
5.80055523249625));
#90710=CARTESIAN_POINT('Ctrl Pts',(-2.28693756719801,0.628581439622927,
5.80579341129805));
#90711=CARTESIAN_POINT('Ctrl Pts',(-2.30771013357672,0.553005612173924,
5.8110372793061));
#90712=CARTESIAN_POINT('Ctrl Pts',(-2.32471964709362,0.476444678008371,
5.81628114731416));
#90713=CARTESIAN_POINT('Ctrl Pts',(-2.33789380848674,0.399312662883799,
5.82152501532221));
#90714=CARTESIAN_POINT('Ctrl Pts',(-2.35070391868011,0.324312092927395,
5.82662397570519));
#90715=CARTESIAN_POINT('Ctrl Pts',(-2.35988791953829,0.248772024280277,
5.83172293608818));
#90716=CARTESIAN_POINT('Ctrl Pts',(-2.36542649454111,0.173076750093528,
5.83682189647117));
#90717=CARTESIAN_POINT('Ctrl Pts',(-2.36152614656945,0.172792042906829,
4.83696616984731));
#90718=CARTESIAN_POINT('Ctrl Pts',(-2.36575283962544,0.114983285525077,
4.84084074386655));
#90719=CARTESIAN_POINT('Ctrl Pts',(-2.36797226345534,0.0570274830161041,
4.84471531788578));
#90720=CARTESIAN_POINT('Ctrl Pts',(-2.36817286055345,-0.000915213407331403,
4.84858989190502));
#90721=CARTESIAN_POINT('Ctrl Pts',(-2.36542650810962,0.173076564653691,
4.64035944112689));
#90722=CARTESIAN_POINT('Ctrl Pts',(-2.36958750437766,0.11620849073354,4.64385816856119));
#90723=CARTESIAN_POINT('Ctrl Pts',(-2.37169861402987,0.0591783395543195,
4.6473459065507));
#90724=CARTESIAN_POINT('Ctrl Pts',(-2.37187441627101,-0.139696801513177,
4.65957190085794));
#90725=CARTESIAN_POINT('Ctrl Pts',(-2.35928471804046,-0.281195179106819,
4.66840388462315));
#90726=CARTESIAN_POINT('Ctrl Pts',(-2.33076725754395,-0.439412277896459,
4.67889885482005));
#90727=CARTESIAN_POINT('Ctrl Pts',(-2.32717196098186,-0.458071815686946,
4.68014611575948));
#90728=CARTESIAN_POINT('Ctrl Pts',(-2.32096629810687,-0.488318044859894,
4.68218432644276));
#90729=CARTESIAN_POINT('Ctrl Pts',(-2.31849238503274,-0.499932117136132,
4.68297093061465));
#90730=CARTESIAN_POINT('Ctrl Pts',(-2.31392669677645,-0.520603209596756,
4.68437824924146));
#90731=CARTESIAN_POINT('Ctrl Pts',(-2.31186868097277,-0.529667497215051,
4.6849978708061));
#90732=CARTESIAN_POINT('Ctrl Pts',(-2.3074103029407,-0.548782778761977,
4.6863099840861));
#90733=CARTESIAN_POINT('Ctrl Pts',(-2.30499743380498,-0.55883062610197,
4.68700286654199));
#90734=CARTESIAN_POINT('Ctrl Pts',(-2.29840578554732,-0.585510890930634,
4.68885132204143));
#90735=CARTESIAN_POINT('Ctrl Pts',(-2.29411220662824,-0.602114038084011,
4.69001057245143));
#90736=CARTESIAN_POINT('Ctrl Pts',(-2.27241353217401,-0.682418933247504,
4.69566223477256));
#90737=CARTESIAN_POINT('Ctrl Pts',(-2.25253471582891,-0.745415806194808,
4.70023399072073));
#90738=CARTESIAN_POINT('Ctrl Pts',(-2.1441084002122,-1.04485580356438,4.72265654250698));
#90739=CARTESIAN_POINT('Ctrl Pts',(-2.02084251121103,-1.26691945733865,
4.74163777198388));
#90740=CARTESIAN_POINT('Ctrl Pts',(-1.84615114052892,-1.48924364290899,
4.76152596786354));
#90741=CARTESIAN_POINT('Ctrl Pts',(-1.82692648703119,-1.51276584154836,
4.76363975863069));
#90742=CARTESIAN_POINT('Ctrl Pts',(-1.80117901025009,-1.54306196977669,
4.76636803702352));
#90743=CARTESIAN_POINT('Ctrl Pts',(-1.79506137817033,-1.55017441779998,
4.76700896340856));
#90744=CARTESIAN_POINT('Ctrl Pts',(-1.78514980427773,-1.56156040215943,
4.76803541661321));
#90745=CARTESIAN_POINT('Ctrl Pts',(-1.78138241755102,-1.56585676149367,
4.76842283420383));
#90746=CARTESIAN_POINT('Ctrl Pts',(-1.77410299657614,-1.57409800046261,
4.76916609350036));
#90747=CARTESIAN_POINT('Ctrl Pts',(-1.77059329011003,-1.57804478994432,
4.7695220899373));
#90748=CARTESIAN_POINT('Ctrl Pts',(-1.76219230082097,-1.58742868910293,
4.77036869305112));
#90749=CARTESIAN_POINT('Ctrl Pts',(-1.75728894690622,-1.59285501811389,
4.77085840217392));
#90750=CARTESIAN_POINT('Ctrl Pts',(-1.74058284090955,-1.61117190299985,
4.7725123198229));
#90751=CARTESIAN_POINT('Ctrl Pts',(-1.72866238350954,-1.62395502880084,
4.77366805130195));
#90752=CARTESIAN_POINT('Ctrl Pts',(-1.65894634051325,-1.69707872011143,
4.78029616251592));
#90753=CARTESIAN_POINT('Ctrl Pts',(-1.59812933158786,-1.75446998754613,
4.78556681533012));
#90754=CARTESIAN_POINT('Ctrl Pts',(-1.42435148284244,-1.90190701722134,
4.79971783485057));
#90755=CARTESIAN_POINT('Ctrl Pts',(-1.30600694536709,-1.98503775872641,
4.80842209538814));
#90756=CARTESIAN_POINT('Ctrl Pts',(-1.0922987666495,-2.10772487749247,4.82373939334999));
#90757=CARTESIAN_POINT('Ctrl Pts',(-1.00058111273251,-2.15277825297358,
4.83019812670082));
#90758=CARTESIAN_POINT('Ctrl Pts',(-0.889486987852479,-2.19871329877147,
4.83805331295552));
#90759=CARTESIAN_POINT('Ctrl Pts',(-0.872641041404239,-2.20545343512256,
4.83924507520915));
#90760=CARTESIAN_POINT('Ctrl Pts',(-0.844886856203886,-2.21619023954085,
4.8412103910151));
#90761=CARTESIAN_POINT('Ctrl Pts',(-0.834023441596768,-2.2203013012546,
4.84198010507378));
#90762=CARTESIAN_POINT('Ctrl Pts',(-0.814438309975678,-2.22754892226577,
4.84336881441311));
#90763=CARTESIAN_POINT('Ctrl Pts',(-0.805727518712207,-2.23071448716302,
4.8439868274527));
#90764=CARTESIAN_POINT('Ctrl Pts',(-0.787118261910398,-2.23735400640073,
4.84530799843798));
#90765=CARTESIAN_POINT('Ctrl Pts',(-0.777214883247635,-2.24081349677068,
4.84601162142694));
#90766=CARTESIAN_POINT('Ctrl Pts',(-0.750386593619699,-2.24998602444108,
4.84791934213024));
#90767=CARTESIAN_POINT('Ctrl Pts',(-0.733419840831615,-2.25557364247925,
4.84912754404924));
#90768=CARTESIAN_POINT('Ctrl Pts',(-0.644421085436879,-2.28377305469086,
4.85547545379374));
#90769=CARTESIAN_POINT('Ctrl Pts',(-0.571410207576451,-2.30312528322894,
4.86072019251129));
#90770=CARTESIAN_POINT('Ctrl Pts',(-0.33247284082339,-2.35439694656636,
4.87801375647445));
#90771=CARTESIAN_POINT('Ctrl Pts',(-0.16403828189332,-2.37208816754432,
4.89044295986019));
#90772=CARTESIAN_POINT('Ctrl Pts',(0.101522155663723,-2.3715486348334,4.90974652416848));
#90773=CARTESIAN_POINT('Ctrl Pts',(0.198135674569337,-2.3654379107527,4.91669603020138));
#90774=CARTESIAN_POINT('Ctrl Pts',(0.30669255033607,-2.35187124861168,4.92424452584912));
#90775=CARTESIAN_POINT('Ctrl Pts',(0.319256184966174,-2.35019875685072,
4.92511410572109));
#90776=CARTESIAN_POINT('Ctrl Pts',(0.338248455308202,-2.34751536240829,
4.92642192582697));
#90777=CARTESIAN_POINT('Ctrl Pts',(0.344687082686873,-2.34657861830053,
4.92686412384191));
#90778=CARTESIAN_POINT('Ctrl Pts',(0.356249778339127,-2.34484776533427,
4.92765603529009));
#90779=CARTESIAN_POINT('Ctrl Pts',(0.361375145359988,-2.34406334238391,
4.92800627822399));
#90780=CARTESIAN_POINT('Ctrl Pts',(0.372605607532094,-2.34230684120044,
4.92877198702889));
#90781=CARTESIAN_POINT('Ctrl Pts',(0.378709481809011,-2.34132770190248,
4.929187050444));
#90782=CARTESIAN_POINT('Ctrl Pts',(0.396176992378167,-2.33845559410089,
4.9303718496153));
#90783=CARTESIAN_POINT('Ctrl Pts',(0.407530956926957,-2.33650365020399,
4.93113834465011));
#90784=CARTESIAN_POINT('Ctrl Pts',(0.486400351730555,-2.3223522241704,4.93644031564106));
#90785=CARTESIAN_POINT('Ctrl Pts',(0.553380133549267,-2.30730960664079,
4.94082880884125));
#90786=CARTESIAN_POINT('Ctrl Pts',(0.728854234898164,-2.25981762930148,
4.95224645218833));
#90787=CARTESIAN_POINT('Ctrl Pts',(0.83583822756689,-2.22247192258956,4.95913039472828));
#90788=CARTESIAN_POINT('Ctrl Pts',(1.08290969665503,-2.11584867866025,4.97563993660907));
#90789=CARTESIAN_POINT('Ctrl Pts',(1.21960572734877,-2.04011299665807,4.98529814030505));
#90790=CARTESIAN_POINT('Ctrl Pts',(1.36343384922581,-1.9407740285796,4.9967102984867));
#90791=CARTESIAN_POINT('Ctrl Pts',(1.37886476396616,-1.92984134578562,4.99795164857562));
#90792=CARTESIAN_POINT('Ctrl Pts',(1.4037472110972,-1.91176153998665,4.99998210467897));
#90793=CARTESIAN_POINT('Ctrl Pts',(1.41327902351697,-1.90472591505883,5.00076692035723));
#90794=CARTESIAN_POINT('Ctrl Pts',(1.43019194971998,-1.89204529243752,5.00217224846935));
#90795=CARTESIAN_POINT('Ctrl Pts',(1.4375934062324,-1.88642773405491,5.0027916797455));
#90796=CARTESIAN_POINT('Ctrl Pts',(1.45316819196475,-1.87446188814205,5.00410465540781));
#90797=CARTESIAN_POINT('Ctrl Pts',(1.46133334156503,-1.86810332240308,5.00479859800287));
#90798=CARTESIAN_POINT('Ctrl Pts',(1.48297289354837,-1.85102295299052,5.00665289413923));
#90799=CARTESIAN_POINT('Ctrl Pts',(1.49637237518405,-1.84020766843638,5.00781696625321));
#90800=CARTESIAN_POINT('Ctrl Pts',(1.56125125142481,-1.78666403670446,5.01353262124101));
#90801=CARTESIAN_POINT('Ctrl Pts',(1.6110200834607,-1.74192037457744,5.01816574555396));
#90802=CARTESIAN_POINT('Ctrl Pts',(1.83330790602957,-1.52439390648444,5.04007413403612));
#90803=CARTESIAN_POINT('Ctrl Pts',(1.98034589048124,-1.32777732985035,5.05838552306888));
#90804=CARTESIAN_POINT('Ctrl Pts',(2.11187042801126,-1.08005885891602,5.07821024427486));
#90805=CARTESIAN_POINT('Ctrl Pts',(2.12820364740383,-1.04750820622824,5.08075355205018));
#90806=CARTESIAN_POINT('Ctrl Pts',(2.1480719863172,-1.00552741363043,5.08394425545566));
#90807=CARTESIAN_POINT('Ctrl Pts',(2.15230465795632,-0.996435299638573,
5.08463002952955));
#90808=CARTESIAN_POINT('Ctrl Pts',(2.15891810099998,-0.981990330373744,
5.0857109177359));
#90809=CARTESIAN_POINT('Ctrl Pts',(2.1613368711605,-0.976655162806269,5.08610828545883));
#90810=CARTESIAN_POINT('Ctrl Pts',(2.16587910907739,-0.966536670357887,
5.08685834226424));
#90811=CARTESIAN_POINT('Ctrl Pts',(2.16800648774321,-0.961755332687051,
5.08721125513887));
#90812=CARTESIAN_POINT('Ctrl Pts',(2.17294213324031,-0.950562746984249,
5.08803391100381));
#90813=CARTESIAN_POINT('Ctrl Pts',(2.17573786586754,-0.944146065265629,
5.08850288922842));
#90814=CARTESIAN_POINT('Ctrl Pts',(2.18470254003402,-0.923319324040966,
5.09001679556104));
#90815=CARTESIAN_POINT('Ctrl Pts',(2.19075720603034,-0.908860087931752,
5.09105507417976));
#90816=CARTESIAN_POINT('Ctrl Pts',(2.25119467072546,-0.760414472366681,
5.10159508530331));
#90817=CARTESIAN_POINT('Ctrl Pts',(2.29336764291616,-0.621759861784053,
5.11046051488164));
#90818=CARTESIAN_POINT('Ctrl Pts',(2.35781706658475,-0.309969334690424,
5.12997518060536));
#90819=CARTESIAN_POINT('Ctrl Pts',(2.37418193872334,-0.136503456506024,
5.14059314729835));
#90820=CARTESIAN_POINT('Ctrl Pts',(2.37100799731868,0.0659147618968592,
5.15371280471681));
#90821=CARTESIAN_POINT('Ctrl Pts',(2.37003547022854,0.094633145941178,5.15558987951059));
#90822=CARTESIAN_POINT('Ctrl Pts',(2.36793325115636,0.135007450346536,5.15825396071149));
#90823=CARTESIAN_POINT('Ctrl Pts',(2.36723860454223,0.146684268029842,5.1590274107023));
#90824=CARTESIAN_POINT('Ctrl Pts',(2.36587830994447,0.167012476841364,5.16037928113094));
#90825=CARTESIAN_POINT('Ctrl Pts',(2.3652515062043,0.175666313959956,5.16095647681534));
#90826=CARTESIAN_POINT('Ctrl Pts',(2.36384040087466,0.193769245611332,5.16216755474158));
#90827=CARTESIAN_POINT('Ctrl Pts',(2.3630468945568,0.203217447485967,5.16280171568578));
#90828=CARTESIAN_POINT('Ctrl Pts',(2.3610227015092,0.225701838432521,5.16431594111428));
#90829=CARTESIAN_POINT('Ctrl Pts',(2.3597406786836,0.238732976973948,5.1651976026863));
#90830=CARTESIAN_POINT('Ctrl Pts',(2.35502413595331,0.282916283050316,5.16820117808642));
#90831=CARTESIAN_POINT('Ctrl Pts',(2.35108020337706,0.314009581510047,5.17033897575745));
#90832=CARTESIAN_POINT('Ctrl Pts',(2.34013327349309,0.388462155081126,5.17551834039632));
#90833=CARTESIAN_POINT('Ctrl Pts',(2.33253995733963,0.431721555801046,5.17857740405909));
#90834=CARTESIAN_POINT('Ctrl Pts',(2.27178070594458,0.729123237045156,5.19995480941339));
#90835=CARTESIAN_POINT('Ctrl Pts',(2.17841193075139,0.973187009647618,5.21952396464893));
#90836=CARTESIAN_POINT('Ctrl Pts',(2.04430468537211,1.20251970749297,5.23810674015734));
#90837=CARTESIAN_POINT('Ctrl Pts',(2.04120420212942,1.20777510343126,5.23853256220397));
#90838=CARTESIAN_POINT('Ctrl Pts',(2.02801149174943,1.2299411657943,5.24032830990421));
#90839=CARTESIAN_POINT('Ctrl Pts',(2.01772874993391,1.24673839973457,5.2416884410536));
#90840=CARTESIAN_POINT('Ctrl Pts',(2.00303092899154,1.27008957250782,5.24357625061562));
#90841=CARTESIAN_POINT('Ctrl Pts',(1.99879086489227,1.2767519366088,5.24411451539301));
#90842=CARTESIAN_POINT('Ctrl Pts',(1.9918904446736,1.28747585967918,5.24498019769833));
#90843=CARTESIAN_POINT('Ctrl Pts',(1.98925080188293,1.29155057242852,5.2453089565948));
#90844=CARTESIAN_POINT('Ctrl Pts',(1.98364644225597,1.30014386155943,5.24600187864994));
#90845=CARTESIAN_POINT('Ctrl Pts',(1.98067875841125,1.30466046377341,5.24636583343412));
#90846=CARTESIAN_POINT('Ctrl Pts',(1.9733015255347,1.31580489534596,5.24726337145888));
#90847=CARTESIAN_POINT('Ctrl Pts',(1.96887394654821,1.32242081822958,5.24779576024279));
#90848=CARTESIAN_POINT('Ctrl Pts',(1.95227969403864,1.34694874307405,5.24976841498195));
#90849=CARTESIAN_POINT('Ctrl Pts',(1.93990076086245,1.36471683538012,5.25119516177622));
#90850=CARTESIAN_POINT('Ctrl Pts',(1.85086551681803,1.48885350594662,5.26116631366842));
#90851=CARTESIAN_POINT('Ctrl Pts',(1.76573782140808,1.58888863719543,5.26922580514489));
#90852=CARTESIAN_POINT('Ctrl Pts',(1.54566112505676,1.80783736319113,5.28826012583066));
#90853=CARTESIAN_POINT('Ctrl Pts',(1.40464485835204,1.91945505622121,5.29919384371791));
#90854=CARTESIAN_POINT('Ctrl Pts',(1.22821865607946,2.02915953439354,5.31266040889249));
#90855=CARTESIAN_POINT('Ctrl Pts',(1.20376035668701,2.04376377622626,5.31452154708535));
#90856=CARTESIAN_POINT('Ctrl Pts',(1.16893312841347,2.06371733494372,5.31716665624335));
#90857=CARTESIAN_POINT('Ctrl Pts',(1.15877804640699,2.06943647601103,5.31793732999073));
#90858=CARTESIAN_POINT('Ctrl Pts',(1.14099931623052,2.0792772117406,5.31928573446121));
#90859=CARTESIAN_POINT('Ctrl Pts',(1.13339440009178,2.0834323347137,5.31986225648868));
#90860=CARTESIAN_POINT('Ctrl Pts',(1.11741350487005,2.09205047633714,5.32107329740393));
#90861=CARTESIAN_POINT('Ctrl Pts',(1.10903318393702,2.09650507483446,5.32170810206271));
#90862=CARTESIAN_POINT('Ctrl Pts',(1.08898256795578,2.10700921200683,5.32322642888515));
#90863=CARTESIAN_POINT('Ctrl Pts',(1.07728837755898,2.1130122082572,5.3241115709997));
#90864=CARTESIAN_POINT('Ctrl Pts',(1.03726896156589,2.13313686657551,5.32713972252509));
#90865=CARTESIAN_POINT('Ctrl Pts',(1.00871229935887,2.14678809347021,5.32929897025036));
#90866=CARTESIAN_POINT('Ctrl Pts',(0.939383021990174,2.17824157422433,5.33454000822777));
#90867=CARTESIAN_POINT('Ctrl Pts',(0.898367281129536,2.19547548390258,5.33763985028059));
#90868=CARTESIAN_POINT('Ctrl Pts',(0.737103522343717,2.25795933809084,5.34982556919109));
#90869=CARTESIAN_POINT('Ctrl Pts',(0.613753556759715,2.29455910305775,5.35915740439147));
#90870=CARTESIAN_POINT('Ctrl Pts',(0.354389522121256,2.34909869588778,5.37851506146658));
#90871=CARTESIAN_POINT('Ctrl Pts',(0.21852482661771,2.36561005147958,5.38851101048582));
#90872=CARTESIAN_POINT('Ctrl Pts',(0.0628804492293648,2.37099334845528,
5.39934586989299));
#90873=CARTESIAN_POINT('Ctrl Pts',(0.0437697607818828,2.37142313301968,
5.40066538804387));
#90874=CARTESIAN_POINT('Ctrl Pts',(0.0168552671086221,2.37170293423537,
5.40250657254142));
#90875=CARTESIAN_POINT('Ctrl Pts',(0.0090548244163033,2.37174554343568,
5.40303816146754));
#90876=CARTESIAN_POINT('Ctrl Pts',(-0.00406417473779834,2.37175248072662,
5.40392863216674));
#90877=CARTESIAN_POINT('Ctrl Pts',(-0.00938260691341935,2.37173740451699,
5.40428864125856));
#90878=CARTESIAN_POINT('Ctrl Pts',(-0.0202378703297897,2.37167011803773,
5.40502136885009));
#90879=CARTESIAN_POINT('Ctrl Pts',(-0.0257746381442902,2.37161640866097,
5.40539400227327));
#90880=CARTESIAN_POINT('Ctrl Pts',(-0.0398906909192325,2.37143003588349,
5.40634135441722));
#90881=CARTESIAN_POINT('Ctrl Pts',(-0.0484696303383252,2.37127020454241,
5.40691457644622));
#90882=CARTESIAN_POINT('Ctrl Pts',(-0.0834092862056551,2.37042955813712,
5.40923955621948));
#90883=CARTESIAN_POINT('Ctrl Pts',(-0.109759861686733,2.36935567541848,
5.41097074639765));
#90884=CARTESIAN_POINT('Ctrl Pts',(-0.17939097030521,2.36535372603805,5.41549951029122));
#90885=CARTESIAN_POINT('Ctrl Pts',(-0.222619909798855,2.36167741628952,
5.41826417015449));
#90886=CARTESIAN_POINT('Ctrl Pts',(-0.484951876279791,2.33210002859751,
5.43488563560312));
#90887=CARTESIAN_POINT('Ctrl Pts',(-0.699658592419328,2.2769185362823,5.44793094355953));
#90888=CARTESIAN_POINT('Ctrl Pts',(-0.958812910309933,2.17012321162726,
5.46571199991051));
#90889=CARTESIAN_POINT('Ctrl Pts',(-1.01308820929539,2.14532241894269,5.46955127722558));
#90890=CARTESIAN_POINT('Ctrl Pts',(-1.0817868368128,2.11074235593228,5.47459211989386));
#90891=CARTESIAN_POINT('Ctrl Pts',(-1.09712049242692,2.10281303313422,5.47572917985459));
#90892=CARTESIAN_POINT('Ctrl Pts',(-1.12151439987146,2.08985904077007,5.47755796441454));
#90893=CARTESIAN_POINT('Ctrl Pts',(-1.13063085337342,2.08494106079851,5.4782459103448));
#90894=CARTESIAN_POINT('Ctrl Pts',(-1.14769912161092,2.07558851446122,5.47954253797135));
#90895=CARTESIAN_POINT('Ctrl Pts',(-1.15565821049458,2.07116755759574,5.48015072492854));
#90896=CARTESIAN_POINT('Ctrl Pts',(-1.17347510705874,2.06113630925734,5.48152030808656));
#90897=CARTESIAN_POINT('Ctrl Pts',(-1.18331846438394,2.05550094047568,5.48228259652656));
#90898=CARTESIAN_POINT('Ctrl Pts',(-1.20389611576184,2.04352334164099,5.483888201854));
#90899=CARTESIAN_POINT('Ctrl Pts',(-1.21462155052786,2.03716665592162,5.48473202691521));
#90900=CARTESIAN_POINT('Ctrl Pts',(-1.24259652983613,2.02028715623742,5.48695149894768));
#90901=CARTESIAN_POINT('Ctrl Pts',(-1.25976228369973,2.009628143272,5.48833206544398));
#90902=CARTESIAN_POINT('Ctrl Pts',(-1.31090147666786,1.97696076157795,5.49250226241416));
#90903=CARTESIAN_POINT('Ctrl Pts',(-1.34444832784393,1.95430163707798,5.49531520107348));
#90904=CARTESIAN_POINT('Ctrl Pts',(-1.53173742655295,1.82069277851525,5.51146902654031));
#90905=CARTESIAN_POINT('Ctrl Pts',(-1.67230338136944,1.6924902086597,5.52543729189875));
#90906=CARTESIAN_POINT('Ctrl Pts',(-1.8565585671351,1.47883808364882,5.54592444941382));
#90907=CARTESIAN_POINT('Ctrl Pts',(-1.9128802612953,1.40522775579877,5.55256759423489));
#90908=CARTESIAN_POINT('Ctrl Pts',(-1.97182491919088,1.31805299950105,5.55982784780263));
#90909=CARTESIAN_POINT('Ctrl Pts',(-1.97880820070951,1.30754554179505,5.56069338749701));
#90910=CARTESIAN_POINT('Ctrl Pts',(-1.98925862857628,1.2915457177675,5.56199635025198));
#90911=CARTESIAN_POINT('Ctrl Pts',(-1.99278747019717,1.2860942164689,5.56243768847128));
#90912=CARTESIAN_POINT('Ctrl Pts',(-1.9990932796895,1.27626447108673,5.56322869672522));
#90913=CARTESIAN_POINT('Ctrl Pts',(-2.00187830768283,1.2718915771005,5.5635788906497));
#90914=CARTESIAN_POINT('Ctrl Pts',(-2.0079582900927,1.2622756873784,5.56434524042111));
#90915=CARTESIAN_POINT('Ctrl Pts',(-2.01124705504146,1.25702891434748,5.56476098901073));
#90916=CARTESIAN_POINT('Ctrl Pts',(-2.02062120504914,1.24194277246746,5.56594971624367));
#90917=CARTESIAN_POINT('Ctrl Pts',(-2.02665530401196,1.23207150631075,5.56671942052561));
#90918=CARTESIAN_POINT('Ctrl Pts',(-2.06863063011897,1.16226065679106,5.57210893393199));
#90919=CARTESIAN_POINT('Ctrl Pts',(-2.10198319899789,1.10079575299984,5.57657615674104));
#90920=CARTESIAN_POINT('Ctrl Pts',(-2.23248519754584,0.832663616592894,
5.59529173423322));
#90921=CARTESIAN_POINT('Ctrl Pts',(-2.30223425814597,0.614040601513204,
5.60878614194203));
#90922=CARTESIAN_POINT('Ctrl Pts',(-2.34765271186541,0.340734190738411,
5.62648121305212));
#90923=CARTESIAN_POINT('Ctrl Pts',(-2.3541576934841,0.292427874392742,5.6296328163226));
#90924=CARTESIAN_POINT('Ctrl Pts',(-2.36081779389675,0.228022097629499,
5.63388261605264));
#90925=CARTESIAN_POINT('Ctrl Pts',(-2.36230416096772,0.212070184214435,
5.63493904269972));
#90926=CARTESIAN_POINT('Ctrl Pts',(-2.36426539688882,0.188431626328554,
5.6365106903392));
#90927=CARTESIAN_POINT('Ctrl Pts',(-2.36486464284438,0.180755533574063,
5.63702200834809));
#90928=CARTESIAN_POINT('Ctrl Pts',(-2.36542649454145,0.17307675008899,5.63753449772568));
#90929=CARTESIAN_POINT('Origin',(0.,0.,-1.84858989190503));
#90930=CARTESIAN_POINT('',(-2.36542649097266,0.173076798863304,6.83516330511797));
#90931=CARTESIAN_POINT('',(-2.36542649458272,0.173076749524953,6.63992069752827));
#90932=CARTESIAN_POINT('',(-2.36542649454111,0.173076750093529,-1.84858989190503));
#90933=CARTESIAN_POINT('',(-2.37174936880892,-0.00173018488177715,5.84847577200946));
#90934=CARTESIAN_POINT('Ctrl Pts',(-2.36542649097266,0.173076798863304,
6.83516330511797));
#90935=CARTESIAN_POINT('Ctrl Pts',(-2.36239649348597,0.214487527335679,
6.83221060003601));
#90936=CARTESIAN_POINT('Ctrl Pts',(-2.35827870088117,0.255823468632288,
6.82929290278159));
#90937=CARTESIAN_POINT('Ctrl Pts',(-2.35149985856541,0.309523430433347,
6.82555870176947));
#90938=CARTESIAN_POINT('Ctrl Pts',(-2.3498248886175,0.321992778120867,6.82469558143828));
#90939=CARTESIAN_POINT('Ctrl Pts',(-2.34714360213076,0.340817188454468,
6.82339917369846));
#90940=CARTESIAN_POINT('Ctrl Pts',(-2.34621055351314,0.34718220871066,6.82296196878176));
#90941=CARTESIAN_POINT('Ctrl Pts',(-2.34448962924959,0.358598062692276,
6.82217997809001));
#90942=CARTESIAN_POINT('Ctrl Pts',(-2.34371131539799,0.363650194419785,
6.82183466813806));
#90943=CARTESIAN_POINT('Ctrl Pts',(-2.34197284299442,0.374697378334203,
6.82108127597791));
#90944=CARTESIAN_POINT('Ctrl Pts',(-2.34100599849535,0.380691265673151,
6.82067357548603));
#90945=CARTESIAN_POINT('Ctrl Pts',(-2.33818227512663,0.397779124639109,
6.81951414891658));
#90946=CARTESIAN_POINT('Ctrl Pts',(-2.33626944621218,0.408863878237154,
6.81876550452044));
#90947=CARTESIAN_POINT('Ctrl Pts',(-2.32282569984133,0.48359317605611,6.81373926659921));
#90948=CARTESIAN_POINT('Ctrl Pts',(-2.30877312776872,0.546763186882581,
6.80959251326109));
#90949=CARTESIAN_POINT('Ctrl Pts',(-2.23457759216252,0.825889316317598,
6.7914090291213));
#90950=CARTESIAN_POINT('Ctrl Pts',(-2.14659191612895,1.03324007164408,6.77816957430384));
#90951=CARTESIAN_POINT('Ctrl Pts',(-2.00129232220707,1.27408424848588,6.76029845111335));
#90952=CARTESIAN_POINT('Ctrl Pts',(-1.97002650167567,1.32191390451803,6.75661758667882));
#90953=CARTESIAN_POINT('Ctrl Pts',(-1.92734144344122,1.38233030482115,6.75176727899503));
#90954=CARTESIAN_POINT('Ctrl Pts',(-1.91747013737626,1.39599081625172,6.75065680995948));
#90955=CARTESIAN_POINT('Ctrl Pts',(-1.90140709650536,1.41772798908525,6.7488668939515));
#90956=CARTESIAN_POINT('Ctrl Pts',(-1.8953073853557,1.42587219174202,6.74819102848461));
#90957=CARTESIAN_POINT('Ctrl Pts',(-1.88361503506092,1.44127597549491,6.74690255842353));
#90958=CARTESIAN_POINT('Ctrl Pts',(-1.87803234479443,1.44854290432811,6.74629035306979));
#90959=CARTESIAN_POINT('Ctrl Pts',(-1.86521349796526,1.46503039152873,6.74489128417443));
#90960=CARTESIAN_POINT('Ctrl Pts',(-1.8579508696085,1.47422996802471,6.74410337659854));
#90961=CARTESIAN_POINT('Ctrl Pts',(-1.83545124181449,1.50229992079303,6.74167660432467));
#90962=CARTESIAN_POINT('Ctrl Pts',(-1.81999313703158,1.52099020965799,6.74002888214876));
#90963=CARTESIAN_POINT('Ctrl Pts',(-1.78369035365146,1.56353774256823,6.73620223779732));
#90964=CARTESIAN_POINT('Ctrl Pts',(-1.76264926320664,1.58722051355428,6.73401550344207));
#90965=CARTESIAN_POINT('Ctrl Pts',(-1.68822861194474,1.66767934887966,6.72638477565455));
#90966=CARTESIAN_POINT('Ctrl Pts',(-1.63253423415591,1.72223694943101,6.72084932730787));
#90967=CARTESIAN_POINT('Ctrl Pts',(-1.47559444271971,1.86151038281402,6.70573375783291));
#90968=CARTESIAN_POINT('Ctrl Pts',(-1.36979656621939,1.94068402486398,6.69602356115621));
#90969=CARTESIAN_POINT('Ctrl Pts',(-1.23861700942068,2.02275735788989,6.68479647408051));
#90970=CARTESIAN_POINT('Ctrl Pts',(-1.219085787577,2.0345882408334,6.68314503689447));
#90971=CARTESIAN_POINT('Ctrl Pts',(-1.1809542949778,2.05693983679522,6.67996320328007));
#90972=CARTESIAN_POINT('Ctrl Pts',(-1.16237655377124,2.06749494178062,6.67843198943586));
#90973=CARTESIAN_POINT('Ctrl Pts',(-1.10166096604134,2.10091392103701,6.67349418857176));
#90974=CARTESIAN_POINT('Ctrl Pts',(-1.05896880896651,2.12275340681874,6.67012446048209));
#90975=CARTESIAN_POINT('Ctrl Pts',(-1.00591391596295,2.14789457557882,6.66608520275205));
#90976=CARTESIAN_POINT('Ctrl Pts',(-0.996155792751487,2.15243758604564,
6.66534830854618));
#90977=CARTESIAN_POINT('Ctrl Pts',(-0.980880856537691,2.15942288535779,
6.66420456417137));
#90978=CARTESIAN_POINT('Ctrl Pts',(-0.975385235201043,2.16191075152279,
6.66379502528418));
#90979=CARTESIAN_POINT('Ctrl Pts',(-0.96521255310511,2.16646923600531,6.66304063980613));
#90980=CARTESIAN_POINT('Ctrl Pts',(-0.960538314210664,2.16854568111346,
6.66269545061306));
#90981=CARTESIAN_POINT('Ctrl Pts',(-0.949924806382464,2.1732194880845,6.66191488758089));
#90982=CARTESIAN_POINT('Ctrl Pts',(-0.943981590558935,2.17580762945389,
6.66148007771738));
#90983=CARTESIAN_POINT('Ctrl Pts',(-0.925863766115912,2.18360933948141,
6.66016126776235));
#90984=CARTESIAN_POINT('Ctrl Pts',(-0.913655775259458,2.18874544095387,
6.6592818166453));
#90985=CARTESIAN_POINT('Ctrl Pts',(-0.784084368184924,2.2419852216568,6.65003775837734));
#90986=CARTESIAN_POINT('Ctrl Pts',(-0.663066909302293,2.28070998719904,
6.6421772597597));
#90987=CARTESIAN_POINT('Ctrl Pts',(-0.346534459684943,2.35465203887098,
6.62220805594224));
#90988=CARTESIAN_POINT('Ctrl Pts',(-0.148687939204253,2.37536420871635,
6.61021155508095));
#90989=CARTESIAN_POINT('Ctrl Pts',(0.0769607245850977,2.37066103469526,
6.59556293067362));
#90990=CARTESIAN_POINT('Ctrl Pts',(0.104484942857661,2.36960745435298,6.59376141024054));
#90991=CARTESIAN_POINT('Ctrl Pts',(0.144164511526693,2.36739593015381,6.59114035539814));
#90992=CARTESIAN_POINT('Ctrl Pts',(0.15633974470815,2.36662307334932,6.59033286143499));
#90993=CARTESIAN_POINT('Ctrl Pts',(0.177746557087909,2.36509830718153,6.58890714294588));
#90994=CARTESIAN_POINT('Ctrl Pts',(0.186980782203273,2.36438618336646,6.58829017892366));
#90995=CARTESIAN_POINT('Ctrl Pts',(0.206034672480333,2.36280446840757,6.58701299270216));
#90996=CARTESIAN_POINT('Ctrl Pts',(0.2158535457556,2.36192770505005,6.58635255650918));
#90997=CARTESIAN_POINT('Ctrl Pts',(0.241004539067627,2.35952373967243,6.58465487561567));
#90998=CARTESIAN_POINT('Ctrl Pts',(0.2563275621908,2.35790831611662,6.58361487549254));
#90999=CARTESIAN_POINT('Ctrl Pts',(0.320629590791626,2.3504951089313,6.57922586537475));
#91000=CARTESIAN_POINT('Ctrl Pts',(0.369434156124747,2.34331994471636,6.57583393054837));
#91001=CARTESIAN_POINT('Ctrl Pts',(0.498794164553883,2.32016018356242,6.56667387718558));
#91002=CARTESIAN_POINT('Ctrl Pts',(0.578797865108882,2.30150591841724,6.56082960592347));
#91003=CARTESIAN_POINT('Ctrl Pts',(0.80300077726726,2.23679887355092,6.543985425435));
#91004=CARTESIAN_POINT('Ctrl Pts',(0.94398233663671,2.18104900126282,6.53280808610936));
#91005=CARTESIAN_POINT('Ctrl Pts',(1.13644471084273,2.0827617950108,6.517269451714));
#91006=CARTESIAN_POINT('Ctrl Pts',(1.1929696263991,2.05090918332885,6.51267288432958));
#91007=CARTESIAN_POINT('Ctrl Pts',(1.25721813593359,2.0111476883741,6.5074667578661));
#91008=CARTESIAN_POINT('Ctrl Pts',(1.26627528432626,2.00545739941599,6.50673330671539));
#91009=CARTESIAN_POINT('Ctrl Pts',(1.28085467965955,1.99615952564365,6.50555379588315));
#91010=CARTESIAN_POINT('Ctrl Pts',(1.28640078951203,1.99258991607556,6.50510536912282));
#91011=CARTESIAN_POINT('Ctrl Pts',(1.2962287643113,1.98620625923233,6.50431131368709));
#91012=CARTESIAN_POINT('Ctrl Pts',(1.30051646938115,1.98340142894344,6.50396508907988));
#91013=CARTESIAN_POINT('Ctrl Pts',(1.30976403916918,1.97730918907636,6.50321881906587));
#91014=CARTESIAN_POINT('Ctrl Pts',(1.31472062827064,1.97401700577413,6.50281909904628));
#91015=CARTESIAN_POINT('Ctrl Pts',(1.32854401471498,1.96476030504954,6.50170492758854));
#91016=CARTESIAN_POINT('Ctrl Pts',(1.33738310919335,1.95875437086076,6.50099319098197));
#91017=CARTESIAN_POINT('Ctrl Pts',(1.3898583082066,1.92257802546464,6.49677004216902));
#91018=CARTESIAN_POINT('Ctrl Pts',(1.43251658981317,1.89100756805329,6.49334612324831));
#91019=CARTESIAN_POINT('Ctrl Pts',(1.57351228088135,1.77914745700038,6.48192647386613));
#91020=CARTESIAN_POINT('Ctrl Pts',(1.66645642123609,1.69240497841442,6.47421228289519));
#91021=CARTESIAN_POINT('Ctrl Pts',(1.85970314041212,1.48061699369025,6.45663122934411));
#91022=CARTESIAN_POINT('Ctrl Pts',(1.95517308434902,1.35203933031459,6.44674944940347));
#91023=CARTESIAN_POINT('Ctrl Pts',(2.04657249037062,1.19878649602293,6.43509740902278));
#91024=CARTESIAN_POINT('Ctrl Pts',(2.05596399159708,1.18260731168867,6.43386926048223));
#91025=CARTESIAN_POINT('Ctrl Pts',(2.07091594983215,1.1561323705261,6.43186185702301));
#91026=CARTESIAN_POINT('Ctrl Pts',(2.07659345541119,1.1459033737946,6.43108681478807));
#91027=CARTESIAN_POINT('Ctrl Pts',(2.08658153605222,1.12759012273576,6.42970000073125));
#91028=CARTESIAN_POINT('Ctrl Pts',(2.090921415242,1.11952205101748,6.42908928938134));
#91029=CARTESIAN_POINT('Ctrl Pts',(2.09998831305486,1.10242955795379,6.42779592282349));
#91030=CARTESIAN_POINT('Ctrl Pts',(2.1047041365032,1.09339944090773,6.4271128863998));
#91031=CARTESIAN_POINT('Ctrl Pts',(2.11709219046754,1.06930100238087,6.42529061481575));
#91032=CARTESIAN_POINT('Ctrl Pts',(2.12466158536467,1.0541807712242,6.42414779940345));
#91033=CARTESIAN_POINT('Ctrl Pts',(2.16054448767759,0.980546327184998,6.41858390131191));
#91034=CARTESIAN_POINT('Ctrl Pts',(2.18660346630006,0.920970921135726,6.4140858473953));
#91035=CARTESIAN_POINT('Ctrl Pts',(2.29725064503045,0.636744068258404,6.39262505281426));
#91036=CARTESIAN_POINT('Ctrl Pts',(2.34985058937652,0.40121469531636,6.37465229600322));
#91037=CARTESIAN_POINT('Ctrl Pts',(2.36910922974393,0.11962189203901,6.35461662334392));
#91038=CARTESIAN_POINT('Ctrl Pts',(2.37086628401135,0.0773405126507377,
6.35165172948856));
#91039=CARTESIAN_POINT('Ctrl Pts',(2.37164411208569,0.0246849394310393,
6.34803110781958));
#91040=CARTESIAN_POINT('Ctrl Pts',(2.37172924227082,0.0143370814770219,
6.34732303521107));
#91041=CARTESIAN_POINT('Ctrl Pts',(2.37175663163015,-0.00194883477221039,
6.34621441346017));
#91042=CARTESIAN_POINT('Ctrl Pts',(2.37174432059112,-0.00788653020719567,
6.34581142806732));
#91043=CARTESIAN_POINT('Ctrl Pts',(2.37168012137295,-0.0189006875714829,
6.3450662263417));
#91044=CARTESIAN_POINT('Ctrl Pts',(2.37163423381124,-0.0239769861441997,
6.34472369387298));
#91045=CARTESIAN_POINT('Ctrl Pts',(2.37149135694326,-0.0356398036958509,
6.34393880520891));
#91046=CARTESIAN_POINT('Ctrl Pts',(2.37138322748416,-0.0422260905602065,
6.34349707517851));
#91047=CARTESIAN_POINT('Ctrl Pts',(2.37096407876875,-0.0625880218969371,
6.34213588968068));
#91048=CARTESIAN_POINT('Ctrl Pts',(2.37056044527093,-0.0763617779763865,
6.34122142065141));
#91049=CARTESIAN_POINT('Ctrl Pts',(2.36549601564208,-0.209532377360633,
6.33243409190259));
#91050=CARTESIAN_POINT('Ctrl Pts',(2.35193797877032,-0.328437652506021,
6.32500495603257));
#91051=CARTESIAN_POINT('Ctrl Pts',(2.29074641445491,-0.648165588870033,
6.30498109131401));
#91052=CARTESIAN_POINT('Ctrl Pts',(2.22583241613452,-0.844570418934279,
6.29254817703081));
#91053=CARTESIAN_POINT('Ctrl Pts',(2.12593444838301,-1.05174980904635,6.27760889007402));
#91054=CARTESIAN_POINT('Ctrl Pts',(2.11517495783682,-1.07322400679646,6.27603828328488));
#91055=CARTESIAN_POINT('Ctrl Pts',(2.0986001394902,-1.10508692452149,6.27367262235648));
#91056=CARTESIAN_POINT('Ctrl Pts',(2.09302948632704,-1.11560172861481,6.27288612652966));
#91057=CARTESIAN_POINT('Ctrl Pts',(2.08327516106729,-1.13368311898736,6.27152334071085));
#91058=CARTESIAN_POINT('Ctrl Pts',(2.07912876433113,-1.14126963901535,6.2709483809903));
#91059=CARTESIAN_POINT('Ctrl Pts',(2.07044794557262,-1.15694831757623,6.26975346474412));
#91060=CARTESIAN_POINT('Ctrl Pts',(2.06590735222598,-1.16503687180161,6.26913329460183));
#91061=CARTESIAN_POINT('Ctrl Pts',(2.05513560747416,-1.18396453015402,6.26767318929662));
#91062=CARTESIAN_POINT('Ctrl Pts',(2.04886601573737,-1.19478132429664,6.26683187729822));
#91063=CARTESIAN_POINT('Ctrl Pts',(2.02802526295338,-1.23009097417759,6.26406252045436));
#91064=CARTESIAN_POINT('Ctrl Pts',(2.01309861498401,-1.2543700070325,6.26212160173201));
#91065=CARTESIAN_POINT('Ctrl Pts',(1.97674626518233,-1.31117852711607,6.25749045480803));
#91066=CARTESIAN_POINT('Ctrl Pts',(1.95495012253785,-1.34345995146858,6.25478708793931));
#91067=CARTESIAN_POINT('Ctrl Pts',(1.82171218888216,-1.5306815527133,6.23867546737853));
#91068=CARTESIAN_POINT('Ctrl Pts',(1.69270118782702,-1.67223290701709,6.22462038490807));
#91069=CARTESIAN_POINT('Ctrl Pts',(1.47644817419918,-1.85856387333622,6.20387963443048));
#91070=CARTESIAN_POINT('Ctrl Pts',(1.40109084863731,-1.91601349107674,6.19708261345989));
#91071=CARTESIAN_POINT('Ctrl Pts',(1.31208938842366,-1.97579769915946,6.18968618277438));
#91072=CARTESIAN_POINT('Ctrl Pts',(1.30163103559756,-1.98270314865796,6.18882646169767));
#91073=CARTESIAN_POINT('Ctrl Pts',(1.28573070573171,-1.99302179191498,6.18753413871277));
#91074=CARTESIAN_POINT('Ctrl Pts',(1.28032899656168,-1.99649617423959,6.18709765501801));
#91075=CARTESIAN_POINT('Ctrl Pts',(1.27060323232783,-2.00269608591159,6.18631642615164));
#91076=CARTESIAN_POINT('Ctrl Pts',(1.26628444068462,-2.00542960569357,6.18597116143956));
#91077=CARTESIAN_POINT('Ctrl Pts',(1.25680901165208,-2.01138413390584,6.18521725031906));
#91078=CARTESIAN_POINT('Ctrl Pts',(1.25164882135281,-2.01459927926368,6.1848089895165));
#91079=CARTESIAN_POINT('Ctrl Pts',(1.23687285453848,-2.02372701297762,6.18364636149306));
#91080=CARTESIAN_POINT('Ctrl Pts',(1.22722698979042,-2.02959094635472,6.1828951027205));
#91081=CARTESIAN_POINT('Ctrl Pts',(1.16120693031008,-2.06908322225391,6.17780290500921));
#91082=CARTESIAN_POINT('Ctrl Pts',(1.10349371200586,-2.10043099382029,6.17359677600057));
#91083=CARTESIAN_POINT('Ctrl Pts',(0.831022780086311,-2.23409127172142,
6.15450100693689));
#91084=CARTESIAN_POINT('Ctrl Pts',(0.602960272125606,-2.30612538574392,
6.14049064105049));
#91085=CARTESIAN_POINT('Ctrl Pts',(0.323316549712038,-2.35004437495338,
6.12236868443929));
#91086=CARTESIAN_POINT('Ctrl Pts',(0.278463526682619,-2.35578008010954,
6.11943997061636));
#91087=CARTESIAN_POINT('Ctrl Pts',(0.218085951187239,-2.36175268805271,
6.11545539589988));
#91088=CARTESIAN_POINT('Ctrl Pts',(0.202681441791024,-2.36312451128064,
6.11443514744303));
#91089=CARTESIAN_POINT('Ctrl Pts',(0.177425231078782,-2.36512489663515,
6.11275598315232));
#91090=CARTESIAN_POINT('Ctrl Pts',(0.167580904629891,-2.36584279373594,
6.11209988370629));
#91091=CARTESIAN_POINT('Ctrl Pts',(0.148496615315916,-2.36711480465946,
6.11082474215954));
#91092=CARTESIAN_POINT('Ctrl Pts',(0.139257311593275,-2.36767631659477,
6.11020594446512));
#91093=CARTESIAN_POINT('Ctrl Pts',(0.117651506328053,-2.36886249157385,
6.10875537773273));
#91094=CARTESIAN_POINT('Ctrl Pts',(0.105283026177298,-2.36944441909614,
6.10792228376503));
#91095=CARTESIAN_POINT('Ctrl Pts',(0.0651145845503644,-2.37101918341653,
6.10520760035641));
#91096=CARTESIAN_POINT('Ctrl Pts',(0.0373024771205957,-2.37161976028034,
6.10331383010153));
#91097=CARTESIAN_POINT('Ctrl Pts',(-0.109459459548115,-2.37220682773543,
6.09324179139596));
#91098=CARTESIAN_POINT('Ctrl Pts',(-0.228254854195834,-2.36373401639321,
6.08480339288133));
#91099=CARTESIAN_POINT('Ctrl Pts',(-0.471229339202864,-2.32791542711345,
6.06703192592368));
#91100=CARTESIAN_POINT('Ctrl Pts',(-0.594874432469824,-2.2994283066647,
6.05770387292772));
#91101=CARTESIAN_POINT('Ctrl Pts',(-0.745299102759525,-2.25182023655606,
6.04628897149488));
#91102=CARTESIAN_POINT('Ctrl Pts',(-0.77476098578532,-2.24185429428373,
6.04405081447384));
#91103=CARTESIAN_POINT('Ctrl Pts',(-0.852195690335419,-2.21395187149007,
6.03817494336151));
#91104=CARTESIAN_POINT('Ctrl Pts',(-0.899801647534457,-2.19503492170247,
6.03456928572836));
#91105=CARTESIAN_POINT('Ctrl Pts',(-0.95594151689227,-2.17059303460668,
6.03035523432686));
#91106=CARTESIAN_POINT('Ctrl Pts',(-0.965096174326821,-2.16653818078733,
6.02966929276538));
#91107=CARTESIAN_POINT('Ctrl Pts',(-0.980050032561339,-2.15980110498478,
6.02855118524911));
#91108=CARTESIAN_POINT('Ctrl Pts',(-0.985864444278068,-2.15715325820128,
6.02811702641031));
#91109=CARTESIAN_POINT('Ctrl Pts',(-0.996309660260205,-2.15234551848709,
6.02733824087445));
#91110=CARTESIAN_POINT('Ctrl Pts',(-1.00094422111427,-2.15019413956728,
6.02699310960761));
#91111=CARTESIAN_POINT('Ctrl Pts',(-1.00558943402976,-2.14801954205282,
6.02664760545554));
#91112=CARTESIAN_POINT('Ctrl Pts',(-1.00560692740749,-2.14801135248936,
6.02664630432953));
#91113=CARTESIAN_POINT('Ctrl Pts',(-1.00564165457892,-2.14799509437007,
6.02664372139654));
#91114=CARTESIAN_POINT('Ctrl Pts',(-1.00565888841172,-2.1479870258036,6.02664243958649));
#91115=CARTESIAN_POINT('Ctrl Pts',(-1.00569310075358,-2.1479710077066,6.02663989496804));
#91116=CARTESIAN_POINT('Ctrl Pts',(-1.00571007929939,-2.14796305816629,
6.02663863215674));
#91117=CARTESIAN_POINT('Ctrl Pts',(-1.00574378533899,-2.1479472761437,6.02663612521757));
#91118=CARTESIAN_POINT('Ctrl Pts',(-1.00576051281802,-2.14793944367554,
6.02663488109065));
#91119=CARTESIAN_POINT('Ctrl Pts',(-1.00579372078305,-2.14792389391816,
6.02663241121784));
#91120=CARTESIAN_POINT('Ctrl Pts',(-1.00581020127874,-2.14791617663139,
6.02663118547109));
#91121=CARTESIAN_POINT('Ctrl Pts',(-1.00584291946799,-2.14790085529514,
6.02662875204647));
#91122=CARTESIAN_POINT('Ctrl Pts',(-1.00585915709539,-2.14789325128341,
6.02662754437337));
#91123=CARTESIAN_POINT('Ctrl Pts',(-1.00589139327967,-2.14787815476995,
6.02662514681806));
#91124=CARTESIAN_POINT('Ctrl Pts',(-1.00590739191761,-2.14787066223682,
6.02662395692967));
#91125=CARTESIAN_POINT('Ctrl Pts',(-1.00593915416863,-2.14785578680541,
6.02662159464244));
#91126=CARTESIAN_POINT('Ctrl Pts',(-1.00595491774891,-2.14784840392887,
6.0266204222459));
#91127=CARTESIAN_POINT('Ctrl Pts',(-1.00598621372859,-2.14783374602929,
6.02661809465605));
#91128=CARTESIAN_POINT('Ctrl Pts',(-1.00600174609874,-2.14782647102611,
6.02661693946477));
#91129=CARTESIAN_POINT('Ctrl Pts',(-1.00603258327955,-2.14781202719547,
6.02661464601571));
#91130=CARTESIAN_POINT('Ctrl Pts',(-1.00604788814422,-2.14780485834868,
6.02661350775376));
#91131=CARTESIAN_POINT('Ctrl Pts',(-1.00607861960909,-2.14779046323324,
6.02661122218509));
#91132=CARTESIAN_POINT('Ctrl Pts',(-1.0060940462051,-2.14778323696337,6.02661007487874));
#91133=CARTESIAN_POINT('Ctrl Pts',(-1.00612485059905,-2.14776880687737,
6.02660778390434));
#91134=CARTESIAN_POINT('Ctrl Pts',(-1.00614022835534,-2.14776160308202,
6.02660664023936));
#91135=CARTESIAN_POINT('Ctrl Pts',(-1.00617093524703,-2.14774721786589,
6.02660435653443));
#91136=CARTESIAN_POINT('Ctrl Pts',(-1.00618626441533,-2.14774003643097,
6.026603216492));
#91137=CARTESIAN_POINT('Ctrl Pts',(-1.00621687448557,-2.14772569577338,
6.02660094000573));
#91138=CARTESIAN_POINT('Ctrl Pts',(-1.00623215537904,-2.14771853655595,
6.02659980356248));
#91139=CARTESIAN_POINT('Ctrl Pts',(-1.00626266914499,-2.14770424022214,
6.02659753425622));
#91140=CARTESIAN_POINT('Ctrl Pts',(-1.00627790204101,-2.14769710309599,
6.02659640139144));
#91141=CARTESIAN_POINT('Ctrl Pts',(-1.00630832007796,-2.14768285082391,
6.02659413922225));
#91142=CARTESIAN_POINT('Ctrl Pts',(-1.00632350524556,-2.1476757356667,6.02659300991583));
#91143=CARTESIAN_POINT('Ctrl Pts',(-1.00635382818239,-2.14766152716906,
6.02659075483677));
#91144=CARTESIAN_POINT('Ctrl Pts',(-1.00636896593287,-2.14765443383862,
6.02658962906549));
#91145=CARTESIAN_POINT('Ctrl Pts',(-1.0063991942562,-2.14764026889472,6.02658738104019));
#91146=CARTESIAN_POINT('Ctrl Pts',(-1.00641428484788,-2.14763319727366,
6.02658625878474));
#91147=CARTESIAN_POINT('Ctrl Pts',(-1.00644441918803,-2.14761907559541,
6.02658401776616));
#91148=CARTESIAN_POINT('Ctrl Pts',(-1.00645946292222,-2.14761202554612,
6.02658289900406));
#91149=CARTESIAN_POINT('Ctrl Pts',(-1.00648950375712,-2.14759794691675,
6.0265806649565));
#91150=CARTESIAN_POINT('Ctrl Pts',(-1.00650450087375,-2.1475909183304,6.02657954966982));
#91151=CARTESIAN_POINT('Ctrl Pts',(-1.00653444889226,-2.1475768824342,6.02657732254188));
#91152=CARTESIAN_POINT('Ctrl Pts',(-1.00654939972445,-2.14756987515819,
6.02657621070577));
#91153=CARTESIAN_POINT('Ctrl Pts',(-1.00657925534405,-2.14755588180656,
6.02657399046623));
#91154=CARTESIAN_POINT('Ctrl Pts',(-1.00659416014469,-2.14754889572591,
6.0265728820618));
#91155=CARTESIAN_POINT('Ctrl Pts',(-1.00662392395113,-2.14753494465132,
6.02657066866696));
#91156=CARTESIAN_POINT('Ctrl Pts',(-1.00663878298614,-2.14752797964485,
6.02656956367435));
#91157=CARTESIAN_POINT('Ctrl Pts',(-1.00666845552237,-2.14751407059974,
6.02656735708365));
#91158=CARTESIAN_POINT('Ctrl Pts',(-1.00668326904571,-2.14750712655188,
6.0265662554839));
#91159=CARTESIAN_POINT('Ctrl Pts',(-1.00671285092441,-2.14749325925594,
6.02656405565164));
#91160=CARTESIAN_POINT('Ctrl Pts',(-1.00672761924087,-2.14748633602723,
6.026562957422));
#91161=CARTESIAN_POINT('Ctrl Pts',(-1.00675711092601,-2.14747251026977,
6.02656076431351));
#91162=CARTESIAN_POINT('Ctrl Pts',(-1.00677183429801,-2.14746560774059,
6.02655966943439));
#91163=CARTESIAN_POINT('Ctrl Pts',(-1.01238901536777,-2.14483212176056,
6.0261419586633));
#91164=CARTESIAN_POINT('Ctrl Pts',(-1.01798125389777,-2.14218358641286,
6.02572670067114));
#91165=CARTESIAN_POINT('Ctrl Pts',(-1.03429204886649,-2.13438034925337,
6.02451708883166));
#91166=CARTESIAN_POINT('Ctrl Pts',(-1.04498247192894,-2.12916677732829,
6.0237262667899));
#91167=CARTESIAN_POINT('Ctrl Pts',(-1.0694490556912,-2.11700609399699,6.02191988688929));
#91168=CARTESIAN_POINT('Ctrl Pts',(-1.08319770121043,-2.11000446768699,
6.02090741321021));
#91169=CARTESIAN_POINT('Ctrl Pts',(-1.12846896679929,-2.08639052339599,
6.01757893478856));
#91170=CARTESIAN_POINT('Ctrl Pts',(-1.15968692821761,-2.06920132863935,
6.01529238185314));
#91171=CARTESIAN_POINT('Ctrl Pts',(-1.30804532298124,-1.98309957077005,
6.00441059785337));
#91172=CARTESIAN_POINT('Ctrl Pts',(-1.4195119398381,-1.90490371468249,5.99617609143742));
#91173=CARTESIAN_POINT('Ctrl Pts',(-1.54207211375442,-1.80216204176423,
5.98635844464451));
#91174=CARTESIAN_POINT('Ctrl Pts',(-1.56023490247544,-1.78646059504067,
5.9848822653925));
#91175=CARTESIAN_POINT('Ctrl Pts',(-1.6725712424867,-1.68632749833562,5.97560057057227));
#91176=CARTESIAN_POINT('Ctrl Pts',(-1.76009059158471,-1.59476314563626,
5.96767438752151));
#91177=CARTESIAN_POINT('Ctrl Pts',(-1.85167919458033,-1.48217118031905,
5.95819656984604));
#91178=CARTESIAN_POINT('Ctrl Pts',(-1.86329908656174,-1.46753661915126,
5.9569697594968));
#91179=CARTESIAN_POINT('Ctrl Pts',(-1.88190675446481,-1.44352407375356,
5.95496411162887));
#91180=CARTESIAN_POINT('Ctrl Pts',(-1.88900037851996,-1.43422883308548,
5.9541894744489));
#91181=CARTESIAN_POINT('Ctrl Pts',(-1.90152828644079,-1.41755851882537,
5.95280311144105));
#91182=CARTESIAN_POINT('Ctrl Pts',(-1.90698915853618,-1.41020364614544,
5.9521924434639));
#91183=CARTESIAN_POINT('Ctrl Pts',(-1.9184348070306,-1.39460023214132,5.95089888285282));
#91184=CARTESIAN_POINT('Ctrl Pts',(-1.92440928686034,-1.38634440429817,
5.95021560733883));
#91185=CARTESIAN_POINT('Ctrl Pts',(-1.94016408816266,-1.36427556750855,
5.94839201912898));
#91186=CARTESIAN_POINT('Ctrl Pts',(-1.94984992336837,-1.35039615057062,
5.94724811702544));
#91187=CARTESIAN_POINT('Ctrl Pts',(-1.99612268973972,-1.28255326662644,
5.94166995331878));
#91188=CARTESIAN_POINT('Ctrl Pts',(-2.03061928624485,-1.22720517826059,
5.93715824062264));
#91189=CARTESIAN_POINT('Ctrl Pts',(-2.14172365008245,-1.03140612123326,
5.92131619744516));
#91190=CARTESIAN_POINT('Ctrl Pts',(-2.20637533085743,-0.88468866950939,
5.9096124632956));
#91191=CARTESIAN_POINT('Ctrl Pts',(-2.27200001914009,-0.682624243660154,
5.89411155682401));
#91192=CARTESIAN_POINT('Ctrl Pts',(-2.28656803566439,-0.632113078932413,
5.89028918052477));
#91193=CARTESIAN_POINT('Ctrl Pts',(-2.31579602479463,-0.516467790260524,
5.88170517114246));
#91194=CARTESIAN_POINT('Ctrl Pts',(-2.32941033004485,-0.451109283366782,
5.87697144602369));
#91195=CARTESIAN_POINT('Ctrl Pts',(-2.34200045216955,-0.374630398346349,
5.87163021230572));
#91196=CARTESIAN_POINT('Ctrl Pts',(-2.34367750884852,-0.363991481848435,
5.87089161974628));
#91197=CARTESIAN_POINT('Ctrl Pts',(-2.34626794910025,-0.346797585288626,
5.86970548411986));
#91198=CARTESIAN_POINT('Ctrl Pts',(-2.34722644651092,-0.340249710716274,
5.86925553185338));
#91199=CARTESIAN_POINT('Ctrl Pts',(-2.34887869886702,-0.328623177020545,
5.86845980859675));
#91200=CARTESIAN_POINT('Ctrl Pts',(-2.34958340881228,-0.323546196627361,
5.86811343196532));
#91201=CARTESIAN_POINT('Ctrl Pts',(-2.35092002050089,-0.313682058718947,
5.86744259054819));
#91202=CARTESIAN_POINT('Ctrl Pts',(-2.35155375974119,-0.308895278150122,
5.86711801917119));
#91203=CARTESIAN_POINT('Ctrl Pts',(-2.35292637112213,-0.298278540813172,
5.86640022251461));
#91204=CARTESIAN_POINT('Ctrl Pts',(-2.35365820599988,-0.292447682505695,
5.86600738738861));
#91205=CARTESIAN_POINT('Ctrl Pts',(-2.35542698095829,-0.27791822282563,
5.86503183372));
#91206=CARTESIAN_POINT('Ctrl Pts',(-2.35643742515107,-0.269216396844644,
5.8644505275705));
#91207=CARTESIAN_POINT('Ctrl Pts',(-2.36689225779544,-0.174608463986798,
5.85816065486418));
#91208=CARTESIAN_POINT('Ctrl Pts',(-2.37168361370965,-0.0882439611840601,
5.85268828811318));
#91209=CARTESIAN_POINT('Ctrl Pts',(-2.37174931491709,-0.00180268974679477,
5.84731037310509));
#91210=CARTESIAN_POINT('Ctrl Pts',(-2.36542649454111,0.173076750093528,
5.83682189647117));
#91211=CARTESIAN_POINT('Ctrl Pts',(-2.36968735820944,0.114843857430324,
5.84074456160273));
#91212=CARTESIAN_POINT('Ctrl Pts',(-2.37179168735252,0.0565192335834641,
5.84466722673429));
#91213=CARTESIAN_POINT('Ctrl Pts',(-2.37174937408619,-0.0017230849568048,
5.84858989186585));
#91214=CARTESIAN_POINT('',(-2.37174917807861,-0.0010014824649929,5.64933374379984));
#91215=CARTESIAN_POINT('Ctrl Pts',(-2.36542649454145,0.17307675008899,5.63753449772568));
#91216=CARTESIAN_POINT('Ctrl Pts',(-2.36560061936644,0.170696999636211,
5.63769332455426));
#91217=CARTESIAN_POINT('Ctrl Pts',(-2.36577115263263,0.168316990748921,
5.63785226386776));
#91218=CARTESIAN_POINT('Ctrl Pts',(-2.36656180708301,0.157043781578322,
5.63860555501616));
#91219=CARTESIAN_POINT('Ctrl Pts',(-2.36713536850584,0.14814749237512,5.63920135913883));
#91220=CARTESIAN_POINT('Ctrl Pts',(-2.36819217453898,0.130178466331304,
5.6404075810499));
#91221=CARTESIAN_POINT('Ctrl Pts',(-2.36867346784838,0.121105769301657,
5.64101804978109));
#91222=CARTESIAN_POINT('Ctrl Pts',(-2.36989028236562,0.0953738939302946,
5.64275364584945));
#91223=CARTESIAN_POINT('Ctrl Pts',(-2.37050224432586,0.0787096876410045,
5.64388261705857));
#91224=CARTESIAN_POINT('Ctrl Pts',(-2.37148822085233,0.0410297989315304,
5.6464470834772));
#91225=CARTESIAN_POINT('Ctrl Pts',(-2.37175868112921,0.0200131535808708,
5.6478857009166));
#91226=CARTESIAN_POINT('Ctrl Pts',(-2.37174978765133,-0.00100363135235019,
5.6493328323041));
#91227=CARTESIAN_POINT('Ctrl Pts',(-2.37174978852891,-0.00100155531720748,
5.64933268935669));
#91228=CARTESIAN_POINT('Ctrl Pts',(-2.37164352059503,-0.25265111013939,
5.66666026014709));
#91229=CARTESIAN_POINT('Ctrl Pts',(-2.3314818712988,-0.502669839439992,
5.68534782967035));
#91230=CARTESIAN_POINT('Ctrl Pts',(-2.23099083816382,-0.807930067335497,
5.7084964503446));
#91231=CARTESIAN_POINT('Ctrl Pts',(-2.20624354312408,-0.8732483324028,5.71345291330625));
#91232=CARTESIAN_POINT('Ctrl Pts',(-2.17407648886176,-0.948010154838691,
5.71905808347072));
#91233=CARTESIAN_POINT('Ctrl Pts',(-2.16942752156901,-0.958601103420047,
5.71985047611426));
#91234=CARTESIAN_POINT('Ctrl Pts',(-2.16217112603119,-0.974808914280169,
5.72106010300624));
#91235=CARTESIAN_POINT('Ctrl Pts',(-2.15961895055886,-0.980450094712068,
5.7214805542687));
#91236=CARTESIAN_POINT('Ctrl Pts',(-2.15488915357983,-0.990796486453308,
5.72225057329077));
#91237=CARTESIAN_POINT('Ctrl Pts',(-2.1527182023096,-0.995504537562328,
5.72260052643411));
#91238=CARTESIAN_POINT('Ctrl Pts',(-2.14779287459998,-1.00609443412296,
5.72338671686396));
#91239=CARTESIAN_POINT('Ctrl Pts',(-2.1450297705687,-1.01197209866505,5.72382241060949));
#91240=CARTESIAN_POINT('Ctrl Pts',(-2.1368268685492,-1.02923673024633,5.72510045028314));
#91241=CARTESIAN_POINT('Ctrl Pts',(-2.13132018810372,-1.04059194030834,
5.72593880518431));
#91242=CARTESIAN_POINT('Ctrl Pts',(-2.08454888549568,-1.13510905485041,
5.73290279492563));
#91243=CARTESIAN_POINT('Ctrl Pts',(-2.03851936991568,-1.21583709985596,
5.73875970763128));
#91244=CARTESIAN_POINT('Ctrl Pts',(-1.88429052296251,-1.45282749523415,
5.75630196704557));
#91245=CARTESIAN_POINT('Ctrl Pts',(-1.76197769473203,-1.59896644506038,
5.767671633576));
#91246=CARTESIAN_POINT('Ctrl Pts',(-1.59427083611109,-1.75644850489534,
5.78226591336158));
#91247=CARTESIAN_POINT('Ctrl Pts',(-1.56430323833072,-1.78318982355163,
5.78483842293011));
#91248=CARTESIAN_POINT('Ctrl Pts',(-1.51834538867038,-1.82214957837045,
5.78874323828754));
#91249=CARTESIAN_POINT('Ctrl Pts',(-1.50285419560241,-1.8349471470548,5.79005283202768));
#91250=CARTESIAN_POINT('Ctrl Pts',(-1.47752655319581,-1.85533491325641,
5.79218463040832));
#91251=CARTESIAN_POINT('Ctrl Pts',(-1.46778958188249,-1.86304752739457,
5.79300199218648));
#91252=CARTESIAN_POINT('Ctrl Pts',(-1.4490539650235,-1.87764988846594,5.79457088144892));
#91253=CARTESIAN_POINT('Ctrl Pts',(-1.44006561842391,-1.88455233524633,
5.79532188206845));
#91254=CARTESIAN_POINT('Ctrl Pts',(-1.43090270378343,-1.89148500908713,
5.79608589365064));
#91255=CARTESIAN_POINT('Ctrl Pts',(-1.43077711925714,-1.89158000684779,
5.79609636469634));
#91256=CARTESIAN_POINT('Ctrl Pts',(-1.43052238465917,-1.89177265962518,
5.79611760347274));
#91257=CARTESIAN_POINT('Ctrl Pts',(-1.43039323404485,-1.89187031392613,
5.79612837123159));
#91258=CARTESIAN_POINT('Ctrl Pts',(-1.4301311075033,-1.89206847276602,5.79615022504056));
#91259=CARTESIAN_POINT('Ctrl Pts',(-1.42999813097738,-1.89216897651477,
5.79616131112176));
#91260=CARTESIAN_POINT('Ctrl Pts',(-1.42972806970698,-1.89237304427792,
5.79618382510407));
#91261=CARTESIAN_POINT('Ctrl Pts',(-1.4295909843142,-1.89247660740768,5.79619525303842));
#91262=CARTESIAN_POINT('Ctrl Pts',(-1.42931239657002,-1.89268702297861,
5.79621847640193));
#91263=CARTESIAN_POINT('Ctrl Pts',(-1.42917089348143,-1.89279387445275,
5.79623027186949));
#91264=CARTESIAN_POINT('Ctrl Pts',(-1.42888313250292,-1.89301111716922,
5.79625425839183));
#91265=CARTESIAN_POINT('Ctrl Pts',(-1.42873687380275,-1.8931215073296,5.79626644948855));
#91266=CARTESIAN_POINT('Ctrl Pts',(-1.42843923104685,-1.89334610192275,
5.79629125807869));
#91267=CARTESIAN_POINT('Ctrl Pts',(-1.42828784608697,-1.89346030515034,
5.79630387561898));
#91268=CARTESIAN_POINT('Ctrl Pts',(-1.42797954331297,-1.89369282752043,
5.79632957097407));
#91269=CARTESIAN_POINT('Ctrl Pts',(-1.42782262448709,-1.89381114531661,
5.79634264884139));
#91270=CARTESIAN_POINT('Ctrl Pts',(-1.42750280463764,-1.89405222917953,
5.79636930220332));
#91271=CARTESIAN_POINT('Ctrl Pts',(-1.4273399024832,-1.89417499373408,5.79638287775658));
#91272=CARTESIAN_POINT('Ctrl Pts',(-1.42700761912436,-1.89442533830914,
5.79641056778808));
#91273=CARTESIAN_POINT('Ctrl Pts',(-1.42683823664427,-1.89455291663139,
5.79642468233264));
#91274=CARTESIAN_POINT('Ctrl Pts',(-1.42656320003674,-1.89476001548673,
5.79644760010651));
#91275=CARTESIAN_POINT('Ctrl Pts',(-1.42645755634096,-1.89483954992081,
5.7964564027934));
#91276=CARTESIAN_POINT('Ctrl Pts',(-1.42622378958899,-1.89501551186902,
5.79647588078437));
#91277=CARTESIAN_POINT('Ctrl Pts',(-1.42609566340418,-1.89511193522535,
5.79648655625138));
#91278=CARTESIAN_POINT('Ctrl Pts',(-1.42581128666588,-1.89532590219913,
5.79651024982894));
#91279=CARTESIAN_POINT('Ctrl Pts',(-1.42565503137244,-1.89544343947615,
5.79652326818584));
#91280=CARTESIAN_POINT('Ctrl Pts',(-1.42530691291307,-1.89570523133822,
5.79655227054785));
#91281=CARTESIAN_POINT('Ctrl Pts',(-1.42511504240005,-1.89584947610455,
5.7965682549352));
#91282=CARTESIAN_POINT('Ctrl Pts',(-1.42468554926835,-1.89617225919652,
5.79660403370901));
#91283=CARTESIAN_POINT('Ctrl Pts',(-1.42444791501096,-1.89635078196553,
5.79662382870145));
#91284=CARTESIAN_POINT('Ctrl Pts',(-1.42297314047316,-1.89745827292467,
5.79674667130934));
#91285=CARTESIAN_POINT('Ctrl Pts',(-1.42173512747768,-1.89838607329354,
5.79684976438959));
#91286=CARTESIAN_POINT('Ctrl Pts',(-1.41318210851119,-1.90478287740268,
5.79756180674377));
#91287=CARTESIAN_POINT('Ctrl Pts',(-1.40583655979324,-1.9102107331337,5.7981723516872));
#91288=CARTESIAN_POINT('Ctrl Pts',(-1.38861814817107,-1.92278084667566,
5.7996013490787));
#91289=CARTESIAN_POINT('Ctrl Pts',(-1.37872130443466,-1.92988966027054,
5.80042107460918));
#91290=CARTESIAN_POINT('Ctrl Pts',(-1.34681535886223,-1.95243672978268,
5.80305883338443));
#91291=CARTESIAN_POINT('Ctrl Pts',(-1.32459906132585,-1.96757668658768,
5.80488812864631));
#91292=CARTESIAN_POINT('Ctrl Pts',(-1.13099670897635,-2.09474772250308,
5.82077267787698));
#91293=CARTESIAN_POINT('Ctrl Pts',(-0.94605809966199,-2.18450462048365,
5.83568150925143));
#91294=CARTESIAN_POINT('Ctrl Pts',(-0.638191641956783,-2.28742140951938,
5.85937213535218));
#91295=CARTESIAN_POINT('Ctrl Pts',(-0.52169745343123,-2.31677017497521,
5.86807495598809));
#91296=CARTESIAN_POINT('Ctrl Pts',(-0.389754124245291,-2.3395477181449,
5.87732743521931));
#91297=CARTESIAN_POINT('Ctrl Pts',(-0.376016943639302,-2.34179484251328,
5.87828345213837));
#91298=CARTESIAN_POINT('Ctrl Pts',(-0.355668554911659,-2.34493975006678,
5.87968800516814));
#91299=CARTESIAN_POINT('Ctrl Pts',(-0.349072372565663,-2.34593073936025,
5.88014151632692));
#91300=CARTESIAN_POINT('Ctrl Pts',(-0.337330317666764,-2.34764420623886,
5.8809455336139));
#91301=CARTESIAN_POINT('Ctrl Pts',(-0.332186171227807,-2.34837761269774,
5.88129664264268));
#91302=CARTESIAN_POINT('Ctrl Pts',(-0.321040608432324,-2.34992929135538,
5.88205491613039));
#91303=CARTESIAN_POINT('Ctrl Pts',(-0.315038459784062,-2.35074148250563,
5.8824617368412));
#91304=CARTESIAN_POINT('Ctrl Pts',(-0.298478904158658,-2.352917704224,5.88358008444642));
#91305=CARTESIAN_POINT('Ctrl Pts',(-0.287915161494948,-2.35423368625574,
5.88428897637085));
#91306=CARTESIAN_POINT('Ctrl Pts',(-0.23266796084399,-2.36073869401767,
5.88797444637277));
#91307=CARTESIAN_POINT('Ctrl Pts',(-0.187849042852606,-2.36472724463345,
5.89088933607169));
#91308=CARTESIAN_POINT('Ctrl Pts',(-0.0985806804751241,-2.37011705757224,
5.89659477654039));
#91309=CARTESIAN_POINT('Ctrl Pts',(-0.0541522024456966,-2.37154821828459,
5.89938525696319));
#91310=CARTESIAN_POINT('Ctrl Pts',(0.179518625458638,-2.3725046498886,5.91392236832583));
#91311=CARTESIAN_POINT('Ctrl Pts',(0.368152876807087,-2.35063204475772,
5.92523604500701));
#91312=CARTESIAN_POINT('Ctrl Pts',(0.617453587024003,-2.29095024475468,
5.94143947561378));
#91313=CARTESIAN_POINT('Ctrl Pts',(0.682022398383635,-2.27256376804027,
5.94574820714996));
#91314=CARTESIAN_POINT('Ctrl Pts',(0.762082865922435,-2.24604649654846,
5.95127597254893));
#91315=CARTESIAN_POINT('Ctrl Pts',(0.778385269496632,-2.24044895173486,
5.95241134983343));
#91316=CARTESIAN_POINT('Ctrl Pts',(0.804379249423792,-2.23120578711897,
5.95423806639015));
#91317=CARTESIAN_POINT('Ctrl Pts',(0.814110685978092,-2.2276734559981,5.95492564229107));
#91318=CARTESIAN_POINT('Ctrl Pts',(0.832531208999378,-2.22085032679191,
5.95623433645183));
#91319=CARTESIAN_POINT('Ctrl Pts',(0.841224715795494,-2.21757195176718,
5.95685502978516));
#91320=CARTESIAN_POINT('Ctrl Pts',(0.86095293595342,-2.20999961659303,5.95827065875023));
#91321=CARTESIAN_POINT('Ctrl Pts',(0.871975135035369,-2.20567396010796,
5.95906664601563));
#91322=CARTESIAN_POINT('Ctrl Pts',(0.90049581829444,-2.19423384100996,5.96113974963232));
#91323=CARTESIAN_POINT('Ctrl Pts',(0.917942232758514,-2.18699265866527,
5.96242110754909));
#91324=CARTESIAN_POINT('Ctrl Pts',(1.07868426769145,-2.11801400971624,5.97435242843188));
#91325=CARTESIAN_POINT('Ctrl Pts',(1.215618887166,-2.04249759000248,5.98548539149245));
#91326=CARTESIAN_POINT('Ctrl Pts',(1.4376130628623,-1.88979934865933,6.00509708836814));
#91327=CARTESIAN_POINT('Ctrl Pts',(1.52636532580569,-1.81886848107397,6.01343689573029));
#91328=CARTESIAN_POINT('Ctrl Pts',(1.65984233522129,-1.69551847548,6.02651924676869));
#91329=CARTESIAN_POINT('Ctrl Pts',(1.70796577252639,-1.64703199426663,6.03136347374993));
#91330=CARTESIAN_POINT('Ctrl Pts',(1.76168020460538,-1.58802182992971,6.03685850539932));
#91331=CARTESIAN_POINT('Ctrl Pts',(1.76936431108184,-1.57945573658155,6.03764681343532));
#91332=CARTESIAN_POINT('Ctrl Pts',(1.78107839695748,-1.56620432473983,6.03885153117371));
#91333=CARTESIAN_POINT('Ctrl Pts',(1.78515278456655,-1.56155876639799,6.03927111834033));
#91334=CARTESIAN_POINT('Ctrl Pts',(1.79261279932702,-1.55298560873611,6.04004031660864));
#91335=CARTESIAN_POINT('Ctrl Pts',(1.79600369016847,-1.54906284417673,6.0403903072451));
#91336=CARTESIAN_POINT('Ctrl Pts',(1.80362263570205,-1.54019019139871,6.04117753168807));
#91337=CARTESIAN_POINT('Ctrl Pts',(1.8078431872828,-1.53523400511345,6.04161421531363));
#91338=CARTESIAN_POINT('Ctrl Pts',(1.82023065230123,-1.52056550615132,6.04289788431874));
#91339=CARTESIAN_POINT('Ctrl Pts',(1.82834024858055,-1.5108047654104,6.04374082597503));
#91340=CARTESIAN_POINT('Ctrl Pts',(1.89831531260124,-1.42519384763072,6.05104171470197));
#91341=CARTESIAN_POINT('Ctrl Pts',(1.9555171070979,-1.34563608436072,6.05720056355624));
#91342=CARTESIAN_POINT('Ctrl Pts',(2.08672304532995,-1.1370337391475,6.07246031657022));
#91343=CARTESIAN_POINT('Ctrl Pts',(2.15381640537072,-1.00415853192139,6.08141817039771));
#91344=CARTESIAN_POINT('Ctrl Pts',(2.23042248411881,-0.808808755687088,
6.09451730864341));
#91345=CARTESIAN_POINT('Ctrl Pts',(2.25058033181989,-0.750895048197857,
6.09838923272766));
#91346=CARTESIAN_POINT('Ctrl Pts',(2.27635558317712,-0.666433015072911,
6.10406517614306));
#91347=CARTESIAN_POINT('Ctrl Pts',(2.28379763817206,-0.640465424549628,
6.1058139657998));
#91348=CARTESIAN_POINT('Ctrl Pts',(2.29634789639335,-0.593669969203855,
6.10897574655151));
#91349=CARTESIAN_POINT('Ctrl Pts',(2.30162026921757,-0.572888977318162,
6.11038344067438));
#91350=CARTESIAN_POINT('Ctrl Pts',(2.30922973128833,-0.541094062931542,
6.11254396789617));
#91351=CARTESIAN_POINT('Ctrl Pts',(2.31177141035443,-0.530129866787261,
6.11329022092351));
#91352=CARTESIAN_POINT('Ctrl Pts',(2.31606234559062,-0.511001931758536,
6.11459441058515));
#91353=CARTESIAN_POINT('Ctrl Pts',(2.31784672710881,-0.502846208584473,
6.1151512100008));
#91354=CARTESIAN_POINT('Ctrl Pts',(2.32176450549418,-0.484475529782045,
6.11640710177646));
#91355=CARTESIAN_POINT('Ctrl Pts',(2.32387360923528,-0.474255627470957,
6.11710695882104));
#91356=CARTESIAN_POINT('Ctrl Pts',(2.32936095095243,-0.446750285774738,
6.11899387208129));
#91357=CARTESIAN_POINT('Ctrl Pts',(2.33261414962988,-0.429440865989278,
6.1201848804274));
#91358=CARTESIAN_POINT('Ctrl Pts',(2.34666763333714,-0.349788886658925,
6.12568291458601));
#91359=CARTESIAN_POINT('Ctrl Pts',(2.35516241993981,-0.287071261502332,
6.130061908112));
#91360=CARTESIAN_POINT('Ctrl Pts',(2.37943180232297,-0.0313597398278462,
6.148130441687));
#91361=CARTESIAN_POINT('Ctrl Pts',(2.37405377868918,0.162873211078528,6.16242613955079));
#91362=CARTESIAN_POINT('Ctrl Pts',(2.3334132936838,0.431914028405834,6.18214234284624));
#91363=CARTESIAN_POINT('Ctrl Pts',(2.317829636573,0.508955494113488,6.18776571030832));
#91364=CARTESIAN_POINT('Ctrl Pts',(2.29426877791969,0.601511447794637,6.19439093476283));
#91365=CARTESIAN_POINT('Ctrl Pts',(2.28991218038564,0.617889549008795,6.19555816849853));
#91366=CARTESIAN_POINT('Ctrl Pts',(2.2834487278293,0.641180274425502,6.19720937229039));
#91367=CARTESIAN_POINT('Ctrl Pts',(2.2814853861732,0.648131678830813,6.19770108555274));
#91368=CARTESIAN_POINT('Ctrl Pts',(2.27803564598726,0.66013589177824,6.198548164334));
#91369=CARTESIAN_POINT('Ctrl Pts',(2.27656412921852,0.665192880184589,6.19890437820197));
#91370=CARTESIAN_POINT('Ctrl Pts',(2.27345035952992,0.675762241054621,6.19964751241828));
#91371=CARTESIAN_POINT('Ctrl Pts',(2.27180489248476,0.681273569104934,6.20003424370884));
#91372=CARTESIAN_POINT('Ctrl Pts',(2.26737398105875,0.6959198927091,6.2010600611649));
#91373=CARTESIAN_POINT('Ctrl Pts',(2.26455334720966,0.705044262775467,6.20169713463655));
#91374=CARTESIAN_POINT('Ctrl Pts',(2.25208683913038,0.744524990166895,6.20444609074892));
#91375=CARTESIAN_POINT('Ctrl Pts',(2.24188459421818,0.774704010454745,6.20652777912287));
#91376=CARTESIAN_POINT('Ctrl Pts',(2.14602509536759,1.04048983149595,6.22476273027979));
#91377=CARTESIAN_POINT('Ctrl Pts',(2.02411829607826,1.26135781528861,6.23938161213371));
#91378=CARTESIAN_POINT('Ctrl Pts',(1.82930402985824,1.5110228754464,6.25941183839382));
#91379=CARTESIAN_POINT('Ctrl Pts',(1.78660642885283,1.56127498276236,6.26364611463614));
#91380=CARTESIAN_POINT('Ctrl Pts',(1.73024200384967,1.62226830023338,6.26909000378854));
#91381=CARTESIAN_POINT('Ctrl Pts',(1.71847367238726,1.63472934808138,6.27021909355155));
#91382=CARTESIAN_POINT('Ctrl Pts',(1.69939691261262,1.65449537148487,6.27203808293578));
#91383=CARTESIAN_POINT('Ctrl Pts',(1.69217385703761,1.66188219578317,6.272724276117));
#91384=CARTESIAN_POINT('Ctrl Pts',(1.67836078779289,1.67582503084034,6.27403189038995));
#91385=CARTESIAN_POINT('Ctrl Pts',(1.6717800266233,1.68238996856526,6.27465289685876));
#91386=CARTESIAN_POINT('Ctrl Pts',(1.65670233121933,1.69725559220843,6.27607140568344));
#91387=CARTESIAN_POINT('Ctrl Pts',(1.64818134407532,1.70553141503085,6.2768699757662));
#91388=CARTESIAN_POINT('Ctrl Pts',(1.62585902272575,1.72688797432641,6.27895425197548));
#91389=CARTESIAN_POINT('Ctrl Pts',(1.61196213608799,1.73986714225083,6.2802442754692));
#91390=CARTESIAN_POINT('Ctrl Pts',(1.49024882828482,1.85083281569976,6.29148047793259));
#91391=CARTESIAN_POINT('Ctrl Pts',(1.37379218172203,1.93884098467862,6.30184377902377));
#91392=CARTESIAN_POINT('Ctrl Pts',(1.17560720141769,2.06174998487815,6.31878451813567));
#91393=CARTESIAN_POINT('Ctrl Pts',(1.09869490774124,2.10374296301721,6.32520396882803));
#91394=CARTESIAN_POINT('Ctrl Pts',(0.935067877722646,2.18165532529008,6.33839261979896));
#91395=CARTESIAN_POINT('Ctrl Pts',(0.848176009214477,2.21688366206929,6.34514384478063));
#91396=CARTESIAN_POINT('Ctrl Pts',(0.741903400349646,2.25280253618081,6.35293952008697));
#91397=CARTESIAN_POINT('Ctrl Pts',(0.724318054424877,2.25851795030297,6.35421469066821));
#91398=CARTESIAN_POINT('Ctrl Pts',(0.699526691615532,2.26625603611395,6.35598994503083));
#91399=CARTESIAN_POINT('Ctrl Pts',(0.69237576046333,2.26845097449551,6.35649940121703));
#91400=CARTESIAN_POINT('Ctrl Pts',(0.680130243775401,2.27214636788819,6.35736722092279));
#91401=CARTESIAN_POINT('Ctrl Pts',(0.675040818855446,2.2736635988542,6.35772654732124));
#91402=CARTESIAN_POINT('Ctrl Pts',(0.665189569395497,2.27656440428095,6.35841940723507));
#91403=CARTESIAN_POINT('Ctrl Pts',(0.660428478575191,2.2779501478118,6.35875307213003));
#91404=CARTESIAN_POINT('Ctrl Pts',(0.64755262969523,2.28165397807519,6.35965230007065));
#91405=CARTESIAN_POINT('Ctrl Pts',(0.639429689354419,2.28394372997664,6.36021623801014));
#91406=CARTESIAN_POINT('Ctrl Pts',(0.608978391316408,2.29235236502331,6.36231839492872));
#91407=CARTESIAN_POINT('Ctrl Pts',(0.586572166600323,2.29818781637954,6.3638412169786));
#91408=CARTESIAN_POINT('Ctrl Pts',(0.310643436690889,2.36575177604356,6.38234250638371));
#91409=CARTESIAN_POINT('Ctrl Pts',(0.0486684398523651,2.38557305746104,
6.39748784648216));
#91410=CARTESIAN_POINT('Ctrl Pts',(-0.277615625657801,2.35638691575043,
6.41820057974612));
#91411=CARTESIAN_POINT('Ctrl Pts',(-0.343637046383645,2.34766735666593,
6.42247557752387));
#91412=CARTESIAN_POINT('Ctrl Pts',(-0.426134999956826,2.33321722491782,
6.42796534867093));
#91413=CARTESIAN_POINT('Ctrl Pts',(-0.443036897512371,2.33006693860655,
6.4290978932103));
#91414=CARTESIAN_POINT('Ctrl Pts',(-0.470049500471686,2.32472762058551,
6.43092112837355));
#91415=CARTESIAN_POINT('Ctrl Pts',(-0.480182944354966,2.32265567335727,
6.43160808131974));
#91416=CARTESIAN_POINT('Ctrl Pts',(-0.499394698549412,2.31859641994398,
6.43291628712508));
#91417=CARTESIAN_POINT('Ctrl Pts',(-0.508475537562165,2.31662190419033,
6.43353711969187));
#91418=CARTESIAN_POINT('Ctrl Pts',(-0.529116236963151,2.31200663321201,
6.43495403717135));
#91419=CARTESIAN_POINT('Ctrl Pts',(-0.5406682927007,2.30933246905127,6.43575118092231));
#91420=CARTESIAN_POINT('Ctrl Pts',(-0.570624589086373,2.30216084944802,
6.43782928490675));
#91421=CARTESIAN_POINT('Ctrl Pts',(-0.58899555068453,2.29752936940754,6.43911452055364));
#91422=CARTESIAN_POINT('Ctrl Pts',(-0.756000064596244,2.25329146984254,
6.45089969773735));
#91423=CARTESIAN_POINT('Ctrl Pts',(-0.900478250844775,2.19954102965899,
6.46186805089603));
#91424=CARTESIAN_POINT('Ctrl Pts',(-1.1370107387608,2.08431288285918,6.48101152832534));
#91425=CARTESIAN_POINT('Ctrl Pts',(-1.23187959060156,2.02968635978568,6.48904571610723));
#91426=CARTESIAN_POINT('Ctrl Pts',(-1.38417757517021,1.92736770765579,6.50228511976788));
#91427=CARTESIAN_POINT('Ctrl Pts',(-1.44374834514962,1.88315878506548,6.50755908708761));
#91428=CARTESIAN_POINT('Ctrl Pts',(-1.51023041583423,1.82880822853708,6.5134743888991));
#91429=CARTESIAN_POINT('Ctrl Pts',(-1.51925006603606,1.82132223859127,6.51427755338328));
#91430=CARTESIAN_POINT('Ctrl Pts',(-1.53297410686293,1.80975887706714,6.51550011692175));
#91431=CARTESIAN_POINT('Ctrl Pts',(-1.53771839746722,1.80572947525135,6.51592283830246));
#91432=CARTESIAN_POINT('Ctrl Pts',(-1.54638402517318,1.79831069955638,6.51669503458054));
#91433=CARTESIAN_POINT('Ctrl Pts',(-1.55031010818538,1.79492715591652,6.51704491017287));
#91434=CARTESIAN_POINT('Ctrl Pts',(-1.55910203802877,1.78729980173313,6.51782847825032));
#91435=CARTESIAN_POINT('Ctrl Pts',(-1.56396165835234,1.78304898417524,6.5182616441885));
#91436=CARTESIAN_POINT('Ctrl Pts',(-1.57813476381062,1.77054893094451,6.51952536040642));
#91437=CARTESIAN_POINT('Ctrl Pts',(-1.5874009497539,1.76224603590044,6.5203520522118));
#91438=CARTESIAN_POINT('Ctrl Pts',(-1.65713257706351,1.69876721218072,6.52658089696703));
#91439=CARTESIAN_POINT('Ctrl Pts',(-1.71477782204225,1.64056046896255,6.53177491707383));
#91440=CARTESIAN_POINT('Ctrl Pts',(-1.86247474059268,1.47511344678568,6.54559967541651));
#91441=CARTESIAN_POINT('Ctrl Pts',(-1.94623076905406,1.36270326896003,6.5540422323445));
#91442=CARTESIAN_POINT('Ctrl Pts',(-2.0749762767777,1.15361578549244,6.5692385193745));
#91443=CARTESIAN_POINT('Ctrl Pts',(-2.12428396047665,1.06007996438854,6.57587846070062));
#91444=CARTESIAN_POINT('Ctrl Pts',(-2.17789213199494,0.939509286126425,
6.58445131741887));
#91445=CARTESIAN_POINT('Ctrl Pts',(-2.18819115352131,0.915265656650994,
6.58617531668177));
#91446=CARTESIAN_POINT('Ctrl Pts',(-2.2026731205161,0.879533093272834,6.58871901368476));
#91447=CARTESIAN_POINT('Ctrl Pts',(-2.20717464032213,0.868174772541766,
6.58952796881525));
#91448=CARTESIAN_POINT('Ctrl Pts',(-2.21496181824128,0.848073949802716,
6.59096049982565));
#91449=CARTESIAN_POINT('Ctrl Pts',(-2.21828399901025,0.839345802425944,
6.59158283554681));
#91450=CARTESIAN_POINT('Ctrl Pts',(-2.22511241544924,0.821082222959828,
6.5928858134757));
#91451=CARTESIAN_POINT('Ctrl Pts',(-2.22860909699271,0.81154344645067,6.59356675975158));
#91452=CARTESIAN_POINT('Ctrl Pts',(-2.23757555413144,0.786588379783388,
6.59534948724987));
#91453=CARTESIAN_POINT('Ctrl Pts',(-2.24294723750275,0.771137669957799,
6.59645449475848));
#91454=CARTESIAN_POINT('Ctrl Pts',(-2.26451733705607,0.70696232798761,6.60105019947246));
#91455=CARTESIAN_POINT('Ctrl Pts',(-2.27929010313608,0.657776875753961,
6.60458710088747));
#91456=CARTESIAN_POINT('Ctrl Pts',(-2.33027845221822,0.465574788540541,
6.61847480376621));
#91457=CARTESIAN_POINT('Ctrl Pts',(-2.35468277218743,0.319910369141827,
6.62916731607634));
#91458=CARTESIAN_POINT('Ctrl Pts',(-2.36542649458273,0.173076749524785,
6.63992069752829));
#91459=CARTESIAN_POINT('Origin',(0.,0.,-1.84858989190503));
#91460=CARTESIAN_POINT('',(-2.36542646504704,0.173077153186224,7.83873326832757));
#91461=CARTESIAN_POINT('',(-2.36542649614281,0.173076728203254,7.64172477676247));
#91462=CARTESIAN_POINT('',(-2.36542649454111,0.173076750093529,-1.84858989190503));
#91463=CARTESIAN_POINT('Ctrl Pts',(-2.36542646504704,0.173077153186224,
7.83873326832757));
#91464=CARTESIAN_POINT('Ctrl Pts',(-2.35859713820071,0.266412813979041,
7.83212657790829));
#91465=CARTESIAN_POINT('Ctrl Pts',(-2.34624650250625,0.359304652133148,
7.82537226129759));
#91466=CARTESIAN_POINT('Ctrl Pts',(-2.30671452143895,0.563280434734312,
7.81024149271578));
#91467=CARTESIAN_POINT('Ctrl Pts',(-2.27695014932979,0.673584236738167,
7.80185481430998));
#91468=CARTESIAN_POINT('Ctrl Pts',(-2.21768175819681,0.843455168062414,
7.78891858434391));
#91469=CARTESIAN_POINT('Ctrl Pts',(-2.19342301360757,0.904669167529441,
7.78425482366189));
#91470=CARTESIAN_POINT('Ctrl Pts',(-2.16205208087438,0.97511867786204,7.77894572581195));
#91471=CARTESIAN_POINT('Ctrl Pts',(-2.15738369884976,0.985404092282611,
7.77817212378772));
#91472=CARTESIAN_POINT('Ctrl Pts',(-2.15008901833257,1.00117543764157,7.77698867212681));
#91473=CARTESIAN_POINT('Ctrl Pts',(-2.14751488053171,1.00668509659365,7.77657576085194));
#91474=CARTESIAN_POINT('Ctrl Pts',(-2.14273828863819,1.01680716577538,7.77581822761812));
#91475=CARTESIAN_POINT('Ctrl Pts',(-2.14054212614924,1.02142233828548,7.7754732403832));
#91476=CARTESIAN_POINT('Ctrl Pts',(-2.13555337036302,1.03181931077721,7.77469696372537));
#91477=CARTESIAN_POINT('Ctrl Pts',(-2.13275221201588,1.03759688336428,7.77426621152597));
#91478=CARTESIAN_POINT('Ctrl Pts',(-2.12441831205146,1.0546097559616,7.77299943289799));
#91479=CARTESIAN_POINT('Ctrl Pts',(-2.11881989795727,1.06581290995251,7.77216735384925));
#91480=CARTESIAN_POINT('Ctrl Pts',(-2.07029449566352,1.16102492091658,7.76510933549118));
#91481=CARTESIAN_POINT('Ctrl Pts',(-2.02247335302033,1.24245899632823,7.75916181418998));
#91482=CARTESIAN_POINT('Ctrl Pts',(-1.86392018407025,1.47892827437336,7.74150957209283));
#91483=CARTESIAN_POINT('Ctrl Pts',(-1.7392797873306,1.62367896159526,7.73011247101089));
#91484=CARTESIAN_POINT('Ctrl Pts',(-1.56957625910148,1.77853325132801,7.71552800930969));
#91485=CARTESIAN_POINT('Ctrl Pts',(-1.53981872293582,1.80435811096509,7.71300279883867));
#91486=CARTESIAN_POINT('Ctrl Pts',(-1.49419925009088,1.84199802308108,7.70916804848646));
#91487=CARTESIAN_POINT('Ctrl Pts',(-1.47880941299403,1.85437612107044,7.70788039866558));
#91488=CARTESIAN_POINT('Ctrl Pts',(-1.45364809009576,1.87410103297913,7.70578363635452));
#91489=CARTESIAN_POINT('Ctrl Pts',(-1.44397103632676,1.88156718950209,7.70497920431179));
#91490=CARTESIAN_POINT('Ctrl Pts',(-1.42535110372405,1.89570482101435,7.70343485548718));
#91491=CARTESIAN_POINT('Ctrl Pts',(-1.4164179895194,1.90238865877847,7.70269544682371));
#91492=CARTESIAN_POINT('Ctrl Pts',(-1.40731247095666,1.9091018034619,7.70194318785404));
#91493=CARTESIAN_POINT('Ctrl Pts',(-1.40718675482854,1.90919446990786,7.70193280199882));
#91494=CARTESIAN_POINT('Ctrl Pts',(-1.40693194857391,1.90938225096314,7.70191175210349));
#91495=CARTESIAN_POINT('Ctrl Pts',(-1.40680285795568,1.90947736489825,7.70190108803752));
#91496=CARTESIAN_POINT('Ctrl Pts',(-1.40654104462256,1.90967022793526,7.70187946044391));
#91497=CARTESIAN_POINT('Ctrl Pts',(-1.40640832136201,1.9097679762929,7.70186849688749));
#91498=CARTESIAN_POINT('Ctrl Pts',(-1.40613896135281,1.90996631191575,7.7018462471179));
#91499=CARTESIAN_POINT('Ctrl Pts',(-1.4060023239998,1.9100668983558,7.70183496087285));
#91500=CARTESIAN_POINT('Ctrl Pts',(-1.40572482820554,1.91027113270616,7.70181204037269));
#91501=CARTESIAN_POINT('Ctrl Pts',(-1.40558396909825,1.91037477969586,7.70180040608258));
#91502=CARTESIAN_POINT('Ctrl Pts',(-1.40529769265285,1.91058537891128,7.7017767617064));
#91503=CARTESIAN_POINT('Ctrl Pts',(-1.4051522745702,1.91069233011366,7.70176475158111));
#91504=CARTESIAN_POINT('Ctrl Pts',(-1.40485650961055,1.91090980549179,7.70174032499689));
#91505=CARTESIAN_POINT('Ctrl Pts',(-1.40470616189514,1.91102032852965,7.70172790849357));
#91506=CARTESIAN_POINT('Ctrl Pts',(-1.40440012916865,1.91124524250924,7.70170263549223));
#91507=CARTESIAN_POINT('Ctrl Pts',(-1.40424444321824,1.91135963217648,7.70168977894445));
#91508=CARTESIAN_POINT('Ctrl Pts',(-1.4039272823144,1.91159260529264,7.70166358863627));
#91509=CARTESIAN_POINT('Ctrl Pts',(-1.40376580631556,1.91171118730194,7.70165025482076));
#91510=CARTESIAN_POINT('Ctrl Pts',(-1.40343656428871,1.91195290627821,7.70162306869952));
#91511=CARTESIAN_POINT('Ctrl Pts',(-1.4032687970762,1.91207604162608,7.70160921633113));
#91512=CARTESIAN_POINT('Ctrl Pts',(-1.40299949606084,1.91227364475057,7.7015869811886));
#91513=CARTESIAN_POINT('Ctrl Pts',(-1.40289797250772,1.91234812654189,7.70157859895711));
#91514=CARTESIAN_POINT('Ctrl Pts',(-1.40267370307335,1.9125126322138,7.70156008267231));
#91515=CARTESIAN_POINT('Ctrl Pts',(-1.40255095446362,1.91260265235726,7.70154994847458));
#91516=CARTESIAN_POINT('Ctrl Pts',(-1.40227892711332,1.91280210877508,7.70152749030266));
#91517=CARTESIAN_POINT('Ctrl Pts',(-1.40212964423217,1.91291153938853,7.70151516610906));
#91518=CARTESIAN_POINT('Ctrl Pts',(-1.40179749090975,1.9131549619345,7.70148774570849));
#91519=CARTESIAN_POINT('Ctrl Pts',(-1.40161461408571,1.91328894510912,7.70147264916351));
#91520=CARTESIAN_POINT('Ctrl Pts',(-1.40120566409264,1.91358846880083,7.7014388914654));
#91521=CARTESIAN_POINT('Ctrl Pts',(-1.40097958081774,1.91375399546139,7.70142022977654));
#91522=CARTESIAN_POINT('Ctrl Pts',(-1.39356384010784,1.91918140482585,7.70080813739702));
#91523=CARTESIAN_POINT('Ctrl Pts',(-1.38634470553244,1.92440271117738,7.70021314441324));
#91524=CARTESIAN_POINT('Ctrl Pts',(-1.36987210244326,1.93617587972856,7.69885736292171));
#91525=CARTESIAN_POINT('Ctrl Pts',(-1.36060078385588,1.94270227093378,7.69809561312119));
#91526=CARTESIAN_POINT('Ctrl Pts',(-1.33688729801939,1.95914197007981,7.69615042720372));
#91527=CARTESIAN_POINT('Ctrl Pts',(-1.32238165640151,1.96896206986078,7.69496349482084));
#91528=CARTESIAN_POINT('Ctrl Pts',(-1.2320120022656,2.02869188236615,7.68758559819184));
#91529=CARTESIAN_POINT('Ctrl Pts',(-1.15345179809127,2.07436484652869,7.68123928101915));
#91530=CARTESIAN_POINT('Ctrl Pts',(-0.887736527611923,2.20907729893899,
7.65998886571653));
#91531=CARTESIAN_POINT('Ctrl Pts',(-0.691549029664566,2.27812341566044,
7.6445434862203));
#91532=CARTESIAN_POINT('Ctrl Pts',(-0.459486059393531,2.32700973565514,
7.62768620384646));
#91533=CARTESIAN_POINT('Ctrl Pts',(-0.429953608869919,2.33264695726725,
7.62556821430839));
#91534=CARTESIAN_POINT('Ctrl Pts',(-0.380501906823794,2.34111525916777,
7.62207538756554));
#91535=CARTESIAN_POINT('Ctrl Pts',(-0.360640094876113,2.34425705667519,
7.62068688401175));
#91536=CARTESIAN_POINT('Ctrl Pts',(-0.333152031406262,2.34824755420108,
7.61878721344964));
#91537=CARTESIAN_POINT('Ctrl Pts',(-0.325558719069628,2.34931231989943,
7.61826475636649));
#91538=CARTESIAN_POINT('Ctrl Pts',(-0.312716905947515,2.35104959432534,
7.6173852267336));
#91539=CARTESIAN_POINT('Ctrl Pts',(-0.307471120690429,2.35174139100683,
7.61702708613879));
#91540=CARTESIAN_POINT('Ctrl Pts',(-0.297444982145176,2.35302948367331,
7.61634481355863));
#91541=CARTESIAN_POINT('Ctrl Pts',(-0.292665083883659,2.35362877662986,
7.6160205087947));
#91542=CARTESIAN_POINT('Ctrl Pts',(-0.279989928832113,2.35517874902322,
7.61516300546171));
#91543=CARTESIAN_POINT('Ctrl Pts',(-0.272091572147632,2.35610430181736,
7.61463120770876));
#91544=CARTESIAN_POINT('Ctrl Pts',(-0.243898549587004,2.35926438048947,
7.61274155579772));
#91545=CARTESIAN_POINT('Ctrl Pts',(-0.223579161974676,2.36127663509652,
7.61139549880651));
#91546=CARTESIAN_POINT('Ctrl Pts',(0.0607325000245537,2.38572926933319,
7.59275074674434));
#91547=CARTESIAN_POINT('Ctrl Pts',(0.32667571273809,2.36404879684728,7.57740314276114));
#91548=CARTESIAN_POINT('Ctrl Pts',(0.626261723691821,2.28799795602327,7.55786075552404));
#91549=CARTESIAN_POINT('Ctrl Pts',(0.668644327702617,2.27597293350804,7.55504683885569));
#91550=CARTESIAN_POINT('Ctrl Pts',(0.740556047261216,2.25338775305678,7.55016975966));
#91551=CARTESIAN_POINT('Ctrl Pts',(0.770256267070677,2.24340918180106,7.54812493260406));
#91552=CARTESIAN_POINT('Ctrl Pts',(0.811970298228573,2.22846826724015,7.545205464371));
#91553=CARTESIAN_POINT('Ctrl Pts',(0.824155219490051,2.22399072529079,7.54434687113046));
#91554=CARTESIAN_POINT('Ctrl Pts',(0.845060926720512,2.21611319502959,7.54286348748364));
#91555=CARTESIAN_POINT('Ctrl Pts',(0.853799563654025,2.21276116285665,7.54224031131249));
#91556=CARTESIAN_POINT('Ctrl Pts',(0.870469810806107,2.20625321273352,7.54104543075245));
#91557=CARTESIAN_POINT('Ctrl Pts',(0.878404688089678,2.20310601897893,7.54047402810891));
#91558=CARTESIAN_POINT('Ctrl Pts',(0.898968075931657,2.19482125323606,7.53898623178626));
#91559=CARTESIAN_POINT('Ctrl Pts',(0.911569436884585,2.1896175655554,7.53806761455233));
#91560=CARTESIAN_POINT('Ctrl Pts',(0.947665605990753,2.17434618032149,7.53541603037497));
#91561=CARTESIAN_POINT('Ctrl Pts',(0.971042823124448,2.164007199402,7.53367391140437));
#91562=CARTESIAN_POINT('Ctrl Pts',(1.16578528582348,2.07408806260248,7.51894640250906));
#91563=CARTESIAN_POINT('Ctrl Pts',(1.32721143025869,1.97468438494245,7.50524676484006));
#91564=CARTESIAN_POINT('Ctrl Pts',(1.58103012016887,1.77308772647009,7.48156875768949));
#91565=CARTESIAN_POINT('Ctrl Pts',(1.67957668927501,1.68003787485905,7.47170427028828));
#91566=CARTESIAN_POINT('Ctrl Pts',(1.77830126663248,1.56939832935967,7.4614706491221));
#91567=CARTESIAN_POINT('Ctrl Pts',(1.78686299040038,1.55964328736992,7.46058005893303));
#91568=CARTESIAN_POINT('Ctrl Pts',(1.79954573528522,1.54495130874593,7.45925676670227));
#91569=CARTESIAN_POINT('Ctrl Pts',(1.80372728270528,1.54006730109177,7.45881980440846));
#91570=CARTESIAN_POINT('Ctrl Pts',(1.81087956535331,1.53164441349969,7.45807134411544));
#91571=CARTESIAN_POINT('Ctrl Pts',(1.81385986391892,1.52811380630679,7.45775914979262));
#91572=CARTESIAN_POINT('Ctrl Pts',(1.82060701070292,1.52007325547495,7.45705165837129));
#91573=CARTESIAN_POINT('Ctrl Pts',(1.82436742448894,1.51555801334149,7.45665683149812));
#91574=CARTESIAN_POINT('Ctrl Pts',(1.83453291579958,1.50325934143804,7.45558793903481));
#91575=CARTESIAN_POINT('Ctrl Pts',(1.84090530920182,1.49544886854054,7.45491618863659));
#91576=CARTESIAN_POINT('Ctrl Pts',(1.87179016287247,1.45709753406977,7.45165073090195));
#91577=CARTESIAN_POINT('Ctrl Pts',(1.89559507612819,1.4259913688188,7.44910358447032));
#91578=CARTESIAN_POINT('Ctrl Pts',(2.06163939350298,1.19750809226236,7.43099581613569));
#91579=CARTESIAN_POINT('Ctrl Pts',(2.17354088267521,0.979862812330626,7.41676360529145));
#91580=CARTESIAN_POINT('Ctrl Pts',(2.27099985204871,0.687036662951345,7.39723536746917));
#91581=CARTESIAN_POINT('Ctrl Pts',(2.28904730857409,0.624276295934643,7.39304057083386));
#91582=CARTESIAN_POINT('Ctrl Pts',(2.3084862870845,0.544404088868842,7.38765113615887));
#91583=CARTESIAN_POINT('Ctrl Pts',(2.31231384060281,0.52791043502709,7.38653559542166));
#91584=CARTESIAN_POINT('Ctrl Pts',(2.3181619934658,0.501424889421902,7.38473944653926));
#91585=CARTESIAN_POINT('Ctrl Pts',(2.32029538919853,0.491458288167029,7.38406246505419));
#91586=CARTESIAN_POINT('Ctrl Pts',(2.32422403100956,0.472508863813081,7.3827731286825));
#91587=CARTESIAN_POINT('Ctrl Pts',(2.32603161068842,0.463528763632339,7.38216118126298));
#91588=CARTESIAN_POINT('Ctrl Pts',(2.33002746611611,0.443065150077618,7.38076446180649));
#91589=CARTESIAN_POINT('Ctrl Pts',(2.33218293781247,0.431575550882417,7.37997865868202));
#91590=CARTESIAN_POINT('Ctrl Pts',(2.33756138311075,0.401688546028813,7.37793025116457));
#91591=CARTESIAN_POINT('Ctrl Pts',(2.34065207857208,0.383268469866972,7.37666348599672));
#91592=CARTESIAN_POINT('Ctrl Pts',(2.36820305419092,0.206284174461328,7.36444853252089));
#91593=CARTESIAN_POINT('Ctrl Pts',(2.37672722837762,0.0456910543134037,
7.35298667603099));
#91594=CARTESIAN_POINT('Ctrl Pts',(2.36552636649971,-0.186047691462226,
7.3360863689165));
#91595=CARTESIAN_POINT('Ctrl Pts',(2.35882902810994,-0.257399111476526,
7.33084011283655));
#91596=CARTESIAN_POINT('Ctrl Pts',(2.33567110919041,-0.423069765918993,
7.31866030556069));
#91597=CARTESIAN_POINT('Ctrl Pts',(2.31670893203323,-0.516924836609715,
7.31176031181739));
#91598=CARTESIAN_POINT('Ctrl Pts',(2.28735364391774,-0.627340815716504,
7.30381981682918));
#91599=CARTESIAN_POINT('Ctrl Pts',(2.28236941463297,-0.645238793559342,
7.30253849389459));
#91600=CARTESIAN_POINT('Ctrl Pts',(2.27509768731547,-0.670211754459335,
7.30076055946019));
#91601=CARTESIAN_POINT('Ctrl Pts',(2.27298661842687,-0.677336783946034,
7.30025443165674));
#91602=CARTESIAN_POINT('Ctrl Pts',(2.26932823599783,-0.689474391795433,
7.29939431075049));
#91603=CARTESIAN_POINT('Ctrl Pts',(2.26779772659917,-0.69449193877369,7.29903935505281));
#91604=CARTESIAN_POINT('Ctrl Pts',(2.26481413523986,-0.704158160772356,
7.29835676261713));
#91605=CARTESIAN_POINT('Ctrl Pts',(2.26336337404955,-0.708807463754769,
7.29802898808188));
#91606=CARTESIAN_POINT('Ctrl Pts',(2.25983605606962,-0.719990319679812,
7.29724183107911));
#91607=CARTESIAN_POINT('Ctrl Pts',(2.25774545759106,-0.726519450813188,
7.29678326213378));
#91608=CARTESIAN_POINT('Ctrl Pts',(2.24995390860999,-0.750494726447138,
7.2951027915529));
#91609=CARTESIAN_POINT('Ctrl Pts',(2.24407863020956,-0.767884156626534,
7.29389060203576));
#91610=CARTESIAN_POINT('Ctrl Pts',(2.18660979501815,-0.931682752912291,
7.2825200662413));
#91611=CARTESIAN_POINT('Ctrl Pts',(2.12095311379356,-1.07278495583558,7.27307084842636));
#91612=CARTESIAN_POINT('Ctrl Pts',(1.95499435336365,-1.35367146213064,7.25308015244388));
#91613=CARTESIAN_POINT('Ctrl Pts',(1.8523766151989,-1.49101280217569,7.24256159582333));
#91614=CARTESIAN_POINT('Ctrl Pts',(1.72118565409415,-1.63192651773559,7.2299992364612));
#91615=CARTESIAN_POINT('Ctrl Pts',(1.7062590404462,-1.64752670732413,7.22858175789613));
#91616=CARTESIAN_POINT('Ctrl Pts',(1.68327644747264,-1.67089906110656,7.22641567090201));
#91617=CARTESIAN_POINT('Ctrl Pts',(1.67537471936943,-1.67882185279682,7.22567380703523));
#91618=CARTESIAN_POINT('Ctrl Pts',(1.66093456843582,-1.69309702014057,7.22432305533289));
#91619=CARTESIAN_POINT('Ctrl Pts',(1.65441498537867,-1.69946821458672,7.22371501354805));
#91620=CARTESIAN_POINT('Ctrl Pts',(1.64029056312016,-1.71311285839444,7.22240148512265));
#91621=CARTESIAN_POINT('Ctrl Pts',(1.63267374706394,-1.72037357178596,7.2216954633815));
#91622=CARTESIAN_POINT('Ctrl Pts',(1.61192434453083,-1.73989099019388,7.21977820898521));
#91623=CARTESIAN_POINT('Ctrl Pts',(1.59870063887065,-1.75204936758964,7.21856281032493));
#91624=CARTESIAN_POINT('Ctrl Pts',(1.53211559611749,-1.81188871202563,7.21247358060979));
#91625=CARTESIAN_POINT('Ctrl Pts',(1.47675875450595,-1.85728312342909,7.20750610062777));
#91626=CARTESIAN_POINT('Ctrl Pts',(1.25232140698049,-2.02494529556847,7.18771044423677));
#91627=CARTESIAN_POINT('Ctrl Pts',(1.06946727708176,-2.12718861147645,7.17220295262649));
#91628=CARTESIAN_POINT('Ctrl Pts',(0.816766957560711,-2.22757811294163,
7.15267450055625));
#91629=CARTESIAN_POINT('Ctrl Pts',(0.756963595577901,-2.2486040724997,7.14818954950338));
#91630=CARTESIAN_POINT('Ctrl Pts',(0.685685497273274,-2.27049746123778,
7.14305709042383));
#91631=CARTESIAN_POINT('Ctrl Pts',(0.674963437966963,-2.2737079171588,7.142290628263));
#91632=CARTESIAN_POINT('Ctrl Pts',(0.658402006244923,-2.27853935124699,
7.14111576685995));
#91633=CARTESIAN_POINT('Ctrl Pts',(0.65257865762519,-2.28021399757045,7.14070437349789));
#91634=CARTESIAN_POINT('Ctrl Pts',(0.641830016151763,-2.28326048265854,
7.13994826637109));
#91635=CARTESIAN_POINT('Ctrl Pts',(0.636906729965374,-2.28463870657681,
7.13960319751137));
#91636=CARTESIAN_POINT('Ctrl Pts',(0.625764110380621,-2.2877191514243,7.13882503332171));
#91637=CARTESIAN_POINT('Ctrl Pts',(0.619542276983423,-2.28941193478995,
7.13839248705704));
#91638=CARTESIAN_POINT('Ctrl Pts',(0.601092864758016,-2.29435077466064,
7.13711547545022));
#91639=CARTESIAN_POINT('Ctrl Pts',(0.588845890504762,-2.29752445994452,
7.13627505308196));
#91640=CARTESIAN_POINT('Ctrl Pts',(0.466933722638177,-2.32807794866601,
7.1279758186843));
#91641=CARTESIAN_POINT('Ctrl Pts',(0.355452973144535,-2.34768707150716,
7.12091856356863));
#91642=CARTESIAN_POINT('Ctrl Pts',(0.0813470902774454,-2.37591760865688,
7.10393650010297));
#91643=CARTESIAN_POINT('Ctrl Pts',(-0.081564445033582,-2.37590973708495,
7.09412794386011));
#91644=CARTESIAN_POINT('Ctrl Pts',(-0.310045515017346,-2.35235763083039,
7.07960934753421));
#91645=CARTESIAN_POINT('Ctrl Pts',(-0.376568074205888,-2.34262882198343,
7.07529433028151));
#91646=CARTESIAN_POINT('Ctrl Pts',(-0.459370191439679,-2.32690116971652,
7.06976955639437));
#91647=CARTESIAN_POINT('Ctrl Pts',(-0.476121682074541,-2.32353139527184,
7.06864394284447));
#91648=CARTESIAN_POINT('Ctrl Pts',(-0.502838253932188,-2.3178559780098,
7.06683541444242));
#91649=CARTESIAN_POINT('Ctrl Pts',(-0.512827580939557,-2.3156663211804,
7.06615621662041));
#91650=CARTESIAN_POINT('Ctrl Pts',(-0.531730766488592,-2.31139443694434,
7.06486513098005));
#91651=CARTESIAN_POINT('Ctrl Pts',(-0.540647364713944,-2.30932506896214,
7.06425366684398));
#91652=CARTESIAN_POINT('Ctrl Pts',(-0.560865676789947,-2.30450928065009,
7.06286147274528));
#91653=CARTESIAN_POINT('Ctrl Pts',(-0.572159544942579,-2.3017312568454,
7.06207973669673));
#91654=CARTESIAN_POINT('Ctrl Pts',(-0.601344154292878,-2.29432446878618,
7.06004889020675));
#91655=CARTESIAN_POINT('Ctrl Pts',(-0.61920175852899,-2.28956954653065,
7.05879573579285));
#91656=CARTESIAN_POINT('Ctrl Pts',(-0.750574781512671,-2.25293968640675,
7.0494969012744));
#91657=CARTESIAN_POINT('Ctrl Pts',(-0.861610127714849,-2.21285331412349,
7.04118363665795));
#91658=CARTESIAN_POINT('Ctrl Pts',(-1.15243018813763,-2.08264496413429,
7.01821288779835));
#91659=CARTESIAN_POINT('Ctrl Pts',(-1.32450408721529,-1.97767385047271,
7.00324126810711));
#91660=CARTESIAN_POINT('Ctrl Pts',(-1.50151292169903,-1.83611737657584,
6.98737059076585));
#91661=CARTESIAN_POINT('Ctrl Pts',(-1.52146327737978,-1.81962021043655,
6.98557561406372));
#91662=CARTESIAN_POINT('Ctrl Pts',(-1.54756118413861,-1.79731015534653,
6.98322358994138));
#91663=CARTESIAN_POINT('Ctrl Pts',(-1.55395256693055,-1.79178705163262,
6.98264725936922));
#91664=CARTESIAN_POINT('Ctrl Pts',(-1.56442345379187,-1.78264048173592,
6.98170273526608));
#91665=CARTESIAN_POINT('Ctrl Pts',(-1.56852013563661,-1.77903693484713,
6.98133311041173));
#91666=CARTESIAN_POINT('Ctrl Pts',(-1.57652818939613,-1.77194368030196,
6.98061047755162));
#91667=CARTESIAN_POINT('Ctrl Pts',(-1.58044047639011,-1.76845509968554,
6.98025739491826));
#91668=CARTESIAN_POINT('Ctrl Pts',(-1.59005897668736,-1.75982088586775,
6.97938912464548));
#91669=CARTESIAN_POINT('Ctrl Pts',(-1.59575187792092,-1.75466037965643,
6.97887504292403));
#91670=CARTESIAN_POINT('Ctrl Pts',(-1.61528609949086,-1.73677927980854,
6.97711002036254));
#91671=CARTESIAN_POINT('Ctrl Pts',(-1.62900164213386,-1.72392144682518,
6.9758689347841));
#91672=CARTESIAN_POINT('Ctrl Pts',(-1.74819459020511,-1.60948938671038,
6.96505167587362));
#91673=CARTESIAN_POINT('Ctrl Pts',(-1.84422319386273,-1.4984971709672,6.956102752247));
#91674=CARTESIAN_POINT('Ctrl Pts',(-2.00122720528134,-1.27888140576905,
6.93956184548723));
#91675=CARTESIAN_POINT('Ctrl Pts',(-2.06508501177404,-1.17297433140261,
6.93200211613002));
#91676=CARTESIAN_POINT('Ctrl Pts',(-2.14906488677702,-1.00539066205684,
6.9201323554964));
#91677=CARTESIAN_POINT('Ctrl Pts',(-2.17539680059664,-0.947068037957572,
6.91601955630612));
#91678=CARTESIAN_POINT('Ctrl Pts',(-2.20563472884328,-0.872156247685243,
6.91072252891918));
#91679=CARTESIAN_POINT('Ctrl Pts',(-2.21176537190557,-0.856489925674334,
6.90961405358843));
#91680=CARTESIAN_POINT('Ctrl Pts',(-2.22133331998129,-0.83125191234857,
6.90782658767819));
#91681=CARTESIAN_POINT('Ctrl Pts',(-2.22487670051025,-0.821720829886908,
6.90715116091621));
#91682=CARTESIAN_POINT('Ctrl Pts',(-2.23149712460786,-0.803556250096017,
6.90586302864958));
#91683=CARTESIAN_POINT('Ctrl Pts',(-2.23458563452362,-0.794927104901584,
6.90525071913964));
#91684=CARTESIAN_POINT('Ctrl Pts',(-2.24151376908877,-0.775210778895963,
6.90385071326976));
#91685=CARTESIAN_POINT('Ctrl Pts',(-2.24532126577143,-0.764112644565494,
6.90306196771814));
#91686=CARTESIAN_POINT('Ctrl Pts',(-2.25502148282346,-0.735139714666286,
6.90100082640634));
#91687=CARTESIAN_POINT('Ctrl Pts',(-2.26078396054019,-0.717222515071759,
6.89972418420463));
#91688=CARTESIAN_POINT('Ctrl Pts',(-2.30786272297779,-0.56463360682363,
6.88883255054628));
#91689=CARTESIAN_POINT('Ctrl Pts',(-2.337311039493,-0.426620982245834,6.87882847603298));
#91690=CARTESIAN_POINT('Ctrl Pts',(-2.36600858523276,-0.191071139730028,
6.86160922248717));
#91691=CARTESIAN_POINT('Ctrl Pts',(-2.37182185185997,-0.0946856752146957,
6.85453038374071));
#91692=CARTESIAN_POINT('Ctrl Pts',(-2.37170635525136,0.05894780034332,6.84335697066085));
#91693=CARTESIAN_POINT('Ctrl Pts',(-2.36959668181367,0.116083140830984,
6.83922711828715));
#91694=CARTESIAN_POINT('Ctrl Pts',(-2.36542649097266,0.173076798863304,
6.83516330511797));
#91695=CARTESIAN_POINT('Ctrl Pts',(-2.36542649458273,0.173076749524786,
6.63992069752828));
#91696=CARTESIAN_POINT('Ctrl Pts',(-2.36967747850252,0.114978882425194,
6.64417550326076));
#91697=CARTESIAN_POINT('Ctrl Pts',(-2.37178999848562,0.0566976894277928,
6.6484358273091));
#91698=CARTESIAN_POINT('Ctrl Pts',(-2.37174753504741,-0.004369630699211,
6.6528635848913));
#91699=CARTESIAN_POINT('Ctrl Pts',(-2.37174096292677,-0.0070899602370591,
6.65306074906281));
#91700=CARTESIAN_POINT('Ctrl Pts',(-2.37138061207792,-0.0942082585031944,
6.65937236008294));
#91701=CARTESIAN_POINT('Ctrl Pts',(-2.36652673115363,-0.178537856873665,
6.66540734168897));
#91702=CARTESIAN_POINT('Ctrl Pts',(-2.35579946062723,-0.274888910244556,
6.67209505017504));
#91703=CARTESIAN_POINT('Ctrl Pts',(-2.35431455585673,-0.287329081406165,
6.67295447783768));
#91704=CARTESIAN_POINT('Ctrl Pts',(-2.35191275908435,-0.306180275712124,
6.67425008836422));
#91705=CARTESIAN_POINT('Ctrl Pts',(-2.35106810000044,-0.312600030835821,
6.67469012229654));
#91706=CARTESIAN_POINT('Ctrl Pts',(-2.34949991417654,-0.324152874232651,
6.67547976544824));
#91707=CARTESIAN_POINT('Ctrl Pts',(-2.34878584499419,-0.329287091343433,
6.67582989003546));
#91708=CARTESIAN_POINT('Ctrl Pts',(-2.34717956071975,-0.340565286268546,
6.67659723469193));
#91709=CARTESIAN_POINT('Ctrl Pts',(-2.34628005439331,-0.346708109314429,
6.67701404011835));
#91710=CARTESIAN_POINT('Ctrl Pts',(-2.34362404520581,-0.364362449084394,
6.67820883628627));
#91711=CARTESIAN_POINT('Ctrl Pts',(-2.34180684115401,-0.375864858847475,
6.67898350036948));
#91712=CARTESIAN_POINT('Ctrl Pts',(-2.32815459406481,-0.458334600875785,
6.68451350013596));
#91713=CARTESIAN_POINT('Ctrl Pts',(-2.31317915540793,-0.528752235816668,
6.6891070262067));
#91714=CARTESIAN_POINT('Ctrl Pts',(-2.26725313977886,-0.704894486627939,
6.7005181392203));
#91715=CARTESIAN_POINT('Ctrl Pts',(-2.23210141579862,-0.80934462105835,
6.70721530085243));
#91716=CARTESIAN_POINT('Ctrl Pts',(-2.13011598400987,-1.05449801690206,
6.72350630122272));
#91717=CARTESIAN_POINT('Ctrl Pts',(-2.0564570265753,-1.19177801976795,6.73313665764792));
#91718=CARTESIAN_POINT('Ctrl Pts',(-1.95936915926106,-1.33657345989726,
6.744518199362));
#91719=CARTESIAN_POINT('Ctrl Pts',(-1.94864364943561,-1.35216271558097,
6.7457602750314));
#91720=CARTESIAN_POINT('Ctrl Pts',(-1.93089961923421,-1.37730358266181,
6.74779168315955));
#91721=CARTESIAN_POINT('Ctrl Pts',(-1.9239938700328,-1.38693405676526,6.74857671851891));
#91722=CARTESIAN_POINT('Ctrl Pts',(-1.91154495403558,-1.40402289777107,
6.7499822908886));
#91723=CARTESIAN_POINT('Ctrl Pts',(-1.90602954113646,-1.41150125499576,
6.75060174530038));
#91724=CARTESIAN_POINT('Ctrl Pts',(-1.89428004116471,-1.42723797955601,
6.75191461388151));
#91725=CARTESIAN_POINT('Ctrl Pts',(-1.88803558789786,-1.43548832721985,
6.7526084253377));
#91726=CARTESIAN_POINT('Ctrl Pts',(-1.87126109194202,-1.45735246310538,
6.75446199891347));
#91727=CARTESIAN_POINT('Ctrl Pts',(-1.86063667590849,-1.4708927251605,6.75562547449794));
#91728=CARTESIAN_POINT('Ctrl Pts',(-1.80806454624123,-1.53641206800181,
6.76133316276216));
#91729=CARTESIAN_POINT('Ctrl Pts',(-1.76408500348182,-1.58671421636419,
6.76595864153161));
#91730=CARTESIAN_POINT('Ctrl Pts',(-1.53526695850398,-1.82714125070671,
6.78933744787219));
#91731=CARTESIAN_POINT('Ctrl Pts',(-1.32162701547217,-1.98714714692027,
6.80935726368658));
#91732=CARTESIAN_POINT('Ctrl Pts',(-1.06828962441027,-2.1176288157243,6.82920024445143));
#91733=CARTESIAN_POINT('Ctrl Pts',(-1.05047339873072,-2.12652303705205,
6.83057568674166));
#91734=CARTESIAN_POINT('Ctrl Pts',(-1.02540401877355,-2.13864620889186,
6.83248110157235));
#91735=CARTESIAN_POINT('Ctrl Pts',(-1.01824406944295,-2.14206443137263,
6.8330219151395));
#91736=CARTESIAN_POINT('Ctrl Pts',(-1.00666913296062,-2.14751925617365,
6.83389060392221));
#91737=CARTESIAN_POINT('Ctrl Pts',(-1.00226487962963,-2.14957828679285,
6.83421983795524));
#91738=CARTESIAN_POINT('Ctrl Pts',(-0.992958637941359,-2.15389422395794,
6.83491272332799));
#91739=CARTESIAN_POINT('Ctrl Pts',(-0.988055222932292,-2.15614796852391,
6.83527617110475));
#91740=CARTESIAN_POINT('Ctrl Pts',(-0.975934158987395,-2.16166911176563,
6.83617068610346));
#91741=CARTESIAN_POINT('Ctrl Pts',(-0.96870766621894,-2.16491715623831,
6.83670057680693));
#91742=CARTESIAN_POINT('Ctrl Pts',(-0.941911915999356,-2.17679983183458,
6.83865330086264));
#91743=CARTESIAN_POINT('Ctrl Pts',(-0.922241673575557,-2.18520615517008,
6.84006296698035));
#91744=CARTESIAN_POINT('Ctrl Pts',(-0.784470417845294,-2.24189261026015,
6.84978987182887));
#91745=CARTESIAN_POINT('Ctrl Pts',(-0.662739767213739,-2.28084655128256,
6.85764699279954));
#91746=CARTESIAN_POINT('Ctrl Pts',(-0.359723184962003,-2.35148403114571,
6.87673112956145));
#91747=CARTESIAN_POINT('Ctrl Pts',(-0.176786174264235,-2.37225951021968,
6.88790408119525));
#91748=CARTESIAN_POINT('Ctrl Pts',(0.0355572932765855,-2.37165891632982,
6.90167095604359));
#91749=CARTESIAN_POINT('Ctrl Pts',(0.0644013643421935,-2.37105096579454,
6.90355642784415));
#91750=CARTESIAN_POINT('Ctrl Pts',(0.104622092786952,-2.36946879026094,
6.90621013316511));
#91751=CARTESIAN_POINT('Ctrl Pts',(0.116014453899781,-2.368938321093,6.90696453246844));
#91752=CARTESIAN_POINT('Ctrl Pts',(0.136855224416032,-2.36781720681523,
6.9083498372584));
#91753=CARTESIAN_POINT('Ctrl Pts',(0.146304819695609,-2.36725211429231,
6.9089799315763));
#91754=CARTESIAN_POINT('Ctrl Pts',(0.165433127955941,-2.36599325841199,
6.91025950565679));
#91755=CARTESIAN_POINT('Ctrl Pts',(0.17511146476788,-2.36529663863489,6.91090906323409));
#91756=CARTESIAN_POINT('Ctrl Pts',(0.198975662538783,-2.36343168913475,
6.91251609512297));
#91757=CARTESIAN_POINT('Ctrl Pts',(0.213155646421861,-2.36219502126307,
6.9134756959265));
#91758=CARTESIAN_POINT('Ctrl Pts',(0.265991845461163,-2.35710744658709,
6.91706939030862));
#91759=CARTESIAN_POINT('Ctrl Pts',(0.304560868446427,-2.35243481159841,
6.91972903956202));
#91760=CARTESIAN_POINT('Ctrl Pts',(0.400841287716569,-2.33836308024794,
6.92646380887083));
#91761=CARTESIAN_POINT('Ctrl Pts',(0.458349912665385,-2.32777361970157,
6.93057355323144));
#91762=CARTESIAN_POINT('Ctrl Pts',(0.627024723069871,-2.29022151486651,
6.94288001599588));
#91763=CARTESIAN_POINT('Ctrl Pts',(0.736692836291548,-2.25733343057093,
6.95121871308962));
#91764=CARTESIAN_POINT('Ctrl Pts',(0.961979604805321,-2.17160068591368,
6.96882529350945));
#91765=CARTESIAN_POINT('Ctrl Pts',(1.07661792128258,-2.11711001523005,6.9780689773271));
#91766=CARTESIAN_POINT('Ctrl Pts',(1.20305591776346,-2.04407098286272,6.98822950905937));
#91767=CARTESIAN_POINT('Ctrl Pts',(1.21963181197995,-2.0342241831658,6.98956055951263));
#91768=CARTESIAN_POINT('Ctrl Pts',(1.24276707430886,-2.02009636785497,6.99141498271036));
#91769=CARTESIAN_POINT('Ctrl Pts',(1.24942758321333,-2.01598364455661,6.99194846467697));
#91770=CARTESIAN_POINT('Ctrl Pts',(1.26058359589859,-2.00901851721435,6.9928411933727));
#91771=CARTESIAN_POINT('Ctrl Pts',(1.2650900330684,-2.00618384374638,6.99320157993477));
#91772=CARTESIAN_POINT('Ctrl Pts',(1.27425751000463,-2.000374073935,6.99393419029286));
#91773=CARTESIAN_POINT('Ctrl Pts',(1.27891775038243,-1.99739781386632,6.99430633388162));
#91774=CARTESIAN_POINT('Ctrl Pts',(1.29075395308675,-1.98978022142828,6.9952509275931));
#91775=CARTESIAN_POINT('Ctrl Pts',(1.29791539407534,-1.9851163019975,6.9958218981866));
#91776=CARTESIAN_POINT('Ctrl Pts',(1.32683481353048,-1.96605900346237,6.99812603503372));
#91777=CARTESIAN_POINT('Ctrl Pts',(1.34838082908326,-1.95134515339099,6.99983909475312));
#91778=CARTESIAN_POINT('Ctrl Pts',(1.40456235934286,-1.91160356667001,7.00430885554283));
#91779=CARTESIAN_POINT('Ctrl Pts',(1.43877304190542,-1.88598945031633,7.00703369645474));
#91780=CARTESIAN_POINT('Ctrl Pts',(1.63674022688492,-1.72924415987663,7.0229411833198));
#91781=CARTESIAN_POINT('Ctrl Pts',(1.78320648917726,-1.57777981865735,7.03537571786528));
#91782=CARTESIAN_POINT('Ctrl Pts',(1.94926867088966,-1.35292699177745,7.05300810713387));
#91783=CARTESIAN_POINT('Ctrl Pts',(1.98819469251165,-1.29504447755104,7.05747648546227));
#91784=CARTESIAN_POINT('Ctrl Pts',(2.03387400029331,-1.22019570889695,7.06321779521482));
#91785=CARTESIAN_POINT('Ctrl Pts',(2.04306088069061,-1.2047502751166,7.06440055973187));
#91786=CARTESIAN_POINT('Ctrl Pts',(2.05739453179471,-1.18001632329284,7.06629223144208));
#91787=CARTESIAN_POINT('Ctrl Pts',(2.06265609893493,-1.1707948556351,7.06699697621043));
#91788=CARTESIAN_POINT('Ctrl Pts',(2.07238728835208,-1.1534706828955,7.06832015347643));
#91789=CARTESIAN_POINT('Ctrl Pts',(2.07687176356292,-1.14537651571552,7.06893803753259));
#91790=CARTESIAN_POINT('Ctrl Pts',(2.08679056294257,-1.12722398364047,7.07032312615786));
#91791=CARTESIAN_POINT('Ctrl Pts',(2.09219972749352,-1.11715220771192,7.07109120879116));
#91792=CARTESIAN_POINT('Ctrl Pts',(2.10794604700161,-1.0873173211394,7.07336544443912));
#91793=CARTESIAN_POINT('Ctrl Pts',(2.11807724541879,-1.0674475242442,7.07487879529841));
#91794=CARTESIAN_POINT('Ctrl Pts',(2.19569824967337,-0.909756352348034,
7.08688272446702));
#91795=CARTESIAN_POINT('Ctrl Pts',(2.24993485982392,-0.765848593577822,
7.09783554292199));
#91796=CARTESIAN_POINT('Ctrl Pts',(2.33495520448039,-0.450687575349145,
7.12159359029764));
#91797=CARTESIAN_POINT('Ctrl Pts',(2.36160806942126,-0.279196776185002,
7.13438916012477));
#91798=CARTESIAN_POINT('Ctrl Pts',(2.37013316012776,-0.0892189002088124,
7.14758966101635));
#91799=CARTESIAN_POINT('Ctrl Pts',(2.37071549403491,-0.0721061564834831,
7.14876970703295));
#91800=CARTESIAN_POINT('Ctrl Pts',(2.37126861349832,-0.0482553432358436,
7.15040046377114));
#91801=CARTESIAN_POINT('Ctrl Pts',(2.37139607531557,-0.0415219496452577,
7.15085930146506));
#91802=CARTESIAN_POINT('Ctrl Pts',(2.3715664709993,-0.0299060913625083,
7.15164807682085));
#91803=CARTESIAN_POINT('Ctrl Pts',(2.3716230108178,-0.0250239153481056,
7.15197875693282));
#91804=CARTESIAN_POINT('Ctrl Pts',(2.37171011657951,-0.014767221435175,
7.15267164218714));
#91805=CARTESIAN_POINT('Ctrl Pts',(2.37173749087287,-0.00939272184908155,
7.15303365792538));
#91806=CARTESIAN_POINT('Ctrl Pts',(2.37175983439651,0.00379579987885965,
7.15391952011867));
#91807=CARTESIAN_POINT('Ctrl Pts',(2.37173445711543,0.0116098851496699,
7.15444224112882));
#91808=CARTESIAN_POINT('Ctrl Pts',(2.3715013737321,0.0400695999226933,7.15633870050681));
#91809=CARTESIAN_POINT('Ctrl Pts',(2.37106269939108,0.0607131454763198,
7.1577002384941));
#91810=CARTESIAN_POINT('Ctrl Pts',(2.36929020506543,0.112360122897574,7.16107726098657));
#91811=CARTESIAN_POINT('Ctrl Pts',(2.36761740900082,0.143348785695668,7.16307703502416));
#91812=CARTESIAN_POINT('Ctrl Pts',(2.35767504763082,0.278273669383143,7.17170311819737));
#91813=CARTESIAN_POINT('Ctrl Pts',(2.34316492297942,0.381640660970419,7.17810526922334));
#91814=CARTESIAN_POINT('Ctrl Pts',(2.28596083380586,0.656222713460131,7.19529894857697));
#91815=CARTESIAN_POINT('Ctrl Pts',(2.23091940197626,0.824156845293147,7.20605719407641));
#91816=CARTESIAN_POINT('Ctrl Pts',(2.14591089768657,1.01048709659728,7.21933111514027));
#91817=CARTESIAN_POINT('Ctrl Pts',(2.13355715005715,1.03631632483864,7.22120155455864));
#91818=CARTESIAN_POINT('Ctrl Pts',(2.11550987449121,1.07235835889184,7.22385773805628));
#91819=CARTESIAN_POINT('Ctrl Pts',(2.11020345435234,1.08276306363527,7.22463003394501));
#91820=CARTESIAN_POINT('Ctrl Pts',(2.10082351689131,1.10082415487385,7.22598046302871));
#91821=CARTESIAN_POINT('Ctrl Pts',(2.09678442025638,1.10849824565853,7.22655737815117));
#91822=CARTESIAN_POINT('Ctrl Pts',(2.08823957142258,1.12451924208615,7.22776843793311));
#91823=CARTESIAN_POINT('Ctrl Pts',(2.08372566054862,1.13286159813459,7.22840286422378));
#91824=CARTESIAN_POINT('Ctrl Pts',(2.0728515061733,1.15267371864003,7.2299187837567));
#91825=CARTESIAN_POINT('Ctrl Pts',(2.0664459846036,1.16411814218372,7.2308018835259));
#91826=CARTESIAN_POINT('Ctrl Pts',(2.04434938040251,1.20283994228793,7.23381559564766));
#91827=CARTESIAN_POINT('Ctrl Pts',(2.02821106694831,1.22985690943136,7.2359622375485));
#91828=CARTESIAN_POINT('Ctrl Pts',(1.98815075427778,1.29398754633503,7.24116700866976));
#91829=CARTESIAN_POINT('Ctrl Pts',(1.96372129336663,1.33076873943882,7.24424286206683));
#91830=CARTESIAN_POINT('Ctrl Pts',(1.78483514075512,1.58444173963456,7.26610763197226));
#91831=CARTESIAN_POINT('Ctrl Pts',(1.5958842059277,1.77460063579503,7.28622068216769));
#91832=CARTESIAN_POINT('Ctrl Pts',(1.36384643705875,1.94048545157253,7.30606342928434));
#91833=CARTESIAN_POINT('Ctrl Pts',(1.34821739987404,1.95137664027384,7.30737832266372));
#91834=CARTESIAN_POINT('Ctrl Pts',(1.32601429871494,1.96645488550723,7.30921419815238));
#91835=CARTESIAN_POINT('Ctrl Pts',(1.31954872931874,1.97079930293002,7.30974502840509));
#91836=CARTESIAN_POINT('Ctrl Pts',(1.30863461214616,1.97805504886825,7.31063459479104));
#91837=CARTESIAN_POINT('Ctrl Pts',(1.30419750845687,1.98098338846003,7.31099445323348));
#91838=CARTESIAN_POINT('Ctrl Pts',(1.29511649541476,1.98693281646046,7.31172723116024));
#91839=CARTESIAN_POINT('Ctrl Pts',(1.29047179064321,1.98995259063937,7.31210006360233));
#91840=CARTESIAN_POINT('Ctrl Pts',(1.27859498283242,1.99761527587033,7.31304853541022));
#91841=CARTESIAN_POINT('Ctrl Pts',(1.27134806854374,2.00223525462293,7.31362267109997));
#91842=CARTESIAN_POINT('Ctrl Pts',(1.24166682895499,2.02093121261976,7.31595616055643));
#91843=CARTESIAN_POINT('Ctrl Pts',(1.21902156079035,2.03467099580191,7.31769475691884));
#91844=CARTESIAN_POINT('Ctrl Pts',(1.01342440518146,2.15474983690623,7.33315290616915));
#91845=CARTESIAN_POINT('Ctrl Pts',(0.817214979028365,2.23655133959443,7.34567959061039));
#91846=CARTESIAN_POINT('Ctrl Pts',(0.50997285230316,2.318715177038,7.36541781445755));
#91847=CARTESIAN_POINT('Ctrl Pts',(0.405495383277972,2.33924805596278,7.37213596680569));
#91848=CARTESIAN_POINT('Ctrl Pts',(0.281857636864072,2.35501356429138,7.38027881608126));
#91849=CARTESIAN_POINT('Ctrl Pts',(0.263688036992343,2.35711713832055,7.38148006405105));
#91850=CARTESIAN_POINT('Ctrl Pts',(0.233899104598512,2.36021719841683,7.38345785203343));
#91851=CARTESIAN_POINT('Ctrl Pts',(0.222293311896435,2.36133853779836,7.38423046803939));
#91852=CARTESIAN_POINT('Ctrl Pts',(0.201444213349857,2.3631978900725,7.38562234298475));
#91853=CARTESIAN_POINT('Ctrl Pts',(0.192203894770174,2.36396736385486,7.38624060068705));
#91854=CARTESIAN_POINT('Ctrl Pts',(0.172529042038899,2.36548963981481,7.38756006212258));
#91855=CARTESIAN_POINT('Ctrl Pts',(0.162093593333101,2.36622762373575,7.38826171749581));
#91856=CARTESIAN_POINT('Ctrl Pts',(0.133958040174383,2.36803034810612,7.39015856236435));
#91857=CARTESIAN_POINT('Ctrl Pts',(0.116250607923798,2.36896565032319,7.39135777627514));
#91858=CARTESIAN_POINT('Ctrl Pts',(0.0249594232379776,2.3727616357525,7.39756953796162));
#91859=CARTESIAN_POINT('Ctrl Pts',(-0.0487106889193495,2.37239245720335,
7.40268178308466));
#91860=CARTESIAN_POINT('Ctrl Pts',(-0.208153470922428,2.36416398570984,
7.41396903815144));
#91861=CARTESIAN_POINT('Ctrl Pts',(-0.293757029317236,2.35505917650116,
7.42017060640061));
#91862=CARTESIAN_POINT('Ctrl Pts',(-0.444638027794583,2.33065670333367,
7.43129146736727));
#91863=CARTESIAN_POINT('Ctrl Pts',(-0.51012502524503,2.31720433865143,7.43618245951646));
#91864=CARTESIAN_POINT('Ctrl Pts',(-0.686168998494371,2.27321596242966,
7.44941510043279));
#91865=CARTESIAN_POINT('Ctrl Pts',(-0.795236002910107,2.23739692145749,
7.45771024258265));
#91866=CARTESIAN_POINT('Ctrl Pts',(-0.913069957599856,2.18898683195156,
7.46650067311795));
#91867=CARTESIAN_POINT('Ctrl Pts',(-0.924805530854167,2.18405468020414,
7.46737410677108));
#91868=CARTESIAN_POINT('Ctrl Pts',(-0.942489636805805,2.17645441787358,
7.4686865581843));
#91869=CARTESIAN_POINT('Ctrl Pts',(-0.948467581317756,2.17385597460957,
7.4691295745721));
#91870=CARTESIAN_POINT('Ctrl Pts',(-0.959182051804963,2.16914608655972,
7.46992234808808));
#91871=CARTESIAN_POINT('Ctrl Pts',(-0.963922412205101,2.16704373242484,
7.47027264005255));
#91872=CARTESIAN_POINT('Ctrl Pts',(-0.96867547128321,2.16491706406728,7.47062341409115));
#91873=CARTESIAN_POINT('Ctrl Pts',(-0.968694951178242,2.16490834783305,
7.47062485169279));
#91874=CARTESIAN_POINT('Ctrl Pts',(-0.968733628915929,2.16489104094172,
7.47062770606584));
#91875=CARTESIAN_POINT('Ctrl Pts',(-0.968752826773134,2.16488245028718,
7.47062912283853));
#91876=CARTESIAN_POINT('Ctrl Pts',(-0.968790945158034,2.16486539246889,
7.47063193590286));
#91877=CARTESIAN_POINT('Ctrl Pts',(-0.968809865627772,2.16485692533987,
7.47063333219043));
#91878=CARTESIAN_POINT('Ctrl Pts',(-0.968847433653024,2.16484011262295,
7.47063610461099));
#91879=CARTESIAN_POINT('Ctrl Pts',(-0.968866081234489,2.16483176703196,
7.4706374807461));
#91880=CARTESIAN_POINT('Ctrl Pts',(-0.96890310781857,2.16481519547627,7.47064021318229));
#91881=CARTESIAN_POINT('Ctrl Pts',(-0.968921486890057,2.16480696948902,
7.47064156948864));
#91882=CARTESIAN_POINT('Ctrl Pts',(-0.968957980969866,2.16479063514436,
7.47064426260116));
#91883=CARTESIAN_POINT('Ctrl Pts',(-0.968976095937338,2.16478252681324,
7.47064559940449));
#91884=CARTESIAN_POINT('Ctrl Pts',(-0.969012065982602,2.16476642593671,
7.47064825381953));
#91885=CARTESIAN_POINT('Ctrl Pts',(-0.969029921085812,2.16475843338769,
7.47064957143328));
#91886=CARTESIAN_POINT('Ctrl Pts',(-0.969065375594583,2.16474256222202,
7.47065218777907));
#91887=CARTESIAN_POINT('Ctrl Pts',(-0.969082975010155,2.16473468360843,
7.47065348651202));
#91888=CARTESIAN_POINT('Ctrl Pts',(-0.969117922355154,2.16471903845079,
7.47065606540751));
#91889=CARTESIAN_POINT('Ctrl Pts',(-0.969135270244155,2.16471127193214,
7.47065734556724));
#91890=CARTESIAN_POINT('Ctrl Pts',(-0.969169718411262,2.16469584925127,
7.47065988760279));
#91891=CARTESIAN_POINT('Ctrl Pts',(-0.969186818747928,2.16468819306992,
7.4706611494831));
#91892=CARTESIAN_POINT('Ctrl Pts',(-0.969220775905205,2.16467298925146,
7.47066365526249));
#91893=CARTESIAN_POINT('Ctrl Pts',(-0.969237632698956,2.16466544163324,
7.47066489915975));
#91894=CARTESIAN_POINT('Ctrl Pts',(-0.969271106567646,2.16465045326136,
7.47066736925373));
#91895=CARTESIAN_POINT('Ctrl Pts',(-0.969287723673151,2.16464301250068,
7.47066859545286));
#91896=CARTESIAN_POINT('Ctrl Pts',(-0.969320722029739,2.16462823613338,
7.47067103043623));
#91897=CARTESIAN_POINT('Ctrl Pts',(-0.969337103265034,2.1646209005403,7.47067223921946));
#91898=CARTESIAN_POINT('Ctrl Pts',(-0.96936963373478,2.16460633280188,7.47067463965583));
#91899=CARTESIAN_POINT('Ctrl Pts',(-0.969385782906217,2.16459910069103,
7.47067583130448));
#91900=CARTESIAN_POINT('Ctrl Pts',(-0.969417852722957,2.1645847383797,7.47067819772855));
#91901=CARTESIAN_POINT('Ctrl Pts',(-0.969433773430796,2.16457760815732,
7.47067937250873));
#91902=CARTESIAN_POINT('Ctrl Pts',(-0.969465390112604,2.1645634479427,7.47068170547613));
#91903=CARTESIAN_POINT('Ctrl Pts',(-0.969481086033776,2.16455641798003,
7.47068286365958));
#91904=CARTESIAN_POINT('Ctrl Pts',(-0.969512256604615,2.16454245675176,
7.47068516368945));
#91905=CARTESIAN_POINT('Ctrl Pts',(-0.969527731275321,2.16453552548246,
7.47068630553754));
#91906=CARTESIAN_POINT('Ctrl Pts',(-0.969558974099726,2.16452153108746,
7.47068861087973));
#91907=CARTESIAN_POINT('Ctrl Pts',(-0.969574742306731,2.16451446793025,
7.47068977437758));
#91908=CARTESIAN_POINT('Ctrl Pts',(-0.969606231288884,2.16450036244915,
7.47069209786356));
#91909=CARTESIAN_POINT('Ctrl Pts',(-0.969621951977121,2.16449332016544,
7.47069325784531));
#91910=CARTESIAN_POINT('Ctrl Pts',(-0.969653346075856,2.16447925636603,
7.47069557431056));
#91911=CARTESIAN_POINT('Ctrl Pts',(-0.969669019503406,2.16447223484393,
7.47069673079534));
#91912=CARTESIAN_POINT('Ctrl Pts',(-0.969700319320073,2.16445821246421,
7.47069904028441));
#91913=CARTESIAN_POINT('Ctrl Pts',(-0.969715945747083,2.16445121159084,
7.47070019329151));
#91914=CARTESIAN_POINT('Ctrl Pts',(-0.969747151920878,2.16443723035176,
7.47070249585174));
#91915=CARTESIAN_POINT('Ctrl Pts',(-0.969762731654559,2.16443024999313,
7.47070364540392));
#91916=CARTESIAN_POINT('Ctrl Pts',(-0.96979384469873,2.16441630967201,7.47070594107336));
#91917=CARTESIAN_POINT('Ctrl Pts',(-0.969809378019336,2.16440934970617,
7.47070708719139));
#91918=CARTESIAN_POINT('Ctrl Pts',(-0.969840398475935,2.16439545006731,
7.4707093760102));
#91919=CARTESIAN_POINT('Ctrl Pts',(-0.969855885643577,2.16438851038129,
7.47071051871336));
#91920=CARTESIAN_POINT('Ctrl Pts',(-0.969886814101103,2.16437465116812,
7.47071280072515));
#91921=CARTESIAN_POINT('Ctrl Pts',(-0.969902255387046,2.16436773164392,
7.47071394003353));
#91922=CARTESIAN_POINT('Ctrl Pts',(-0.969933092459339,2.16435391258844,
7.47071621528377));
#91923=CARTESIAN_POINT('Ctrl Pts',(-0.969948488187533,2.1643470130844,7.47071735122136));
#91924=CARTESIAN_POINT('Ctrl Pts',(-0.969979234282175,2.16433323401096,
7.47071961974028));
#91925=CARTESIAN_POINT('Ctrl Pts',(-0.969994584680246,2.16432635442855,
7.47072075232397));
#91926=CARTESIAN_POINT('Ctrl Pts',(-0.970025240459214,2.16431261504741,
7.47072301416059));
#91927=CARTESIAN_POINT('Ctrl Pts',(-0.970040545821809,2.16430575525803,
7.4707241434122));
#91928=CARTESIAN_POINT('Ctrl Pts',(-0.97007111179331,2.1642920553483,7.47072639860418));
#91929=CARTESIAN_POINT('Ctrl Pts',(-0.970086372399844,2.16428521523014,
7.47072752454441));
#91930=CARTESIAN_POINT('Ctrl Pts',(-0.970116849044107,2.16427155458339,
7.47072977312735));
#91931=CARTESIAN_POINT('Ctrl Pts',(-0.970132065120514,2.16426473403857,
7.47073089577295));
#91932=CARTESIAN_POINT('Ctrl Pts',(-0.975890890559293,2.16168329085297,
7.4711557815007));
#91933=CARTESIAN_POINT('Ctrl Pts',(-0.981624312343408,2.15908577688989,
7.47157814153987));
#91934=CARTESIAN_POINT('Ctrl Pts',(-0.998369713610735,2.15141881950578,
7.47280999994709));
#91935=CARTESIAN_POINT('Ctrl Pts',(-1.00935345471363,2.14628764170618,7.47361583151524));
#91936=CARTESIAN_POINT('Ctrl Pts',(-1.03453348052094,2.1342884575082,7.47545926161316));
#91937=CARTESIAN_POINT('Ctrl Pts',(-1.04870173042696,2.1273625580462,7.47649362354299));
#91938=CARTESIAN_POINT('Ctrl Pts',(-1.20186067440457,2.05059148676722,7.48765488850947));
#91939=CARTESIAN_POINT('Ctrl Pts',(-1.33374647243368,1.96736585007179,7.49710094675346));
#91940=CARTESIAN_POINT('Ctrl Pts',(-1.57626001286983,1.77865467242176,7.51593822353582));
#91941=CARTESIAN_POINT('Ctrl Pts',(-1.68674752221328,1.67424096733691,7.52528955580757));
#91942=CARTESIAN_POINT('Ctrl Pts',(-1.80566593341802,1.53805636379962,7.53700254907519));
#91943=CARTESIAN_POINT('Ctrl Pts',(-1.82442178815007,1.51576114831558,7.53890532760568));
#91944=CARTESIAN_POINT('Ctrl Pts',(-1.85016868956254,1.4839852819524,7.54159998222408));
#91945=CARTESIAN_POINT('Ctrl Pts',(-1.85750757462526,1.47478883189998,7.54237787851772));
#91946=CARTESIAN_POINT('Ctrl Pts',(-1.87014944143273,1.45870309031739,7.54373530864932));
#91947=CARTESIAN_POINT('Ctrl Pts',(-1.87548357993214,1.45183848170299,7.54431359192015));
#91948=CARTESIAN_POINT('Ctrl Pts',(-1.88654756158331,1.43743729941374,7.54552477550449));
#91949=CARTESIAN_POINT('Ctrl Pts',(-1.89227024922733,1.42989544766634,7.54615794336183));
#91950=CARTESIAN_POINT('Ctrl Pts',(-1.90575234386216,1.41190490034321,7.54766578293109));
#91951=CARTESIAN_POINT('Ctrl Pts',(-1.91347113405706,1.4014262917159,7.54854201620449));
#91952=CARTESIAN_POINT('Ctrl Pts',(-1.93920219614779,1.36588630856477,7.55150756280816));
#91953=CARTESIAN_POINT('Ctrl Pts',(-1.95681077813004,1.34053794697499,7.55361221960913));
#91954=CARTESIAN_POINT('Ctrl Pts',(-2.02043138975053,1.24502778759721,7.56150767920599));
#91955=CARTESIAN_POINT('Ctrl Pts',(-2.06320064658656,1.1727904492665,7.56741410073814));
#91956=CARTESIAN_POINT('Ctrl Pts',(-2.1362946858041,1.03291352832711,7.57871912391117));
#91957=CARTESIAN_POINT('Ctrl Pts',(-2.16745445830077,0.965818513013279,
7.58408824787615));
#91958=CARTESIAN_POINT('Ctrl Pts',(-2.22509976008393,0.824790273751776,
7.59520399922622));
#91959=CARTESIAN_POINT('Ctrl Pts',(-2.25115318195857,0.750771356717332,
7.60094729694803));
#91960=CARTESIAN_POINT('Ctrl Pts',(-2.29750938951388,0.594775286730919,
7.61273704543889));
#91961=CARTESIAN_POINT('Ctrl Pts',(-2.31720265793425,0.51272039465409,7.61876580320549));
#91962=CARTESIAN_POINT('Ctrl Pts',(-2.33475443212655,0.417464582372106,
7.62544747915636));
#91963=CARTESIAN_POINT('Ctrl Pts',(-2.33692651305717,0.405128900106705,
7.62630669642189));
#91964=CARTESIAN_POINT('Ctrl Pts',(-2.34007301325301,0.386391345390974,
7.62760205377453));
#91965=CARTESIAN_POINT('Ctrl Pts',(-2.34111906580965,0.380001975506996,
7.62804204273221));
#91966=CARTESIAN_POINT('Ctrl Pts',(-2.34295550212509,0.368489412840857,
7.628831638922));
#91967=CARTESIAN_POINT('Ctrl Pts',(-2.34375526114331,0.363367871113592,
7.62918176122784));
#91968=CARTESIAN_POINT('Ctrl Pts',(-2.3452845483387,0.35335939506694,7.62986373736462));
#91969=CARTESIAN_POINT('Ctrl Pts',(-2.34601559299617,0.348472830088667,
7.63019567854787));
#91970=CARTESIAN_POINT('Ctrl Pts',(-2.34762075728033,0.337509310768287,
7.63093819007921));
#91971=CARTESIAN_POINT('Ctrl Pts',(-2.34848656618602,0.331431147298305,
7.63134830091514));
#91972=CARTESIAN_POINT('Ctrl Pts',(-2.35060748290207,0.316116142845398,
7.63237793594942));
#91973=CARTESIAN_POINT('Ctrl Pts',(-2.3518317696138,0.306875037714167,7.63299582431652));
#91974=CARTESIAN_POINT('Ctrl Pts',(-2.35823918987495,0.256218741601184,
7.63636546432904));
#91975=CARTESIAN_POINT('Ctrl Pts',(-2.36238186104507,0.214687524790751,
7.63906453097502));
#91976=CARTESIAN_POINT('Ctrl Pts',(-2.36542649614281,0.173076728203254,
7.64172477676247));
#91977=CARTESIAN_POINT('Origin',(0.,0.,-1.84858989190503));
#91978=CARTESIAN_POINT('',(-2.36542648836857,0.173076834453233,8.83818724301668));
#91979=CARTESIAN_POINT('',(-2.36542651242649,0.173076505655319,8.63818628587103));
#91980=CARTESIAN_POINT('',(-2.36542649454111,0.173076750093529,-1.84858989190503));
#91981=CARTESIAN_POINT('',(-2.37174984266889,0.000863886614090527,7.85072532400096));
#91982=CARTESIAN_POINT('Ctrl Pts',(-2.36542648836857,0.173076834453233,
8.83818724301668));
#91983=CARTESIAN_POINT('Ctrl Pts',(-2.35876889342097,0.264065622684951,
8.83249593822389));
#91984=CARTESIAN_POINT('Ctrl Pts',(-2.34686578487537,0.354611150249955,
8.82670376988962));
#91985=CARTESIAN_POINT('Ctrl Pts',(-2.32629063658811,0.462509364048279,
8.81953001257228));
#91986=CARTESIAN_POINT('Ctrl Pts',(-2.32259742656982,0.480712179483354,
8.81831050730852));
#91987=CARTESIAN_POINT('Ctrl Pts',(-2.31623859978643,0.510267321550908,
8.81631444510768));
#91988=CARTESIAN_POINT('Ctrl Pts',(-2.3137023336149,0.5216469052677,8.81554202140753));
#91989=CARTESIAN_POINT('Ctrl Pts',(-2.30902450150786,0.541929662981707,
8.81415811915313));
#91990=CARTESIAN_POINT('Ctrl Pts',(-2.3069150664522,0.550840067815803,8.81354768413038));
#91991=CARTESIAN_POINT('Ctrl Pts',(-2.30234449119464,0.569659682490639,
8.81225304335078));
#91992=CARTESIAN_POINT('Ctrl Pts',(-2.29987086093921,0.579565636772957,
8.81156844553908));
#91993=CARTESIAN_POINT('Ctrl Pts',(-2.29310521796342,0.605933947780758,
8.80973757438763));
#91994=CARTESIAN_POINT('Ctrl Pts',(-2.28869997504526,0.622366361225135,
8.80858766082402));
#91995=CARTESIAN_POINT('Ctrl Pts',(-2.26626953676803,0.702575848602684,
8.80292974437382));
#91996=CARTESIAN_POINT('Ctrl Pts',(-2.2457549291516,0.765619830370065,8.79834157775914));
#91997=CARTESIAN_POINT('Ctrl Pts',(-2.13286566276937,1.06875600474037,8.77556502443014));
#91998=CARTESIAN_POINT('Ctrl Pts',(-2.00451654065907,1.29353476881524,8.75619300901502));
#91999=CARTESIAN_POINT('Ctrl Pts',(-1.82575394459939,1.51411287992846,8.7362863785228));
#92000=CARTESIAN_POINT('Ctrl Pts',(-1.80853997549951,1.53463304732701,8.73442714537895));
#92001=CARTESIAN_POINT('Ctrl Pts',(-1.78517098548093,1.56155088444538,8.73198324857461));
#92002=CARTESIAN_POINT('Ctrl Pts',(-1.77932316163247,1.56821098865054,8.73137815513024));
#92003=CARTESIAN_POINT('Ctrl Pts',(-1.76975442316424,1.5789864217645,8.7303987134258));
#92004=CARTESIAN_POINT('Ctrl Pts',(-1.76605623044131,1.58312167282589,8.73002272594953));
#92005=CARTESIAN_POINT('Ctrl Pts',(-1.7588332155937,1.59114150698706,8.72929339289365));
#92006=CARTESIAN_POINT('Ctrl Pts',(-1.75530998635767,1.59502740664373,8.72893994248078));
#92007=CARTESIAN_POINT('Ctrl Pts',(-1.74676597404571,1.60438831873584,8.72808826386245));
#92008=CARTESIAN_POINT('Ctrl Pts',(-1.74173224656889,1.60985155539242,8.7275910062397));
#92009=CARTESIAN_POINT('Ctrl Pts',(-1.72403117362975,1.62888278259217,8.72585772063192));
#92010=CARTESIAN_POINT('Ctrl Pts',(-1.71122988842416,1.64232607273957,8.72463141666329));
#92011=CARTESIAN_POINT('Ctrl Pts',(-1.63161718176271,1.72398982781426,8.71715937238237));
#92012=CARTESIAN_POINT('Ctrl Pts',(-1.56088621668562,1.78828246408518,8.71117651172074));
#92013=CARTESIAN_POINT('Ctrl Pts',(-1.42878393351868,1.89453254393126,8.70070126151164));
#92014=CARTESIAN_POINT('Ctrl Pts',(-1.3689638637378,1.93819900896571,8.69618242963897));
#92015=CARTESIAN_POINT('Ctrl Pts',(-1.17525104806262,2.06615330351451,8.6819439599089));
#92016=CARTESIAN_POINT('Ctrl Pts',(-1.03493810967471,2.13988258034999,8.67215654690258));
#92017=CARTESIAN_POINT('Ctrl Pts',(-0.870985476867069,2.20611261868149,
8.66061009057379));
#92018=CARTESIAN_POINT('Ctrl Pts',(-0.853544047491532,2.21291913841129,
8.65938096467967));
#92019=CARTESIAN_POINT('Ctrl Pts',(-0.825071909566361,2.22364371690574,
8.65737227909002));
#92020=CARTESIAN_POINT('Ctrl Pts',(-0.814089336649769,2.2276879447796,8.65659694110482));
#92021=CARTESIAN_POINT('Ctrl Pts',(-0.794456834981467,2.23475285846302,
8.65520979757175));
#92022=CARTESIAN_POINT('Ctrl Pts',(-0.785818426973752,2.23780503995142,
8.65459905440992));
#92023=CARTESIAN_POINT('Ctrl Pts',(-0.767540112934206,2.24414437336899,
8.65330582884267));
#92024=CARTESIAN_POINT('Ctrl Pts',(-0.757896306951808,2.24741962609871,
8.65262296643389));
#92025=CARTESIAN_POINT('Ctrl Pts',(-0.732197274724079,2.25596337235392,
8.65080165307633));
#92026=CARTESIAN_POINT('Ctrl Pts',(-0.716106579494251,2.26112249280876,
8.64965962853309));
#92027=CARTESIAN_POINT('Ctrl Pts',(-0.637987453753924,2.28525215939675,
8.64410608392915));
#92028=CARTESIAN_POINT('Ctrl Pts',(-0.575259000557079,2.30184297636762,
8.63961793987635));
#92029=CARTESIAN_POINT('Ctrl Pts',(-0.279153485851427,2.36729937622403,
8.61828198487702));
#92030=CARTESIAN_POINT('Ctrl Pts',(-0.0399982439119246,2.38335918752959,
8.60043946926061));
#92031=CARTESIAN_POINT('Ctrl Pts',(0.241216999428088,2.35985938088234,8.5803867455497));
#92032=CARTESIAN_POINT('Ctrl Pts',(0.284820498405838,2.35499465639849,8.57731028643348));
#92033=CARTESIAN_POINT('Ctrl Pts',(0.338629641142923,2.34747470812399,8.57357408241161));
#92034=CARTESIAN_POINT('Ctrl Pts',(0.348982594264789,2.34595794896039,8.57285801840938));
#92035=CARTESIAN_POINT('Ctrl Pts',(0.365220566769256,2.34346913130864,8.57173964947988));
#92036=CARTESIAN_POINT('Ctrl Pts',(0.371112377254393,2.34254332665123,8.5713348393428));
#92037=CARTESIAN_POINT('Ctrl Pts',(0.382057495152985,2.34078114456698,8.57058473251952));
#92038=CARTESIAN_POINT('Ctrl Pts',(0.387111544944955,2.33995062959239,8.5702391253836));
#92039=CARTESIAN_POINT('Ctrl Pts',(0.398648027104586,2.33801647778497,8.56945194466544));
#92040=CARTESIAN_POINT('Ctrl Pts',(0.405128582778107,2.33690225169225,8.56901097549462));
#92041=CARTESIAN_POINT('Ctrl Pts',(0.425115921310742,2.33338011110503,8.56765448665391));
#92042=CARTESIAN_POINT('Ctrl Pts',(0.438606809088545,2.33088188862414,8.56674390393655));
#92043=CARTESIAN_POINT('Ctrl Pts',(0.567195089944457,2.30591411662454,8.55810596860091));
#92044=CARTESIAN_POINT('Ctrl Pts',(0.680515752676439,2.27505086800216,8.55080612054963));
#92045=CARTESIAN_POINT('Ctrl Pts',(0.98799911929464,2.16625893379207,8.53073319167251));
#92046=CARTESIAN_POINT('Ctrl Pts',(1.17480939033113,2.07090186645032,8.51814212041526));
#92047=CARTESIAN_POINT('Ctrl Pts',(1.3683783238774,1.93737744295705,8.50286380845404));
#92048=CARTESIAN_POINT('Ctrl Pts',(1.38978954523985,1.92207583697046,8.50114130932855));
#92049=CARTESIAN_POINT('Ctrl Pts',(1.42057046738588,1.89929490219257,8.49861480063135));
#92050=CARTESIAN_POINT('Ctrl Pts',(1.43014559536455,1.89209543772177,8.49782163396893));
#92051=CARTESIAN_POINT('Ctrl Pts',(1.44699769638005,1.87922347067598,8.49641256373866));
#92052=CARTESIAN_POINT('Ctrl Pts',(1.45429693751029,1.87358042247481,8.49579782838899));
#92053=CARTESIAN_POINT('Ctrl Pts',(1.46939857081102,1.86176391876256,8.49451665440732));
#92054=CARTESIAN_POINT('Ctrl Pts',(1.47719540021764,1.85558367999035,8.4938499530639));
#92055=CARTESIAN_POINT('Ctrl Pts',(1.49729287859935,1.83944626087682,8.4921176334833));
#92056=CARTESIAN_POINT('Ctrl Pts',(1.50953299652158,1.82941483052731,8.49104903856798));
#92057=CARTESIAN_POINT('Ctrl Pts',(1.56250548174605,1.78510745215525,8.48636397954637));
#92058=CARTESIAN_POINT('Ctrl Pts',(1.6021748125262,1.74959054456431,8.48269701622513));
#92059=CARTESIAN_POINT('Ctrl Pts',(1.70704027012669,1.64914303044285,8.47255037412201));
#92060=CARTESIAN_POINT('Ctrl Pts',(1.76970252691558,1.58171075697425,8.46597227153812));
#92061=CARTESIAN_POINT('Ctrl Pts',(1.91170094895162,1.40987415689578,8.44981530758467));
#92062=CARTESIAN_POINT('Ctrl Pts',(1.98661126025481,1.30219848747345,8.44016550861144));
#92063=CARTESIAN_POINT('Ctrl Pts',(2.05906393767271,1.17713145764383,8.42974857155937));
#92064=CARTESIAN_POINT('Ctrl Pts',(2.06577544222655,1.16531309167152,8.42877172448446));
#92065=CARTESIAN_POINT('Ctrl Pts',(2.10036778901294,1.10316090489159,8.42367586822666));
#92066=CARTESIAN_POINT('Ctrl Pts',(2.12651441470661,1.05187762720501,8.41961165031398));
#92067=CARTESIAN_POINT('Ctrl Pts',(2.15513346251164,0.990305459410694,8.41493595426291));
#92068=CARTESIAN_POINT('Ctrl Pts',(2.15943378223277,0.980892906555262,8.41422668229754));
#92069=CARTESIAN_POINT('Ctrl Pts',(2.16633105318418,0.96553092199153,8.41307838007262));
#92070=CARTESIAN_POINT('Ctrl Pts',(2.16896537157686,0.959598568553732,8.41263717656038));
#92071=CARTESIAN_POINT('Ctrl Pts',(2.17363214511731,0.9489718259161,8.41185093082263));
#92072=CARTESIAN_POINT('Ctrl Pts',(2.17567379245244,0.944281620699652,8.41150533877518));
#92073=CARTESIAN_POINT('Ctrl Pts',(2.18008747530667,0.934051911191164,8.41075468265436));
#92074=CARTESIAN_POINT('Ctrl Pts',(2.18245357690786,0.928509967358067,8.41034997935679));
#92075=CARTESIAN_POINT('Ctrl Pts',(2.18909317251914,0.912792932091501,8.40920762206317));
#92076=CARTESIAN_POINT('Ctrl Pts',(2.19331687699893,0.902596778058855,8.40847290886138));
#92077=CARTESIAN_POINT('Ctrl Pts',(2.22000570597938,0.836875383718948,8.40377567745109));
#92078=CARTESIAN_POINT('Ctrl Pts',(2.24043396472986,0.780540077435654,8.39992512984583));
#92079=CARTESIAN_POINT('Ctrl Pts',(2.3128200488446,0.554552274222488,8.38493956171926));
#92080=CARTESIAN_POINT('Ctrl Pts',(2.3478113708967,0.380072681827114,8.3743378858184));
#92081=CARTESIAN_POINT('Ctrl Pts',(2.37186095108942,0.100554209268612,8.35690583426247));
#92082=CARTESIAN_POINT('Ctrl Pts',(2.37398912139002,-0.00265914512425559,
8.35038293476816));
#92083=CARTESIAN_POINT('Ctrl Pts',(2.36859164943295,-0.123678800109922,
8.3424665500662));
#92084=CARTESIAN_POINT('Ctrl Pts',(2.36758351739713,-0.141672530689988,
8.34128272957081));
#92085=CARTESIAN_POINT('Ctrl Pts',(2.36559687395829,-0.171118550420209,
8.33933354068602));
#92086=CARTESIAN_POINT('Ctrl Pts',(2.36473998606553,-0.182578527741134,
8.33857198474456));
#92087=CARTESIAN_POINT('Ctrl Pts',(2.36305216669293,-0.203140467344562,
8.33720005823731));
#92088=CARTESIAN_POINT('Ctrl Pts',(2.36225183797834,-0.212244768903336,
8.33659066098494));
#92089=CARTESIAN_POINT('Ctrl Pts',(2.36043664863537,-0.231610028606325,
8.33529020313934));
#92090=CARTESIAN_POINT('Ctrl Pts',(2.35940745846572,-0.24186942070689,8.3345987033529));
#92091=CARTESIAN_POINT('Ctrl Pts',(2.35645420963427,-0.269493707664435,
8.33272976843025));
#92092=CARTESIAN_POINT('Ctrl Pts',(2.35440515101737,-0.286844307729571,
8.33154842272809));
#92093=CARTESIAN_POINT('Ctrl Pts',(2.34289546637464,-0.375849296777698,
8.32544862964116));
#92094=CARTESIAN_POINT('Ctrl Pts',(2.33035567060752,-0.447059686599547,
8.32043405970765));
#92095=CARTESIAN_POINT('Ctrl Pts',(2.27777143017788,-0.682213004957853,
8.30341206738335));
#92096=CARTESIAN_POINT('Ctrl Pts',(2.22349953377891,-0.842433419120874,
8.29100927223934));
#92097=CARTESIAN_POINT('Ctrl Pts',(2.11026041442282,-1.08730179754128,8.2713781832903));
#92098=CARTESIAN_POINT('Ctrl Pts',(2.06198217251954,-1.17629027647838,8.26409827929705));
#92099=CARTESIAN_POINT('Ctrl Pts',(2.00145534194759,-1.27260894965185,8.25624975431905));
#92100=CARTESIAN_POINT('Ctrl Pts',(1.99466180926581,-1.28323080886447,8.25538474084757));
#92101=CARTESIAN_POINT('Ctrl Pts',(1.98427135987478,-1.2991946313424,8.25408605884288));
#92102=CARTESIAN_POINT('Ctrl Pts',(1.98073699658057,-1.30457674078761,8.25364845284415));
#92103=CARTESIAN_POINT('Ctrl Pts',(1.97435726533354,-1.3142060661623,8.25286603772219));
#92104=CARTESIAN_POINT('Ctrl Pts',(1.97152005631048,-1.31845851837971,8.25252070184516));
#92105=CARTESIAN_POINT('Ctrl Pts',(1.9652857622723,-1.32773745085457,8.25176759482862));
#92106=CARTESIAN_POINT('Ctrl Pts',(1.96188313840014,-1.33276007561216,8.25136020325772));
#92107=CARTESIAN_POINT('Ctrl Pts',(1.95212915438269,-1.34703966358553,8.25020254034004));
#92108=CARTESIAN_POINT('Ctrl Pts',(1.94573118338759,-1.35626482115504,8.24945533597536));
#92109=CARTESIAN_POINT('Ctrl Pts',(1.90233027635461,-1.41790481135023,8.24446482271152));
#92110=CARTESIAN_POINT('Ctrl Pts',(1.86327531870815,-1.46885034293609,8.24035023002256));
#92111=CARTESIAN_POINT('Ctrl Pts',(1.68289114297404,-1.68536047254136,8.22260247412023));
#92112=CARTESIAN_POINT('Ctrl Pts',(1.52123285040937,-1.83260045205038,8.20972833868825));
#92113=CARTESIAN_POINT('Ctrl Pts',(1.28977074012306,-1.99139731878356,8.19195582127505));
#92114=CARTESIAN_POINT('Ctrl Pts',(1.23639293640038,-2.02496993568435,8.18790440629867));
#92115=CARTESIAN_POINT('Ctrl Pts',(1.16662423612708,-2.06506418658737,8.18263168299683));
#92116=CARTESIAN_POINT('Ctrl Pts',(1.1514085504619,-2.07358639220383,8.18148317239406));
#92117=CARTESIAN_POINT('Ctrl Pts',(1.12705565001879,-2.08687560652988,8.17964650319509));
#92118=CARTESIAN_POINT('Ctrl Pts',(1.11797875783969,-2.09175231006692,8.1789622704766));
#92119=CARTESIAN_POINT('Ctrl Pts',(1.10159859758542,-2.10041573628207,8.17772796926519));
#92120=CARTESIAN_POINT('Ctrl Pts',(1.09430681774201,-2.10422392371223,8.17717867315257));
#92121=CARTESIAN_POINT('Ctrl Pts',(1.07715976245044,-2.11306587041922,8.17588727331216));
#92122=CARTESIAN_POINT('Ctrl Pts',(1.0672888443581,-2.11806870569773,8.17514409528101));
#92123=CARTESIAN_POINT('Ctrl Pts',(1.03859135786244,-2.13236178855202,8.17298392631309));
#92124=CARTESIAN_POINT('Ctrl Pts',(1.01967640112659,-2.14147117499374,8.17156067936806));
#92125=CARTESIAN_POINT('Ctrl Pts',(0.836290734516628,-2.22680870456615,
8.15776344523456));
#92126=CARTESIAN_POINT('Ctrl Pts',(0.663746004042504,-2.28417906291392,
8.14472321476231));
#92127=CARTESIAN_POINT('Ctrl Pts',(0.344160640759544,-2.35114227672244,
8.12088072388546));
#92128=CARTESIAN_POINT('Ctrl Pts',(0.199476075607933,-2.36781203045311,
8.11021703771134));
#92129=CARTESIAN_POINT('Ctrl Pts',(0.0353569518289831,-2.37156105958021,
8.09880003056622));
#92130=CARTESIAN_POINT('Ctrl Pts',(0.0165441405859353,-2.37176691956004,
8.09750167556997));
#92131=CARTESIAN_POINT('Ctrl Pts',(-0.00995573825995391,-2.37174155814028,
8.0956892207875));
#92132=CARTESIAN_POINT('Ctrl Pts',(-0.0176416755835647,-2.3716968420938,
8.09516548809294));
#92133=CARTESIAN_POINT('Ctrl Pts',(-0.0305692244275301,-2.37155878378138,
8.0942880073471));
#92134=CARTESIAN_POINT('Ctrl Pts',(-0.0358109398957473,-2.37148542497318,
8.09393316368678));
#92135=CARTESIAN_POINT('Ctrl Pts',(-0.0465069566268487,-2.37130026060064,
8.09321107532711));
#92136=CARTESIAN_POINT('Ctrl Pts',(-0.0519611810340661,-2.37118701500951,
8.09284391253337));
#92137=CARTESIAN_POINT('Ctrl Pts',(-0.0658565801804263,-2.37085053826371,
8.09191108360727));
#92138=CARTESIAN_POINT('Ctrl Pts',(-0.0742971329552926,-2.37060104307359,
8.09134686699118));
#92139=CARTESIAN_POINT('Ctrl Pts',(-0.108581203077959,-2.36940434622817,
8.0890642777744));
#92140=CARTESIAN_POINT('Ctrl Pts',(-0.134410921354802,-2.36807953309005,
8.08736572004124));
#92141=CARTESIAN_POINT('Ctrl Pts',(-0.360520509866732,-2.35277053793205,
8.07264165946409));
#92142=CARTESIAN_POINT('Ctrl Pts',(-0.558320797704371,-2.31382923208865,
8.06070309561615));
#92143=CARTESIAN_POINT('Ctrl Pts',(-0.860767319413871,-2.21318439430736,
8.04099562808946));
#92144=CARTESIAN_POINT('Ctrl Pts',(-0.969716783353863,-2.16765985527582,
8.03358012009086));
#92145=CARTESIAN_POINT('Ctrl Pts',(-1.0912807338481,-2.10585977164396,8.02467274331321));
#92146=CARTESIAN_POINT('Ctrl Pts',(-1.10764212331602,-2.09730014847816,
8.02346025613574));
#92147=CARTESIAN_POINT('Ctrl Pts',(-1.13413942925326,-2.08304128240529,
8.02147340620565));
#92148=CARTESIAN_POINT('Ctrl Pts',(-1.14433652488689,-2.07745689217284,
8.0207031126838));
#92149=CARTESIAN_POINT('Ctrl Pts',(-1.16226797640115,-2.0674647409578,8.01933828437396));
#92150=CARTESIAN_POINT('Ctrl Pts',(-1.17001940492398,-2.06308795073163,
8.01874486844552));
#92151=CARTESIAN_POINT('Ctrl Pts',(-1.1863607543088,-2.05373920650361,8.0174864791963));
#92152=CARTESIAN_POINT('Ctrl Pts',(-1.19494445140899,-2.04875677437307,
8.01682113541318));
#92153=CARTESIAN_POINT('Ctrl Pts',(-1.21245708504015,-2.03844401798555,
8.01545464581285));
#92154=CARTESIAN_POINT('Ctrl Pts',(-1.22138273210964,-2.03310855913109,
8.01475332309753));
#92155=CARTESIAN_POINT('Ctrl Pts',(-1.24339138801022,-2.01975527369345,
8.01301178948753));
#92156=CARTESIAN_POINT('Ctrl Pts',(-1.25643206796592,-2.01166894608116,
8.01196908684175));
#92157=CARTESIAN_POINT('Ctrl Pts',(-1.29264916749593,-1.98872174001718,
8.00904250121894));
#92158=CARTESIAN_POINT('Ctrl Pts',(-1.31564601595939,-1.97358341095718,
8.00714852719978));
#92159=CARTESIAN_POINT('Ctrl Pts',(-1.39066111803529,-1.92230878743477,
8.00084988638151));
#92160=CARTESIAN_POINT('Ctrl Pts',(-1.44149201230967,-1.88449170563035,
7.99638539179347));
#92161=CARTESIAN_POINT('Ctrl Pts',(-1.60078961471317,-1.75575880720873,
7.98175300785968));
#92162=CARTESIAN_POINT('Ctrl Pts',(-1.70264950944771,-1.65716481953111,
7.97135555914241));
#92163=CARTESIAN_POINT('Ctrl Pts',(-1.86194245144197,-1.47269351742679,
7.95361625203662));
#92164=CARTESIAN_POINT('Ctrl Pts',(-1.92371118887939,-1.39104146408768,
7.94625102844911));
#92165=CARTESIAN_POINT('Ctrl Pts',(-1.98696804917734,-1.29511207146093,
7.93832299433738));
#92166=CARTESIAN_POINT('Ctrl Pts',(-1.99383090314272,-1.28452156596603,
7.9374572047261));
#92167=CARTESIAN_POINT('Ctrl Pts',(-2.00406863443511,-1.26844332110184,
7.93615759046452));
#92168=CARTESIAN_POINT('Ctrl Pts',(-2.00750608479414,-1.26299599064703,
7.93571982015363));
#92169=CARTESIAN_POINT('Ctrl Pts',(-2.01363190087266,-1.25320020933298,
7.93493723099745));
#92170=CARTESIAN_POINT('Ctrl Pts',(-2.01632842653346,-1.24885702738557,
7.93459188434299));
#92171=CARTESIAN_POINT('Ctrl Pts',(-2.02219322290946,-1.23934233036292,
7.93383889343509));
#92172=CARTESIAN_POINT('Ctrl Pts',(-2.02535570431436,-1.23416737750688,
7.93343162787353));
#92173=CARTESIAN_POINT('Ctrl Pts',(-2.03431085518383,-1.21938641718053,
7.93227468406153));
#92174=CARTESIAN_POINT('Ctrl Pts',(-2.04005537293105,-1.20975120488291,
7.93152806680918));
#92175=CARTESIAN_POINT('Ctrl Pts',(-2.07808902374704,-1.14491641343749,
7.92655199813902));
#92176=CARTESIAN_POINT('Ctrl Pts',(-2.10820591393473,-1.08846548071594,
7.92245040934162));
#92177=CARTESIAN_POINT('Ctrl Pts',(-2.24113877611426,-0.813020374338387,
7.9031862369006));
#92178=CARTESIAN_POINT('Ctrl Pts',(-2.31233108382151,-0.580382811643949,
7.88895642212421));
#92179=CARTESIAN_POINT('Ctrl Pts',(-2.35336661572382,-0.297921456548396,
7.87066208574375));
#92180=CARTESIAN_POINT('Ctrl Pts',(-2.35843608009614,-0.254696857708671,
7.86784093345273));
#92181=CARTESIAN_POINT('Ctrl Pts',(-2.36366943302811,-0.196204919219565,
7.86398302944334));
#92182=CARTESIAN_POINT('Ctrl Pts',(-2.3648794395102,-0.181038055292338,
7.86297906487534));
#92183=CARTESIAN_POINT('Ctrl Pts',(-2.36662986864864,-0.156068839904069,
7.86131983878432));
#92184=CARTESIAN_POINT('Ctrl Pts',(-2.36725551966758,-0.146272750762116,
7.86066726308839));
#92185=CARTESIAN_POINT('Ctrl Pts',(-2.36832248139079,-0.127760882139914,
7.85943090178037));
#92186=CARTESIAN_POINT('Ctrl Pts',(-2.36877653456722,-0.119045976952484,
7.85884752688647));
#92187=CARTESIAN_POINT('Ctrl Pts',(-2.36960235079768,-0.101312545565581,
7.85765766889985));
#92188=CARTESIAN_POINT('Ctrl Pts',(-2.36997074746637,-0.0922940140209736,
7.85705108989024));
#92189=CARTESIAN_POINT('Ctrl Pts',(-2.37074905561044,-0.0701403924997397,
7.85555736416993));
#92190=CARTESIAN_POINT('Ctrl Pts',(-2.37110128939492,-0.0570037069790923,
7.8546684259942));
#92191=CARTESIAN_POINT('Ctrl Pts',(-2.371620102822,-0.0289566246185791,
7.85276350603436));
#92192=CARTESIAN_POINT('Ctrl Pts',(-2.37175527357193,-0.0140463379688937,
7.85174658567412));
#92193=CARTESIAN_POINT('Ctrl Pts',(-2.37174984266889,0.000863886614090527,
7.85072532400096));
#92194=CARTESIAN_POINT('Ctrl Pts',(-2.37174984331459,0.000862112068730794,
7.85072544554674));
#92195=CARTESIAN_POINT('Ctrl Pts',(-2.37172894381041,0.0583585763559521,
7.84678728115609));
#92196=CARTESIAN_POINT('Ctrl Pts',(-2.36961730594813,0.115801390350126,
7.8427874875871));
#92197=CARTESIAN_POINT('Ctrl Pts',(-2.36542646504704,0.173077153186224,
7.83873326832757));
#92198=CARTESIAN_POINT('',(-2.3717492188972,0.0019248793473943,7.65246806900456));
#92199=CARTESIAN_POINT('Ctrl Pts',(-2.36542649614281,0.173076728203254,
7.64172477676247));
#92200=CARTESIAN_POINT('Ctrl Pts',(-2.36959267265298,0.11613791033294,7.64536496783797));
#92201=CARTESIAN_POINT('Ctrl Pts',(-2.37170285684927,0.0590500966492621,
7.64893264892313));
#92202=CARTESIAN_POINT('Ctrl Pts',(-2.3717492188972,0.00192487934712052,
7.65246806900458));
#92203=CARTESIAN_POINT('Ctrl Pts',(-2.37174921666776,0.00192762440904576,
7.65246789911553));
#92204=CARTESIAN_POINT('Ctrl Pts',(-2.37192860088264,-0.218786726951562,
7.66612768429334));
#92205=CARTESIAN_POINT('Ctrl Pts',(-2.34130138544471,-0.43844049729506,
7.67932270627705));
#92206=CARTESIAN_POINT('Ctrl Pts',(-2.27218153710609,-0.680707332112222,
7.69562531301407));
#92207=CARTESIAN_POINT('Ctrl Pts',(-2.26303122594774,-0.710535664963517,
7.69766164811093));
#92208=CARTESIAN_POINT('Ctrl Pts',(-2.24921652196154,-0.752591482057263,
7.70057829124152));
#92209=CARTESIAN_POINT('Ctrl Pts',(-2.24503496904491,-0.764975083100874,
7.7014427783787));
#92210=CARTESIAN_POINT('Ctrl Pts',(-2.23764523888286,-0.786277092369439,
7.70293993684019));
#92211=CARTESIAN_POINT('Ctrl Pts',(-2.23448553535929,-0.795212090500742,
7.70357099320596));
#92212=CARTESIAN_POINT('Ctrl Pts',(-2.22832899839354,-0.812295085289945,
7.70478354842714));
#92213=CARTESIAN_POINT('Ctrl Pts',(-2.22534080625714,-0.820446051367029,
7.70536475100197));
#92214=CARTESIAN_POINT('Ctrl Pts',(-2.21821441266406,-0.839559516379358,
7.70673394995192));
#92215=CARTESIAN_POINT('Ctrl Pts',(-2.2140396190855,-0.850508035601309,
7.7075231597099));
#92216=CARTESIAN_POINT('Ctrl Pts',(-2.19930539126171,-0.888305243557391,
7.71026505002614));
#92217=CARTESIAN_POINT('Ctrl Pts',(-2.18833768312951,-0.914990965097235,
7.71223135801434));
#92218=CARTESIAN_POINT('Ctrl Pts',(-2.10917336351463,-1.09803653285982,
7.72593677724298));
#92219=CARTESIAN_POINT('Ctrl Pts',(-2.02477969696945,-1.24681300971397,
7.73824124994806));
#92220=CARTESIAN_POINT('Ctrl Pts',(-1.86186624881698,-1.47322976706895,
7.75860934982358));
#92221=CARTESIAN_POINT('Ctrl Pts',(-1.79258339652364,-1.55679129554724,
7.76654784187988));
#92222=CARTESIAN_POINT('Ctrl Pts',(-1.69595415681631,-1.65829537400793,
7.77652525571581));
#92223=CARTESIAN_POINT('Ctrl Pts',(-1.67362526589386,-1.68082798967231,
7.77876311605866));
#92224=CARTESIAN_POINT('Ctrl Pts',(-1.64060205390072,-1.71284169736762,
7.78196812842707));
#92225=CARTESIAN_POINT('Ctrl Pts',(-1.630264365805,-1.72268392360885,7.78295710178009));
#92226=CARTESIAN_POINT('Ctrl Pts',(-1.61176502101676,-1.73998095802047,
7.78470066641895));
#92227=CARTESIAN_POINT('Ctrl Pts',(-1.60363901473207,-1.7474730726551,7.78545776194948));
#92228=CARTESIAN_POINT('Ctrl Pts',(-1.59091844608578,-1.7590378751639,7.78662894665626));
#92229=CARTESIAN_POINT('Ctrl Pts',(-1.58636007589046,-1.76314986888534,
7.78704588081393));
#92230=CARTESIAN_POINT('Ctrl Pts',(-1.5817632737829,-1.76726427257486,7.7874635243222));
#92231=CARTESIAN_POINT('Ctrl Pts',(-1.58174082104448,-1.76728436830338,
7.78746556420386));
#92232=CARTESIAN_POINT('Ctrl Pts',(-1.58169573582957,-1.76732471908279,
7.78746966016217));
#92233=CARTESIAN_POINT('Ctrl Pts',(-1.58167310334443,-1.76734497412907,
7.78747171623854));
#92234=CARTESIAN_POINT('Ctrl Pts',(-1.58162765563735,-1.76738564619058,
7.78747584485546));
#92235=CARTESIAN_POINT('Ctrl Pts',(-1.58160484041494,-1.76740606319358,
7.78747791739495));
#92236=CARTESIAN_POINT('Ctrl Pts',(-1.58155902418017,-1.76744706186265,
7.78748207921214));
#92237=CARTESIAN_POINT('Ctrl Pts',(-1.58153602315364,-1.76746764352845,
7.78748416848999));
#92238=CARTESIAN_POINT('Ctrl Pts',(-1.58148983220547,-1.76750897426265,
7.78748836406255));
#92239=CARTESIAN_POINT('Ctrl Pts',(-1.58146664225343,-1.76752972334497,
7.78749047035887));
#92240=CARTESIAN_POINT('Ctrl Pts',(-1.58142007026705,-1.76757139172394,
7.78749470025433));
#92241=CARTESIAN_POINT('Ctrl Pts',(-1.58139668821649,-1.76759231102148,
7.78749682385378));
#92242=CARTESIAN_POINT('Ctrl Pts',(-1.58134972876095,-1.76763432271736,
7.78750108864911));
#92243=CARTESIAN_POINT('Ctrl Pts',(-1.58132615137002,-1.76765541508917,
7.78750322984251));
#92244=CARTESIAN_POINT('Ctrl Pts',(-1.57743751763007,-1.77113405301657,
7.78785636601053));
#92245=CARTESIAN_POINT('Ctrl Pts',(-1.57356118211384,-1.77457886918644,
7.78820639012734));
#92246=CARTESIAN_POINT('Ctrl Pts',(-1.56478425285835,-1.78232736593142,
7.78899446159449));
#92247=CARTESIAN_POINT('Ctrl Pts',(-1.55987719428778,-1.78662355818461,
7.78943195334877));
#92248=CARTESIAN_POINT('Ctrl Pts',(-1.54532731845717,-1.79925651951637,
7.79072022669069));
#92249=CARTESIAN_POINT('Ctrl Pts',(-1.53563475392933,-1.80753602028861,
7.79156692120089));
#92250=CARTESIAN_POINT('Ctrl Pts',(-1.44567199322042,-1.88313726106466,
7.79932543103659));
#92251=CARTESIAN_POINT('Ctrl Pts',(-1.36107906131502,-1.94515894084533,
7.80589398461622));
#92252=CARTESIAN_POINT('Ctrl Pts',(-1.13573497658213,-2.0884515400315,7.82239169432572));
#92253=CARTESIAN_POINT('Ctrl Pts',(-0.990252594035798,-2.16123178770184,
7.83216958849789));
#92254=CARTESIAN_POINT('Ctrl Pts',(-0.769153371904203,-2.24479261153157,
7.84705451056726));
#92255=CARTESIAN_POINT('Ctrl Pts',(-0.698642810193412,-2.26772733455831,
7.85179919609393));
#92256=CARTESIAN_POINT('Ctrl Pts',(-0.610046009439683,-2.29202040896952,
7.85781694461759));
#92257=CARTESIAN_POINT('Ctrl Pts',(-0.592860705422668,-2.29652560277634,
7.85898667980493));
#92258=CARTESIAN_POINT('Ctrl Pts',(-0.565470826512183,-2.30337804242389,
7.86085562220351));
#92259=CARTESIAN_POINT('Ctrl Pts',(-0.555298291578314,-2.30585157010133,
7.86155074862283));
#92260=CARTESIAN_POINT('Ctrl Pts',(-0.536086811353472,-2.3103884844237,
7.86286558426991));
#92261=CARTESIAN_POINT('Ctrl Pts',(-0.527051467169752,-2.31246638137894,
7.86348481334003));
#92262=CARTESIAN_POINT('Ctrl Pts',(-0.50663728074524,-2.31703526280935,
7.86488590661512));
#92263=CARTESIAN_POINT('Ctrl Pts',(-0.495251872755064,-2.31949548769823,
7.86566874061982));
#92264=CARTESIAN_POINT('Ctrl Pts',(-0.465980398223726,-2.32559529631513,
7.86768522608391));
#92265=CARTESIAN_POINT('Ctrl Pts',(-0.448069880514236,-2.32911239819154,
7.86892274457843));
#92266=CARTESIAN_POINT('Ctrl Pts',(-0.328360836412189,-2.35118789048866,
7.87722016717372));
#92267=CARTESIAN_POINT('Ctrl Pts',(-0.225496517827373,-2.36327129190197,
7.8844833949992));
#92268=CARTESIAN_POINT('Ctrl Pts',(0.0538466149963302,-2.37768121172518,
7.90454373892599));
#92269=CARTESIAN_POINT('Ctrl Pts',(0.230325737271339,-2.36711033042453,
7.91761175438503));
#92270=CARTESIAN_POINT('Ctrl Pts',(0.443561688708806,-2.33024959707788,
7.93312658520144));
#92271=CARTESIAN_POINT('Ctrl Pts',(0.48294823245229,-2.32240641399065,7.93597778851135));
#92272=CARTESIAN_POINT('Ctrl Pts',(0.538527055449659,-2.30986354852391,
7.93996398265532));
#92273=CARTESIAN_POINT('Ctrl Pts',(0.554895914538838,-2.30598602851345,
7.94113334416176));
#92274=CARTESIAN_POINT('Ctrl Pts',(0.583741168348567,-2.29882810880787,
7.9431841770056));
#92275=CARTESIAN_POINT('Ctrl Pts',(0.596234479738183,-2.29561950015035,
7.94406914674796));
#92276=CARTESIAN_POINT('Ctrl Pts',(0.614952451714953,-2.29064911681129,
7.94538948207015));
#92277=CARTESIAN_POINT('Ctrl Pts',(0.621196840156112,-2.28896360445724,
7.94582901771423));
#92278=CARTESIAN_POINT('Ctrl Pts',(0.631949179193921,-2.28601404522876,
7.94658415966411));
#92279=CARTESIAN_POINT('Ctrl Pts',(0.636460340536291,-2.28476217937959,
7.94690045797753));
#92280=CARTESIAN_POINT('Ctrl Pts',(0.646750228662881,-2.2818738514643,7.94762072521921));
#92281=CARTESIAN_POINT('Ctrl Pts',(0.652526458891404,-2.28022879438711,
7.94802419000673));
#92282=CARTESIAN_POINT('Ctrl Pts',(0.668309623487413,-2.27566889989062,
7.94912444201026));
#92283=CARTESIAN_POINT('Ctrl Pts',(0.678303840366494,-2.27270996938229,
7.94981873144103));
#92284=CARTESIAN_POINT('Ctrl Pts',(0.728555636433139,-2.257471191399,7.95329903446736));
#92285=CARTESIAN_POINT('Ctrl Pts',(0.768503642656891,-2.24418630722255,
7.956031232103));
#92286=CARTESIAN_POINT('Ctrl Pts',(1.03125768702466,-2.14896609673899,7.97390302597769));
#92287=CARTESIAN_POINT('Ctrl Pts',(1.2410444322419,-2.03503842775949,7.98782459160855));
#92288=CARTESIAN_POINT('Ctrl Pts',(1.48381414625764,-1.85147833532065,8.007064662004));
#92289=CARTESIAN_POINT('Ctrl Pts',(1.53545725290334,-1.80887980730665,8.0113615115092));
#92290=CARTESIAN_POINT('Ctrl Pts',(1.59803648104308,-1.75264772171217,8.01687589567338));
#92291=CARTESIAN_POINT('Ctrl Pts',(1.61071991894831,-1.74099854906542,8.01801027817766));
#92292=CARTESIAN_POINT('Ctrl Pts',(1.6308206832079,-1.72212922594299,8.01983577216126));
#92293=CARTESIAN_POINT('Ctrl Pts',(1.63831971673366,-1.71499669725583,8.02052312930039));
#92294=CARTESIAN_POINT('Ctrl Pts',(1.65246244522582,-1.7013677637352,8.02183165162688));
#92295=CARTESIAN_POINT('Ctrl Pts',(1.65911513084298,-1.69488093349532,8.02245239351364));
#92296=CARTESIAN_POINT('Ctrl Pts',(1.67416254690773,-1.6800351692993,8.02386847330971));
#92297=CARTESIAN_POINT('Ctrl Pts',(1.68253305669345,-1.6716521491691,8.02466486537424));
#92298=CARTESIAN_POINT('Ctrl Pts',(1.70410035296448,-1.64972652268232,8.02673971882568));
#92299=CARTESIAN_POINT('Ctrl Pts',(1.71719839197827,-1.63608840195997,8.02802243360856));
#92300=CARTESIAN_POINT('Ctrl Pts',(1.83688724967364,-1.50844366412966,8.03995840314521));
#92301=CARTESIAN_POINT('Ctrl Pts',(1.93212338863065,-1.38435502843599,8.05109492036227));
#92302=CARTESIAN_POINT('Ctrl Pts',(2.0743639600938,-1.15546021201152,8.0707105500214));
#92303=CARTESIAN_POINT('Ctrl Pts',(2.12726296739755,-1.05490624095178,8.07905072621117));
#92304=CARTESIAN_POINT('Ctrl Pts',(2.20010305575462,-0.888478979701357,
8.09212713522253));
#92305=CARTESIAN_POINT('Ctrl Pts',(2.2247410068928,-0.824850162908237,8.09696539607802));
#92306=CARTESIAN_POINT('Ctrl Pts',(2.25029175812542,-0.749344650721646,
8.10245456541853));
#92307=CARTESIAN_POINT('Ctrl Pts',(2.253899987388,-0.738420789667044,8.10324265207015));
#92308=CARTESIAN_POINT('Ctrl Pts',(2.25932372613631,-0.721590282000285,
8.10444710367688));
#92309=CARTESIAN_POINT('Ctrl Pts',(2.26119581323298,-0.715702264209388,
8.1048666439587));
#92310=CARTESIAN_POINT('Ctrl Pts',(2.26459672681886,-0.704859287063302,
8.10563579782369));
#92311=CARTESIAN_POINT('Ctrl Pts',(2.2661323075919,-0.699906647503912,8.10598579062392));
#92312=CARTESIAN_POINT('Ctrl Pts',(2.26955931475563,-0.688724157550284,
8.10677307175319));
#92313=CARTESIAN_POINT('Ctrl Pts',(2.27144133725613,-0.682491540135342,
8.10720980953822));
#92314=CARTESIAN_POINT('Ctrl Pts',(2.27691692184927,-0.664084719363218,
8.10849378687591));
#92315=CARTESIAN_POINT('Ctrl Pts',(2.28043851452818,-0.651889087697727,
8.10933697980915));
#92316=CARTESIAN_POINT('Ctrl Pts',(2.31616581103711,-0.524328312352295,
8.11808383156427));
#92317=CARTESIAN_POINT('Ctrl Pts',(2.33969111922926,-0.406691781487523,
8.12553671988815));
#92318=CARTESIAN_POINT('Ctrl Pts',(2.3699649896917,-0.159019687854613,8.14089061698964));
#92319=CARTESIAN_POINT('Ctrl Pts',(2.37511420731575,-0.0292037167191159,
8.14875802649651));
#92320=CARTESIAN_POINT('Ctrl Pts',(2.36711062306637,0.159731648666867,8.16057761604705));
#92321=CARTESIAN_POINT('Ctrl Pts',(2.36236770825756,0.218963284601689,8.16433398724319));
#92322=CARTESIAN_POINT('Ctrl Pts',(2.3508003038964,0.316987426391103,8.17068231363855));
#92323=CARTESIAN_POINT('Ctrl Pts',(2.34522436061761,0.355900976238753,8.17323716232165));
#92324=CARTESIAN_POINT('Ctrl Pts',(2.33630524755926,0.408754540364765,8.17676280494017));
#92325=CARTESIAN_POINT('Ctrl Pts',(2.3337987543899,0.422830749852764,8.1777071672099));
#92326=CARTESIAN_POINT('Ctrl Pts',(2.32937537323449,0.446433471574632,8.17930011228693));
#92327=CARTESIAN_POINT('Ctrl Pts',(2.32752690736601,0.455972548133588,8.17994650763121));
#92328=CARTESIAN_POINT('Ctrl Pts',(2.32376397221013,0.474772030843289,8.18122568152593));
#92329=CARTESIAN_POINT('Ctrl Pts',(2.32185263144854,0.484032884386455,8.18185834925603));
#92330=CARTESIAN_POINT('Ctrl Pts',(2.31752246192929,0.504397504801937,8.18325527716475));
#92331=CARTESIAN_POINT('Ctrl Pts',(2.31507911671761,0.515495761283541,8.1840203096959));
#92332=CARTESIAN_POINT('Ctrl Pts',(2.30620814969534,0.554454267931089,8.186719255279));
#92333=CARTESIAN_POINT('Ctrl Pts',(2.29935680906721,0.582214483461349,8.18866667231378));
#92334=CARTESIAN_POINT('Ctrl Pts',(2.24384275921103,0.790855894249398,8.20349341156407));
#92335=CARTESIAN_POINT('Ctrl Pts',(2.17441525541434,0.965491793292687,8.21706902191983));
#92336=CARTESIAN_POINT('Ctrl Pts',(2.02036184227032,1.24974074686779,8.24068413450164));
#92337=CARTESIAN_POINT('Ctrl Pts',(1.94534172660645,1.36358655212556,8.25060977062618));
#92338=CARTESIAN_POINT('Ctrl Pts',(1.85282875956584,1.48067409651524,8.26091026115462));
#92339=CARTESIAN_POINT('Ctrl Pts',(1.8446095353432,1.49090102765728,8.26181064853863));
#92340=CARTESIAN_POINT('Ctrl Pts',(1.83218401506842,1.50610165938006,8.26314931483075));
#92341=CARTESIAN_POINT('Ctrl Pts',(1.82804158145697,1.51112688167012,8.2635919330658));
#92342=CARTESIAN_POINT('Ctrl Pts',(1.82088280583333,1.51973873750585,8.26435047673394));
#92343=CARTESIAN_POINT('Ctrl Pts',(1.81787648893822,1.52333354693099,8.26466711330541));
#92344=CARTESIAN_POINT('Ctrl Pts',(1.81101366923395,1.53149052771232,8.26538558280907));
#92345=CARTESIAN_POINT('Ctrl Pts',(1.80715057696887,1.5360470503172,8.26578692680853));
#92346=CARTESIAN_POINT('Ctrl Pts',(1.79659103315127,1.54840707065965,8.26687577904613));
#92347=CARTESIAN_POINT('Ctrl Pts',(1.78986088544994,1.55618180725455,8.2675608742569));
#92348=CARTESIAN_POINT('Ctrl Pts',(1.75641457487899,1.59431530098481,8.27092347074607));
#92349=CARTESIAN_POINT('Ctrl Pts',(1.72897372689929,1.62403317956031,8.27355139607813));
#92350=CARTESIAN_POINT('Ctrl Pts',(1.53399854410094,1.82464016462,8.29146545822072));
#92351=CARTESIAN_POINT('Ctrl Pts',(1.34219277605546,1.97002747896156,8.30548813971534));
#92352=CARTESIAN_POINT('Ctrl Pts',(1.07304659711696,2.11618681682525,8.3248494805174));
#92353=CARTESIAN_POINT('Ctrl Pts',(1.01292294352818,2.14561446678293,8.32914595517858));
#92354=CARTESIAN_POINT('Ctrl Pts',(0.935866155060962,2.17936898076047,8.33465991717734));
#92355=CARTESIAN_POINT('Ctrl Pts',(0.920018041369216,2.18610644572128,8.33579426824626));
#92356=CARTESIAN_POINT('Ctrl Pts',(0.894530480204811,2.19661566720407,8.33761972359626));
#92357=CARTESIAN_POINT('Ctrl Pts',(0.884937067056213,2.20049802339901,8.3383070738224));
#92358=CARTESIAN_POINT('Ctrl Pts',(0.866682794901249,2.20774666431054,8.33961559072481));
#92359=CARTESIAN_POINT('Ctrl Pts',(0.858026940167629,2.21112509064001,8.34023633415188));
#92360=CARTESIAN_POINT('Ctrl Pts',(0.838290503027163,2.21869498591577,8.34165242822353));
#92361=CARTESIAN_POINT('Ctrl Pts',(0.827197991733631,2.22285444453782,8.34244883310317));
#92362=CARTESIAN_POINT('Ctrl Pts',(0.798319962038955,2.23343700927993,8.34452374195813));
#92363=CARTESIAN_POINT('Ctrl Pts',(0.780488254253281,2.23973071707422,8.34580649970427));
#92364=CARTESIAN_POINT('Ctrl Pts',(0.614948161600429,2.295941235759,8.35773166301482));
#92365=CARTESIAN_POINT('Ctrl Pts',(0.46275844444034,2.33138256170428,8.36885627705974));
#92366=CARTESIAN_POINT('Ctrl Pts',(0.195684482133528,2.36638706698536,8.38846172109897));
#92367=CARTESIAN_POINT('Ctrl Pts',(0.0822331865416702,2.37303995511256,
8.3968039434546));
#92368=CARTESIAN_POINT('Ctrl Pts',(-0.0995696787147946,2.37064358595411,
8.40989181736451));
#92369=CARTESIAN_POINT('Ctrl Pts',(-0.167816555524349,2.36679207601819,
8.41473907387445));
#92370=CARTESIAN_POINT('Ctrl Pts',(-0.247260229332893,2.35885414806334,
8.42023708203639));
#92371=CARTESIAN_POINT('Ctrl Pts',(-0.258703727371872,2.35762654120908,
8.42102550232202));
#92372=CARTESIAN_POINT('Ctrl Pts',(-0.27627728828819,2.35561183287246,8.42223035499623));
#92373=CARTESIAN_POINT('Ctrl Pts',(-0.282413767332848,2.35488401273431,
8.42264996593309));
#92374=CARTESIAN_POINT('Ctrl Pts',(-0.293694126550658,2.35350137222549,
8.4234191867187));
#92375=CARTESIAN_POINT('Ctrl Pts',(-0.298838685741296,2.35285366948261,
8.42376917626327));
#92376=CARTESIAN_POINT('Ctrl Pts',(-0.310436767805653,2.35135481063076,
8.42455637198977));
#92377=CARTESIAN_POINT('Ctrl Pts',(-0.31688892664277,2.35049395723892,8.42499302817472));
#92378=CARTESIAN_POINT('Ctrl Pts',(-0.335906663700115,2.34787686006161,
8.42627654097232));
#92379=CARTESIAN_POINT('Ctrl Pts',(-0.348462034237727,2.34604630497996,
8.42711935532858));
#92380=CARTESIAN_POINT('Ctrl Pts',(-0.4575920556738,2.32923987488406,8.43441013059238));
#92381=CARTESIAN_POINT('Ctrl Pts',(-0.553183364220935,2.30840683760629,
8.44055992959317));
#92382=CARTESIAN_POINT('Ctrl Pts',(-0.790172107251115,2.24118347439208,
8.45581457527896));
#92383=CARTESIAN_POINT('Ctrl Pts',(-0.92898848343422,2.1872943136355,8.4647755324396));
#92384=CARTESIAN_POINT('Ctrl Pts',(-1.11672165895345,2.09329794651781,8.47788145550354));
#92385=CARTESIAN_POINT('Ctrl Pts',(-1.17050135962174,2.06370764981427,8.48175709537557));
#92386=CARTESIAN_POINT('Ctrl Pts',(-1.24622957730996,2.0181279808486,8.48743803975325));
#92387=CARTESIAN_POINT('Ctrl Pts',(-1.26914793891468,2.003794431307,8.48918800053778));
#92388=CARTESIAN_POINT('Ctrl Pts',(-1.30980528736982,1.97738926464679,8.49235171782997));
#92389=CARTESIAN_POINT('Ctrl Pts',(-1.32763511780299,1.96546257635707,8.49376016772213));
#92390=CARTESIAN_POINT('Ctrl Pts',(-1.35457147497543,1.94691060670137,8.4959216170941));
#92391=CARTESIAN_POINT('Ctrl Pts',(-1.36379697557336,1.94045937687495,8.49666802771135));
#92392=CARTESIAN_POINT('Ctrl Pts',(-1.3797838419841,1.92910972120071,8.4979723906345));
#92393=CARTESIAN_POINT('Ctrl Pts',(-1.38656597413737,1.92424077582012,8.49852920472557));
#92394=CARTESIAN_POINT('Ctrl Pts',(-1.40176556114031,1.91320679333387,8.49978499549225));
#92395=CARTESIAN_POINT('Ctrl Pts',(-1.41016828185193,1.90702184918722,8.50048473607025));
#92396=CARTESIAN_POINT('Ctrl Pts',(-1.43263859721201,1.89025253199371,8.50237100638169));
#92397=CARTESIAN_POINT('Ctrl Pts',(-1.44662937794588,1.87956681142386,8.5035614835849));
#92398=CARTESIAN_POINT('Ctrl Pts',(-1.51028752365827,1.82981491280577,8.50905344744782));
#92399=CARTESIAN_POINT('Ctrl Pts',(-1.55849601299402,1.78893261151242,8.51342670799578));
#92400=CARTESIAN_POINT('Ctrl Pts',(-1.76462150752,1.59947094617974,8.53311995723026));
#92401=CARTESIAN_POINT('Ctrl Pts',(-1.90335367581959,1.43157781383691,8.54923751710816));
#92402=CARTESIAN_POINT('Ctrl Pts',(-2.04001914724145,1.21052969990413,8.56790986979901));
#92403=CARTESIAN_POINT('Ctrl Pts',(-2.06170774698637,1.17321008760432,8.57098062684834));
#92404=CARTESIAN_POINT('Ctrl Pts',(-2.09082889556275,1.11979688937596,8.57524215404591));
#92405=CARTESIAN_POINT('Ctrl Pts',(-2.09911716692401,1.10418191730466,8.57647232002537));
#92406=CARTESIAN_POINT('Ctrl Pts',(-2.11338497739413,1.07656019193318,8.5786191602735));
#92407=CARTESIAN_POINT('Ctrl Pts',(-2.11943861144178,1.06459283434656,8.57953978729675));
#92408=CARTESIAN_POINT('Ctrl Pts',(-2.12830648222711,1.04668655750896,8.58090247118137));
#92409=CARTESIAN_POINT('Ctrl Pts',(-2.13119794544306,1.04078650642126,8.58134909413646));
#92410=CARTESIAN_POINT('Ctrl Pts',(-2.13632888775373,1.03020574067668,8.58214569343673));
#92411=CARTESIAN_POINT('Ctrl Pts',(-2.13857755262276,1.02552963775957,8.582496228079));
#92412=CARTESIAN_POINT('Ctrl Pts',(-2.14344956230167,1.01531257161977,8.58325881612217));
#92413=CARTESIAN_POINT('Ctrl Pts',(-2.14606677335011,1.00976881052047,8.58367049097765));
#92414=CARTESIAN_POINT('Ctrl Pts',(-2.1533067591757,0.994277817243223,8.5848151531173));
#92415=CARTESIAN_POINT('Ctrl Pts',(-2.15788214205157,0.984308411828276,
8.58554530008407));
#92416=CARTESIAN_POINT('Ctrl Pts',(-2.18273764902182,0.929143831821751,
8.58955162580048));
#92417=CARTESIAN_POINT('Ctrl Pts',(-2.20166883701195,0.883349916415549,
8.59275267570003));
#92418=CARTESIAN_POINT('Ctrl Pts',(-2.27089344763987,0.699811890386293,
8.60522293157261));
#92419=CARTESIAN_POINT('Ctrl Pts',(-2.30980639830815,0.558117742458064,
8.61408114242414));
#92420=CARTESIAN_POINT('Ctrl Pts',(-2.34950444186218,0.334032260774997,
8.62807067485331));
#92421=CARTESIAN_POINT('Ctrl Pts',(-2.35952658917613,0.253710412752258,
8.63307805857323));
#92422=CARTESIAN_POINT('Ctrl Pts',(-2.36542651242649,0.173076505655319,
8.63818628587103));
#92423=CARTESIAN_POINT('Origin',(0.,0.,-1.84858989190503));
#92424=CARTESIAN_POINT('',(-2.36542649454068,0.173076750099461,9.83480414144792));
#92425=CARTESIAN_POINT('',(-2.36542652525385,0.173076330344439,9.63839747301829));
#92426=CARTESIAN_POINT('',(-2.36542649454111,0.173076750093529,-1.84858989190503));
#92427=CARTESIAN_POINT('Ctrl Pts',(-2.36542649454068,0.173076750099461,
9.83480414144792));
#92428=CARTESIAN_POINT('Ctrl Pts',(-2.36520189196563,0.176146376039912,
9.83460373033529));
#92429=CARTESIAN_POINT('Ctrl Pts',(-2.36497131147088,0.179215601897425,
9.83440358283108));
#92430=CARTESIAN_POINT('Ctrl Pts',(-2.35354069918992,0.327502370317676,
9.82474474557395));
#92431=CARTESIAN_POINT('Ctrl Pts',(-2.32899219074479,0.471400117259506,
9.8158733937563));
#92432=CARTESIAN_POINT('Ctrl Pts',(-2.26306492284725,0.718177746968243,
9.80022191436453));
#92433=CARTESIAN_POINT('Ctrl Pts',(-2.22741598848653,0.822105685596256,
9.79348664564198));
#92434=CARTESIAN_POINT('Ctrl Pts',(-2.16708713367593,0.964872791272013,
9.78369709492289));
#92435=CARTESIAN_POINT('Ctrl Pts',(-2.14828304071982,1.00604459915777,9.78080854905148));
#92436=CARTESIAN_POINT('Ctrl Pts',(-2.11419972312488,1.07535132719678,9.77581374263377));
#92437=CARTESIAN_POINT('Ctrl Pts',(-2.09950736217764,1.10376157850436,9.77372705491302));
#92438=CARTESIAN_POINT('Ctrl Pts',(-2.07799984048058,1.14336608750461,9.77075806051486));
#92439=CARTESIAN_POINT('Ctrl Pts',(-2.07165910538677,1.15481508761203,9.76989256217579));
#92440=CARTESIAN_POINT('Ctrl Pts',(-2.06061226594895,1.17437775826175,9.76840097692716));
#92441=CARTESIAN_POINT('Ctrl Pts',(-2.05595214116193,1.18251715361473,9.76777655166614));
#92442=CARTESIAN_POINT('Ctrl Pts',(-2.04696906422128,1.19799341717992,9.76658184145591));
#92443=CARTESIAN_POINT('Ctrl Pts',(-2.04265462618595,1.20533507885905,9.76601187248871));
#92444=CARTESIAN_POINT('Ctrl Pts',(-2.03138946095268,1.22427024845548,9.7645333909355));
#92445=CARTESIAN_POINT('Ctrl Pts',(-2.02437906953714,1.23582771976395,9.76362271000136));
#92446=CARTESIAN_POINT('Ctrl Pts',(-2.00405767501777,1.26869306460819,9.76100896875709));
#92447=CARTESIAN_POINT('Ctrl Pts',(-1.99050672531021,1.28984966128162,9.75929712727667));
#92448=CARTESIAN_POINT('Ctrl Pts',(-1.86907764731955,1.47296072131843,9.74421756642246));
#92449=CARTESIAN_POINT('Ctrl Pts',(-1.74200303042382,1.62125244916112,9.73008637235316));
#92450=CARTESIAN_POINT('Ctrl Pts',(-1.50247742827674,1.83972176791455,9.7064085107244));
#92451=CARTESIAN_POINT('Ctrl Pts',(-1.39964843200042,1.91911620584917,9.69696848790556));
#92452=CARTESIAN_POINT('Ctrl Pts',(-1.28292133501019,1.99484330885392,9.68736024983176));
#92453=CARTESIAN_POINT('Ctrl Pts',(-1.27497999778377,1.99992824651159,9.68671178875491));
#92454=CARTESIAN_POINT('Ctrl Pts',(-1.26021409805653,2.00925933778014,9.68551599387643));
#92455=CARTESIAN_POINT('Ctrl Pts',(-1.25339790479187,2.01351840230391,9.68496787610201));
#92456=CARTESIAN_POINT('Ctrl Pts',(-1.24203767474033,2.02053674431366,9.68406095336158));
#92457=CARTESIAN_POINT('Ctrl Pts',(-1.23750584331412,2.02331549932154,9.68370089515491));
#92458=CARTESIAN_POINT('Ctrl Pts',(-1.22860481534658,2.02873219466124,9.68299714712032));
#92459=CARTESIAN_POINT('Ctrl Pts',(-1.22423638900692,2.03137130400507,9.68265338328671));
#92460=CARTESIAN_POINT('Ctrl Pts',(-1.21327839092734,2.03794320251537,9.68179502696464));
#92461=CARTESIAN_POINT('Ctrl Pts',(-1.20667811319793,2.04185819434838,9.68128158563876));
#92462=CARTESIAN_POINT('Ctrl Pts',(-1.18403173280879,2.05514286081245,9.67953166228116));
#92463=CARTESIAN_POINT('Ctrl Pts',(-1.16789408199821,2.06435626503,9.67830476949922));
#92464=CARTESIAN_POINT('Ctrl Pts',(-1.0206219417993,2.14615790831986,9.66727346053435));
#92465=CARTESIAN_POINT('Ctrl Pts',(-0.882970506837756,2.2063633660639,9.65812785016056));
#92466=CARTESIAN_POINT('Ctrl Pts',(-0.625473537362864,2.2909934830777,9.6415209574469));
#92467=CARTESIAN_POINT('Ctrl Pts',(-0.507689059251745,2.31993901576067,
9.63409869145891));
#92468=CARTESIAN_POINT('Ctrl Pts',(-0.34699157199473,2.3466020146696,9.62377954905083));
#92469=CARTESIAN_POINT('Ctrl Pts',(-0.305597189333393,2.35235078384599,
9.62110585660863));
#92470=CARTESIAN_POINT('Ctrl Pts',(-0.234172470778824,2.3603530798215,9.61645085986825));
#92471=CARTESIAN_POINT('Ctrl Pts',(-0.204210733580883,2.36313377736749,
9.6144856860689));
#92472=CARTESIAN_POINT('Ctrl Pts',(-0.161464333748262,2.36628200846518,
9.61166069401964));
#92473=CARTESIAN_POINT('Ctrl Pts',(-0.1487162320301,2.36711739172401,9.61081552563933));
#92474=CARTESIAN_POINT('Ctrl Pts',(-0.126655034203364,2.36838414830745,
9.60934801565149));
#92475=CARTESIAN_POINT('Ctrl Pts',(-0.117344903516852,2.36886368138811,
9.60872719694399));
#92476=CARTESIAN_POINT('Ctrl Pts',(-0.0994612697117868,2.36967912039415,
9.60753167908212));
#92477=CARTESIAN_POINT('Ctrl Pts',(-0.0908882804715545,2.37002341653476,
9.60695725319674));
#92478=CARTESIAN_POINT('Ctrl Pts',(-0.0706803264661093,2.37072517444266,
9.60560003110327));
#92479=CARTESIAN_POINT('Ctrl Pts',(-0.0590443128458333,2.37104350908495,
9.60481602069325));
#92480=CARTESIAN_POINT('Ctrl Pts',(-0.018453770702516,2.37185499610628,
9.60207210368493));
#92481=CARTESIAN_POINT('Ctrl Pts',(0.0105060580608178,2.3719034881719,9.60009839474749));
#92482=CARTESIAN_POINT('Ctrl Pts',(0.199348752340831,2.36876130716535,9.58711812374626));
#92483=CARTESIAN_POINT('Ctrl Pts',(0.358530818626417,2.34993788862567,9.57562028805024));
#92484=CARTESIAN_POINT('Ctrl Pts',(0.629010982030408,2.2898219260021,9.55540219832456));
#92485=CARTESIAN_POINT('Ctrl Pts',(0.741403372251917,2.25593944473134,9.54679811897857));
#92486=CARTESIAN_POINT('Ctrl Pts',(0.881642877724792,2.20204298512529,9.53608940688557));
#92487=CARTESIAN_POINT('Ctrl Pts',(0.91220334418794,2.18955994830343,9.53375824717464));
#92488=CARTESIAN_POINT('Ctrl Pts',(0.962276262662096,2.16787618209389,9.52995362663431));
#92489=CARTESIAN_POINT('Ctrl Pts',(0.981940860696813,2.15904029043049,9.5284633827208));
#92490=CARTESIAN_POINT('Ctrl Pts',(1.00862514531156,2.14661022444421,9.52644917482649));
#92491=CARTESIAN_POINT('Ctrl Pts',(1.0157506886507,2.1432476950747,9.52591210702048));
#92492=CARTESIAN_POINT('Ctrl Pts',(1.02767198261674,2.13754925341554,9.52501506167504));
#92493=CARTESIAN_POINT('Ctrl Pts',(1.03247679351684,2.13523258387519,9.52465392047672));
#92494=CARTESIAN_POINT('Ctrl Pts',(1.04157043220184,2.13081015678448,9.52397125208002));
#92495=CARTESIAN_POINT('Ctrl Pts',(1.04586076690678,2.1287076236016,9.52364952299442));
#92496=CARTESIAN_POINT('Ctrl Pts',(1.05708453075358,2.12316515178113,9.52280870418981));
#92497=CARTESIAN_POINT('Ctrl Pts',(1.06400759976011,2.11970417718637,9.52229091402527));
#92498=CARTESIAN_POINT('Ctrl Pts',(1.08798775889966,2.10756894965,9.52049990127624));
#92499=CARTESIAN_POINT('Ctrl Pts',(1.10495727519752,2.09872192508316,9.51923692534458));
#92500=CARTESIAN_POINT('Ctrl Pts',(1.22821083714572,2.03255448285871,9.51008248028603));
#92501=CARTESIAN_POINT('Ctrl Pts',(1.33010087785581,1.96738889500319,9.50261310290126));
#92502=CARTESIAN_POINT('Ctrl Pts',(1.4489786919158,1.8778828294221,9.49347600666313));
#92503=CARTESIAN_POINT('Ctrl Pts',(1.47106272451258,1.8606336674621,9.4917594240051));
#92504=CARTESIAN_POINT('Ctrl Pts',(1.62676629172135,1.73451307769844,9.47948263031945));
#92505=CARTESIAN_POINT('Ctrl Pts',(1.74845382970668,1.61177010573905,9.46890531361234));
#92506=CARTESIAN_POINT('Ctrl Pts',(1.87074092980995,1.45811690787918,9.45612114315037));
#92507=CARTESIAN_POINT('Ctrl Pts',(1.88543076012493,1.4390716878166,9.45454465251164));
#92508=CARTESIAN_POINT('Ctrl Pts',(1.90682099968558,1.4104496440876,9.45218551511266));
#92509=CARTESIAN_POINT('Ctrl Pts',(1.91374467864785,1.40104097727905,9.45141160440398));
#92510=CARTESIAN_POINT('Ctrl Pts',(1.92597251759125,1.38416466384984,9.4500260497854));
#92511=CARTESIAN_POINT('Ctrl Pts',(1.93130349278154,1.37671666289269,9.44941545902557));
#92512=CARTESIAN_POINT('Ctrl Pts',(1.94247806415959,1.36091183212375,9.4481215475961));
#92513=CARTESIAN_POINT('Ctrl Pts',(1.9483111597683,1.35254784153293,9.44743784105016));
#92514=CARTESIAN_POINT('Ctrl Pts',(1.96369811552364,1.33017863186738,9.44561187905386));
#92515=CARTESIAN_POINT('Ctrl Pts',(1.9731559046308,1.31610836617445,9.44446601766467));
#92516=CARTESIAN_POINT('Ctrl Pts',(2.01435077393326,1.25338092329324,9.43936832574352));
#92517=CARTESIAN_POINT('Ctrl Pts',(2.04444230851287,1.20367246493395,9.43535623231626));
#92518=CARTESIAN_POINT('Ctrl Pts',(2.08873433556382,1.12404542988136,9.4289666005604));
#92519=CARTESIAN_POINT('Ctrl Pts',(2.10418634657431,1.09484652142193,9.42663124077175));
#92520=CARTESIAN_POINT('Ctrl Pts',(2.20569757851536,0.892933953617337,9.41053913073493));
#92521=CARTESIAN_POINT('Ctrl Pts',(2.27099862109687,0.7106234248208,9.39620940827867));
#92522=CARTESIAN_POINT('Ctrl Pts',(2.32710144998697,0.462181791152007,9.3779314621572));
#92523=CARTESIAN_POINT('Ctrl Pts',(2.33834956741056,0.401417499436738,9.37356259380762));
#92524=CARTESIAN_POINT('Ctrl Pts',(2.34880872559759,0.329270902366803,9.36854521282627));
#92525=CARTESIAN_POINT('Ctrl Pts',(2.35032698020423,0.318252816124755,9.36778362040301));
#92526=CARTESIAN_POINT('Ctrl Pts',(2.352550647189,0.3012308874422,9.36661462145224));
#92527=CARTESIAN_POINT('Ctrl Pts',(2.35331068267,0.295234530586414,9.36620426648454));
#92528=CARTESIAN_POINT('Ctrl Pts',(2.35467142248465,0.284159647507261,9.36544912624676));
#92529=CARTESIAN_POINT('Ctrl Pts',(2.35527862234446,0.279082111928869,9.36510399286932));
#92530=CARTESIAN_POINT('Ctrl Pts',(2.35661652340815,0.267578858182082,9.36432449836086));
#92531=CARTESIAN_POINT('Ctrl Pts',(2.35733736820994,0.261152098791384,9.36389069458228));
#92532=CARTESIAN_POINT('Ctrl Pts',(2.35913481146385,0.244512694488986,9.3627717312804));
#92533=CARTESIAN_POINT('Ctrl Pts',(2.36017139992501,0.234295729535626,9.3620887433842));
#92534=CARTESIAN_POINT('Ctrl Pts',(2.36642921652624,0.168354501121797,9.35770510325752));
#92535=CARTESIAN_POINT('Ctrl Pts',(2.36974344180738,0.112461846610562,9.35410177303053));
#92536=CARTESIAN_POINT('Ctrl Pts',(2.37140407190246,0.0427710456632706,
9.34969042645262));
#92537=CARTESIAN_POINT('Ctrl Pts',(2.37161196783422,0.029039983881964,9.34882520885645));
#92538=CARTESIAN_POINT('Ctrl Pts',(2.3725930481777,-0.122964073143172,9.3392834176185));
#92539=CARTESIAN_POINT('Ctrl Pts',(2.36139199002595,-0.261055317107764,
9.33093240578155));
#92540=CARTESIAN_POINT('Ctrl Pts',(2.31821498148863,-0.515106691217405,
9.31505383116086));
#92541=CARTESIAN_POINT('Ctrl Pts',(2.2893502809727,-0.631130404778904,9.30759351119729));
#92542=CARTESIAN_POINT('Ctrl Pts',(2.24312793718267,-0.770942248187741,
9.29803877405604));
#92543=CARTESIAN_POINT('Ctrl Pts',(2.23391370119492,-0.797247992177152,
9.29621612283714));
#92544=CARTESIAN_POINT('Ctrl Pts',(2.21993636764402,-0.835005474911228,
9.29356098745198));
#92545=CARTESIAN_POINT('Ctrl Pts',(2.21554344669009,-0.846592490807026,
9.29274081049707));
#92546=CARTESIAN_POINT('Ctrl Pts',(2.20771030289488,-0.866775051649364,
9.29130255072214));
#92547=CARTESIAN_POINT('Ctrl Pts',(2.20431014576016,-0.875385942765652,
9.29068582350849));
#92548=CARTESIAN_POINT('Ctrl Pts',(2.19762632783627,-0.892026819330015,
9.28948786743112));
#92549=CARTESIAN_POINT('Ctrl Pts',(2.19434884699582,-0.900059141069041,
9.2889068555393));
#92550=CARTESIAN_POINT('Ctrl Pts',(2.1864277805681,-0.919171337620204,9.28751766561146));
#92551=CARTESIAN_POINT('Ctrl Pts',(2.18174397115656,-0.930234176211502,
9.28670813182155));
#92552=CARTESIAN_POINT('Ctrl Pts',(2.16458174195331,-0.969927498892542,
9.28378364918555));
#92553=CARTESIAN_POINT('Ctrl Pts',(2.15162261820875,-0.998345339520149,
9.28165239554018));
#92554=CARTESIAN_POINT('Ctrl Pts',(2.05031897660155,-1.20935210231319,9.26553638234899));
#92555=CARTESIAN_POINT('Ctrl Pts',(1.93945180592142,-1.38015729330138,9.25072930718572));
#92556=CARTESIAN_POINT('Ctrl Pts',(1.80190608146297,-1.54221551038247,9.23522290546875));
#92557=CARTESIAN_POINT('Ctrl Pts',(1.79551481273734,-1.54965182077825,9.23450802531616));
#92558=CARTESIAN_POINT('Ctrl Pts',(1.72470893824493,-1.63100909300906,9.22665130722154));
#92559=CARTESIAN_POINT('Ctrl Pts',(1.65580844288439,-1.70091569263711,9.21957143679109));
#92560=CARTESIAN_POINT('Ctrl Pts',(1.56876772387876,-1.77890961465014,9.21144674283251));
#92561=CARTESIAN_POINT('Ctrl Pts',(1.55461543361571,-1.79129073525429,9.2101496888465));
#92562=CARTESIAN_POINT('Ctrl Pts',(1.53463913596735,-1.80835188380253,9.20835381458728));
#92563=CARTESIAN_POINT('Ctrl Pts',(1.52893845758087,-1.81317429114479,9.20784522651959));
#92564=CARTESIAN_POINT('Ctrl Pts',(1.51918905033865,-1.82134298764981,9.20698219471009));
#92565=CARTESIAN_POINT('Ctrl Pts',(1.51515183434381,-1.82470287179815,9.20662677256867));
#92566=CARTESIAN_POINT('Ctrl Pts',(1.50735621729631,-1.83114688995727,9.20594428490517));
#92567=CARTESIAN_POINT('Ctrl Pts',(1.50359947248328,-1.8342328984792,9.20561707614002));
#92568=CARTESIAN_POINT('Ctrl Pts',(1.49454753598834,-1.84162218744801,9.20483262764584));
#92569=CARTESIAN_POINT('Ctrl Pts',(1.48924317284971,-1.84591424330824,9.20437618918943));
#92570=CARTESIAN_POINT('Ctrl Pts',(1.46978982726902,-1.86151659589891,9.20271373241415));
#92571=CARTESIAN_POINT('Ctrl Pts',(1.45552947405767,-1.87268795389406,9.20151715240743));
#92572=CARTESIAN_POINT('Ctrl Pts',(1.31338811377681,-1.98143478227515,9.18979066995703));
#92573=CARTESIAN_POINT('Ctrl Pts',(1.17600210827924,-2.06593974715203,9.1800243688471));
#92574=CARTESIAN_POINT('Ctrl Pts',(0.881795074411039,-2.20796793785566,
9.16000188126156));
#92575=CARTESIAN_POINT('Ctrl Pts',(0.725367668171613,-2.26418109451874,
9.14977911098919));
#92576=CARTESIAN_POINT('Ctrl Pts',(0.543470229237293,-2.30874449922894,
9.13755865589627));
#92577=CARTESIAN_POINT('Ctrl Pts',(0.522502956301095,-2.31357983723299,
9.13614592234454));
#92578=CARTESIAN_POINT('Ctrl Pts',(0.490551404705045,-2.32049181277647,
9.13398561797963));
#92579=CARTESIAN_POINT('Ctrl Pts',(0.479613058329547,-2.32277726888243,
9.13324473605734));
#92580=CARTESIAN_POINT('Ctrl Pts',(0.459723931464479,-2.32678642145354,
9.13189501964167));
#92581=CARTESIAN_POINT('Ctrl Pts',(0.45077853689879,-2.32853598874835,9.13128702483692));
#92582=CARTESIAN_POINT('Ctrl Pts',(0.431473009342262,-2.33219640818158,
9.12997274569269));
#92583=CARTESIAN_POINT('Ctrl Pts',(0.421109820271893,-2.33408987769741,
9.12926592105249));
#92584=CARTESIAN_POINT('Ctrl Pts',(0.39299194474948,-2.33903397263712,9.12734437900463));
#92585=CARTESIAN_POINT('Ctrl Pts',(0.375214859107551,-2.3419514025647,9.12612546420861));
#92586=CARTESIAN_POINT('Ctrl Pts',(0.285959804033519,-2.35555690274467,
9.11998397377182));
#92587=CARTESIAN_POINT('Ctrl Pts',(0.214059881794555,-2.36317535496498,
9.11496578204031));
#92588=CARTESIAN_POINT('Ctrl Pts',(-0.0655618299436858,-2.37993856128543,
9.09516440347429));
#92589=CARTESIAN_POINT('Ctrl Pts',(-0.273782438354002,-2.36504308950549,
9.07971214783137));
#92590=CARTESIAN_POINT('Ctrl Pts',(-0.51898160293378,-2.31466257876956,
9.06173482832672));
#92591=CARTESIAN_POINT('Ctrl Pts',(-0.560382267570449,-2.30498957142429,
9.05871163232421));
#92592=CARTESIAN_POINT('Ctrl Pts',(-0.626572449331334,-2.28763561508439,
9.05392001808731));
#92593=CARTESIAN_POINT('Ctrl Pts',(-0.651533821969743,-2.2806520034939,
9.05212277039272));
#92594=CARTESIAN_POINT('Ctrl Pts',(-0.684476875384432,-2.27085025622631,
9.04976825552857));
#92595=CARTESIAN_POINT('Ctrl Pts',(-0.69256399944137,-2.2683969210278,9.04919165499968));
#92596=CARTESIAN_POINT('Ctrl Pts',(-0.705851263772948,-2.26428837223786,
9.04824680348178));
#92597=CARTESIAN_POINT('Ctrl Pts',(-0.711059024590557,-2.26265837110255,
9.04787711926342));
#92598=CARTESIAN_POINT('Ctrl Pts',(-0.721257578827817,-2.2594275905038,
9.04715446714972));
#92599=CARTESIAN_POINT('Ctrl Pts',(-0.726248753622761,-2.25782822209685,
9.04680142411276));
#92600=CARTESIAN_POINT('Ctrl Pts',(-0.738540945992169,-2.2538443431419,
9.04593339947194));
#92601=CARTESIAN_POINT('Ctrl Pts',(-0.745835845271915,-2.25144086044164,
9.04541952235339));
#92602=CARTESIAN_POINT('Ctrl Pts',(-0.77092710820583,-2.24303859621651,
9.04365593493442));
#92603=CARTESIAN_POINT('Ctrl Pts',(-0.788664384890333,-2.2368637180327,
9.04241605848102));
#92604=CARTESIAN_POINT('Ctrl Pts',(-0.944546952691713,-2.18051153217965,
9.03156427346055));
#92605=CARTESIAN_POINT('Ctrl Pts',(-1.07784418527555,-2.11779698370409,
9.0225844487537));
#92606=CARTESIAN_POINT('Ctrl Pts',(-1.35938433772344,-1.951820251428,9.00256000739569));
#92607=CARTESIAN_POINT('Ctrl Pts',(-1.50336804236012,-1.84320396967908,
8.99153373785449));
#92608=CARTESIAN_POINT('Ctrl Pts',(-1.64884126313963,-1.70498012457662,
8.97843151933963));
#92609=CARTESIAN_POINT('Ctrl Pts',(-1.6637988173455,-1.69038699284462,8.97705893090721));
#92610=CARTESIAN_POINT('Ctrl Pts',(-1.68636509985702,-1.6677808097898,8.97494759886285));
#92611=CARTESIAN_POINT('Ctrl Pts',(-1.6941141673487,-1.6599088108952,8.97421508177893));
#92612=CARTESIAN_POINT('Ctrl Pts',(-1.70753634483157,-1.64608181271799,
8.97293293578471));
#92613=CARTESIAN_POINT('Ctrl Pts',(-1.71323404026693,-1.64015085385968,
8.97238439351282));
#92614=CARTESIAN_POINT('Ctrl Pts',(-1.72601046993488,-1.62671214227964,
8.97114458379453));
#92615=CARTESIAN_POINT('Ctrl Pts',(-1.73307125040729,-1.61918762696858,
8.97045255751335));
#92616=CARTESIAN_POINT('Ctrl Pts',(-1.75197810223576,-1.59877367232673,
8.96858071473014));
#92617=CARTESIAN_POINT('Ctrl Pts',(-1.76373074192346,-1.58579896812263,
8.96739696667838));
#92618=CARTESIAN_POINT('Ctrl Pts',(-1.81760174686676,-1.52498665263576,
8.96187497913036));
#92619=CARTESIAN_POINT('Ctrl Pts',(-1.85792092575417,-1.47559780792352,
8.95746344392764));
#92620=CARTESIAN_POINT('Ctrl Pts',(-2.01351003323371,-1.2685096652912,8.93923915566434));
#92621=CARTESIAN_POINT('Ctrl Pts',(-2.1110752860731,-1.0984899039839,8.92480825251539));
#92622=CARTESIAN_POINT('Ctrl Pts',(-2.21655854128162,-0.847358704857114,
8.90507971733241));
#92623=CARTESIAN_POINT('Ctrl Pts',(-2.24294715210715,-0.774815532470435,
8.89956068515517));
#92624=CARTESIAN_POINT('Ctrl Pts',(-2.27069117934062,-0.685155802919529,
8.8930520889899));
#92625=CARTESIAN_POINT('Ctrl Pts',(-2.2754589910058,-0.669151198371343,
8.89190219002932));
#92626=CARTESIAN_POINT('Ctrl Pts',(-2.28201817632592,-0.646252119589848,
8.89027516723342));
#92627=CARTESIAN_POINT('Ctrl Pts',(-2.28394801826896,-0.639398320570791,
8.88979050839142));
#92628=CARTESIAN_POINT('Ctrl Pts',(-2.28723157933368,-0.627532244476332,
8.88895553632869));
#92629=CARTESIAN_POINT('Ctrl Pts',(-2.28859974949358,-0.622524059112043,
8.88860439746934));
#92630=CARTESIAN_POINT('Ctrl Pts',(-2.29142644237332,-0.612041676562383,
8.8878721402448));
#92631=CARTESIAN_POINT('Ctrl Pts',(-2.29288180459949,-0.606566720578268,
8.88749120401116));
#92632=CARTESIAN_POINT('Ctrl Pts',(-2.29669765174823,-0.592001820726257,
8.88648172038356));
#92633=CARTESIAN_POINT('Ctrl Pts',(-2.29902381830876,-0.582902864597313,
8.88585511915429));
#92634=CARTESIAN_POINT('Ctrl Pts',(-2.30883533425678,-0.543551889266812,
8.88316167265519));
#92635=CARTESIAN_POINT('Ctrl Pts',(-2.31577848234547,-0.513166161440208,
8.88112378289746));
#92636=CARTESIAN_POINT('Ctrl Pts',(-2.35497110526431,-0.324603234757285,
8.86868512712059));
#92637=CARTESIAN_POINT('Ctrl Pts',(-2.3716039949965,-0.16359555102086,8.85894060335103));
#92638=CARTESIAN_POINT('Ctrl Pts',(-2.37177458044386,0.0262972234964526,
8.84728189501136));
#92639=CARTESIAN_POINT('Ctrl Pts',(-2.3712890111722,0.0547228818911722,
8.84553307096252));
#92640=CARTESIAN_POINT('Ctrl Pts',(-2.36923976809993,0.113151281512263,
8.84192204702261));
#92641=CARTESIAN_POINT('Ctrl Pts',(-2.36761709190539,0.143138040807685,
8.84005990011078));
#92642=CARTESIAN_POINT('Ctrl Pts',(-2.36542648836857,0.173076834453233,
8.83818724301668));
#92643=CARTESIAN_POINT('Ctrl Pts',(-2.36542651242649,0.173076505655319,
8.63818628587103));
#92644=CARTESIAN_POINT('Ctrl Pts',(-2.36962632261321,0.115677944682464,
8.64182253402733));
#92645=CARTESIAN_POINT('Ctrl Pts',(-2.37173733137448,0.0581212205746936,
8.64550929040616));
#92646=CARTESIAN_POINT('Ctrl Pts',(-2.37175497626484,-0.0224685146569301,
8.65075947075785));
#92647=CARTESIAN_POINT('Ctrl Pts',(-2.37142580119415,-0.0454544850129582,
8.65226686390312));
#92648=CARTESIAN_POINT('Ctrl Pts',(-2.37042425669134,-0.0801523632701318,
8.65455888830174));
#92649=CARTESIAN_POINT('Ctrl Pts',(-2.36999902211517,-0.0918704786881775,
8.6553358016766));
#92650=CARTESIAN_POINT('Ctrl Pts',(-2.36908166996873,-0.112854776213844,
8.65673238966705));
#92651=CARTESIAN_POINT('Ctrl Pts',(-2.36862203074418,-0.122122196023677,
8.65735103490929));
#92652=CARTESIAN_POINT('Ctrl Pts',(-2.36753077267549,-0.141791002591501,
8.65866808656538));
#92653=CARTESIAN_POINT('Ctrl Pts',(-2.36688496297963,-0.15219137290288,
8.65936692527951));
#92654=CARTESIAN_POINT('Ctrl Pts',(-2.36496793368108,-0.180090394642471,
8.66124821789653));
#92655=CARTESIAN_POINT('Ctrl Pts',(-2.36357106943291,-0.197579473713945,
8.66243458326398));
#92656=CARTESIAN_POINT('Ctrl Pts',(-2.35553516918909,-0.285840558268255,
8.66845856914897));
#92657=CARTESIAN_POINT('Ctrl Pts',(-2.3459115789052,-0.356297308643696,
8.67338878018612));
#92658=CARTESIAN_POINT('Ctrl Pts',(-2.30635524148394,-0.572835056575161,
8.68892982256238));
#92659=CARTESIAN_POINT('Ctrl Pts',(-2.2658105080888,-0.716594330411137,
8.6998280447763));
#92660=CARTESIAN_POINT('Ctrl Pts',(-2.20053914221121,-0.885349883215016,
8.71303297864381));
#92661=CARTESIAN_POINT('Ctrl Pts',(-2.1884245001186,-0.914885347992949,
8.71535883541839));
#92662=CARTESIAN_POINT('Ctrl Pts',(-2.16660252609903,-0.965171378149387,
8.71933637498095));
#92663=CARTESIAN_POINT('Ctrl Pts',(-2.15718397326766,-0.986042414329511,
8.72099254777867));
#92664=CARTESIAN_POINT('Ctrl Pts',(-2.13821088330868,-1.02651230058111,
8.72421066881572));
#92665=CARTESIAN_POINT('Ctrl Pts',(-2.12868532350061,-1.04612242540049,
8.72577318698067));
#92666=CARTESIAN_POINT('Ctrl Pts',(-2.09734896757605,-1.10843321121665,
8.73074253412488));
#92667=CARTESIAN_POINT('Ctrl Pts',(-2.07451162863634,-1.15060816663103,
8.73411298027638));
#92668=CARTESIAN_POINT('Ctrl Pts',(-2.04494996107893,-1.20145566246044,
8.73816000155135));
#92669=CARTESIAN_POINT('Ctrl Pts',(-2.03942587868433,-1.21080888208674,
8.7389037264827));
#92670=CARTESIAN_POINT('Ctrl Pts',(-2.03069630302183,-1.22536030356853,
8.74005928066867));
#92671=CARTESIAN_POINT('Ctrl Pts',(-2.02753475108883,-1.2305844887444,8.74047383616278));
#92672=CARTESIAN_POINT('Ctrl Pts',(-2.02164832336969,-1.24022702121712,
8.74123834963527));
#92673=CARTESIAN_POINT('Ctrl Pts',(-2.0189291356747,-1.24464860646999,8.74158865283869));
#92674=CARTESIAN_POINT('Ctrl Pts',(-2.01271849882378,-1.25467362009719,
8.74238232236784));
#92675=CARTESIAN_POINT('Ctrl Pts',(-2.00921815909397,-1.26027141533578,
8.74282509780112));
#92676=CARTESIAN_POINT('Ctrl Pts',(-1.99845141842993,-1.27733087203546,
8.74417349284185));
#92677=CARTESIAN_POINT('Ctrl Pts',(-1.99110982302307,-1.28874509607784,
8.74507432908905));
#92678=CARTESIAN_POINT('Ctrl Pts',(-1.90625401701813,-1.41821703789537,
8.75528466789832));
#92679=CARTESIAN_POINT('Ctrl Pts',(-1.81842875071117,-1.52920678757551,
8.76397154266167));
#92680=CARTESIAN_POINT('Ctrl Pts',(-1.59684677354469,-1.76294258663607,
8.78372151378255));
#92681=CARTESIAN_POINT('Ctrl Pts',(-1.4578819743076,-1.87948316306415,8.79474049263908));
#92682=CARTESIAN_POINT('Ctrl Pts',(-1.28333160107688,-1.99475940035968,
8.80830047156384));
#92683=CARTESIAN_POINT('Ctrl Pts',(-1.25934829473174,-2.00998677191907,
8.81015661926821));
#92684=CARTESIAN_POINT('Ctrl Pts',(-1.22515973721308,-2.03084150125402,
8.81279578483931));
#92685=CARTESIAN_POINT('Ctrl Pts',(-1.21517703997988,-2.03683046380086,
8.81356558613831));
#92686=CARTESIAN_POINT('Ctrl Pts',(-1.19768972217314,-2.04714738975556,
8.81491290231444));
#92687=CARTESIAN_POINT('Ctrl Pts',(-1.19020466524666,-2.05150821528912,
8.81548921353275));
#92688=CARTESIAN_POINT('Ctrl Pts',(-1.1744668651392,-2.0605620047019,8.81670024755024));
#92689=CARTESIAN_POINT('Ctrl Pts',(-1.16620951489329,-2.06524660885105,
8.81733525835841));
#92690=CARTESIAN_POINT('Ctrl Pts',(-1.14643828797032,-2.07630694534312,
8.81885489271948));
#92691=CARTESIAN_POINT('Ctrl Pts',(-1.13489913327376,-2.08263660404983,
8.81974114352013));
#92692=CARTESIAN_POINT('Ctrl Pts',(-1.09534574361167,-2.10390678712963,
8.82277715546308));
#92693=CARTESIAN_POINT('Ctrl Pts',(-1.06708552786829,-2.11838012938699,
8.82494326916661));
#92694=CARTESIAN_POINT('Ctrl Pts',(-0.998388615044404,-2.15183950443047,
8.83020408755262));
#92695=CARTESIAN_POINT('Ctrl Pts',(-0.957690724404734,-2.17025830378376,
8.83331702416739));
#92696=CARTESIAN_POINT('Ctrl Pts',(-0.797154893031354,-2.23751768285175,
8.84558287365063));
#92697=CARTESIAN_POINT('Ctrl Pts',(-0.673931672605224,-2.27766332592869,
8.85498532734097));
#92698=CARTESIAN_POINT('Ctrl Pts',(-0.416445526935439,-2.33881853555108,
8.87431531214732));
#92699=CARTESIAN_POINT('Ctrl Pts',(-0.28237934662137,-2.35876413175264,
8.88421102616375));
#92700=CARTESIAN_POINT('Ctrl Pts',(-0.128208483058595,-2.36835972722455,
8.89495821683115));
#92701=CARTESIAN_POINT('Ctrl Pts',(-0.10906982688684,-2.36931826574877,
8.89628103808177));
#92702=CARTESIAN_POINT('Ctrl Pts',(-0.0821183035926551,-2.37034082252714,
8.89812601441873));
#92703=CARTESIAN_POINT('Ctrl Pts',(-0.0743141473511144,-2.37059833008507,
8.8986581453927));
#92704=CARTESIAN_POINT('Ctrl Pts',(-0.0611909234637201,-2.37096647690985,
8.89954926241502));
#92705=CARTESIAN_POINT('Ctrl Pts',(-0.0558725492665126,-2.37109776768551,
8.89990937936327));
#92706=CARTESIAN_POINT('Ctrl Pts',(-0.0450201580608888,-2.37132913820439,
8.90064207217382));
#92707=CARTESIAN_POINT('Ctrl Pts',(-0.039486163225334,-2.37142774312308,
8.90101456435898));
#92708=CARTESIAN_POINT('Ctrl Pts',(-0.0253823291256551,-2.37162966138745,
8.90196112153543));
#92709=CARTESIAN_POINT('Ctrl Pts',(-0.0168120891537472,-2.37170589929428,
8.90253369478753));
#92710=CARTESIAN_POINT('Ctrl Pts',(0.0180461933905542,-2.37182702708564,
8.90485265002706));
#92711=CARTESIAN_POINT('Ctrl Pts',(0.0443349192699614,-2.37148132396956,
8.90657859828215));
#92712=CARTESIAN_POINT('Ctrl Pts',(0.11378101368949,-2.36941279742469,8.91109027499615));
#92713=CARTESIAN_POINT('Ctrl Pts',(0.156907818014744,-2.36694814654502,
8.91384339670428));
#92714=CARTESIAN_POINT('Ctrl Pts',(0.416495358282921,-2.34498593478084,
8.93024855392571));
#92715=CARTESIAN_POINT('Ctrl Pts',(0.629501782824453,-2.29699064208031,
8.94310846051508));
#92716=CARTESIAN_POINT('Ctrl Pts',(0.89168089883922,-2.1986429226313,8.96084089238226));
#92717=CARTESIAN_POINT('Ctrl Pts',(0.949457878661102,-2.17431694421023,
8.96486891190848));
#92718=CARTESIAN_POINT('Ctrl Pts',(1.02209700695599,-2.14028594916207,8.97012465307386));
#92719=CARTESIAN_POINT('Ctrl Pts',(1.03791023769322,-2.13266231428339,8.97128069528669));
#92720=CARTESIAN_POINT('Ctrl Pts',(1.06297477228998,-2.12023379092967,8.97313280939849));
#92721=CARTESIAN_POINT('Ctrl Pts',(1.07228175556549,-2.11554213512653,8.97382492829369));
#92722=CARTESIAN_POINT('Ctrl Pts',(1.0889891192128,-2.10698136965817,8.97507545698759));
#92723=CARTESIAN_POINT('Ctrl Pts',(1.0964006049871,-2.10313420973515,8.97563308689087));
#92724=CARTESIAN_POINT('Ctrl Pts',(1.1137693626783,-2.09400165966002,8.97694677865921));
#92725=CARTESIAN_POINT('Ctrl Pts',(1.12370950261315,-2.08868429639477,8.97770396368377));
#92726=CARTESIAN_POINT('Ctrl Pts',(1.15251948421948,-2.07300754541329,8.97991442872988));
#92727=CARTESIAN_POINT('Ctrl Pts',(1.17128624230547,-2.0624621039113,8.98137431009816));
#92728=CARTESIAN_POINT('Ctrl Pts',(1.34065740498663,-1.96423163348068,8.99473678233262));
#92729=CARTESIAN_POINT('Ctrl Pts',(1.48128218888033,-1.860469746035,9.00724920071136));
#92730=CARTESIAN_POINT('Ctrl Pts',(1.64497509807223,-1.70927472136154,9.02351044388771));
#92731=CARTESIAN_POINT('Ctrl Pts',(1.6796766227282,-1.67518643919963,9.0270669025429));
#92732=CARTESIAN_POINT('Ctrl Pts',(1.79051095765451,-1.55940188045593,9.03875070838621));
#92733=CARTESIAN_POINT('Ctrl Pts',(1.86193490647083,-1.47338669467082,9.04682115229852));
#92734=CARTESIAN_POINT('Ctrl Pts',(1.93448386768207,-1.37227304613091,9.05540904303976));
#92735=CARTESIAN_POINT('Ctrl Pts',(1.94184490158232,-1.36183682720062,9.05628533974151));
#92736=CARTESIAN_POINT('Ctrl Pts',(1.95284029734137,-1.34597750213653,9.05760123061125));
#92737=CARTESIAN_POINT('Ctrl Pts',(1.95653701051005,-1.34059822179549,9.05804485387336));
#92738=CARTESIAN_POINT('Ctrl Pts',(1.96313110165603,-1.33091744141755,9.05883826814351));
#92739=CARTESIAN_POINT('Ctrl Pts',(1.96603660770064,-1.32662165556134,9.05918859794148));
#92740=CARTESIAN_POINT('Ctrl Pts',(1.97236517538594,-1.31719842202372,9.05995326957908));
#92741=CARTESIAN_POINT('Ctrl Pts',(1.97578234046013,-1.31206715276877,9.06036721680782));
#92742=CARTESIAN_POINT('Ctrl Pts',(1.98548368259754,-1.29737561833183,9.06154562784371));
#92743=CARTESIAN_POINT('Ctrl Pts',(1.99171885554696,-1.28778296404881,9.06230690528831));
#92744=CARTESIAN_POINT('Ctrl Pts',(2.033778286188,-1.22203935582186,9.06747174443961));
#92745=CARTESIAN_POINT('Ctrl Pts',(2.06729661304694,-1.16444016649089,9.07173687960242));
#92746=CARTESIAN_POINT('Ctrl Pts',(2.21595558095432,-0.882270802454319,
9.09179224375771));
#92747=CARTESIAN_POINT('Ctrl Pts',(2.29718953497639,-0.641712378138874,
9.10662158362829));
#92748=CARTESIAN_POINT('Ctrl Pts',(2.34448585980821,-0.360119479720636,
9.12506045220821));
#92749=CARTESIAN_POINT('Ctrl Pts',(2.34929619407533,-0.327272365608154,
9.12722363898407));
#92750=CARTESIAN_POINT('Ctrl Pts',(2.35512525281256,-0.280665160301797,
9.13031531517297));
#92751=CARTESIAN_POINT('Ctrl Pts',(2.35671589341879,-0.266979536440849,
9.13122584416864));
#92752=CARTESIAN_POINT('Ctrl Pts',(2.35911096424843,-0.244680099184098,
9.13271417619122));
#92753=CARTESIAN_POINT('Ctrl Pts',(2.35998767860667,-0.23607423833236,9.13328969659055));
#92754=CARTESIAN_POINT('Ctrl Pts',(2.36172887365599,-0.218002606303909,
9.13450072547387));
#92755=CARTESIAN_POINT('Ctrl Pts',(2.36258356729768,-0.208536068825818,
9.13513653047752));
#92756=CARTESIAN_POINT('Ctrl Pts',(2.3644911755096,-0.185888135289726,9.13666117663078));
#92757=CARTESIAN_POINT('Ctrl Pts',(2.36549079185537,-0.172702690214517,
9.13755167303423));
#92758=CARTESIAN_POINT('Ctrl Pts',(2.36854097440014,-0.127452235392275,
9.14061793002016));
#92759=CARTESIAN_POINT('Ctrl Pts',(2.37005011931908,-0.0953555181348098,
9.14281048671159));
#92760=CARTESIAN_POINT('Ctrl Pts',(2.3721164954073,-0.0178850345327514,
9.14814766429079));
#92761=CARTESIAN_POINT('Ctrl Pts',(2.37202450810648,0.0274918853529142,
9.15131122205681));
#92762=CARTESIAN_POINT('Ctrl Pts',(2.36654545312782,0.205822125817044,9.16389161436422));
#92763=CARTESIAN_POINT('Ctrl Pts',(2.35127696754213,0.338214631970212,9.17357235665783));
#92764=CARTESIAN_POINT('Ctrl Pts',(2.29924680597671,0.596359174655232,9.19280747632642));
#92765=CARTESIAN_POINT('Ctrl Pts',(2.26301158391534,0.721779510893022,9.20232486185348));
#92766=CARTESIAN_POINT('Ctrl Pts',(2.20981690241613,0.861554682222548,9.21273077038045));
#92767=CARTESIAN_POINT('Ctrl Pts',(2.20276478514976,0.879428549291975,9.21405724569522));
#92768=CARTESIAN_POINT('Ctrl Pts',(2.19253888584593,0.904451436174484,9.2159064167852));
#92769=CARTESIAN_POINT('Ctrl Pts',(2.18954600424891,0.911672894195848,9.21643914756089));
#92770=CARTESIAN_POINT('Ctrl Pts',(2.18445569023125,0.923785537526782,9.21733097998198));
#92771=CARTESIAN_POINT('Ctrl Pts',(2.18237741984973,0.928684651099779,9.21769121649204));
#92772=CARTESIAN_POINT('Ctrl Pts',(2.17810495260959,0.938662604725189,9.21842387195382));
#92773=CARTESIAN_POINT('Ctrl Pts',(2.17590944741803,0.943740826889446,9.2187962087721));
#92774=CARTESIAN_POINT('Ctrl Pts',(2.17027195784503,0.956656132955809,9.21974189108977));
#92775=CARTESIAN_POINT('Ctrl Pts',(2.16680524346824,0.964482436476965,9.22031375029429));
#92776=CARTESIAN_POINT('Ctrl Pts',(2.15255621023962,0.996185817704722,9.22262609215604));
#92777=CARTESIAN_POINT('Ctrl Pts',(2.14142049797384,1.01990333591292,9.22434628745731));
#92778=CARTESIAN_POINT('Ctrl Pts',(2.11098443126376,1.08203056511512,9.22883923747315));
#92779=CARTESIAN_POINT('Ctrl Pts',(2.0910284398587,1.12010978881651,9.23157972017456));
#92780=CARTESIAN_POINT('Ctrl Pts',(1.96566184749095,1.34428785871322,9.24775714819749));
#92781=CARTESIAN_POINT('Ctrl Pts',(1.83650935308992,1.51597513370259,9.26042220332708));
#92782=CARTESIAN_POINT('Ctrl Pts',(1.63980411836318,1.71480915078621,9.27810206327147));
#92783=CARTESIAN_POINT('Ctrl Pts',(1.59160325287495,1.75963797673998,9.28232564652624));
#92784=CARTESIAN_POINT('Ctrl Pts',(1.5280081836301,1.81403118618313,9.2878065983153));
#92785=CARTESIAN_POINT('Ctrl Pts',(1.51428108923734,1.82550565798871,9.28898445816654));
#92786=CARTESIAN_POINT('Ctrl Pts',(1.49229675273782,1.84346376125227,9.29086338480878));
#92787=CARTESIAN_POINT('Ctrl Pts',(1.48412382836435,1.85004991644244,9.29156029416924));
#92788=CARTESIAN_POINT('Ctrl Pts',(1.46937868866442,1.86177170892422,9.29281490488252));
#92789=CARTESIAN_POINT('Ctrl Pts',(1.46282255230251,1.8669273698413,9.29337179253914));
#92790=CARTESIAN_POINT('Ctrl Pts',(1.44742237804409,1.87890694384315,9.29467777707004));
#92791=CARTESIAN_POINT('Ctrl Pts',(1.43855711548826,1.88570312142178,9.2954279550198));
#92792=CARTESIAN_POINT('Ctrl Pts',(1.41286165109868,1.90511480462051,9.29759786609441));
#92793=CARTESIAN_POINT('Ctrl Pts',(1.39591157639649,1.91756910828018,9.29902383426654));
#92794=CARTESIAN_POINT('Ctrl Pts',(1.23429796531139,2.03303862780482,9.31257303714797));
#92795=CARTESIAN_POINT('Ctrl Pts',(1.07868877385576,2.11970354443408,9.32533261465925));
#92796=CARTESIAN_POINT('Ctrl Pts',(0.777641943609366,2.24557477326343,9.34914951043757));
#92797=CARTESIAN_POINT('Ctrl Pts',(0.635270787945736,2.28992841935837,9.36007722903795));
#92798=CARTESIAN_POINT('Ctrl Pts',(0.471345468078818,2.32451764902733,9.3717278269597));
#92799=CARTESIAN_POINT('Ctrl Pts',(0.452973753577782,2.32816745201715,9.37302038375747));
#92800=CARTESIAN_POINT('Ctrl Pts',(0.427708913268281,2.33287627537178,9.37477813671027));
#92801=CARTESIAN_POINT('Ctrl Pts',(0.420852098504893,2.33412299268297,9.37525319544622));
#92802=CARTESIAN_POINT('Ctrl Pts',(0.409121321794179,2.33620252830729,9.37606242005481));
#92803=CARTESIAN_POINT('Ctrl Pts',(0.404250120019786,2.33705035265215,9.37639741610734));
#92804=CARTESIAN_POINT('Ctrl Pts',(0.394131223301339,2.33877894517377,9.37709110375955));
#92805=CARTESIAN_POINT('Ctrl Pts',(0.388883184150452,2.33965729227496,9.37744964475139));
#92806=CARTESIAN_POINT('Ctrl Pts',(0.376195269292256,2.34173695695617,9.37831358652662));
#92807=CARTESIAN_POINT('Ctrl Pts',(0.368752451929149,2.34292050426898,9.37881798971167));
#92808=CARTESIAN_POINT('Ctrl Pts',(0.342684314513197,2.34693852754792,9.38057667982159));
#92809=CARTESIAN_POINT('Ctrl Pts',(0.324030374661536,2.34958663666366,9.38182096909038));
#92810=CARTESIAN_POINT('Ctrl Pts',(0.208803179687195,2.36454581840011,9.38943069511205));
#92811=CARTESIAN_POINT('Ctrl Pts',(0.111567831877113,2.37112481919005,9.39552395343879));
#92812=CARTESIAN_POINT('Ctrl Pts',(-0.158034189348343,2.3727381803667,9.41217307620285));
#92813=CARTESIAN_POINT('Ctrl Pts',(-0.329852312699817,2.35500684364521,
9.42254311645145));
#92814=CARTESIAN_POINT('Ctrl Pts',(-0.559948787033967,2.30556713860022,
9.43744291146647));
#92815=CARTESIAN_POINT('Ctrl Pts',(-0.621103668563766,2.28984968856897,
9.44149924988571));
#92816=CARTESIAN_POINT('Ctrl Pts',(-0.698410960853611,2.26665610282416,
9.44678723255796));
#92817=CARTESIAN_POINT('Ctrl Pts',(-0.715209687019322,2.26141169064095,
9.4479460862781));
#92818=CARTESIAN_POINT('Ctrl Pts',(-0.741871104669624,2.25276145144577,
9.44980165574627));
#92819=CARTESIAN_POINT('Ctrl Pts',(-0.75177259382262,2.24947657340868,9.45049439239136));
#92820=CARTESIAN_POINT('Ctrl Pts',(-0.769558860075498,2.24344532612811,
9.45174543990293));
#92821=CARTESIAN_POINT('Ctrl Pts',(-0.777451462484111,2.24072242610582,
9.45230296648972));
#92822=CARTESIAN_POINT('Ctrl Pts',(-0.793679845935531,2.23502766883712,
9.45345430773837));
#92823=CARTESIAN_POINT('Ctrl Pts',(-0.802013688984742,2.23205072014589,
9.45404828429249));
#92824=CARTESIAN_POINT('Ctrl Pts',(-0.826656222314673,2.22309228393259,
9.45581282414033));
#92825=CARTESIAN_POINT('Ctrl Pts',(-0.842915779074156,2.21697829807081,
9.45698778294039));
#92826=CARTESIAN_POINT('Ctrl Pts',(-0.92593641094033,2.18471521853626,9.46304330273811));
#92827=CARTESIAN_POINT('Ctrl Pts',(-0.991547559256512,2.15572965950817,
9.46801827281449));
#92828=CARTESIAN_POINT('Ctrl Pts',(-1.19255304698623,2.0558108882291,9.483873936327));
#92829=CARTESIAN_POINT('Ctrl Pts',(-1.32246130990822,1.97474731860099,9.49505906586337));
#92830=CARTESIAN_POINT('Ctrl Pts',(-1.53618215957587,1.81078504311349,9.51470779779012));
#92831=CARTESIAN_POINT('Ctrl Pts',(-1.62335960850776,1.73306332172986,9.52315324084593));
#92832=CARTESIAN_POINT('Ctrl Pts',(-1.71335438094739,1.64005425639804,9.53208431524276));
#92833=CARTESIAN_POINT('Ctrl Pts',(-1.72216187966619,1.63080338396,9.53296075133178));
#92834=CARTESIAN_POINT('Ctrl Pts',(-1.73535697456397,1.61671792208454,9.53427680962436));
#92835=CARTESIAN_POINT('Ctrl Pts',(-1.73979987481099,1.61193581353731,9.5347204624079));
#92836=CARTESIAN_POINT('Ctrl Pts',(-1.74773724408093,1.60332139137802,9.5355139078793));
#92837=CARTESIAN_POINT('Ctrl Pts',(-1.75123892213695,1.59949591986223,9.53586423954936));
#92838=CARTESIAN_POINT('Ctrl Pts',(-1.75887548206202,1.59109808069195,9.53662889003227));
#92839=CARTESIAN_POINT('Ctrl Pts',(-1.76300509074128,1.58652107328972,9.53704281439525));
#92840=CARTESIAN_POINT('Ctrl Pts',(-1.77151072676885,1.57701972218525,9.5378963771138));
#92841=CARTESIAN_POINT('Ctrl Pts',(-1.77588418336301,1.5720931362526,9.53833582740061));
#92842=CARTESIAN_POINT('Ctrl Pts',(-1.79859711824453,1.54629187080716,9.54062140092057));
#92843=CARTESIAN_POINT('Ctrl Pts',(-1.81659018403407,1.52511324645551,9.54244349859954));
#92844=CARTESIAN_POINT('Ctrl Pts',(-1.89607076218975,1.42815810455137,9.55057102023391));
#92845=CARTESIAN_POINT('Ctrl Pts',(-1.95322441610578,1.34893971075471,9.55663748857416));
#92846=CARTESIAN_POINT('Ctrl Pts',(-2.05489644764827,1.18794466448773,9.56835860503939));
#92847=CARTESIAN_POINT('Ctrl Pts',(-2.09980461433089,1.10663117327879,9.57400927256932));
#92848=CARTESIAN_POINT('Ctrl Pts',(-2.19357494328737,0.910469576203566,
9.58742649032757));
#92849=CARTESIAN_POINT('Ctrl Pts',(-2.23836674049381,0.793998641665065,
9.59524060475712));
#92850=CARTESIAN_POINT('Ctrl Pts',(-2.27915308345591,0.656516160423915,
9.60460404083347));
#92851=CARTESIAN_POINT('Ctrl Pts',(-2.28429062017896,0.638410977156685,
9.60583949042992));
#92852=CARTESIAN_POINT('Ctrl Pts',(-2.29230306591027,0.608838585120078,
9.60786220334127));
#92853=CARTESIAN_POINT('Ctrl Pts',(-2.2953087255795,0.597407410754678,9.60864523114045));
#92854=CARTESIAN_POINT('Ctrl Pts',(-2.30052362662366,0.576953540634747,
9.6100485738735));
#92855=CARTESIAN_POINT('Ctrl Pts',(-2.30276555769597,0.567939368923619,
9.61066781937295));
#92856=CARTESIAN_POINT('Ctrl Pts',(-2.3073969372521,0.548839560944614,9.61198167872364));
#92857=CARTESIAN_POINT('Ctrl Pts',(-2.30977333362695,0.538750991688016,
9.61267669833822));
#92858=CARTESIAN_POINT('Ctrl Pts',(-2.3144740352816,0.518192077350102,9.61409527194614));
#92859=CARTESIAN_POINT('Ctrl Pts',(-2.31679359562083,0.507720905336232,
9.61481896064311));
#92860=CARTESIAN_POINT('Ctrl Pts',(-2.32239524507094,0.481595485183429,
9.61662762177996));
#92861=CARTESIAN_POINT('Ctrl Pts',(-2.32559010917364,0.465923285432438,
9.61771534497657));
#92862=CARTESIAN_POINT('Ctrl Pts',(-2.34634386083236,0.35858088256934,9.62518513949623));
#92863=CARTESIAN_POINT('Ctrl Pts',(-2.35862460268534,0.266037904201847,
9.63172812560892));
#92864=CARTESIAN_POINT('Ctrl Pts',(-2.36542652525385,0.173076330344439,
9.63839747301829));
#92865=CARTESIAN_POINT('Origin',(0.,0.,-1.84858989190503));
#92866=CARTESIAN_POINT('',(-2.36516017494062,0.173060140022867,10.8371116396001));
#92867=CARTESIAN_POINT('',(-2.36916488281964,0.173362644194442,10.6397478783738));
#92868=CARTESIAN_POINT('',(-2.36542649454111,0.173076750093529,-1.84858989190503));
#92869=CARTESIAN_POINT('',(-2.37536570805869,0.000359094737715843,9.84846194679725));
#92870=CARTESIAN_POINT('Ctrl Pts',(-2.37558966658059,0.000367530682965326,
9.84859046225436));
#92871=CARTESIAN_POINT('Ctrl Pts',(-2.37390141785161,-0.765575782524014,
9.90022107850398));
#92872=CARTESIAN_POINT('Ctrl Pts',(-1.55507573763911,-2.32069515122134,
10.0048399834818));
#92873=CARTESIAN_POINT('Ctrl Pts',(1.09527631218182,-2.58173452929509,10.162447177188));
#92874=CARTESIAN_POINT('Ctrl Pts',(2.7636678171772,-0.476574837858771,10.3214120433727));
#92875=CARTESIAN_POINT('Ctrl Pts',(1.89670849126738,2.06578805276227,10.4803769095575));
#92876=CARTESIAN_POINT('Ctrl Pts',(-0.710265108221614,2.71302540640962,
10.6393417757422));
#92877=CARTESIAN_POINT('Ctrl Pts',(-2.17296599975294,1.33539974380505,10.7582533524231));
#92878=CARTESIAN_POINT('Ctrl Pts',(-2.35302712705762,0.365443290256533,
10.8241766403757));
#92879=CARTESIAN_POINT('Ctrl Pts',(-2.36516017494062,0.173060140022867,
10.8371116396001));
#92880=CARTESIAN_POINT('Ctrl Pts',(-2.3717499895258,0.000222899859654739,
9.84638711742221));
#92881=CARTESIAN_POINT('Ctrl Pts',(-2.37174950122911,0.00541858581568568,
9.84602924011033));
#92882=CARTESIAN_POINT('Ctrl Pts',(-2.37173193999369,0.0106143209615235,
9.84567219836226));
#92883=CARTESIAN_POINT('Ctrl Pts',(-2.3716568922996,0.0218723968884325,
9.8449004406146));
#92884=CARTESIAN_POINT('Ctrl Pts',(-2.3715932349913,0.0279346790041509,
9.84448604178746));
#92885=CARTESIAN_POINT('Ctrl Pts',(-2.37143325691739,0.0390942518433647,
9.84372546045836));
#92886=CARTESIAN_POINT('Ctrl Pts',(-2.37134374517283,0.044191583019491,
9.84337891679726));
#92887=CARTESIAN_POINT('Ctrl Pts',(-2.37113535589589,0.0542170263237478,
9.84269908764649));
#92888=CARTESIAN_POINT('Ctrl Pts',(-2.37101754869356,0.0591451400162158,
9.84236574627927));
#92889=CARTESIAN_POINT('Ctrl Pts',(-2.37075013236532,0.0690403132418933,
9.84169814098856));
#92890=CARTESIAN_POINT('Ctrl Pts',(-2.37060027827655,0.0740072750536078,
9.84136388963095));
#92891=CARTESIAN_POINT('Ctrl Pts',(-2.37014416960029,0.0876975882252386,
9.8404448768716));
#92892=CARTESIAN_POINT('Ctrl Pts',(-2.36980536385545,0.0964198896047411,
9.83986190791111));
#92893=CARTESIAN_POINT('Ctrl Pts',(-2.36841278027883,0.127802845351948,
9.8377729058658));
#92894=CARTESIAN_POINT('Ctrl Pts',(-2.36708203068683,0.150450666234089,
9.83628136334072));
#92895=CARTESIAN_POINT('Ctrl Pts',(-2.36542649454068,0.173076750099461,
9.83480414144792));
#92896=CARTESIAN_POINT('',(-2.37115431906008,-0.00217150823245576,9.65141047674274));
#92897=CARTESIAN_POINT('Ctrl Pts',(-2.36542652525385,0.173076330344439,
9.63839747301829));
#92898=CARTESIAN_POINT('Ctrl Pts',(-2.36969210259616,0.114778874124177,
9.64257991069099));
#92899=CARTESIAN_POINT('Ctrl Pts',(-2.37180304718333,0.0563167111270467,
9.64681082413871));
#92900=CARTESIAN_POINT('Ctrl Pts',(-2.37174898760129,-0.00219141786265223,
9.65106845735155));
#92901=CARTESIAN_POINT('Ctrl Pts',(-2.37115431906008,-0.00217150823245576,
9.65141047674274));
#92902=CARTESIAN_POINT('Ctrl Pts',(-2.37298013798662,-0.205892024950704,
9.66507633933387));
#92903=CARTESIAN_POINT('Ctrl Pts',(-2.25564024368453,-1.1970881612814,9.73170618041963));
#92904=CARTESIAN_POINT('Ctrl Pts',(-0.868335570250338,-2.66618442166349,
9.8513));
#92905=CARTESIAN_POINT('Ctrl Pts',(1.77076269460301,-2.17415397621359,10.0101919354839));
#92906=CARTESIAN_POINT('Ctrl Pts',(2.78675196561196,0.310740269422676,10.1690838709677));
#92907=CARTESIAN_POINT('Ctrl Pts',(1.24836046454784,2.51080508670764,10.3279758064516));
#92908=CARTESIAN_POINT('Ctrl Pts',(-1.40046442942458,2.41070497057955,10.4848638089203));
#92909=CARTESIAN_POINT('Ctrl Pts',(-2.31145126867504,0.927232679798168,
10.5887878328943));
#92910=CARTESIAN_POINT('Ctrl Pts',(-2.36916488281964,0.173362644194442,
10.6397478783738));
#92911=CARTESIAN_POINT('Origin',(0.,0.,-1.84858989190503));
#92912=CARTESIAN_POINT('',(-2.36542649454111,0.173076750093535,11.8369288124872));
#92913=CARTESIAN_POINT('',(-2.36542649946083,0.173076682856166,11.6396027579113));
#92914=CARTESIAN_POINT('',(-2.36542649454111,0.173076750093529,-1.84858989190503));
#92915=CARTESIAN_POINT('',(-2.37174919443444,0.00195478888988407,10.848589891905));
#92916=CARTESIAN_POINT('Ctrl Pts',(-2.37174919443444,0.00195478888988407,
10.848589891905));
#92917=CARTESIAN_POINT('Ctrl Pts',(-2.37181439280241,-0.0771505188548095,
10.8538849196891));
#92918=CARTESIAN_POINT('Ctrl Pts',(-2.36791767540096,-0.156314771560316,
10.8591799474733));
#92919=CARTESIAN_POINT('Ctrl Pts',(-2.36006804502609,-0.23511036843734,
10.8644749752574));
#92920=CARTESIAN_POINT('Ctrl Pts',(-2.35222055250515,-0.313884505262257,
10.869768560936));
#92921=CARTESIAN_POINT('Ctrl Pts',(-2.34042233132756,-0.392289716004928,
10.8750621466145));
#92922=CARTESIAN_POINT('Ctrl Pts',(-2.32473434191077,-0.469902438853748,
10.880355732293));
#92923=CARTESIAN_POINT('Ctrl Pts',(-2.30904565535801,-0.547518610622591,
10.8856495532056));
#92924=CARTESIAN_POINT('Ctrl Pts',(-2.28946695249902,-0.624341762057178,
10.8909433741181));
#92925=CARTESIAN_POINT('Ctrl Pts',(-2.26611021311493,-0.699958973452166,
10.8962371950307));
#92926=CARTESIAN_POINT('Ctrl Pts',(-2.24272845082305,-0.775657196262196,
10.9015366874024));
#92927=CARTESIAN_POINT('Ctrl Pts',(-2.21556070906728,-0.850146446906356,
10.906836179774));
#92928=CARTESIAN_POINT('Ctrl Pts',(-2.18476855053317,-0.923030033694034,
10.9121356721457));
#92929=CARTESIAN_POINT('Ctrl Pts',(-2.15395976457295,-0.995952976814975,
10.9174380261848));
#92930=CARTESIAN_POINT('Ctrl Pts',(-2.11952287114002,-1.06726810453033,
10.9227403802239));
#92931=CARTESIAN_POINT('Ctrl Pts',(-2.08166607241455,-1.1366021403544,10.9280427342631));
#92932=CARTESIAN_POINT('Ctrl Pts',(-2.04373945114354,-1.20606405489607,
10.9333548678892));
#92933=CARTESIAN_POINT('Ctrl Pts',(-2.0023805726807,-1.27353717604168,10.9386670015153));
#92934=CARTESIAN_POINT('Ctrl Pts',(-1.95784158605713,-1.33867635610901,
10.9439791351414));
#92935=CARTESIAN_POINT('Ctrl Pts',(-1.92069211758932,-1.39300821454088,
10.9484099261315));
#92936=CARTESIAN_POINT('Ctrl Pts',(-1.8813310926315,-1.44571678485983,10.9528407171216));
#92937=CARTESIAN_POINT('Ctrl Pts',(-1.83992524872408,-1.49662057369516,
10.9572715081117));
#92938=CARTESIAN_POINT('Ctrl Pts',(-1.79010081493234,-1.5578740639572,10.9626031625715));
#92939=CARTESIAN_POINT('Ctrl Pts',(-1.73711971794155,-1.61675294397844,
10.9679348170314));
#92940=CARTESIAN_POINT('Ctrl Pts',(-1.68123688280041,-1.67291380722725,
10.9732664714912));
#92941=CARTESIAN_POINT('Ctrl Pts',(-1.62543493638254,-1.72899337931546,
10.9785904085415));
#92942=CARTESIAN_POINT('Ctrl Pts',(-1.56673992068801,-1.78236241789962,
10.9839143455918));
#92943=CARTESIAN_POINT('Ctrl Pts',(-1.50544717353461,-1.8327102526577,10.9892382826422));
#92944=CARTESIAN_POINT('Ctrl Pts',(-1.44422591298779,-1.88299936601688,
10.9945560103087));
#92945=CARTESIAN_POINT('Ctrl Pts',(-1.38041330222577,-1.93027398176313,
10.9998737379752));
#92946=CARTESIAN_POINT('Ctrl Pts',(-1.31434060260554,-1.97426108781045,
11.0051914656416));
#92947=CARTESIAN_POINT('Ctrl Pts',(-1.24831011197238,-2.01822009373169,
11.0105057962031));
#92948=CARTESIAN_POINT('Ctrl Pts',(-1.18002278741972,-2.05889549922399,
11.0158201267646));
#92949=CARTESIAN_POINT('Ctrl Pts',(-1.10984098717517,-2.09605606930875,
11.0211344573261));
#92950=CARTESIAN_POINT('Ctrl Pts',(-1.03968214854198,-2.13320448144707,
11.0264470491805));
#92951=CARTESIAN_POINT('Ctrl Pts',(-0.967630479063115,-2.16684012240153,
11.031759641035));
#92952=CARTESIAN_POINT('Ctrl Pts',(-0.894073896701073,-2.19677716888577,
11.0370722328894));
#92953=CARTESIAN_POINT('Ctrl Pts',(-0.820518456434641,-2.22671375054458,
11.0423847422564));
#92954=CARTESIAN_POINT('Ctrl Pts',(-0.745458584526182,-2.25295167635402,
11.0476972516235));
#92955=CARTESIAN_POINT('Ctrl Pts',(-0.669301793910461,-2.2753534167615,
11.0530097609906));
#92956=CARTESIAN_POINT('Ctrl Pts',(-0.593068959586898,-2.29777752564577,
11.0583275749786));
#92957=CARTESIAN_POINT('Ctrl Pts',(-0.515737469459638,-2.31635766453079,
11.0636453889667));
#92958=CARTESIAN_POINT('Ctrl Pts',(-0.437729032617402,-2.33100651146749,
11.0689632029547));
#92959=CARTESIAN_POINT('Ctrl Pts',(-0.359683267706368,-2.3456623680712,
11.0742835615871));
#92960=CARTESIAN_POINT('Ctrl Pts',(-0.280960376007474,-2.35638312176981,
11.0796039202195));
#92961=CARTESIAN_POINT('Ctrl Pts',(-0.201988715865797,-2.36313322120504,
11.0849242788519));
#92962=CARTESIAN_POINT('Ctrl Pts',(-0.122872789652276,-2.36989565177687,
11.0902543567587));
#92963=CARTESIAN_POINT('Ctrl Pts',(-0.0435076567296367,-2.37267291702921,
11.0955844346656));
#92964=CARTESIAN_POINT('Ctrl Pts',(0.035676974233163,-2.37148164994157,
11.1009145125724));
#92965=CARTESIAN_POINT('Ctrl Pts',(0.111551785538755,-2.37034017634511,
11.1060217998138));
#92966=CARTESIAN_POINT('Ctrl Pts',(0.187260521157683,-2.36555539903782,
11.1111290870551));
#92967=CARTESIAN_POINT('Ctrl Pts',(0.262431960950489,-2.35718635843068,
11.1162363742965));
#92968=CARTESIAN_POINT('Ctrl Pts',(0.340905742291385,-2.34844965916766,
11.1215680287563));
#92969=CARTESIAN_POINT('Ctrl Pts',(0.419091615225448,-2.33577336537002,
11.1268996832161));
#92970=CARTESIAN_POINT('Ctrl Pts',(0.496562842236019,-2.31918593610139,
11.1322313376759));
#92971=CARTESIAN_POINT('Ctrl Pts',(0.573921931975342,-2.30262251663778,
11.1375552747263));
#92972=CARTESIAN_POINT('Ctrl Pts',(0.650567975390163,-2.28215930145448,
11.1428792117766));
#92973=CARTESIAN_POINT('Ctrl Pts',(0.726079884680871,-2.25787645002153,
11.1482031488269));
#92974=CARTESIAN_POINT('Ctrl Pts',(0.801503723353056,-2.23362192002509,
11.1535208764934));
#92975=CARTESIAN_POINT('Ctrl Pts',(0.87579561244242,-2.20555674940822,11.1588386041599));
#92976=CARTESIAN_POINT('Ctrl Pts',(0.948546682480867,-2.17381168771689,
11.1641563318264));
#92977=CARTESIAN_POINT('Ctrl Pts',(1.02125127721261,-2.14208690561014,11.1694706623879));
#92978=CARTESIAN_POINT('Ctrl Pts',(1.09241657798509,-2.10668708537788,11.1747849929494));
#92979=CARTESIAN_POINT('Ctrl Pts',(1.161652009621,-2.06779173783132,11.1800993235109));
#92980=CARTESIAN_POINT('Ctrl Pts',(1.23086478927222,-2.02890911580401,11.1854119153653));
#92981=CARTESIAN_POINT('Ctrl Pts',(1.29814854507141,-1.98653346686885,11.1907245072197));
#92982=CARTESIAN_POINT('Ctrl Pts',(1.363137049472,-1.94089037476535,11.1960370990742));
#92983=CARTESIAN_POINT('Ctrl Pts',(1.42812454481162,-1.89524799135122,11.2013496084412));
#92984=CARTESIAN_POINT('Ctrl Pts',(1.49081647664435,-1.84633853618342,11.2066621178083));
#92985=CARTESIAN_POINT('Ctrl Pts',(1.55087661711426,-1.79443021067642,11.2119746271754));
#92986=CARTESIAN_POINT('Ctrl Pts',(1.61099672854311,-1.74247005392106,11.2172924411634));
#92987=CARTESIAN_POINT('Ctrl Pts',(1.66847944342655,-1.68750535237616,11.2226102551515));
#92988=CARTESIAN_POINT('Ctrl Pts',(1.7230230652465,-1.62984342166006,11.2279280691395));
#92989=CARTESIAN_POINT('Ctrl Pts',(1.77759278691089,-1.57215389894746,11.2332484277719));
#92990=CARTESIAN_POINT('Ctrl Pts',(1.82922030863834,-1.51176493275674,11.2385687864043));
#92991=CARTESIAN_POINT('Ctrl Pts',(1.87764386463513,-1.44901745334487,11.2438891450367));
#92992=CARTESIAN_POINT('Ctrl Pts',(1.92615588117835,-1.38615534632663,11.2492192229435));
#92993=CARTESIAN_POINT('Ctrl Pts',(1.97145196796719,-1.3209265026474,11.2545493008504));
#92994=CARTESIAN_POINT('Ctrl Pts',(2.0133135061698,-1.25370123569145,11.2598793787572));
#92995=CARTESIAN_POINT('Ctrl Pts',(2.05342528383996,-1.189285901766,11.2649866659986));
#92996=CARTESIAN_POINT('Ctrl Pts',(2.09038378236208,-1.12303806308547,11.2700939532399));
#92997=CARTESIAN_POINT('Ctrl Pts',(2.12403770038088,-1.05530180984433,11.2752012404812));
#92998=CARTESIAN_POINT('Ctrl Pts',(2.15917006196871,-0.984589848754286,
11.280532894941));
#92999=CARTESIAN_POINT('Ctrl Pts',(2.190834066755,-0.911987438658024,11.2858645494009));
#93000=CARTESIAN_POINT('Ctrl Pts',(2.21882264788155,-0.83786879626103,11.2911962038607));
#93001=CARTESIAN_POINT('Ctrl Pts',(2.24677071637878,-0.763857438369515,
11.296520140911));
#93002=CARTESIAN_POINT('Ctrl Pts',(2.27105376183779,-0.688334641479644,
11.3018440779614));
#93003=CARTESIAN_POINT('Ctrl Pts',(2.29151124663089,-0.611697857658614,
11.3071680150117));
#93004=CARTESIAN_POINT('Ctrl Pts',(2.31194487156715,-0.535150456413677,
11.3124857426782));
#93005=CARTESIAN_POINT('Ctrl Pts',(2.32856168209565,-0.457492100816392,
11.3178034703447));
#93006=CARTESIAN_POINT('Ctrl Pts',(2.3412502918617,-0.379137354210184,11.3231211980112));
#93007=CARTESIAN_POINT('Ctrl Pts',(2.35393079580842,-0.300832662687369,
11.3284355285727));
#93008=CARTESIAN_POINT('Ctrl Pts',(2.36268800501659,-0.221832924754916,
11.3337498591342));
#93009=CARTESIAN_POINT('Ctrl Pts',(2.36746143565309,-0.142563716265519,
11.3390641896957));
#93010=CARTESIAN_POINT('Ctrl Pts',(2.37223330455052,-0.0633204425448197,
11.3443767815501));
#93011=CARTESIAN_POINT('Ctrl Pts',(2.37302395483914,0.0161916589820648,
11.3496893734045));
#93012=CARTESIAN_POINT('Ctrl Pts',(2.36982482150072,0.0955425449686583,
11.3550019652589));
#93013=CARTESIAN_POINT('Ctrl Pts',(2.36662573783448,0.174892198893011,11.360314474626));
#93014=CARTESIAN_POINT('Ctrl Pts',(2.35943701388961,0.254080173799275,11.365626983993));
#93015=CARTESIAN_POINT('Ctrl Pts',(2.34830215769798,0.332678581593434,11.3709394933601));
#93016=CARTESIAN_POINT('Ctrl Pts',(2.33715618318396,0.411355471087036,11.3762573073482));
#93017=CARTESIAN_POINT('Ctrl Pts',(2.32205627107895,0.489441152109287,11.3815751213362));
#93018=CARTESIAN_POINT('Ctrl Pts',(2.30309750967023,0.566515598594419,11.3868929353243));
#93019=CARTESIAN_POINT('Ctrl Pts',(2.28412967624341,0.643626926221623,11.3922132939566));
#93020=CARTESIAN_POINT('Ctrl Pts',(2.26129944989605,0.719725605594071,11.397533652589));
#93021=CARTESIAN_POINT('Ctrl Pts',(2.23475179772338,0.7944069895665,11.4028540112214));
#93022=CARTESIAN_POINT('Ctrl Pts',(2.20815564808352,0.869224802099382,11.4081840891283));
#93023=CARTESIAN_POINT('Ctrl Pts',(2.17782868193531,0.942619710985243,11.4135141670351));
#93024=CARTESIAN_POINT('Ctrl Pts',(2.14396392819246,1.01420744283878,11.418844244942));
#93025=CARTESIAN_POINT('Ctrl Pts',(2.11151467928016,1.08280289602355,11.4239515321833));
#93026=CARTESIAN_POINT('Ctrl Pts',(2.07581772266374,1.14973894035833,11.4290588194247));
#93027=CARTESIAN_POINT('Ctrl Pts',(2.03708047755367,1.2147020994753,11.434166106666));
#93028=CARTESIAN_POINT('Ctrl Pts',(1.99664147424469,1.28251914219552,11.4394977611258));
#93029=CARTESIAN_POINT('Ctrl Pts',(1.95273548854899,1.34844321648543,11.4448294155856));
#93030=CARTESIAN_POINT('Ctrl Pts',(1.90556508455358,1.41209764925458,11.4501610700454));
#93031=CARTESIAN_POINT('Ctrl Pts',(1.85846295829933,1.47565994414665,11.4554850070958));
#93032=CARTESIAN_POINT('Ctrl Pts',(1.80810607400236,1.53695874797413,11.4608089441461));
#93033=CARTESIAN_POINT('Ctrl Pts',(1.75474171921775,1.59564393313068,11.4661328811964));
#93034=CARTESIAN_POINT('Ctrl Pts',(1.70143960404243,1.65426067291746,11.4714506088629));
#93035=CARTESIAN_POINT('Ctrl Pts',(1.64513730265756,1.71026950655098,11.4767683365294));
#93036=CARTESIAN_POINT('Ctrl Pts',(1.5861230961311,1.76335237159777,11.4820860641959));
#93037=CARTESIAN_POINT('Ctrl Pts',(1.52714658943978,1.81640132590716,11.4874003947574));
#93038=CARTESIAN_POINT('Ctrl Pts',(1.46546196384419,1.86652770889706,11.4927147253189));
#93039=CARTESIAN_POINT('Ctrl Pts',(1.40139431389172,1.9134502971052,11.4980290558804));
#93040=CARTESIAN_POINT('Ctrl Pts',(1.33734762516381,1.96035753349522,11.5033416477348));
#93041=CARTESIAN_POINT('Ctrl Pts',(1.2709198382455,2.00406277965911,11.5086542395892));
#93042=CARTESIAN_POINT('Ctrl Pts',(1.20246790807677,2.04432604849263,11.5139668314436));
#93043=CARTESIAN_POINT('Ctrl Pts',(1.1340170407448,2.08458869216798,11.5192793408107));
#93044=CARTESIAN_POINT('Ctrl Pts',(1.06354249746166,2.12140922816019,11.5245918501778));
#93045=CARTESIAN_POINT('Ctrl Pts',(0.991427608477204,2.15459262034594,11.5299043595448));
#93046=CARTESIAN_POINT('Ctrl Pts',(0.919240711684985,2.18780914665085,11.5352221735329));
#93047=CARTESIAN_POINT('Ctrl Pts',(0.845410624200989,2.21738107774086,11.5405399875209));
#93048=CARTESIAN_POINT('Ctrl Pts',(0.770341986431395,2.24316100323649,11.545857801509));
#93049=CARTESIAN_POINT('Ctrl Pts',(0.695237427325773,2.26895326476743,11.5511781601414));
#93050=CARTESIAN_POINT('Ctrl Pts',(0.618893588439674,2.29094977588689,11.5564985187737));
#93051=CARTESIAN_POINT('Ctrl Pts',(0.541729178938679,2.30905339028495,11.5618188774061));
#93052=CARTESIAN_POINT('Ctrl Pts',(0.464423804866006,2.32719007651323,11.567148955313));
#93053=CARTESIAN_POINT('Ctrl Pts',(0.386295327264472,2.3414195710149,11.5724790332198));
#93054=CARTESIAN_POINT('Ctrl Pts',(0.307771340723714,2.35169616752019,11.5778091111267));
#93055=CARTESIAN_POINT('Ctrl Pts',(0.232529559720264,2.36154321499924,11.582916398368));
#93056=CARTESIAN_POINT('Ctrl Pts',(0.156925044820003,2.3677612588708,11.5880236856094));
#93057=CARTESIAN_POINT('Ctrl Pts',(0.0813336522693424,2.37035501550053,
11.5931309728507));
#93058=CARTESIAN_POINT('Ctrl Pts',(0.00242146930970082,2.37306271793611,
11.5984626273105));
#93059=CARTESIAN_POINT('Ctrl Pts',(-0.0767757596815532,2.37183061769798,
11.6037942817703));
#93060=CARTESIAN_POINT('Ctrl Pts',(-0.155831669178614,2.36662514002134,
11.6091259362302));
#93061=CARTESIAN_POINT('Ctrl Pts',(-0.234773147624385,2.36142719711707,
11.6144498732805));
#93062=CARTESIAN_POINT('Ctrl Pts',(-0.313573248870372,2.35226732864514,
11.6197738103308));
#93063=CARTESIAN_POINT('Ctrl Pts',(-0.391803718379393,2.33916393370881,
11.6250977473812));
#93064=CARTESIAN_POINT('Ctrl Pts',(-0.469942946574139,2.32607582144921,
11.6304154750477));
#93065=CARTESIAN_POINT('Ctrl Pts',(-0.547513403230365,2.30905339975424,
11.6357332027142));
#93066=CARTESIAN_POINT('Ctrl Pts',(-0.624091604942801,2.28816689320074,
11.6410509303807));
#93067=CARTESIAN_POINT('Ctrl Pts',(-0.700620886475727,2.26729372949973,
11.6463652609422));
#93068=CARTESIAN_POINT('Ctrl Pts',(-0.776158720056143,2.24256150346772,
11.6516795915036));
#93069=CARTESIAN_POINT('Ctrl Pts',(-0.850292670021049,2.21409133456786,
11.6569939220651));
#93070=CARTESIAN_POINT('Ctrl Pts',(-0.924402365336662,2.1856304803472,11.6623065139195));
#93071=CARTESIAN_POINT('Ctrl Pts',(-0.99710865170529,2.15343427964622,11.667619105774));
#93072=CARTESIAN_POINT('Ctrl Pts',(-1.06801651977944,2.11767296247041,11.6729316976284));
#93073=CARTESIAN_POINT('Ctrl Pts',(-1.13892328688408,2.08191220055203,11.6782442069954));
#93074=CARTESIAN_POINT('Ctrl Pts',(-1.20803127313806,2.0425866445149,11.6835567163625));
#93075=CARTESIAN_POINT('Ctrl Pts',(-1.27496898797061,1.99991303366252,11.6888692257296));
#93076=CARTESIAN_POINT('Ctrl Pts',(-1.34197354112422,1.95719681256403,11.6941870397176));
#93077=CARTESIAN_POINT('Ctrl Pts',(-1.40680309753799,1.91112611101221,11.6995048537057));
#93078=CARTESIAN_POINT('Ctrl Pts',(-1.46911467622812,1.86196136656783,11.7048226676937));
#93079=CARTESIAN_POINT('Ctrl Pts',(-1.53145607183287,1.81277309614292,11.7101430263261));
#93080=CARTESIAN_POINT('Ctrl Pts',(-1.59127673585833,1.76048814235256,11.7154633849585));
#93081=CARTESIAN_POINT('Ctrl Pts',(-1.6482683350962,1.7054059804103,11.7207837435909));
#93082=CARTESIAN_POINT('Ctrl Pts',(-1.70536404705162,1.65022319392607,11.7261138214977));
#93083=CARTESIAN_POINT('Ctrl Pts',(-1.75962004570391,1.59223333156763,11.7314438994046));
#93084=CARTESIAN_POINT('Ctrl Pts',(-1.81076644018087,1.53177118448374,11.7367739773114));
#93085=CARTESIAN_POINT('Ctrl Pts',(-1.85977497861462,1.47383628038247,11.7418812645528));
#93086=CARTESIAN_POINT('Ctrl Pts',(-1.90592851005167,1.41363197589522,11.7469885517941));
#93087=CARTESIAN_POINT('Ctrl Pts',(-1.94902754655883,1.35147685339219,11.7520958390355));
#93088=CARTESIAN_POINT('Ctrl Pts',(-1.99459973994361,1.28575507647748,11.7574961983172));
#93089=CARTESIAN_POINT('Ctrl Pts',(-2.03692704740659,1.21760624616623,11.7628965575989));
#93090=CARTESIAN_POINT('Ctrl Pts',(-2.07574541907485,1.1473791952488,11.7682969168806));
#93091=CARTESIAN_POINT('Ctrl Pts',(-2.11450324092046,1.07726168616158,11.773688852553));
#93092=CARTESIAN_POINT('Ctrl Pts',(-2.14976278316903,1.00507278974043,11.7790807882254));
#93093=CARTESIAN_POINT('Ctrl Pts',(-2.1813026563105,0.931191056697159,11.7844727238978));
#93094=CARTESIAN_POINT('Ctrl Pts',(-2.21279447910213,0.85742188095884,11.7898564450668));
#93095=CARTESIAN_POINT('Ctrl Pts',(-2.24057772870709,0.781965413353284,
11.7952401662358));
#93096=CARTESIAN_POINT('Ctrl Pts',(-2.26447718931189,0.705224164068507,
11.8006238874048));
#93097=CARTESIAN_POINT('Ctrl Pts',(-2.2883555098361,0.628550795654401,11.8060028464455));
#93098=CARTESIAN_POINT('Ctrl Pts',(-2.30835673213667,0.550595334368634,
11.8113818054861));
#93099=CARTESIAN_POINT('Ctrl Pts',(-2.32435427522725,0.471778831374215,
11.8167607645267));
#93100=CARTESIAN_POINT('Ctrl Pts',(-2.34034131720126,0.393014065154663,
11.8221361927079));
#93101=CARTESIAN_POINT('Ctrl Pts',(-2.3523298160296,0.313389824482069,11.8275116208891));
#93102=CARTESIAN_POINT('Ctrl Pts',(-2.36024378681681,0.233339515069065,
11.8328870490703));
#93103=CARTESIAN_POINT('Ctrl Pts',(-2.36222728137341,0.213276343591111,
11.8342343035426));
#93104=CARTESIAN_POINT('Ctrl Pts',(-2.36395508028738,0.193186454362623,
11.8355815580149));
#93105=CARTESIAN_POINT('Ctrl Pts',(-2.36542649454111,0.173076750093539,
11.8369288124873));
#93106=CARTESIAN_POINT('Ctrl Pts',(-2.36516017494062,0.173060140022867,
10.8371116396001));
#93107=CARTESIAN_POINT('Ctrl Pts',(-2.36874872137079,0.116159691458484,
10.8409373761948));
#93108=CARTESIAN_POINT('Ctrl Pts',(-2.3703080243951,0.0590785852099101,
10.8447631127894));
#93109=CARTESIAN_POINT('Ctrl Pts',(-2.36986628361774,0.00196879943266851,
10.8485888493841));
#93110=CARTESIAN_POINT('',(-2.37530980438986,0.000525500814253238,10.6515288999801));
#93111=CARTESIAN_POINT('Ctrl Pts',(-2.36916488281964,0.173362644194442,
10.6397478783738));
#93112=CARTESIAN_POINT('Ctrl Pts',(-2.37143439054323,0.143717752018713,
10.641751811389));
#93113=CARTESIAN_POINT('Ctrl Pts',(-2.37467009649357,0.0861306150212709,
10.645639221296));
#93114=CARTESIAN_POINT('Ctrl Pts',(-2.37559956836887,0.0284615660624313,
10.6495266312031));
#93115=CARTESIAN_POINT('Ctrl Pts',(-2.37551677123795,0.000517782250847756,
10.651410108095));
#93116=CARTESIAN_POINT('Ctrl Pts',(-2.37174990865192,0.000658262564380199,
10.6535721582573));
#93117=CARTESIAN_POINT('Ctrl Pts',(-2.37177855672722,-0.102562053547647,
10.6603515320337));
#93118=CARTESIAN_POINT('Ctrl Pts',(-2.36506879052359,-0.205690967288313,
10.6668060514094));
#93119=CARTESIAN_POINT('Ctrl Pts',(-2.34197585620198,-0.38197192072136,
10.6777762038329));
#93120=CARTESIAN_POINT('Ctrl Pts',(-2.32881606256741,-0.455378403733495,
10.6823250941134));
#93121=CARTESIAN_POINT('Ctrl Pts',(-2.27881465861748,-0.674326638542228,
10.6961102588934));
#93122=CARTESIAN_POINT('Ctrl Pts',(-2.23160731925022,-0.817087733319469,
10.7054176415574));
#93123=CARTESIAN_POINT('Ctrl Pts',(-2.16230900018982,-0.974735953336503,
10.716647787053));
#93124=CARTESIAN_POINT('Ctrl Pts',(-2.15309571846237,-0.994921687018294,
10.7181039410699));
#93125=CARTESIAN_POINT('Ctrl Pts',(-2.13871840384251,-1.02528621285605,
10.7203235351299));
#93126=CARTESIAN_POINT('Ctrl Pts',(-2.13376170475477,-1.03556226698929,
10.7210798203346));
#93127=CARTESIAN_POINT('Ctrl Pts',(-2.1246515962004,-1.05410590289595,10.7224540779902));
#93128=CARTESIAN_POINT('Ctrl Pts',(-2.12052355982764,-1.0623857528218,10.7230711561611));
#93129=CARTESIAN_POINT('Ctrl Pts',(-2.11154677544505,-1.08013025387168,
10.7244011880773));
#93130=CARTESIAN_POINT('Ctrl Pts',(-2.10668262037068,-1.08958683951847,
10.7251146729013));
#93131=CARTESIAN_POINT('Ctrl Pts',(-2.09339287495878,-1.11500224390189,
10.7270450469932));
#93132=CARTESIAN_POINT('Ctrl Pts',(-2.08484860798215,-1.13089786593802,
10.7282661091733));
#93133=CARTESIAN_POINT('Ctrl Pts',(-2.04193293605268,-1.20859797680012,
10.7343041385278));
#93134=CARTESIAN_POINT('Ctrl Pts',(-2.0049938152364,-1.26893544663137,10.7392122268613));
#93135=CARTESIAN_POINT('Ctrl Pts',(-1.85958502749163,-1.48421459737501,
10.757562006479));
#93136=CARTESIAN_POINT('Ctrl Pts',(-1.73540061895271,-1.62767234238671,
10.7715377553805));
#93137=CARTESIAN_POINT('Ctrl Pts',(-1.55431056427747,-1.79232279465742,
10.7892498975896));
#93138=CARTESIAN_POINT('Ctrl Pts',(-1.5117757750581,-1.82834274679318,10.7932450418659));
#93139=CARTESIAN_POINT('Ctrl Pts',(-1.45150583049823,-1.87583857981293,
10.798644656267));
#93140=CARTESIAN_POINT('Ctrl Pts',(-1.43482995696554,-1.88862453060262,
10.8001123835859));
#93141=CARTESIAN_POINT('Ctrl Pts',(-1.40942806208962,-1.90757033221001,
10.8023062709012));
#93142=CARTESIAN_POINT('Ctrl Pts',(-1.40082720587638,-1.91389529079522,
10.8030420073151));
#93143=CARTESIAN_POINT('Ctrl Pts',(-1.38676238195868,-1.92409277318672,
10.8042332712554));
#93144=CARTESIAN_POINT('Ctrl Pts',(-1.38132431680734,-1.92800052861667,
10.8046910087846));
#93145=CARTESIAN_POINT('Ctrl Pts',(-1.37085666863622,-1.93545548475865,
10.8055665222849));
#93146=CARTESIAN_POINT('Ctrl Pts',(-1.36582969442947,-1.93900623707863,
10.8059845302999));
#93147=CARTESIAN_POINT('Ctrl Pts',(-1.36076363840581,-1.94255511732426,
10.806403288096));
#93148=CARTESIAN_POINT('Ctrl Pts',(-1.36073839288779,-1.9425728016142,10.8064053748164));
#93149=CARTESIAN_POINT('Ctrl Pts',(-1.36068774231298,-1.94260828047789,
10.8064095613193));
#93150=CARTESIAN_POINT('Ctrl Pts',(-1.36066233724572,-1.94262607504972,
10.8064116611019));
#93151=CARTESIAN_POINT('Ctrl Pts',(-1.36061136416369,-1.94266177683688,
10.8064158740086));
#93152=CARTESIAN_POINT('Ctrl Pts',(-1.36058579616253,-1.94267968403316,
10.8064179871308));
#93153=CARTESIAN_POINT('Ctrl Pts',(-1.36053449373456,-1.94271561347654,
10.8064222270018));
#93154=CARTESIAN_POINT('Ctrl Pts',(-1.36050875931149,-1.94273363571123,
10.8064243537494));
#93155=CARTESIAN_POINT('Ctrl Pts',(-1.36045712051414,-1.94276979767096,
10.8064286211599));
#93156=CARTESIAN_POINT('Ctrl Pts',(-1.36043121610644,-1.94278793740934,
10.8064307618248));
#93157=CARTESIAN_POINT('Ctrl Pts',(-1.36037923366798,-1.94282433691737,
10.8064350573708));
#93158=CARTESIAN_POINT('Ctrl Pts',(-1.36035315568065,-1.94284259664626,
10.8064372122475));
#93159=CARTESIAN_POINT('Ctrl Pts',(-1.36030082241604,-1.94287923867169,
10.8064415365173));
#93160=CARTESIAN_POINT('Ctrl Pts',(-1.36027456707164,-1.94289762100459,
10.8064437059152));
#93161=CARTESIAN_POINT('Ctrl Pts',(-1.36022187528905,-1.9429345108692,10.8064480595391));
#93162=CARTESIAN_POINT('Ctrl Pts',(-1.36019543884565,-1.94295301839363,
10.8064502437646));
#93163=CARTESIAN_POINT('Ctrl Pts',(-1.36014238094027,-1.94299016135598,
10.8064546273652));
#93164=CARTESIAN_POINT('Ctrl Pts',(-1.36011575949941,-1.94300879676787,
10.8064568267376));
#93165=CARTESIAN_POINT('Ctrl Pts',(-1.36006232760328,-1.94304619826841,
10.8064612409593));
#93166=CARTESIAN_POINT('Ctrl Pts',(-1.36003551718488,-1.94306496431968,
10.8064634558045));
#93167=CARTESIAN_POINT('Ctrl Pts',(-1.35998541134579,-1.94310003454148,
10.806467594985));
#93168=CARTESIAN_POINT('Ctrl Pts',(-1.35996211603031,-1.94311633884101,
10.8064695193288));
#93169=CARTESIAN_POINT('Ctrl Pts',(-1.35991474648953,-1.94314949132684,
10.8064734322516));
#93170=CARTESIAN_POINT('Ctrl Pts',(-1.35989067217942,-1.94316633953011,
10.8064754208341));
#93171=CARTESIAN_POINT('Ctrl Pts',(-1.35984171027439,-1.94320060375164,
10.8064794650627));
#93172=CARTESIAN_POINT('Ctrl Pts',(-1.35981682265666,-1.94321801974011,
10.8064815207069));
#93173=CARTESIAN_POINT('Ctrl Pts',(-1.35976619771028,-1.94325344488342,
10.8064857020559));
#93174=CARTESIAN_POINT('Ctrl Pts',(-1.35974046038036,-1.94327145398973,
10.8064878277565));
#93175=CARTESIAN_POINT('Ctrl Pts',(-1.3596880974565,-1.94330809219513,10.8064921523899));
#93176=CARTESIAN_POINT('Ctrl Pts',(-1.35966147181243,-1.94332672127587,
10.8064943513222));
#93177=CARTESIAN_POINT('Ctrl Pts',(-1.35960729133036,-1.94336462790497,
10.8064988257853));
#93178=CARTESIAN_POINT('Ctrl Pts',(-1.35957973645772,-1.94338390541973,
10.806501101314));
#93179=CARTESIAN_POINT('Ctrl Pts',(-1.35952365400987,-1.94342313917986,
10.806505732548));
#93180=CARTESIAN_POINT('Ctrl Pts',(-1.35949512643571,-1.94344309536184,
10.8065080882479));
#93181=CARTESIAN_POINT('Ctrl Pts',(-1.35943705237479,-1.94348371859161,
10.8065128836238));
#93182=CARTESIAN_POINT('Ctrl Pts',(-1.35940750584423,-1.94350438560208,
10.8065153232977));
#93183=CARTESIAN_POINT('Ctrl Pts',(-1.35934734466194,-1.94354646470216,
10.8065202906673));
#93184=CARTESIAN_POINT('Ctrl Pts',(-1.35931672999974,-1.94356787672531,
10.8065228183576));
#93185=CARTESIAN_POINT('Ctrl Pts',(-1.35925438013928,-1.94361148228545,
10.8065279660684));
#93186=CARTESIAN_POINT('Ctrl Pts',(-1.35922264490275,-1.94363367576899,
10.8065305860854));
#93187=CARTESIAN_POINT('Ctrl Pts',(-1.35915799801078,-1.94367888308644,
10.8065359230424));
#93188=CARTESIAN_POINT('Ctrl Pts',(-1.35912508628047,-1.9437018968854,10.8065386399813));
#93189=CARTESIAN_POINT('Ctrl Pts',(-1.35905802666991,-1.94374878633537,
10.8065441756904));
#93190=CARTESIAN_POINT('Ctrl Pts',(-1.35902387876052,-1.94377266191158,
10.8065469944551));
#93191=CARTESIAN_POINT('Ctrl Pts',(-1.3589542829551,-1.94382131925974,10.8065527390607));
#93192=CARTESIAN_POINT('Ctrl Pts',(-1.35891883499726,-1.94384610097105,
10.8065556648979));
#93193=CARTESIAN_POINT('Ctrl Pts',(-1.35884657077098,-1.94389661803854,
10.806561629261));
#93194=CARTESIAN_POINT('Ctrl Pts',(-1.35880975442627,-1.94392235333456,
10.8065646677836));
#93195=CARTESIAN_POINT('Ctrl Pts',(-1.35873468015481,-1.94397482844385,
10.8065708635353));
#93196=CARTESIAN_POINT('Ctrl Pts',(-1.35869642217958,-1.94400156816683,
10.8065740207579));
#93197=CARTESIAN_POINT('Ctrl Pts',(-1.35861838601825,-1.94405610670789,
10.8065804603662));
#93198=CARTESIAN_POINT('Ctrl Pts',(-1.35857860776842,-1.94408390543441,
10.8065837427457));
#93199=CARTESIAN_POINT('Ctrl Pts',(-1.35849744653652,-1.94414062063485,
10.8065904396068));
#93200=CARTESIAN_POINT('Ctrl Pts',(-1.35845606350983,-1.94416953699056,
10.8065938540795));
#93201=CARTESIAN_POINT('Ctrl Pts',(-1.35427288750917,-1.94709232899285,
10.8069389868935));
#93202=CARTESIAN_POINT('Ctrl Pts',(-1.3501219320337,-1.94997291280233,10.8072797771417));
#93203=CARTESIAN_POINT('Ctrl Pts',(-1.34042327662125,-1.9566575447366,10.8080721621889));
#93204=CARTESIAN_POINT('Ctrl Pts',(-1.33486856848885,-1.9604512785472,10.8085230579424));
#93205=CARTESIAN_POINT('Ctrl Pts',(-1.32000824304342,-1.97050808614307,
10.8097217575619));
#93206=CARTESIAN_POINT('Ctrl Pts',(-1.31067407003795,-1.97672895805159,
10.8104668286348));
#93207=CARTESIAN_POINT('Ctrl Pts',(-1.23701135038108,-2.02507117940273,
10.8162882146222));
#93208=CARTESIAN_POINT('Ctrl Pts',(-1.17070558587072,-2.06411276854797,
10.8211803458188));
#93209=CARTESIAN_POINT('Ctrl Pts',(-0.976450919664753,-2.16611333880979,
10.8348906635437));
#93210=CARTESIAN_POINT('Ctrl Pts',(-0.844572163153181,-2.22085670258079,
10.8434847809167));
#93211=CARTESIAN_POINT('Ctrl Pts',(-0.59548473626215,-2.29883408201945,
10.8596255141512));
#93212=CARTESIAN_POINT('Ctrl Pts',(-0.479918009171846,-2.32570702472925,
10.8670794224785));
#93213=CARTESIAN_POINT('Ctrl Pts',(-0.343099502869632,-2.34688723851706,
10.8761275621036));
#93214=CARTESIAN_POINT('Ctrl Pts',(-0.323324416631526,-2.34969322689631,
10.8774403677106));
#93215=CARTESIAN_POINT('Ctrl Pts',(-0.292659917557485,-2.35364994597511,
10.8794848910023));
#93216=CARTESIAN_POINT('Ctrl Pts',(-0.281793686033334,-2.35497562773259,
10.8802110890818));
#93217=CARTESIAN_POINT('Ctrl Pts',(-0.26264991655199,-2.35717677795537,
10.8814936418762));
#93218=CARTESIAN_POINT('Ctrl Pts',(-0.254376158224509,-2.3580839909304,
10.8820489862936));
#93219=CARTESIAN_POINT('Ctrl Pts',(-0.235477565867177,-2.36005559198576,
10.8833199321225));
#93220=CARTESIAN_POINT('Ctrl Pts',(-0.224850038448066,-2.36109180995202,
10.8840364077769));
#93221=CARTESIAN_POINT('Ctrl Pts',(-0.196053529897931,-2.36370337929788,
10.8859827443179));
#93222=CARTESIAN_POINT('Ctrl Pts',(-0.177873098454385,-2.36514096414576,
10.887216895677));
#93223=CARTESIAN_POINT('Ctrl Pts',(-0.086739341266469,-2.3712905071774,
10.8934314899476));
#93224=CARTESIAN_POINT('Ctrl Pts',(-0.0136194423552338,-2.37283688671384,
10.8985096179776));
#93225=CARTESIAN_POINT('Ctrl Pts',(0.2195631141867,-2.36699024645351,10.9150063657144));
#93226=CARTESIAN_POINT('Ctrl Pts',(0.378844997908836,-2.34676716671444,
10.9267627423823));
#93227=CARTESIAN_POINT('Ctrl Pts',(0.630116044658595,-2.28860518083762,
10.9455482804648));
#93228=CARTESIAN_POINT('Ctrl Pts',(0.723937916130801,-2.26068086315785,
10.9526083175941));
#93229=CARTESIAN_POINT('Ctrl Pts',(0.833504231121622,-2.22054615047882,
10.9607207934211));
#93230=CARTESIAN_POINT('Ctrl Pts',(0.851154649697953,-2.21384062855498,
10.9620233016448));
#93231=CARTESIAN_POINT('Ctrl Pts',(0.875742191003425,-2.20416210104155,
10.9638297776904));
#93232=CARTESIAN_POINT('Ctrl Pts',(0.882747486997461,-2.20136590119113,
10.9643435533696));
#93233=CARTESIAN_POINT('Ctrl Pts',(0.894672872541858,-2.19653974207446,
10.9652164705167));
#93234=CARTESIAN_POINT('Ctrl Pts',(0.899599651557467,-2.1945265677448,10.9655766029113));
#93235=CARTESIAN_POINT('Ctrl Pts',(0.909088931904526,-2.19061174274308,
10.9662692245031));
#93236=CARTESIAN_POINT('Ctrl Pts',(0.913652292164789,-2.18871240315491,
10.9666018549363));
#93237=CARTESIAN_POINT('Ctrl Pts',(0.924629923519784,-2.18410303167298,
10.9674010272745));
#93238=CARTESIAN_POINT('Ctrl Pts',(0.931038311020611,-2.18137897095283,
10.9678667298372));
#93239=CARTESIAN_POINT('Ctrl Pts',(0.954601457577117,-2.17124005563474,
10.9695763584362));
#93240=CARTESIAN_POINT('Ctrl Pts',(0.971680963947044,-2.16365049862781,
10.9708102298911));
#93241=CARTESIAN_POINT('Ctrl Pts',(1.12509251781218,-2.09329649848442,10.9818604945114));
#93242=CARTESIAN_POINT('Ctrl Pts',(1.25528997691375,-2.01791570185769,10.9910179840959));
#93243=CARTESIAN_POINT('Ctrl Pts',(1.5207523723073,-1.82851758322732,11.0110010064882));
#93244=CARTESIAN_POINT('Ctrl Pts',(1.65216231956746,-1.71070528831344,11.0218081618593));
#93245=CARTESIAN_POINT('Ctrl Pts',(1.78347217173396,-1.56360997290639,11.0346784623678));
#93246=CARTESIAN_POINT('Ctrl Pts',(1.7974019591043,-1.54757723034504,11.0360731839114));
#93247=CARTESIAN_POINT('Ctrl Pts',(1.81835426685494,-1.52279728181172,11.0382178780451));
#93248=CARTESIAN_POINT('Ctrl Pts',(1.82553341708056,-1.51418345555346,11.0389614206063));
#93249=CARTESIAN_POINT('Ctrl Pts',(1.8379479943042,-1.49907133394873,11.0402626374283));
#93250=CARTESIAN_POINT('Ctrl Pts',(1.84321075281791,-1.49259566248446,11.040819191603));
#93251=CARTESIAN_POINT('Ctrl Pts',(1.85499633158649,-1.47793646289439,11.0420768589956));
#93252=CARTESIAN_POINT('Ctrl Pts',(1.86149934665385,-1.46973730811498,11.0427787505235));
#93253=CARTESIAN_POINT('Ctrl Pts',(1.87888411045545,-1.44751771776724,11.0446769001864));
#93254=CARTESIAN_POINT('Ctrl Pts',(1.8896629184369,-1.43341796715046,11.0458771922744));
#93255=CARTESIAN_POINT('Ctrl Pts',(1.93899187717406,-1.36736736419656,11.0514818078453));
#93256=CARTESIAN_POINT('Ctrl Pts',(1.97556114519041,-1.3139786028395,11.0559615453137));
#93257=CARTESIAN_POINT('Ctrl Pts',(2.12413037728108,-1.07683018355432,11.0756627160543));
#93258=CARTESIAN_POINT('Ctrl Pts',(2.21300974533638,-0.879804498679115,
11.0916583939711));
#93259=CARTESIAN_POINT('Ctrl Pts',(2.28632543187786,-0.632272086991002,
11.1102057817263));
#93260=CARTESIAN_POINT('Ctrl Pts',(2.29742756513531,-0.59065981831843,11.1132694871275));
#93261=CARTESIAN_POINT('Ctrl Pts',(2.31346054361505,-0.523246091727197,
11.1181233129115));
#93262=CARTESIAN_POINT('Ctrl Pts',(2.319106438672,-0.497625994748596,11.1199428559617));
#93263=CARTESIAN_POINT('Ctrl Pts',(2.32603031119974,-0.463523880779648,
11.1223269979846));
#93264=CARTESIAN_POINT('Ctrl Pts',(2.32768879956987,-0.455122241550293,
11.1229113453561));
#93265=CARTESIAN_POINT('Ctrl Pts',(2.33034395619426,-0.441277379507445,
11.1238690959426));
#93266=CARTESIAN_POINT('Ctrl Pts',(2.33136712796991,-0.435839415464244,
11.124243967043));
#93267=CARTESIAN_POINT('Ctrl Pts',(2.33333686830551,-0.42516518513809,11.1249771653168));
#93268=CARTESIAN_POINT('Ctrl Pts',(2.33428485943968,-0.419929245928414,
11.1253355673542));
#93269=CARTESIAN_POINT('Ctrl Pts',(2.33658141546411,-0.406996811739778,
11.1262178177399));
#93270=CARTESIAN_POINT('Ctrl Pts',(2.33790959851112,-0.399296668401241,
11.1267405206304));
#93271=CARTESIAN_POINT('Ctrl Pts',(2.34236875254388,-0.372659489656154,
11.1285401726563));
#93272=CARTESIAN_POINT('Ctrl Pts',(2.34530798860914,-0.353690493072396,
11.1298068562175));
#93273=CARTESIAN_POINT('Ctrl Pts',(2.36677574686537,-0.203082220411515,
11.1397611699796));
#93274=CARTESIAN_POINT('Ctrl Pts',(2.37443966949902,-0.0701137673008996,
11.1479364903347));
#93275=CARTESIAN_POINT('Ctrl Pts',(2.36744621573709,0.193863576813738,11.1641290464489));
#93276=CARTESIAN_POINT('Ctrl Pts',(2.35311514737728,0.324393138668978,11.1721235850249));
#93277=CARTESIAN_POINT('Ctrl Pts',(2.31505593657268,0.519959955708822,11.1847100432378));
#93278=CARTESIAN_POINT('Ctrl Pts',(2.2991617468733,0.586256108800425,11.1890835433532));
#93279=CARTESIAN_POINT('Ctrl Pts',(2.27567736287208,0.668423934099408,11.1946842220737));
#93280=CARTESIAN_POINT('Ctrl Pts',(2.27073580381394,0.685023283094217,11.1958249652052));
#93281=CARTESIAN_POINT('Ctrl Pts',(2.26254527836951,0.71147345789522,11.1976582764114));
#93282=CARTESIAN_POINT('Ctrl Pts',(2.25941265103047,0.721359885563684,11.198347032247));
#93283=CARTESIAN_POINT('Ctrl Pts',(2.25335188690899,0.740060535785525,11.1996566594698));
#93284=CARTESIAN_POINT('Ctrl Pts',(2.25043661090854,0.748878747803039,11.2002770971877));
#93285=CARTESIAN_POINT('Ctrl Pts',(2.24369713021494,0.768869757562372,11.2016903249018));
#93286=CARTESIAN_POINT('Ctrl Pts',(2.23984114709551,0.78003150143302,11.2024841530864));
#93287=CARTESIAN_POINT('Ctrl Pts',(2.22963599977951,0.808872190675591,11.2045479311926));
#93288=CARTESIAN_POINT('Ctrl Pts',(2.22315997791522,0.826505045049896,11.2058220598898));
#93289=CARTESIAN_POINT('Ctrl Pts',(2.17269392282489,0.959027545669819,11.2154937460931));
#93290=CARTESIAN_POINT('Ctrl Pts',(2.12004130056399,1.07039650467926,11.2241831913187));
#93291=CARTESIAN_POINT('Ctrl Pts',(2.0222061583261,1.24152155047438,11.2384173882982));
#93292=CARTESIAN_POINT('Ctrl Pts',(1.98241694261831,1.30411496245312,11.2438289013861));
#93293=CARTESIAN_POINT('Ctrl Pts',(1.86050162841416,1.47739843223089,11.2593049109378));
#93294=CARTESIAN_POINT('Ctrl Pts',(1.7715662487696,1.58295115751608,11.2693599836763));
#93295=CARTESIAN_POINT('Ctrl Pts',(1.66449802284079,1.68962208789066,11.2797958728282));
#93296=CARTESIAN_POINT('Ctrl Pts',(1.6549560191809,1.69896941212699,11.2807127519123));
#93297=CARTESIAN_POINT('Ctrl Pts',(1.6406107325798,1.71278647700723,11.282070992248));
#93298=CARTESIAN_POINT('Ctrl Pts',(1.63586725167142,1.71731750972871,11.2825168772102));
#93299=CARTESIAN_POINT('Ctrl Pts',(1.62733861081879,1.72539677278599,11.2833126902217));
#93300=CARTESIAN_POINT('Ctrl Pts',(1.62356056461951,1.72895230487403,11.2836631717741));
#93301=CARTESIAN_POINT('Ctrl Pts',(1.61528659344259,1.73668793039233,11.2844262602746));
#93302=CARTESIAN_POINT('Ctrl Pts',(1.61078610150729,1.74086297102386,11.2848384847793));
#93303=CARTESIAN_POINT('Ctrl Pts',(1.59817196586284,1.75247412362819,11.2859861380486));
#93304=CARTESIAN_POINT('Ctrl Pts',(1.59002256790987,1.75987142476776,11.2867187027113));
#93305=CARTESIAN_POINT('Ctrl Pts',(1.54449145517604,1.80062607637464,11.2907645736694));
#93306=CARTESIAN_POINT('Ctrl Pts',(1.50610847805551,1.83285194131579,11.2940009934202));
#93307=CARTESIAN_POINT('Ctrl Pts',(1.30102694656459,1.99423877474508,11.3105843018611));
#93308=CARTESIAN_POINT('Ctrl Pts',(1.11866633077756,2.10196591509147,11.3230613631996));
#93309=CARTESIAN_POINT('Ctrl Pts',(0.848706595088635,2.21622653481581,11.3414479702813));
#93310=CARTESIAN_POINT('Ctrl Pts',(0.771354097194692,2.24432027448511,11.3466963436107));
#93311=CARTESIAN_POINT('Ctrl Pts',(0.675197604079128,2.2736845301268,11.3532783993091));
#93312=CARTESIAN_POINT('Ctrl Pts',(0.657629539709259,2.27882787951193,11.3544831292475));
#93313=CARTESIAN_POINT('Ctrl Pts',(0.629809855633368,2.28662408200232,11.356395069229));
#93314=CARTESIAN_POINT('Ctrl Pts',(0.619596740980551,2.28941259257102,11.3570978640954));
#93315=CARTESIAN_POINT('Ctrl Pts',(0.600419709634012,2.29451082299095,11.3584193085699));
#93316=CARTESIAN_POINT('Ctrl Pts',(0.591460246160596,2.29683663275421,11.3590374234211));
#93317=CARTESIAN_POINT('Ctrl Pts',(0.57136509858727,2.3019278084078,11.3604255549814));
#93318=CARTESIAN_POINT('Ctrl Pts',(0.560222563250849,2.30466491763578,11.3611964673644));
#93319=CARTESIAN_POINT('Ctrl Pts',(0.531860436445721,2.31141410039507,11.3631620169667));
#93320=CARTESIAN_POINT('Ctrl Pts',(0.514615287644154,2.31531461004938,11.3643601978426));
#93321=CARTESIAN_POINT('Ctrl Pts',(0.408761535603934,2.33801560008784,11.3717349708054));
#93322=CARTESIAN_POINT('Ctrl Pts',(0.319190585564614,2.35191763971444,11.3780657518827));
#93323=CARTESIAN_POINT('Ctrl Pts',(0.0211372339985953,2.38083756738751,
11.3994253363191));
#93324=CARTESIAN_POINT('Ctrl Pts',(-0.188506739709662,2.37345469328646,
11.4150076524176));
#93325=CARTESIAN_POINT('Ctrl Pts',(-0.42283064741599,2.33393231051761,11.4318773788699));
#93326=CARTESIAN_POINT('Ctrl Pts',(-0.451112161884432,2.32863130775204,
11.4339022048689));
#93327=CARTESIAN_POINT('Ctrl Pts',(-0.498398188326327,2.31887427747176,
11.4372613320045));
#93328=CARTESIAN_POINT('Ctrl Pts',(-0.517456236963645,2.31469604352611,
11.4386079390715));
#93329=CARTESIAN_POINT('Ctrl Pts',(-0.543904654977684,2.30855456494735,
11.4404646187811));
#93330=CARTESIAN_POINT('Ctrl Pts',(-0.551339724609984,2.30679018664924,
11.4409852210558));
#93331=CARTESIAN_POINT('Ctrl Pts',(-0.563956642936235,2.30373164464393,
11.4418662265307));
#93332=CARTESIAN_POINT('Ctrl Pts',(-0.569142845125659,2.30245586487086,
11.4422276651516));
#93333=CARTESIAN_POINT('Ctrl Pts',(-0.57909769858926,2.29997132972138,11.4429200426354));
#93334=CARTESIAN_POINT('Ctrl Pts',(-0.583866933553731,2.29876524836399,
11.4432511379014));
#93335=CARTESIAN_POINT('Ctrl Pts',(-0.595292538389803,2.2958380005397,11.444042944065));
#93336=CARTESIAN_POINT('Ctrl Pts',(-0.601945292991285,2.29410270000961,
11.4445028493042));
#93337=CARTESIAN_POINT('Ctrl Pts',(-0.626015994683947,2.28771219491465,
11.4461630490712));
#93338=CARTESIAN_POINT('Ctrl Pts',(-0.64338881346191,2.28288720608032,11.4473540451668));
#93339=CARTESIAN_POINT('Ctrl Pts',(-0.817337143860965,2.23243265314062,
11.4592219516021));
#93340=CARTESIAN_POINT('Ctrl Pts',(-0.968890003654601,2.17095925573655,
11.4691145955441));
#93341=CARTESIAN_POINT('Ctrl Pts',(-1.25812779523953,2.0172606012759,11.4891947057542));
#93342=CARTESIAN_POINT('Ctrl Pts',(-1.39486856756935,1.92524203110561,11.499343595851));
#93343=CARTESIAN_POINT('Ctrl Pts',(-1.53703297539754,1.8064232512149,11.5114411077934));
#93344=CARTESIAN_POINT('Ctrl Pts',(-1.55289935963413,1.79280195859577,11.5128146386954));
#93345=CARTESIAN_POINT('Ctrl Pts',(-1.57694263880225,1.77160215253361,11.5149334510505));
#93346=CARTESIAN_POINT('Ctrl Pts',(-1.58524994161057,1.76417257896049,11.5156725441102));
#93347=CARTESIAN_POINT('Ctrl Pts',(-1.59968032694304,1.75108264797422,11.5169689112878));
#93348=CARTESIAN_POINT('Ctrl Pts',(-1.60582654567861,1.74544799137146,11.5175250934476));
#93349=CARTESIAN_POINT('Ctrl Pts',(-1.6196565730175,1.73263418752943,11.5187858389059));
#93350=CARTESIAN_POINT('Ctrl Pts',(-1.62732256226536,1.72543615195478,11.5194912036206));
#93351=CARTESIAN_POINT('Ctrl Pts',(-1.64796510647271,1.70579375062703,11.5214085604858));
#93352=CARTESIAN_POINT('Ctrl Pts',(-1.66084821713925,1.69325263335334,11.5226247280902));
#93353=CARTESIAN_POINT('Ctrl Pts',(-1.72095515472534,1.63339531856916,11.5283932516556));
#93354=CARTESIAN_POINT('Ctrl Pts',(-1.76630308487858,1.58424707079025,11.5330263867347));
#93355=CARTESIAN_POINT('Ctrl Pts',(-1.94707024446076,1.37090971740908,11.5527365772127));
#93356=CARTESIAN_POINT('Ctrl Pts',(-2.06214801574062,1.19079725388771,11.5685542276648));
#93357=CARTESIAN_POINT('Ctrl Pts',(-2.16969885759295,0.958877706868799,
11.5869189200287));
#93358=CARTESIAN_POINT('Ctrl Pts',(-2.18669386321987,0.919461798898741,
11.5899720803374));
#93359=CARTESIAN_POINT('Ctrl Pts',(-2.21231607607138,0.855301382189059,
11.5948111416863));
#93360=CARTESIAN_POINT('Ctrl Pts',(-2.22161890366568,0.830838411411903,
11.5966262597013));
#93361=CARTESIAN_POINT('Ctrl Pts',(-2.23342380052921,0.798178797977387,
11.5990055486539));
#93362=CARTESIAN_POINT('Ctrl Pts',(-2.23628869706746,0.790116532790123,
11.5995893693795));
#93363=CARTESIAN_POINT('Ctrl Pts',(-2.2409339050709,0.776816512772163,11.6005464813377));
#93364=CARTESIAN_POINT('Ctrl Pts',(-2.24273960143134,0.77158780653715,11.6009212366968));
#93365=CARTESIAN_POINT('Ctrl Pts',(-2.24624670962633,0.761316036843849,
11.6016543986206));
#93366=CARTESIAN_POINT('Ctrl Pts',(-2.24794946250798,0.756273497769942,
11.6020128790296));
#93367=CARTESIAN_POINT('Ctrl Pts',(-2.25211206999747,0.743808063695026,
11.6028956137971));
#93368=CARTESIAN_POINT('Ctrl Pts',(-2.25455224422846,0.736378566939867,
11.6034187198306));
#93369=CARTESIAN_POINT('Ctrl Pts',(-2.26286603288817,0.710637175936623,
11.6052212001177));
#93370=CARTESIAN_POINT('Ctrl Pts',(-2.268553841912,0.692265414048133,11.6064902657382));
#93371=CARTESIAN_POINT('Ctrl Pts',(-2.30894440194742,0.555955919685495,
11.6157922643299));
#93372=CARTESIAN_POINT('Ctrl Pts',(-2.33465867338339,0.4355321568156,11.6233886281484));
#93373=CARTESIAN_POINT('Ctrl Pts',(-2.35715246984246,0.266929441770081,
11.6338307018606));
#93374=CARTESIAN_POINT('Ctrl Pts',(-2.36198927731126,0.220052949231025,
11.636712856545));
#93375=CARTESIAN_POINT('Ctrl Pts',(-2.36542649946083,0.173076682856166,
11.6396027579113));
#93376=CARTESIAN_POINT('Origin',(0.,0.,-1.84858989190503));
#93377=CARTESIAN_POINT('',(-2.36542647041237,0.173077079858841,12.8360489723836));
#93378=CARTESIAN_POINT('',(-2.36542649456986,0.173076749700613,12.6375766332401));
#93379=CARTESIAN_POINT('',(-2.36542649454111,0.173076750093529,-1.84858989190503));
#93380=CARTESIAN_POINT('',(-2.37174963818669,-0.00131006156719779,11.848589891905));
#93381=CARTESIAN_POINT('Ctrl Pts',(-2.36542647041237,0.173077079858945,
12.8360489723835));
#93382=CARTESIAN_POINT('Ctrl Pts',(-2.35606773494392,0.300981945279007,
12.8281521841122));
#93383=CARTESIAN_POINT('Ctrl Pts',(-2.3363431353734,0.428017049067247,12.8203717055505));
#93384=CARTESIAN_POINT('Ctrl Pts',(-2.28464375495091,0.643667315178936,
12.8065390961138));
#93385=CARTESIAN_POINT('Ctrl Pts',(-2.25755720211513,0.733032737755073,
12.800615170079));
#93386=CARTESIAN_POINT('Ctrl Pts',(-2.21917847626778,0.837111715874048,
12.7933629177622));
#93387=CARTESIAN_POINT('Ctrl Pts',(-2.21289219884968,0.853590781881691,
12.7922039820895));
#93388=CARTESIAN_POINT('Ctrl Pts',(-2.20225036896525,0.880579787429406,
12.7902875255786));
#93389=CARTESIAN_POINT('Ctrl Pts',(-2.19800187463305,0.891131416285915,
12.789533600331));
#93390=CARTESIAN_POINT('Ctrl Pts',(-2.19020719438395,0.910095515251465,
12.7881699665518));
#93391=CARTESIAN_POINT('Ctrl Pts',(-2.18668800523133,0.918518897451735,
12.7875611820615));
#93392=CARTESIAN_POINT('Ctrl Pts',(-2.17906042183177,0.936483665279753,
12.7862560801617));
#93393=CARTESIAN_POINT('Ctrl Pts',(-2.17493780693871,0.946018766890751,
12.7855592881573));
#93394=CARTESIAN_POINT('Ctrl Pts',(-2.16357194478324,0.971839589622956,
12.7836610889731));
#93395=CARTESIAN_POINT('Ctrl Pts',(-2.15620766256164,0.988070965971559,
12.7824555578848));
#93396=CARTESIAN_POINT('Ctrl Pts',(-2.1159048721436,1.07430433019118,12.7759835140258));
#93397=CARTESIAN_POINT('Ctrl Pts',(-2.07974251957415,1.14273877256405,12.7706061953141));
#93398=CARTESIAN_POINT('Ctrl Pts',(-1.94880486517025,1.36365799016943,12.7524168287233));
#93399=CARTESIAN_POINT('Ctrl Pts',(-1.8400835003389,1.50714380891038,12.739166396794));
#93400=CARTESIAN_POINT('Ctrl Pts',(-1.65761357994921,1.69844996953126,12.7200089406634));
#93401=CARTESIAN_POINT('Ctrl Pts',(-1.59571137233223,1.75673666041239,12.7139331338335));
#93402=CARTESIAN_POINT('Ctrl Pts',(-1.52132145846156,1.81959702240994,12.7072155350567));
#93403=CARTESIAN_POINT('Ctrl Pts',(-1.51177224445391,1.82753850895172,12.7063636368404));
#93404=CARTESIAN_POINT('Ctrl Pts',(-1.49720938408593,1.83945727371353,12.7050807199793));
#93405=CARTESIAN_POINT('Ctrl Pts',(-1.49224148378928,1.84348972281503,12.7046459012025));
#93406=CARTESIAN_POINT('Ctrl Pts',(-1.48327676998334,1.8507064051526,12.7038664240597));
#93407=CARTESIAN_POINT('Ctrl Pts',(-1.4792859518208,1.8538978528328,12.7035212568702));
#93408=CARTESIAN_POINT('Ctrl Pts',(-1.47050864244129,1.86087065690813,12.7027661165795));
#93409=CARTESIAN_POINT('Ctrl Pts',(-1.4657178742443,1.86464645026411,12.7023565382014));
#93410=CARTESIAN_POINT('Ctrl Pts',(-1.45194618439726,1.87541459067877,12.7011863685152));
#93411=CARTESIAN_POINT('Ctrl Pts',(-1.44292926979051,1.88236094961915,12.7004289491399));
#93412=CARTESIAN_POINT('Ctrl Pts',(-1.37969775193045,1.93035124743972,12.6951753731801));
#93413=CARTESIAN_POINT('Ctrl Pts',(-1.32378416836302,1.96911637460261,12.6908240028276));
#93414=CARTESIAN_POINT('Ctrl Pts',(-1.17005891447933,2.06618221427086,12.679400865298));
#93415=CARTESIAN_POINT('Ctrl Pts',(-1.06958912676756,2.11993603110896,12.672479844408));
#93416=CARTESIAN_POINT('Ctrl Pts',(-0.82255275993492,2.23005571265998,12.6558891548033));
#93417=CARTESIAN_POINT('Ctrl Pts',(-0.673516270180621,2.27949717173543,
12.6461870604574));
#93418=CARTESIAN_POINT('Ctrl Pts',(-0.50242712754327,2.31799829278613,12.6347358987047));
#93419=CARTESIAN_POINT('Ctrl Pts',(-0.484100493126899,2.32189486912513,
12.6335058811391));
#93420=CARTESIAN_POINT('Ctrl Pts',(-0.454250284891734,2.32787280823238,
12.6314960258739));
#93421=CARTESIAN_POINT('Ctrl Pts',(-0.442753842407921,2.33008672785577,
12.6307204181275));
#93422=CARTESIAN_POINT('Ctrl Pts',(-0.422232100826143,2.33388133006991,
12.6293329739657));
#93423=CARTESIAN_POINT('Ctrl Pts',(-0.413213082437357,2.33549501268254,
12.6287222016824));
#93424=CARTESIAN_POINT('Ctrl Pts',(-0.394151465843454,2.33879164707092,
12.6274291042052));
#93425=CARTESIAN_POINT('Ctrl Pts',(-0.384106951172826,2.34046226008409,
12.6267464001119));
#93426=CARTESIAN_POINT('Ctrl Pts',(-0.357376503131531,2.3447313847967,12.6249259585009));
#93427=CARTESIAN_POINT('Ctrl Pts',(-0.340673302158004,2.34721641679052,
12.6237846534411));
#93428=CARTESIAN_POINT('Ctrl Pts',(-0.259814788672728,2.35836495300144,
12.618240506892));
#93429=CARTESIAN_POINT('Ctrl Pts',(-0.19535506929162,2.36457691001498,12.6137613558711));
#93430=CARTESIAN_POINT('Ctrl Pts',(-0.00485393088076005,2.37509301603323,
12.6003388772199));
#93431=CARTESIAN_POINT('Ctrl Pts',(0.121358647631846,2.37199399727277,12.5911966475466));
#93432=CARTESIAN_POINT('Ctrl Pts',(0.388785252323727,2.34402424437078,12.571560140891));
#93433=CARTESIAN_POINT('Ctrl Pts',(0.529238990277415,2.31635868357233,12.5610858361816));
#93434=CARTESIAN_POINT('Ctrl Pts',(0.684493093102304,2.2709082493408,12.5498341333594));
#93435=CARTESIAN_POINT('Ctrl Pts',(0.702563347279203,2.2653829413902,12.5485300207484));
#93436=CARTESIAN_POINT('Ctrl Pts',(0.72790197640617,2.25730282832479,12.5467109541578));
#93437=CARTESIAN_POINT('Ctrl Pts',(0.735226307769165,2.25492785396476,12.5461862754249));
#93438=CARTESIAN_POINT('Ctrl Pts',(0.747520226384744,2.25087518130282,12.5453076664023));
#93439=CARTESIAN_POINT('Ctrl Pts',(0.752496001043641,2.24921660604805,12.5449526343317));
#93440=CARTESIAN_POINT('Ctrl Pts',(0.76263239081832,2.24580044050981,12.5442306053293));
#93441=CARTESIAN_POINT('Ctrl Pts',(0.767792511293143,2.24404154223208,12.5438636878979));
#93442=CARTESIAN_POINT('Ctrl Pts',(0.780913427851679,2.2395185405404,12.5429322405364));
#93443=CARTESIAN_POINT('Ctrl Pts',(0.788865726378963,2.23672974370719,12.5423691516418));
#93444=CARTESIAN_POINT('Ctrl Pts',(0.821028324450116,2.22525775496071,12.5400969700308));
#93445=CARTESIAN_POINT('Ctrl Pts',(0.845112589981845,2.21622301019967,12.5384074654129));
#93446=CARTESIAN_POINT('Ctrl Pts',(1.05600421064026,2.13317299647554,12.5236793870371));
#93447=CARTESIAN_POINT('Ctrl Pts',(1.23287404369968,2.03607888089212,12.5117313107034));
#93448=CARTESIAN_POINT('Ctrl Pts',(1.49074142258947,1.84845630951112,12.4920147250766));
#93449=CARTESIAN_POINT('Ctrl Pts',(1.58076641462966,1.77208143429755,12.4846005599742));
#93450=CARTESIAN_POINT('Ctrl Pts',(1.67789638566955,1.67636610087405,12.4756936648348));
#93451=CARTESIAN_POINT('Ctrl Pts',(1.6909070854809,1.66324164860357,12.4744801846674));
#93452=CARTESIAN_POINT('Ctrl Pts',(1.71185400983552,1.64161176466272,12.4724920311026));
#93453=CARTESIAN_POINT('Ctrl Pts',(1.7198835383517,1.63319745995434,12.471721435965));
#93454=CARTESIAN_POINT('Ctrl Pts',(1.73412126837785,1.61805601823492,12.4703395612563));
#93455=CARTESIAN_POINT('Ctrl Pts',(1.74035306812792,1.61135131048464,12.4697293133933));
#93456=CARTESIAN_POINT('Ctrl Pts',(1.7534645154553,1.59708009659783,12.4684337546282));
#93457=CARTESIAN_POINT('Ctrl Pts',(1.76033433176788,1.58950485265617,12.4677480439879));
#93458=CARTESIAN_POINT('Ctrl Pts',(1.77855096422581,1.56915470088022,12.465911041696));
#93459=CARTESIAN_POINT('Ctrl Pts',(1.78980890449678,1.55630140599897,12.4647560668156));
#93460=CARTESIAN_POINT('Ctrl Pts',(1.8446541315599,1.49230189122682,12.4590298785491));
#93461=CARTESIAN_POINT('Ctrl Pts',(1.88618897482562,1.43944551079255,12.4543761387991));
#93462=CARTESIAN_POINT('Ctrl Pts',(2.02113660601206,1.25182860022656,12.4380949475774));
#93463=CARTESIAN_POINT('Ctrl Pts',(2.10278865374118,1.10920459075496,12.4260786076668));
#93464=CARTESIAN_POINT('Ctrl Pts',(2.21422658430922,0.857239424342937,12.4059936371435));
#93465=CARTESIAN_POINT('Ctrl Pts',(2.25212017600938,0.752076971148706,12.3979248669931));
#93466=CARTESIAN_POINT('Ctrl Pts',(2.28590605106344,0.632448935515872,12.3893479250914));
#93467=CARTESIAN_POINT('Ctrl Pts',(2.2892473344159,0.620245749674566,12.3884798672354));
#93468=CARTESIAN_POINT('Ctrl Pts',(2.29414390523984,0.601783500918453,12.3871775289299));
#93469=CARTESIAN_POINT('Ctrl Pts',(2.2957715147325,0.59554411640029,12.3867392788263));
#93470=CARTESIAN_POINT('Ctrl Pts',(2.29864398228552,0.584345825407138,12.3859561809711));
#93471=CARTESIAN_POINT('Ctrl Pts',(2.29989826553795,0.579389481063552,12.3856108023295));
#93472=CARTESIAN_POINT('Ctrl Pts',(2.30260404487247,0.568550250927201,12.3848581481269));
#93473=CARTESIAN_POINT('Ctrl Pts',(2.30404902610744,0.562665853478704,12.3844512487079));
#93474=CARTESIAN_POINT('Ctrl Pts',(2.30809865683415,0.545897333012012,12.3832963934355));
#93475=CARTESIAN_POINT('Ctrl Pts',(2.31064888673934,0.535000039638957,12.3825514812315));
#93476=CARTESIAN_POINT('Ctrl Pts',(2.32711912547624,0.462306330343109,12.3776169731133));
#93477=CARTESIAN_POINT('Ctrl Pts',(2.33863719708616,0.399985348311733,12.3735528005308));
#93478=CARTESIAN_POINT('Ctrl Pts',(2.37728317734301,0.130982429178014,12.3564287251144));
#93479=CARTESIAN_POINT('Ctrl Pts',(2.37960264702573,-0.0783174123443216,
12.3440742507437));
#93480=CARTESIAN_POINT('Ctrl Pts',(2.34591034384298,-0.356435490283239,
12.3264204073041));
#93481=CARTESIAN_POINT('Ctrl Pts',(2.33406101627076,-0.427199238427661,
12.32182770077));
#93482=CARTESIAN_POINT('Ctrl Pts',(2.31525624335746,-0.514888038666354,
12.3159560017653));
#93483=CARTESIAN_POINT('Ctrl Pts',(2.31128761459492,-0.532419663290725,
12.3147730170809));
#93484=CARTESIAN_POINT('Ctrl Pts',(2.30467974237471,-0.560142961923467,
12.3128871800042));
#93485=CARTESIAN_POINT('Ctrl Pts',(2.30217120102222,-0.570365328364844,
12.3121885351723));
#93486=CARTESIAN_POINT('Ctrl Pts',(2.29758651514182,-0.588524913025164,
12.3109414253755));
#93487=CARTESIAN_POINT('Ctrl Pts',(2.29553706142036,-0.59646874565259,12.3103938314597));
#93488=CARTESIAN_POINT('Ctrl Pts',(2.29069739161007,-0.614833226718215,
12.3091230737177));
#93489=CARTESIAN_POINT('Ctrl Pts',(2.28787722908984,-0.62524572331864,12.3083989486524));
#93490=CARTESIAN_POINT('Ctrl Pts',(2.27971428742474,-0.654589776074706,
12.3063478230348));
#93491=CARTESIAN_POINT('Ctrl Pts',(2.27420698443403,-0.673474244801376,
12.3050155035089));
#93492=CARTESIAN_POINT('Ctrl Pts',(2.23483163110694,-0.802498137360569,
12.2958257456054));
#93493=CARTESIAN_POINT('Ctrl Pts',(2.19321637907314,-0.910093476021869,
12.2877138794145));
#93494=CARTESIAN_POINT('Ctrl Pts',(2.09129036916141,-1.12555323577651,12.2705542391789));
#93495=CARTESIAN_POINT('Ctrl Pts',(2.03003559349758,-1.23260631517048,12.2615050221484));
#93496=CARTESIAN_POINT('Ctrl Pts',(1.90464445431768,-1.41685284445431,12.24529276088));
#93497=CARTESIAN_POINT('Ctrl Pts',(1.84338731891017,-1.49568398995831,12.2381178430359));
#93498=CARTESIAN_POINT('Ctrl Pts',(1.76900299540287,-1.57986867898435,12.2303673485928));
#93499=CARTESIAN_POINT('Ctrl Pts',(1.76058954843799,-1.58923915760572,12.2295033946705));
#93500=CARTESIAN_POINT('Ctrl Pts',(1.74776416978858,-1.60329656791619,12.2282059854648));
#93501=CARTESIAN_POINT('Ctrl Pts',(1.74340730599584,-1.60803309847282,12.2277686038911));
#93502=CARTESIAN_POINT('Ctrl Pts',(1.73555516583002,-1.61650006496254,12.2269864263259));
#93503=CARTESIAN_POINT('Ctrl Pts',(1.73206707478199,-1.62023697147171,12.2266411050223));
#93504=CARTESIAN_POINT('Ctrl Pts',(1.72441117933843,-1.62838600526204,12.2258878387564));
#93505=CARTESIAN_POINT('Ctrl Pts',(1.72023851783465,-1.6327934166372,12.2254802745631));
#93506=CARTESIAN_POINT('Ctrl Pts',(1.70829116152186,-1.64531628372208,12.2243216262572));
#93507=CARTESIAN_POINT('Ctrl Pts',(1.70047550841215,-1.65339270102136,12.2235736173354));
#93508=CARTESIAN_POINT('Ctrl Pts',(1.64745543957182,-1.70740809577045,12.2185631966282));
#93509=CARTESIAN_POINT('Ctrl Pts',(1.60044747670877,-1.7515482964563,12.2144306823717));
#93510=CARTESIAN_POINT('Ctrl Pts',(1.38441620311257,-1.93843036952047,12.1964443020986));
#93511=CARTESIAN_POINT('Ctrl Pts',(1.1977177272017,-2.05902993834745,12.1833703320896));
#93512=CARTESIAN_POINT('Ctrl Pts',(0.942756714893098,-2.17714994840492,
12.1655455347075));
#93513=CARTESIAN_POINT('Ctrl Pts',(0.887585217542133,-2.20021899945823,
12.1616979643798));
#93514=CARTESIAN_POINT('Ctrl Pts',(0.815566149410654,-2.22718279675057,
12.1566572614387));
#93515=CARTESIAN_POINT('Ctrl Pts',(0.799463421086969,-2.23301356174213,
12.1555291278441));
#93516=CARTESIAN_POINT('Ctrl Pts',(0.773638538234104,-2.24204956037999,
12.1537175022365));
#93517=CARTESIAN_POINT('Ctrl Pts',(0.763956123348106,-2.24536719826278,
12.1530377500073));
#93518=CARTESIAN_POINT('Ctrl Pts',(0.746443533552262,-2.25124142587276,
12.1518071974261));
#93519=CARTESIAN_POINT('Ctrl Pts',(0.738620895303357,-2.25382010737616,
12.1512571380354));
#93520=CARTESIAN_POINT('Ctrl Pts',(0.720162245803472,-2.25979846083852,
12.1499581981002));
#93521=CARTESIAN_POINT('Ctrl Pts',(0.709515421087032,-2.26316384817905,
12.1492082028278));
#93522=CARTESIAN_POINT('Ctrl Pts',(0.678322916728101,-2.27278184126134,
12.1470084213232));
#93523=CARTESIAN_POINT('Ctrl Pts',(0.657716059689079,-2.27883057928905,
12.1455520207085));
#93524=CARTESIAN_POINT('Ctrl Pts',(0.610867650235644,-2.29189364710916,
12.142232947073));
#93525=CARTESIAN_POINT('Ctrl Pts',(0.584582417250348,-2.29873858178577,
12.1403650455487));
#93526=CARTESIAN_POINT('Ctrl Pts',(0.49783069366546,-2.31974547509101,12.1341802218074));
#93527=CARTESIAN_POINT('Ctrl Pts',(0.436929231563304,-2.33198331257253,
12.1298058532488));
#93528=CARTESIAN_POINT('Ctrl Pts',(0.225629867591638,-2.36587525163351,
12.114529217183));
#93529=CARTESIAN_POINT('Ctrl Pts',(0.073680596841483,-2.37546600742856,
12.1033444936368));
#93530=CARTESIAN_POINT('Ctrl Pts',(-0.17207963563285,-2.36736646961638,
12.0854811719907));
#93531=CARTESIAN_POINT('Ctrl Pts',(-0.265780658862212,-2.35868615061329,
12.0787329602207));
#93532=CARTESIAN_POINT('Ctrl Pts',(-0.371103757731314,-2.34257055062827,
12.0713827347762));
#93533=CARTESIAN_POINT('Ctrl Pts',(-0.383463724610208,-2.34057906784625,
12.0705239228831));
#93534=CARTESIAN_POINT('Ctrl Pts',(-0.402137332892034,-2.33741841361116,
12.0692326926835));
#93535=CARTESIAN_POINT('Ctrl Pts',(-0.408462706337029,-2.33632135948874,
12.0687964021201));
#93536=CARTESIAN_POINT('Ctrl Pts',(-0.419815897497135,-2.33430477814219,
12.0680153769536));
#93537=CARTESIAN_POINT('Ctrl Pts',(-0.4248452432866,-2.3333946742645,12.0676701240523));
#93538=CARTESIAN_POINT('Ctrl Pts',(-0.435853078785655,-2.33136594027574,
12.0669160725928));
#93539=CARTESIAN_POINT('Ctrl Pts',(-0.441830213195607,-2.33024057096689,
12.0665076606881));
#93540=CARTESIAN_POINT('Ctrl Pts',(-0.458898566651858,-2.32695892307695,
12.0653441687326));
#93541=CARTESIAN_POINT('Ctrl Pts',(-0.46997898575835,-2.32474632805144,
12.0645922043718));
#93542=CARTESIAN_POINT('Ctrl Pts',(-0.545578830159945,-2.30908754625109,
12.0594819550371));
#93543=CARTESIAN_POINT('Ctrl Pts',(-0.609536025152879,-2.29303493789077,
12.0552595773158));
#93544=CARTESIAN_POINT('Ctrl Pts',(-0.904911489605285,-2.205663028194,12.0358813908219));
#93545=CARTESIAN_POINT('Ctrl Pts',(-1.12518949672044,-2.10185057478262,
12.0216307117774));
#93546=CARTESIAN_POINT('Ctrl Pts',(-1.36050765592221,-1.9431814559665,12.0034170239728));
#93547=CARTESIAN_POINT('Ctrl Pts',(-1.39444328665845,-1.91897442120173,
12.0007125620712));
#93548=CARTESIAN_POINT('Ctrl Pts',(-1.43968765107578,-1.88486659373644,
11.9969892736025));
#93549=CARTESIAN_POINT('Ctrl Pts',(-1.4515673593749,-1.8757331347399,11.9960002774887));
#93550=CARTESIAN_POINT('Ctrl Pts',(-1.47027699438294,-1.86106445018852,
11.9944240809229));
#93551=CARTESIAN_POINT('Ctrl Pts',(-1.47716420689636,-1.85560265958887,
11.9938398024196));
#93552=CARTESIAN_POINT('Ctrl Pts',(-1.49092078031622,-1.84456811508778,
11.9926644770238));
#93553=CARTESIAN_POINT('Ctrl Pts',(-1.49778964198804,-1.83899496711279,
11.9920734201814));
#93554=CARTESIAN_POINT('Ctrl Pts',(-1.51342276000333,-1.82616512999928,
11.9907184680965));
#93555=CARTESIAN_POINT('Ctrl Pts',(-1.52216623614718,-1.81888357906503,
11.9899535705416));
#93556=CARTESIAN_POINT('Ctrl Pts',(-1.54048618929852,-1.80340214702337,
11.988335715211));
#93557=CARTESIAN_POINT('Ctrl Pts',(-1.55005032989432,-1.79518828187048,
11.9874821960715));
#93558=CARTESIAN_POINT('Ctrl Pts',(-1.57513333713836,-1.7732966305736,11.9852198552338));
#93559=CARTESIAN_POINT('Ctrl Pts',(-1.59053923865441,-1.75949164615021,
11.9838057957537));
#93560=CARTESIAN_POINT('Ctrl Pts',(-1.63672087828426,-1.71700681629142,
11.9794908104552));
#93561=CARTESIAN_POINT('Ctrl Pts',(-1.66691460379,-1.68770938383527,11.976564478804));
#93562=CARTESIAN_POINT('Ctrl Pts',(-1.78195078869128,-1.56998848409578,
11.964991870471));
#93563=CARTESIAN_POINT('Ctrl Pts',(-1.86065982669846,-1.47585600260169,
11.9561175708611));
#93564=CARTESIAN_POINT('Ctrl Pts',(-2.01750629648703,-1.25567487222783,
11.9363815122469));
#93565=CARTESIAN_POINT('Ctrl Pts',(-2.09183833882191,-1.12750675773355,
11.9255257575701));
#93566=CARTESIAN_POINT('Ctrl Pts',(-2.16160415564647,-0.976225718645316,
11.9139406478406));
#93567=CARTESIAN_POINT('Ctrl Pts',(-2.1692496899174,-0.959116790364344,
11.9126475062581));
#93568=CARTESIAN_POINT('Ctrl Pts',(-2.17973939876882,-0.93487598023036,
11.9108410383354));
#93569=CARTESIAN_POINT('Ctrl Pts',(-2.18275271289591,-0.927818701829088,
11.9103181619321));
#93570=CARTESIAN_POINT('Ctrl Pts',(-2.18776590014456,-0.915918054796384,
11.90944170194));
#93571=CARTESIAN_POINT('Ctrl Pts',(-2.18978405116351,-0.911082503444913,
11.9090870283239));
#93572=CARTESIAN_POINT('Ctrl Pts',(-2.19387196532615,-0.901195683531819,
11.9083648836178));
#93573=CARTESIAN_POINT('Ctrl Pts',(-2.19594033983021,-0.896143897883778,
11.9079974966213));
#93574=CARTESIAN_POINT('Ctrl Pts',(-2.2011696350024,-0.883245076971879,
11.9070634061276));
#93575=CARTESIAN_POINT('Ctrl Pts',(-2.20430608135312,-0.875388104350973,
11.9064981599046));
#93576=CARTESIAN_POINT('Ctrl Pts',(-2.21690665526246,-0.843325796305487,
11.9042060289159));
#93577=CARTESIAN_POINT('Ctrl Pts',(-2.2260150938633,-0.818981353842017,
11.9024991681499));
#93578=CARTESIAN_POINT('Ctrl Pts',(-2.24901633442402,-0.754284099745273,
11.8980386295231));
#93579=CARTESIAN_POINT('Ctrl Pts',(-2.26222390730116,-0.713696310960525,
11.8953169159556));
#93580=CARTESIAN_POINT('Ctrl Pts',(-2.3388271031152,-0.454736390244581,
11.8783027396771));
#93581=CARTESIAN_POINT('Ctrl Pts',(-2.37163529115258,-0.228570848616063,
11.8648854578643));
#93582=CARTESIAN_POINT('Ctrl Pts',(-2.37174969976493,-0.00119338383973933,
11.8504244921034));
#93583=CARTESIAN_POINT('Ctrl Pts',(-2.36542649454111,0.173076750093539,
11.8369288124873));
#93584=CARTESIAN_POINT('Ctrl Pts',(-2.36967174016765,0.115057307993937,
11.8408158389598));
#93585=CARTESIAN_POINT('Ctrl Pts',(-2.37178177616025,0.0568728735571407,
11.8447028654324));
#93586=CARTESIAN_POINT('Ctrl Pts',(-2.37174963818669,-0.00131006156719779,
11.848589891905));
#93587=CARTESIAN_POINT('Ctrl Pts',(-2.36542649946083,0.173076682856166,
11.6396027579113));
#93588=CARTESIAN_POINT('Ctrl Pts',(-2.36959623365429,0.1160892273876,11.6431085308926));
#93589=CARTESIAN_POINT('Ctrl Pts',(-2.37170628631787,0.0589549541247075,
11.6466259165959));
#93590=CARTESIAN_POINT('Ctrl Pts',(-2.37182455093614,-0.0981284232074804,
11.6563981685599));
#93591=CARTESIAN_POINT('Ctrl Pts',(-2.36558630217958,-0.197935735150465,
11.6627245204279));
#93592=CARTESIAN_POINT('Ctrl Pts',(-2.35081326271615,-0.314962274922296,
11.6704326954118));
#93593=CARTESIAN_POINT('Ctrl Pts',(-2.34834683170767,-0.332853359734494,
11.6716190245502));
#93594=CARTESIAN_POINT('Ctrl Pts',(-2.34396258522252,-0.362176453446736,
11.6735771943546));
#93595=CARTESIAN_POINT('Ctrl Pts',(-2.34216482705472,-0.373625881301496,
11.6743452435663));
#93596=CARTESIAN_POINT('Ctrl Pts',(-2.33877890187598,-0.394204474395164,
11.6757321432583));
#93597=CARTESIAN_POINT('Ctrl Pts',(-2.33722100363748,-0.403338437863,11.6763500223956));
#93598=CARTESIAN_POINT('Ctrl Pts',(-2.33378238593744,-0.422809930002291,
11.6776722053028));
#93599=CARTESIAN_POINT('Ctrl Pts',(-2.33188641944024,-0.433144528398698,
11.678376981936));
#93600=CARTESIAN_POINT('Ctrl Pts',(-2.32656749480987,-0.461089573958851,
11.680291084235));
#93601=CARTESIAN_POINT('Ctrl Pts',(-2.32301335243347,-0.478674040081191,
11.6815045612319));
#93602=CARTESIAN_POINT('Ctrl Pts',(-2.30323052530042,-0.571136828715468,
11.687934324282));
#93603=CARTESIAN_POINT('Ctrl Pts',(-2.28358180661259,-0.645228611194144,
11.6932589213851));
#93604=CARTESIAN_POINT('Ctrl Pts',(-2.20751111334827,-0.884634207657342,
11.7110456201859));
#93605=CARTESIAN_POINT('Ctrl Pts',(-2.1364273626775,-1.04467606348235,11.7239177483709));
#93606=CARTESIAN_POINT('Ctrl Pts',(-2.03686802877451,-1.21527527682117,
11.7382509404802));
#93607=CARTESIAN_POINT('Ctrl Pts',(-2.02500620526152,-1.23493938154839,
11.7399120354391));
#93608=CARTESIAN_POINT('Ctrl Pts',(-2.00184950378918,-1.27209670753443,
11.7430644666016));
#93609=CARTESIAN_POINT('Ctrl Pts',(-1.99060611869413,-1.2896196311958,11.7445570357783));
#93610=CARTESIAN_POINT('Ctrl Pts',(-1.95217770154501,-1.34781043652375,
11.7495284848437));
#93611=CARTESIAN_POINT('Ctrl Pts',(-1.9239635207587,-1.38778814670646,11.7529687934974));
#93612=CARTESIAN_POINT('Ctrl Pts',(-1.88795647903233,-1.43559667391641,
11.7570874539934));
#93613=CARTESIAN_POINT('Ctrl Pts',(-1.88132186638304,-1.44428027874177,
11.7578357159257));
#93614=CARTESIAN_POINT('Ctrl Pts',(-1.87087758208135,-1.45775601626811,
11.7589967919351));
#93615=CARTESIAN_POINT('Ctrl Pts',(-1.8671090815316,-1.46257964224885,11.7594123731986));
#93616=CARTESIAN_POINT('Ctrl Pts',(-1.86011117379989,-1.47146573681321,
11.7601778280249));
#93617=CARTESIAN_POINT('Ctrl Pts',(-1.8568871262365,-1.47553217344705,11.7605280538438));
#93618=CARTESIAN_POINT('Ctrl Pts',(-1.84954328921449,-1.48473263993862,
11.7613203479538));
#93619=CARTESIAN_POINT('Ctrl Pts',(-1.84541546175541,-1.48986011656763,
11.7617618339506));
#93620=CARTESIAN_POINT('Ctrl Pts',(-1.83277473702483,-1.50542894647073,
11.7631023779214));
#93621=CARTESIAN_POINT('Ctrl Pts',(-1.82419399567672,-1.51581523833169,
11.7639967333131));
#93622=CARTESIAN_POINT('Ctrl Pts',(-1.73479520031837,-1.62216655976194,
11.7731618589147));
#93623=CARTESIAN_POINT('Ctrl Pts',(-1.64655942654343,-1.71166299888996,
11.7809415742957));
#93624=CARTESIAN_POINT('Ctrl Pts',(-1.40119912694303,-1.92390444857523,
11.8008780037958));
#93625=CARTESIAN_POINT('Ctrl Pts',(-1.23500072290513,-2.03458386946986,
11.8129164911346));
#93626=CARTESIAN_POINT('Ctrl Pts',(-1.03229502946698,-2.13549133354626,
11.8276128455799));
#93627=CARTESIAN_POINT('Ctrl Pts',(-1.0074340089395,-2.14733157146981,11.8294138310938));
#93628=CARTESIAN_POINT('Ctrl Pts',(-0.971175851169719,-2.16383152693151,
11.8320410710148));
#93629=CARTESIAN_POINT('Ctrl Pts',(-0.959939098430491,-2.16883985773658,
11.8328553571061));
#93630=CARTESIAN_POINT('Ctrl Pts',(-0.940063593668559,-2.17751384803638,
11.8342960449378));
#93631=CARTESIAN_POINT('Ctrl Pts',(-0.931441029128828,-2.18121611112737,
11.8349211823653));
#93632=CARTESIAN_POINT('Ctrl Pts',(-0.913555284592143,-2.18877030450605,
11.8362182739056));
#93633=CARTESIAN_POINT('Ctrl Pts',(-0.904289196384707,-2.19261481976058,
11.8368904646495));
#93634=CARTESIAN_POINT('Ctrl Pts',(-0.880390017669219,-2.20235336472459,
11.8386248621339));
#93635=CARTESIAN_POINT('Ctrl Pts',(-0.865722204170377,-2.20816031359601,
11.8396899778674));
#93636=CARTESIAN_POINT('Ctrl Pts',(-0.80299897555544,-2.23227127284158,
11.8442482423697));
#93637=CARTESIAN_POINT('Ctrl Pts',(-0.754416266272933,-2.24915490192749,
11.8477881597181));
#93638=CARTESIAN_POINT('Ctrl Pts',(-0.622281848918048,-2.2903119527519,
11.8574482534792));
#93639=CARTESIAN_POINT('Ctrl Pts',(-0.537885812885933,-2.31158810627116,
11.8636547190824));
#93640=CARTESIAN_POINT('Ctrl Pts',(-0.327848848092087,-2.35241221418634,
11.8791328044994));
#93641=CARTESIAN_POINT('Ctrl Pts',(-0.201437396552722,-2.36659033516052,
11.8884831905037));
#93642=CARTESIAN_POINT('Ctrl Pts',(-0.0426416812214114,-2.37158085773896,
11.8999769382039));
#93643=CARTESIAN_POINT('Ctrl Pts',(-0.0107643246538707,-2.37193978609064,
11.9022707201288));
#93644=CARTESIAN_POINT('Ctrl Pts',(0.071640998922669,-2.37120624349076,
11.908151461428));
#93645=CARTESIAN_POINT('Ctrl Pts',(0.122147670897993,-2.36914168456474,
11.911708426109));
#93646=CARTESIAN_POINT('Ctrl Pts',(0.182594302802936,-2.3647322741372,11.9158798583456));
#93647=CARTESIAN_POINT('Ctrl Pts',(0.19263012313159,-2.36393592393366,11.9165695873291));
#93648=CARTESIAN_POINT('Ctrl Pts',(0.209090280969267,-2.36252427697597,
11.9176958406146));
#93649=CARTESIAN_POINT('Ctrl Pts',(0.215517592028784,-2.36194662829993,
11.9181343640749));
#93650=CARTESIAN_POINT('Ctrl Pts',(0.227102627741073,-2.36085775100345,
11.9189224341041));
#93651=CARTESIAN_POINT('Ctrl Pts',(0.232261071664863,-2.36035584608223,
11.919272486155));
#93652=CARTESIAN_POINT('Ctrl Pts',(0.243613907791586,-2.35921366228933,
11.9200410179082));
#93653=CARTESIAN_POINT('Ctrl Pts',(0.249807431062139,-2.35856589690526,
11.9204590742562));
#93654=CARTESIAN_POINT('Ctrl Pts',(0.267664225999971,-2.35662717030328,
11.9216610701236));
#93655=CARTESIAN_POINT('Ctrl Pts',(0.279320770099191,-2.35527401361631,
11.9224416204349));
#93656=CARTESIAN_POINT('Ctrl Pts',(0.364929552630402,-2.34469156202545,
11.928147306832));
#93657=CARTESIAN_POINT('Ctrl Pts',(0.438428712567298,-2.33206665864493,
11.9328986979669));
#93658=CARTESIAN_POINT('Ctrl Pts',(0.617695503759055,-2.2924964502961,11.9443907556221));
#93659=CARTESIAN_POINT('Ctrl Pts',(0.722429270633916,-2.26167766636787,
11.9510242136761));
#93660=CARTESIAN_POINT('Ctrl Pts',(0.841401620177135,-2.21755713456954,
11.9588110880807));
#93661=CARTESIAN_POINT('Ctrl Pts',(0.858057935173975,-2.21116550814914,
11.9599070361984));
#93662=CARTESIAN_POINT('Ctrl Pts',(1.0008640482178,-2.15450907927809,11.9693628610977));
#93663=CARTESIAN_POINT('Ctrl Pts',(1.12253593727548,-2.09369138937848,11.9778412394494));
#93664=CARTESIAN_POINT('Ctrl Pts',(1.25449414574158,-2.01290879205647,11.9879421080169));
#93665=CARTESIAN_POINT('Ctrl Pts',(1.27054103798402,-2.00281871455946,11.9891863179932));
#93666=CARTESIAN_POINT('Ctrl Pts',(1.29642903469795,-1.98610435061953,11.9912205263249));
#93667=CARTESIAN_POINT('Ctrl Pts',(1.30634462536221,-1.97959653583522,11.9920062076588));
#93668=CARTESIAN_POINT('Ctrl Pts',(1.32394184032688,-1.96785732032023,11.9934124986577));
#93669=CARTESIAN_POINT('Ctrl Pts',(1.33164236760114,-1.9626545876158,11.994032021487));
#93670=CARTESIAN_POINT('Ctrl Pts',(1.34784685583916,-1.95156702726821,11.9953445770752));
#93671=CARTESIAN_POINT('Ctrl Pts',(1.35634328089878,-1.94567158256411,11.9960380044172));
#93672=CARTESIAN_POINT('Ctrl Pts',(1.37885570983498,-1.92983168460018,11.9978894616934));
#93673=CARTESIAN_POINT('Ctrl Pts',(1.39280242502703,-1.91979029508999,11.9990511901485));
#93674=CARTESIAN_POINT('Ctrl Pts',(1.46016377223315,-1.87017093023593,12.0047356264163));
#93675=CARTESIAN_POINT('Ctrl Pts',(1.51200260238899,-1.82851419447806,12.0093387995779));
#93676=CARTESIAN_POINT('Ctrl Pts',(1.75722529389617,-1.6138930943348,12.0322888624608));
#93677=CARTESIAN_POINT('Ctrl Pts',(1.92303952204303,-1.41222304429458,12.0518396134128));
#93678=CARTESIAN_POINT('Ctrl Pts',(2.05509743430012,-1.18397280798937,12.0702881863535));
#93679=CARTESIAN_POINT('Ctrl Pts',(2.0572706208332,-1.18019264012371,12.0705927341295));
#93680=CARTESIAN_POINT('Ctrl Pts',(2.06992069561689,-1.15804724477495,12.0723710057368));
#93681=CARTESIAN_POINT('Ctrl Pts',(2.08016249855412,-1.13954778968523,12.0738329796942));
#93682=CARTESIAN_POINT('Ctrl Pts',(2.09400056181127,-1.113744083999,12.0758373220238));
#93683=CARTESIAN_POINT('Ctrl Pts',(2.0978083152236,-1.10655524715962,12.0763920251162));
#93684=CARTESIAN_POINT('Ctrl Pts',(2.10385009840324,-1.0950054024846,12.0772771467267));
#93685=CARTESIAN_POINT('Ctrl Pts',(2.10610768911218,-1.09065689884886,12.0776090203251));
#93686=CARTESIAN_POINT('Ctrl Pts',(2.11080590477986,-1.08153835061618,12.078302018622));
#93687=CARTESIAN_POINT('Ctrl Pts',(2.11324386204848,-1.07676699050575,12.078662965112));
#93688=CARTESIAN_POINT('Ctrl Pts',(2.11915984456469,-1.06509125500273,12.0795422396565));
#93689=CARTESIAN_POINT('Ctrl Pts',(2.12262036283622,-1.05817797547843,12.0800594809004));
#93690=CARTESIAN_POINT('Ctrl Pts',(2.13495283817513,-1.03323673545039,12.081913847832));
#93691=CARTESIAN_POINT('Ctrl Pts',(2.143629734571,-1.01511250628012,12.0832394708479));
#93692=CARTESIAN_POINT('Ctrl Pts',(2.16465192985967,-0.969729533079284,
12.0865100515522));
#93693=CARTESIAN_POINT('Ctrl Pts',(2.17671398905196,-0.942342683477747,
12.0884405395596));
#93694=CARTESIAN_POINT('Ctrl Pts',(2.22599369737009,-0.824454177647528,
12.0965980069319));
#93695=CARTESIAN_POINT('Ctrl Pts',(2.25811241954266,-0.731918091040898,
12.1026251091618));
#93696=CARTESIAN_POINT('Ctrl Pts',(2.3043770643698,-0.566173328804962,12.113181562417));
#93697=CARTESIAN_POINT('Ctrl Pts',(2.32096374930366,-0.493794461356115,
12.1177144400559));
#93698=CARTESIAN_POINT('Ctrl Pts',(2.35597017178445,-0.299598544768957,
12.1298964545494));
#93699=CARTESIAN_POINT('Ctrl Pts',(2.36834145458165,-0.176938656559848,
12.1376211682771));
#93700=CARTESIAN_POINT('Ctrl Pts',(2.37156465605216,-0.035101155465809,
12.1468849867973));
#93701=CARTESIAN_POINT('Ctrl Pts',(2.37176828342757,-0.0163151867064924,
12.1481183089271));
#93702=CARTESIAN_POINT('Ctrl Pts',(2.37173641006333,0.0142806083841101,
12.1501382294368));
#93703=CARTESIAN_POINT('Ctrl Pts',(2.37163589921045,0.0260899909288855,
12.150920611989));
#93704=CARTESIAN_POINT('Ctrl Pts',(2.37129878920259,0.0471844971881024,
12.1523232393106));
#93705=CARTESIAN_POINT('Ctrl Pts',(2.37109583571387,0.0564699751180214,
12.1529424188753));
#93706=CARTESIAN_POINT('Ctrl Pts',(2.3705508428335,0.0761203660757453,12.1542566025492));
#93707=CARTESIAN_POINT('Ctrl Pts',(2.37019535117976,0.0864846801857484,
12.1549520151703));
#93708=CARTESIAN_POINT('Ctrl Pts',(2.36906479111327,0.11414885080847,12.1568144126208));
#93709=CARTESIAN_POINT('Ctrl Pts',(2.36816821565367,0.131442836331636,12.1579851734868));
#93710=CARTESIAN_POINT('Ctrl Pts',(2.36281053925323,0.216714687991474,12.163791139602));
#93711=CARTESIAN_POINT('Ctrl Pts',(2.35561186015997,0.284482039724925,12.1685110432529));
#93712=CARTESIAN_POINT('Ctrl Pts',(2.32607193976808,0.481407029463875,12.1825474469187));
#93713=CARTESIAN_POINT('Ctrl Pts',(2.29593568101464,0.60912673094418,12.1920733039751));
#93714=CARTESIAN_POINT('Ctrl Pts',(2.21425895627556,0.860206724232895,12.2113588759056));
#93715=CARTESIAN_POINT('Ctrl Pts',(2.16252631554485,0.98304904004922,12.2210839994846));
#93716=CARTESIAN_POINT('Ctrl Pts',(2.0918434375424,1.11792574540072,12.2316790887953));
#93717=CARTESIAN_POINT('Ctrl Pts',(2.08272168500248,1.13482923011275,12.2330050654514));
#93718=CARTESIAN_POINT('Ctrl Pts',(2.06960026308547,1.15845323550954,12.2348536640962));
#93719=CARTESIAN_POINT('Ctrl Pts',(2.06577146885511,1.16526708984569,12.2353863130099));
#93720=CARTESIAN_POINT('Ctrl Pts',(2.05927930157816,1.17668820744282,12.236278047779));
#93721=CARTESIAN_POINT('Ctrl Pts',(2.05663400446042,1.18130561374802,12.2366382679579));
#93722=CARTESIAN_POINT('Ctrl Pts',(2.05120668336528,1.19070559576255,12.237370928447));
#93723=CARTESIAN_POINT('Ctrl Pts',(2.0484234304241,1.19548740058673,12.2377432864134));
#93724=CARTESIAN_POINT('Ctrl Pts',(2.04129101825791,1.20764329658035,12.238689087837));
#93725=CARTESIAN_POINT('Ctrl Pts',(2.03691857258858,1.21500373962633,12.2392610442586));
#93726=CARTESIAN_POINT('Ctrl Pts',(2.01899799476063,1.24480205475699,12.2415742854662));
#93727=CARTESIAN_POINT('Ctrl Pts',(2.00511759058134,1.26703932402075,12.2432952630239));
#93728=CARTESIAN_POINT('Ctrl Pts',(1.96749549299831,1.32514501049946,12.2477907577836));
#93729=CARTESIAN_POINT('Ctrl Pts',(1.94314113353665,1.36060678087692,12.2505329575978));
#93730=CARTESIAN_POINT('Ctrl Pts',(1.79173811225853,1.56869640990903,12.2667407956411));
#93731=CARTESIAN_POINT('Ctrl Pts',(1.64273217358128,1.72411594418627,12.279431850364));
#93732=CARTESIAN_POINT('Ctrl Pts',(1.42367214432899,1.89805920507518,12.2971177079821));
#93733=CARTESIAN_POINT('Ctrl Pts',(1.37082497087268,1.93657140220284,12.3013142259393));
#93734=CARTESIAN_POINT('Ctrl Pts',(1.301607315422,1.98275949601139,12.3067645800443));
#93735=CARTESIAN_POINT('Ctrl Pts',(1.28664519333607,1.99250117694115,12.3079400237889));
#93736=CARTESIAN_POINT('Ctrl Pts',(1.26272136039388,2.00769590129888,12.3098159814015));
#93737=CARTESIAN_POINT('Ctrl Pts',(1.25383079439422,2.01326014193278,12.310512360691));
#93738=CARTESIAN_POINT('Ctrl Pts',(1.23780365927248,2.02314353045753,12.3117665132733));
#93739=CARTESIAN_POINT('Ctrl Pts',(1.23068061410725,2.02748436904839,12.3123234765885));
#93740=CARTESIAN_POINT('Ctrl Pts',(1.2139560950548,2.03755581241342,12.313630282861));
#93741=CARTESIAN_POINT('Ctrl Pts',(1.20433676778924,2.04325623251864,12.3143812114017));
#93742=CARTESIAN_POINT('Ctrl Pts',(1.17646210309063,2.05950955284682,12.3165554504598));
#93743=CARTESIAN_POINT('Ctrl Pts',(1.15810627582052,2.06988706987253,12.3179850346368));
#93744=CARTESIAN_POINT('Ctrl Pts',(0.984458652182627,2.16502635445306,12.3314924124387));
#93745=CARTESIAN_POINT('Ctrl Pts',(0.820310167817592,2.23238986534783,12.3442011988481));
#93746=CARTESIAN_POINT('Ctrl Pts',(0.506586040439996,2.32182723903128,12.3680112371111));
#93747=CARTESIAN_POINT('Ctrl Pts',(0.359373580767939,2.34912108670558,12.3789848293889));
#93748=CARTESIAN_POINT('Ctrl Pts',(0.191913245509808,2.36404692431366,12.3906763078027));
#93749=CARTESIAN_POINT('Ctrl Pts',(0.17324597908839,2.36548820330306,12.391968309503));
#93750=CARTESIAN_POINT('Ctrl Pts',(0.147609761539131,2.36716243061672,12.3937254366186));
#93751=CARTESIAN_POINT('Ctrl Pts',(0.140654558942902,2.3675858828726,12.3942004156932));
#93752=CARTESIAN_POINT('Ctrl Pts',(0.128761289452412,2.36825738392118,12.3950095395531));
#93753=CARTESIAN_POINT('Ctrl Pts',(0.123824180457617,2.3685206521464,12.3953445140816));
#93754=CARTESIAN_POINT('Ctrl Pts',(0.113571682611726,2.36903521521545,12.3960381953154));
#93755=CARTESIAN_POINT('Ctrl Pts',(0.108256239259344,2.36928406176334,12.3963967512297));
#93756=CARTESIAN_POINT('Ctrl Pts',(0.0954096551299932,2.36984216198566,
12.3972607907708));
#93757=CARTESIAN_POINT('Ctrl Pts',(0.0878777035675075,2.37013341146655,
12.3977652762332));
#93758=CARTESIAN_POINT('Ctrl Pts',(0.0615077822137425,2.3710272203427,12.3995245668751));
#93759=CARTESIAN_POINT('Ctrl Pts',(0.0426635241664532,2.37144115803878,
12.4007693653004));
#93760=CARTESIAN_POINT('Ctrl Pts',(-0.0736162715846883,2.37260882471755,
12.4083850094455));
#93761=CARTESIAN_POINT('Ctrl Pts',(-0.171028244247414,2.3675822971823,12.4144832196951));
#93762=CARTESIAN_POINT('Ctrl Pts',(-0.38699248975838,2.34303426534386,12.4279052284509));
#93763=CARTESIAN_POINT('Ctrl Pts',(-0.504920945193207,2.32048010060413,
12.4351737066231));
#93764=CARTESIAN_POINT('Ctrl Pts',(-0.726984499523905,2.26027262403236,
12.449434223003));
#93765=CARTESIAN_POINT('Ctrl Pts',(-0.831178292872454,2.22406758929908,
12.4563830462601));
#93766=CARTESIAN_POINT('Ctrl Pts',(-0.949403136286887,2.17351579106401,
12.4647821621643));
#93767=CARTESIAN_POINT('Ctrl Pts',(-0.966250752038867,2.16607863705785,
12.4659915030737));
#93768=CARTESIAN_POINT('Ctrl Pts',(-0.993655430551495,2.15359787018783,
12.4679799277809));
#93769=CARTESIAN_POINT('Ctrl Pts',(-1.0042650113724,2.14867091006672,12.4687550148228));
#93770=CARTESIAN_POINT('Ctrl Pts',(-1.02322153107276,2.13969666203909,12.4701495962316));
#93771=CARTESIAN_POINT('Ctrl Pts',(-1.03158204922485,2.13567848205318,12.4707680731842));
#93772=CARTESIAN_POINT('Ctrl Pts',(-1.04009433183799,2.13152571684589,12.4714013268687));
#93773=CARTESIAN_POINT('Ctrl Pts',(-1.04026997319318,2.13144000233868,12.4714143948922));
#93774=CARTESIAN_POINT('Ctrl Pts',(-1.04060645738165,2.13127574363226,12.4714394328693));
#93775=CARTESIAN_POINT('Ctrl Pts',(-1.0407673019214,2.13119720293333,12.4714514027003));
#93776=CARTESIAN_POINT('Ctrl Pts',(-1.04107545160036,2.13104668964666,12.4714743372676));
#93777=CARTESIAN_POINT('Ctrl Pts',(-1.04122275817543,2.13097471998999,12.4714853019015));
#93778=CARTESIAN_POINT('Ctrl Pts',(-1.04150498435649,2.13083679633468,12.4715063112451));
#93779=CARTESIAN_POINT('Ctrl Pts',(-1.04163990517566,2.13077084478807,12.4715163558697));
#93780=CARTESIAN_POINT('Ctrl Pts',(-1.0418984140125,2.13064445093627,12.4715356031645));
#93781=CARTESIAN_POINT('Ctrl Pts',(-1.04202200304191,2.13058401068904,12.4715448057629));
#93782=CARTESIAN_POINT('Ctrl Pts',(-1.0422588121497,2.13046817551535,12.4715624403462));
#93783=CARTESIAN_POINT('Ctrl Pts',(-1.0423720330766,2.13041278231406,12.4715708722709));
#93784=CARTESIAN_POINT('Ctrl Pts',(-1.04258898701066,2.13030661642931,12.4715870307606));
#93785=CARTESIAN_POINT('Ctrl Pts',(-1.04269272073395,2.13025584519016,12.4715947572753));
#93786=CARTESIAN_POINT('Ctrl Pts',(-1.04289150550433,2.13015853434611,12.4716095646214));
#93787=CARTESIAN_POINT('Ctrl Pts',(-1.04298655714295,2.13011199595696,12.4716166454099));
#93788=CARTESIAN_POINT('Ctrl Pts',(-1.04316871362991,2.1300227949041,12.4716302158695));
#93789=CARTESIAN_POINT('Ctrl Pts',(-1.04325581898201,2.12998013325653,12.4716367055054));
#93790=CARTESIAN_POINT('Ctrl Pts',(-1.04342275544403,2.12989835997503,12.4716491435545));
#93791=CARTESIAN_POINT('Ctrl Pts',(-1.04350258697463,2.12985924919465,12.471655091938));
#93792=CARTESIAN_POINT('Ctrl Pts',(-1.04365559050866,2.12978427957857,12.4716664931076));
#93793=CARTESIAN_POINT('Ctrl Pts',(-1.0437287628526,2.12974842146536,12.4716719458679));
#93794=CARTESIAN_POINT('Ctrl Pts',(-1.04386900990307,2.129679684423,12.4716823975132));
#93795=CARTESIAN_POINT('Ctrl Pts',(-1.04393608489663,2.12964680609972,12.4716873963766));
#93796=CARTESIAN_POINT('Ctrl Pts',(-1.04410194566876,2.12956549597682,12.4716997579575));
#93797=CARTESIAN_POINT('Ctrl Pts',(-1.04420072964193,2.12951706046688,12.4717071208057));
#93798=CARTESIAN_POINT('Ctrl Pts',(-1.04439642669855,2.12942108988594,12.4717217080304));
#93799=CARTESIAN_POINT('Ctrl Pts',(-1.04449333991292,2.12937355506949,12.4717289323984));
#93800=CARTESIAN_POINT('Ctrl Pts',(-1.04468533924511,2.12927936534509,12.4717432458725));
#93801=CARTESIAN_POINT('Ctrl Pts',(-1.04478042547185,2.1292327106892,12.4717503349692));
#93802=CARTESIAN_POINT('Ctrl Pts',(-1.04496881345674,2.12914026128041,12.4717643810266));
#93803=CARTESIAN_POINT('Ctrl Pts',(-1.04506211533331,2.12909446676221,12.4717713379793));
#93804=CARTESIAN_POINT('Ctrl Pts',(-1.04524697613467,2.12900371812387,12.471785122794));
#93805=CARTESIAN_POINT('Ctrl Pts',(-1.04533853518691,2.12895876422189,12.4717919506493));
#93806=CARTESIAN_POINT('Ctrl Pts',(-1.05531578320218,2.1240593101988,12.4725360325113));
#93807=CARTESIAN_POINT('Ctrl Pts',(-1.06516739419824,2.11913609066062,12.4732756811296));
#93808=CARTESIAN_POINT('Ctrl Pts',(-1.09334605887655,2.10480801627165,12.4754057344253));
#93809=CARTESIAN_POINT('Ctrl Pts',(-1.11158496277867,2.09523297358137,12.4768020883032));
#93810=CARTESIAN_POINT('Ctrl Pts',(-1.1525208588623,2.07305754060438,12.4799771116146));
#93811=CARTESIAN_POINT('Ctrl Pts',(-1.17514002949346,2.06031980901287,12.4817605032576));
#93812=CARTESIAN_POINT('Ctrl Pts',(-1.24749779103941,2.01799317851041,12.4875614169866));
#93813=CARTESIAN_POINT('Ctrl Pts',(-1.29636070971872,1.98695625979924,12.4916284047477));
#93814=CARTESIAN_POINT('Ctrl Pts',(-1.44229871816888,1.88658298241549,12.5042373231318));
#93815=CARTESIAN_POINT('Ctrl Pts',(-1.53531590764749,1.81169022638074,12.512940913135));
#93816=CARTESIAN_POINT('Ctrl Pts',(-1.71190293098036,1.64610892557766,12.530620566465));
#93817=CARTESIAN_POINT('Ctrl Pts',(-1.79485426386195,1.55524620907425,12.5395695978527));
#93818=CARTESIAN_POINT('Ctrl Pts',(-1.88222654201364,1.44318789416437,12.5494566685689));
#93819=CARTESIAN_POINT('Ctrl Pts',(-1.89386948253923,1.42787481803066,12.5507846769232));
#93820=CARTESIAN_POINT('Ctrl Pts',(-1.90998256562061,1.4061386213042,12.5526356078951));
#93821=CARTESIAN_POINT('Ctrl Pts',(-1.91460882232325,1.39983294902466,12.5531685903577));
#93822=CARTESIAN_POINT('Ctrl Pts',(-1.92233097592744,1.38919761321403,12.5540607230377));
#93823=CARTESIAN_POINT('Ctrl Pts',(-1.9254436107507,1.38488024511726,12.5544210097842));
#93824=CARTESIAN_POINT('Ctrl Pts',(-1.93176148022677,1.37605459290164,12.5551536499277));
#93825=CARTESIAN_POINT('Ctrl Pts',(-1.93496551799876,1.37154551688877,12.5555259218375));
#93826=CARTESIAN_POINT('Ctrl Pts',(-1.94308469893013,1.36003422860753,12.5564712385453));
#93827=CARTESIAN_POINT('Ctrl Pts',(-1.94797783835804,1.35301648072788,12.5570427993218));
#93828=CARTESIAN_POINT('Ctrl Pts',(-1.96767951567693,1.324431875986,12.5593523825381));
#93829=CARTESIAN_POINT('Ctrl Pts',(-1.98216939720738,1.30264618866939,12.5610701785135));
#93830=CARTESIAN_POINT('Ctrl Pts',(-2.01945780458749,1.24451928008548,12.565555326491));
#93831=CARTESIAN_POINT('Ctrl Pts',(-2.041636772729,1.20779046664347,12.568290545376));
#93832=CARTESIAN_POINT('Ctrl Pts',(-2.1596350224321,0.999834582011131,12.5833511462278));
#93833=CARTESIAN_POINT('Ctrl Pts',(-2.23491679923123,0.817831754420744,
12.5950212159477));
#93834=CARTESIAN_POINT('Ctrl Pts',(-2.30329808334263,0.569062273779928,
12.6111996525701));
#93835=CARTESIAN_POINT('Ctrl Pts',(-2.31733639411244,0.508886068116333,
12.6151234148213));
#93836=CARTESIAN_POINT('Ctrl Pts',(-2.33487580045077,0.417751880656847,
12.6211265200322));
#93837=CARTESIAN_POINT('Ctrl Pts',(-2.34014306905024,0.387158762642001,
12.6231516827518));
#93838=CARTESIAN_POINT('Ctrl Pts',(-2.34662453405432,0.344524884550173,
12.6259915670192));
#93839=CARTESIAN_POINT('Ctrl Pts',(-2.34834947241183,0.332564048314625,
12.6267902035345));
#93840=CARTESIAN_POINT('Ctrl Pts',(-2.35116892690733,0.311896982424793,
12.6281736951931));
#93841=CARTESIAN_POINT('Ctrl Pts',(-2.35230668444913,0.303196816041569,
12.6287571777211));
#93842=CARTESIAN_POINT('Ctrl Pts',(-2.35449624798838,0.285699110753148,
12.6299329291525));
#93843=CARTESIAN_POINT('Ctrl Pts',(-2.35554708435261,0.27690159514424,12.6305252185997));
#93844=CARTESIAN_POINT('Ctrl Pts',(-2.35758279689081,0.259007964596773,
12.6317323104543));
#93845=CARTESIAN_POINT('Ctrl Pts',(-2.35856438140266,0.249911633614706,
12.6323472061039));
#93846=CARTESIAN_POINT('Ctrl Pts',(-2.36070927484612,0.228895635389493,
12.6337708608584));
#93847=CARTESIAN_POINT('Ctrl Pts',(-2.36183497138468,0.216972465989632,
12.6345807877068));
#93848=CARTESIAN_POINT('Ctrl Pts',(-2.36379441443448,0.194392108121133,
12.6361190171284));
#93849=CARTESIAN_POINT('Ctrl Pts',(-2.36464649384007,0.183736959088881,
12.6368467111825));
#93850=CARTESIAN_POINT('Ctrl Pts',(-2.36542649456986,0.173076749700613,
12.6375766332401));
#93851=CARTESIAN_POINT('Origin',(0.,0.,-1.84858989190503));
#93852=CARTESIAN_POINT('',(-2.36542648366643,0.173076898716907,13.8355365560746));
#93853=CARTESIAN_POINT('',(-2.3654265016339,0.173076653156924,13.6406850658798));
#93854=CARTESIAN_POINT('',(-2.36542649454111,0.173076750093529,-1.84858989190503));
#93855=CARTESIAN_POINT('Ctrl Pts',(-2.36542648366643,0.173076898716907,
13.8355365560746));
#93856=CARTESIAN_POINT('Ctrl Pts',(-2.36039328004673,0.24186524209487,13.83056564983));
#93857=CARTESIAN_POINT('Ctrl Pts',(-2.35235946872098,0.310433940184986,
13.825661792469));
#93858=CARTESIAN_POINT('Ctrl Pts',(-2.33989547454688,0.387516525628758,
13.8202743280973));
#93859=CARTESIAN_POINT('Ctrl Pts',(-2.33840044556258,0.396438207113654,
13.8196527003806));
#93860=CARTESIAN_POINT('Ctrl Pts',(-2.33583000553576,0.411256820455127,
13.8186236458865));
#93861=CARTESIAN_POINT('Ctrl Pts',(-2.33478323446111,0.417158527634897,
13.8182147228627));
#93862=CARTESIAN_POINT('Ctrl Pts',(-2.33284797204356,0.427834055557162,
13.8174767548542));
#93863=CARTESIAN_POINT('Ctrl Pts',(-2.33196717621284,0.432609211541442,
13.8171472892113));
#93864=CARTESIAN_POINT('Ctrl Pts',(-2.33012887926652,0.442406608578485,
13.8164726446466));
#93865=CARTESIAN_POINT('Ctrl Pts',(-2.32916981436925,0.44742840555511,13.8161275757743));
#93866=CARTESIAN_POINT('Ctrl Pts',(-2.32696445708651,0.458776692019071,
13.815349411315));
#93867=CARTESIAN_POINT('Ctrl Pts',(-2.32570860150079,0.465101215955899,
13.8149168647948));
#93868=CARTESIAN_POINT('Ctrl Pts',(-2.32191238044717,0.483819188576863,
13.8136398517279));
#93869=CARTESIAN_POINT('Ctrl Pts',(-2.31929858034927,0.496197765470347,
13.8127994281688));
#93870=CARTESIAN_POINT('Ctrl Pts',(-2.29357002253575,0.613397264204295,
13.8048760668163));
#93871=CARTESIAN_POINT('Ctrl Pts',(-2.26346006946904,0.716571441766442,
13.7981546891627));
#93872=CARTESIAN_POINT('Ctrl Pts',(-2.19789797818924,0.895159504927388,
13.7864117145909));
#93873=CARTESIAN_POINT('Ctrl Pts',(-2.16527958724309,0.971406573064843,
13.7813605706524));
#93874=CARTESIAN_POINT('Ctrl Pts',(-2.09042789357284,1.12376934530554,13.7709323698037));
#93875=CARTESIAN_POINT('Ctrl Pts',(-2.04786542696937,1.19957989734769,13.765558792318));
#93876=CARTESIAN_POINT('Ctrl Pts',(-1.96600263086737,1.32828585809461,13.7559094906364));
#93877=CARTESIAN_POINT('Ctrl Pts',(-1.92847971265286,1.38219912244799,13.7516910781001));
#93878=CARTESIAN_POINT('Ctrl Pts',(-1.87848018240435,1.44803307300398,13.7462716803244));
#93879=CARTESIAN_POINT('Ctrl Pts',(-1.86804381456948,1.46147181221751,13.7451507323851));
#93880=CARTESIAN_POINT('Ctrl Pts',(-1.85111476396641,1.48279346237557,13.7433479380973));
#93881=CARTESIAN_POINT('Ctrl Pts',(-1.84471406296757,1.49074891975858,13.7426697668066));
#93882=CARTESIAN_POINT('Ctrl Pts',(-1.83247638555565,1.50575967623371,13.7413794960421));
#93883=CARTESIAN_POINT('Ctrl Pts',(-1.82664951626461,1.51282300579344,13.7407678127598));
#93884=CARTESIAN_POINT('Ctrl Pts',(-1.8133114434909,1.5288020070386,13.7393735454297));
#93885=CARTESIAN_POINT('Ctrl Pts',(-1.80577516040635,1.53769633849624,13.7385899438308));
#93886=CARTESIAN_POINT('Ctrl Pts',(-1.78606470464423,1.56061391397602,13.7365510478609));
#93887=CARTESIAN_POINT('Ctrl Pts',(-1.77379105415041,1.57455015149746,13.735291656171));
#93888=CARTESIAN_POINT('Ctrl Pts',(-1.68017385631382,1.67836488813536,13.7257595597905));
#93889=CARTESIAN_POINT('Ctrl Pts',(-1.59222375240875,1.76201811243754,13.7172032883976));
#93890=CARTESIAN_POINT('Ctrl Pts',(-1.47574810763962,1.8569357616957,13.7063596416695));
#93891=CARTESIAN_POINT('Ctrl Pts',(-1.45288097843942,1.87488124862787,13.7042527262708));
#93892=CARTESIAN_POINT('Ctrl Pts',(-1.29374400778341,1.99510762089445,13.6897512397618));
#93893=CARTESIAN_POINT('Ctrl Pts',(-1.14712143387038,2.08286977202426,13.6771410648638));
#93894=CARTESIAN_POINT('Ctrl Pts',(-0.970580455281716,2.16419646848831,
13.6635539405041));
#93895=CARTESIAN_POINT('Ctrl Pts',(-0.948654688567413,2.17389677047183,
13.6618935112987));
#93896=CARTESIAN_POINT('Ctrl Pts',(-0.919180933683756,2.18640553428428,
13.6597008988304));
#93897=CARTESIAN_POINT('Ctrl Pts',(-0.911761231965697,2.18951003876113,
13.6591522333199));
#93898=CARTESIAN_POINT('Ctrl Pts',(-0.899274624711374,2.19466012538113,
13.6582345897609));
#93899=CARTESIAN_POINT('Ctrl Pts',(-0.894216253192675,2.19672602084789,
13.6578644133508));
#93900=CARTESIAN_POINT('Ctrl Pts',(-0.884296465316073,2.2007374311934,13.6571415970444));
#93901=CARTESIAN_POINT('Ctrl Pts',(-0.879435687226764,2.20268435153908,
13.6567888777625));
#93902=CARTESIAN_POINT('Ctrl Pts',(-0.867452894753732,2.20743791237579,
13.6559228677528));
#93903=CARTESIAN_POINT('Ctrl Pts',(-0.860323581052744,2.21022623312512,
13.6554106697709));
#93904=CARTESIAN_POINT('Ctrl Pts',(-0.835800607028149,2.2196806924828,13.653658866025));
#93905=CARTESIAN_POINT('Ctrl Pts',(-0.8183414399862,2.22617662650169,13.6524289190563));
#93906=CARTESIAN_POINT('Ctrl Pts',(-0.659740015757757,2.28306846175177,
13.641395595291));
#93907=CARTESIAN_POINT('Ctrl Pts',(-0.51417260351606,2.32019359606721,13.6322508311655));
#93908=CARTESIAN_POINT('Ctrl Pts',(-0.246378246363884,2.36202629424293,
13.6156442953703));
#93909=CARTESIAN_POINT('Ctrl Pts',(-0.125452686478198,2.37152461733269,
13.6082215094878));
#93910=CARTESIAN_POINT('Ctrl Pts',(0.0374522253702291,2.37182243152562,
13.5979017024351));
#93911=CARTESIAN_POINT('Ctrl Pts',(0.0792330355859025,2.37079440863415,
13.5952278989353));
#93912=CARTESIAN_POINT('Ctrl Pts',(0.151013878122831,2.36712869859553,13.5905727258431));
#93913=CARTESIAN_POINT('Ctrl Pts',(0.1810315572974,2.36502239065536,13.5886074884343));
#93914=CARTESIAN_POINT('Ctrl Pts',(0.223724930469734,2.36120910433829,13.5857824208118));
#93915=CARTESIAN_POINT('Ctrl Pts',(0.236440285312464,2.35996975819975,13.5849372415586));
#93916=CARTESIAN_POINT('Ctrl Pts',(0.258415757523683,2.35764846159353,13.5834697187558));
#93917=CARTESIAN_POINT('Ctrl Pts',(0.267680745052979,2.35661451804419,13.5828488981799));
#93918=CARTESIAN_POINT('Ctrl Pts',(0.285460491560588,2.35452415254588,13.5816533810088));
#93919=CARTESIAN_POINT('Ctrl Pts',(0.293976101758224,2.35347609407967,13.5810789577061));
#93920=CARTESIAN_POINT('Ctrl Pts',(0.314030930789906,2.35089730365247,13.5797217483405));
#93921=CARTESIAN_POINT('Ctrl Pts',(0.325564850883407,2.34932779263571,13.5789377481315));
#93922=CARTESIAN_POINT('Ctrl Pts',(0.365750351163728,2.34355782812522,13.5761939014556));
#93923=CARTESIAN_POINT('Ctrl Pts',(0.394335183571449,2.33891775109844,13.5742202535806));
#93924=CARTESIAN_POINT('Ctrl Pts',(0.58028056685533,2.30522840748879,13.5612328580375));
#93925=CARTESIAN_POINT('Ctrl Pts',(0.734414311209268,2.26084530820466,13.549727132066));
#93926=CARTESIAN_POINT('Ctrl Pts',(0.991601984140914,2.15769446205777,13.5295072282718));
#93927=CARTESIAN_POINT('Ctrl Pts',(1.09694831991385,2.10609276666328,13.5209093982515));
#93928=CARTESIAN_POINT('Ctrl Pts',(1.2265289986424,2.03024955620763,13.5102075939812));
#93929=CARTESIAN_POINT('Ctrl Pts',(1.25465458333209,2.01299000431196,13.5078773429947));
#93930=CARTESIAN_POINT('Ctrl Pts',(1.30054086387953,1.98349589023642,13.5040740432057));
#93931=CARTESIAN_POINT('Ctrl Pts',(1.31851057437324,1.97159641748497,13.5025842252221));
#93932=CARTESIAN_POINT('Ctrl Pts',(1.34282491584763,1.95501441714933,13.5005704948672));
#93933=CARTESIAN_POINT('Ctrl Pts',(1.34931141997606,1.95054321210731,13.5000334865263));
#93934=CARTESIAN_POINT('Ctrl Pts',(1.36015212862049,1.94299065868512,13.4991365127062));
#93935=CARTESIAN_POINT('Ctrl Pts',(1.36451838486048,1.93992682642096,13.49877538396));
#93936=CARTESIAN_POINT('Ctrl Pts',(1.37277613083524,1.93409063528804,13.4980927183124));
#93937=CARTESIAN_POINT('Ctrl Pts',(1.3766696283295,1.93132121263565,13.4977709796384));
#93938=CARTESIAN_POINT('Ctrl Pts',(1.3868488862342,1.9240343412104,13.4969300975687));
#93939=CARTESIAN_POINT('Ctrl Pts',(1.39312101369233,1.91949780537734,13.4964122541083));
#93940=CARTESIAN_POINT('Ctrl Pts',(1.41482491354248,1.90363727911342,13.4946208680794));
#93941=CARTESIAN_POINT('Ctrl Pts',(1.4301422333882,1.89215688475472,13.4933575778346));
#93942=CARTESIAN_POINT('Ctrl Pts',(1.54664703806597,1.80261293735058,13.4837418965744));
#93943=CARTESIAN_POINT('Ctrl Pts',(1.64152889021988,1.716660232144,13.475863433109));
#93944=CARTESIAN_POINT('Ctrl Pts',(1.8072308338674,1.54018384037335,13.461013656878));
#93945=CARTESIAN_POINT('Ctrl Pts',(1.87930914125581,1.45135981633843,13.454053060609));
#93946=CARTESIAN_POINT('Ctrl Pts',(1.97808110277971,1.30988281367792,13.4432604213924));
#93947=CARTESIAN_POINT('Ctrl Pts',(2.00968241662254,1.26086226877601,13.4395706140131));
#93948=CARTESIAN_POINT('Ctrl Pts',(2.05918342507402,1.177479062386,13.4333307939119));
#93949=CARTESIAN_POINT('Ctrl Pts',(2.07810583053971,1.14375224578573,13.4308165191582));
#93950=CARTESIAN_POINT('Ctrl Pts',(2.10278489984987,1.09712905939844,13.4273460676678));
#93951=CARTESIAN_POINT('Ctrl Pts',(2.10926409742982,1.08462042250214,13.4264154909385));
#93952=CARTESIAN_POINT('Ctrl Pts',(2.11996004870427,1.06351265349513,13.4248456889899));
#93953=CARTESIAN_POINT('Ctrl Pts',(2.1242369000706,1.05494424497924,13.4242085884163));
#93954=CARTESIAN_POINT('Ctrl Pts',(2.13257380404312,1.03798550648644,13.4229477842765));
#93955=CARTESIAN_POINT('Ctrl Pts',(2.13663652184993,1.02959667373577,13.4223241878986));
#93956=CARTESIAN_POINT('Ctrl Pts',(2.14547258275653,1.01107414830746,13.4209473451508));
#93957=CARTESIAN_POINT('Ctrl Pts',(2.15022377211647,1.00093019689202,13.4201933473122));
#93958=CARTESIAN_POINT('Ctrl Pts',(2.16667049002365,0.96515833941974,13.4175343046081));
#93959=CARTESIAN_POINT('Ctrl Pts',(2.17798072385046,0.939356949997527,13.4156161355481));
#93960=CARTESIAN_POINT('Ctrl Pts',(2.26258656372062,0.736602921597457,13.4005343066456));
#93961=CARTESIAN_POINT('Ctrl Pts',(2.31464818703371,0.551594475501066,13.3866370705455));
#93962=CARTESIAN_POINT('Ctrl Pts',(2.34800823595653,0.335824232937742,13.3706890154025));
#93963=CARTESIAN_POINT('Ctrl Pts',(2.35166345550595,0.309191857148216,13.3687266205685));
#93964=CARTESIAN_POINT('Ctrl Pts',(2.36648996811652,0.185602206031561,13.3596598783068));
#93965=CARTESIAN_POINT('Ctrl Pts',(2.3721238684653,0.0880651570359345,13.3526140453319));
#93966=CARTESIAN_POINT('Ctrl Pts',(2.37165522313945,-0.0283108917064951,
13.3445241688066));
#93967=CARTESIAN_POINT('Ctrl Pts',(2.37135709480836,-0.0470700397291419,
13.3432300691523));
#93968=CARTESIAN_POINT('Ctrl Pts',(2.37062935403039,-0.0732815094306271,
13.3414375620916));
#93969=CARTESIAN_POINT('Ctrl Pts',(2.37038712809214,-0.0807377273862422,
13.3409294343541));
#93970=CARTESIAN_POINT('Ctrl Pts',(2.36991446201371,-0.0934402427160046,
13.340066947583));
#93971=CARTESIAN_POINT('Ctrl Pts',(2.36970177305517,-0.0986871072482835,
13.339711613109));
#93972=CARTESIAN_POINT('Ctrl Pts',(2.36925853960096,-0.108791941354843,
13.339029107453));
#93973=CARTESIAN_POINT('Ctrl Pts',(2.36903047824806,-0.113649937096084,
13.3387017940419));
#93974=CARTESIAN_POINT('Ctrl Pts',(2.36844624464178,-0.125327916391205,
13.3379168439044));
#93975=CARTESIAN_POINT('Ctrl Pts',(2.36807555327816,-0.132147180282065,
13.3374600107162));
#93976=CARTESIAN_POINT('Ctrl Pts',(2.36661142138493,-0.157092977580794,
13.3357941475678));
#93977=CARTESIAN_POINT('Ctrl Pts',(2.36533923369439,-0.17520896865986,13.3345946076372));
#93978=CARTESIAN_POINT('Ctrl Pts',(2.35084015901665,-0.35250918177748,13.3229393548876));
#93979=CARTESIAN_POINT('Ctrl Pts',(2.3217699103028,-0.510012011121038,13.3132362294613));
#93980=CARTESIAN_POINT('Ctrl Pts',(2.23004281438386,-0.824852486863105,
13.2931391911143));
#93981=CARTESIAN_POINT('Ctrl Pts',(2.16598237862899,-0.980806740607857,
13.282774641262));
#93982=CARTESIAN_POINT('Ctrl Pts',(2.07610837368012,-1.14690988412821,13.2704417206349));
#93983=CARTESIAN_POINT('Ctrl Pts',(2.06599943664818,-1.16502126345027,13.2690791965614));
#93984=CARTESIAN_POINT('Ctrl Pts',(2.05016104543447,-1.19254310258095,13.2669801551541));
#93985=CARTESIAN_POINT('Ctrl Pts',(2.04460122202787,-1.20205041477193,13.2662497508523));
#93986=CARTESIAN_POINT('Ctrl Pts',(2.03477590275371,-1.21858634427434,13.2649699110149));
#93987=CARTESIAN_POINT('Ctrl Pts',(2.03053966992972,-1.22563220371696,13.2644215489439));
#93988=CARTESIAN_POINT('Ctrl Pts',(2.02089170451218,-1.24149174293454,13.2631802962078));
#93989=CARTESIAN_POINT('Ctrl Pts',(2.01545881076356,-1.25029228797385,13.2624866359622));
#93990=CARTESIAN_POINT('Ctrl Pts',(2.0006176350015,-1.27398486087205,13.2606057640455));
#93991=CARTESIAN_POINT('Ctrl Pts',(1.99110087953804,-1.28880782331417,13.2594145553667));
#93992=CARTESIAN_POINT('Ctrl Pts',(1.94600431330749,-1.35735685484944,13.2538367794574));
#93993=CARTESIAN_POINT('Ctrl Pts',(1.90841258660702,-1.40971998305166,13.2493752408948));
#93994=CARTESIAN_POINT('Ctrl Pts',(1.73568300298879,-1.63073338083704,13.2296310212395));
#93995=CARTESIAN_POINT('Ctrl Pts',(1.57998933007677,-1.78199188103808,13.2135630328312));
#93996=CARTESIAN_POINT('Ctrl Pts',(1.37138139678238,-1.93555198726543,13.1949535309795));
#93997=CARTESIAN_POINT('Ctrl Pts',(1.33604961543301,-1.960107222092,13.1918929568441));
#93998=CARTESIAN_POINT('Ctrl Pts',(1.2782053044385,-1.99801714214975,13.1870490232091));
#93999=CARTESIAN_POINT('Ctrl Pts',(1.25610672041074,-2.01198343719811,13.1852361040396));
#94000=CARTESIAN_POINT('Ctrl Pts',(1.2265403199795,-2.02999230950436,13.1828644113082));
#94001=CARTESIAN_POINT('Ctrl Pts',(1.21927628106825,-2.03436360790525,13.1822859562581));
#94002=CARTESIAN_POINT('Ctrl Pts',(1.20729324094542,-2.04148743168327,13.1813388552885));
#94003=CARTESIAN_POINT('Ctrl Pts',(1.20258797026574,-2.04426272251901,13.1809687630233));
#94004=CARTESIAN_POINT('Ctrl Pts',(1.19335313459514,-2.04966674964374,13.1802459753584));
#94005=CARTESIAN_POINT('Ctrl Pts',(1.18882439710042,-2.05229677243919,13.1798932012966));
#94006=CARTESIAN_POINT('Ctrl Pts',(1.1776508183472,-2.05873633032665,13.1790268496123));
#94007=CARTESIAN_POINT('Ctrl Pts',(1.17099608640866,-2.06252876282544,13.1785143667254));
#94008=CARTESIAN_POINT('Ctrl Pts',(1.1480722880759,-2.07544598099605,13.1767605629602));
#94009=CARTESIAN_POINT('Ctrl Pts',(1.13171350431815,-2.08441133093501,13.1755289304902));
#94010=CARTESIAN_POINT('Ctrl Pts',(0.983055214052431,-2.16361661537799,
13.1644995247509));
#94011=CARTESIAN_POINT('Ctrl Pts',(0.844464836077715,-2.22137948812558,
13.1553594494784));
#94012=CARTESIAN_POINT('Ctrl Pts',(0.58558938442156,-2.30151329482222,13.1387558390886));
#94013=CARTESIAN_POINT('Ctrl Pts',(0.467278928116707,-2.32841699627352,
13.1313311560334));
#94014=CARTESIAN_POINT('Ctrl Pts',(0.306092334984067,-2.35228662032879,
13.1210089236276));
#94015=CARTESIAN_POINT('Ctrl Pts',(0.264595884242198,-2.35731490592322,
13.1183347149211));
#94016=CARTESIAN_POINT('Ctrl Pts',(0.193029779732385,-2.36407343133189,
13.1136788983949));
#94017=CARTESIAN_POINT('Ctrl Pts',(0.16301956448586,-2.36633221929618,13.111713428907));
#94018=CARTESIAN_POINT('Ctrl Pts',(0.120219438727262,-2.36873565030719,
13.1088880855567));
#94019=CARTESIAN_POINT('Ctrl Pts',(0.107457943977824,-2.36934887130852,
13.1080428666357));
#94020=CARTESIAN_POINT('Ctrl Pts',(0.0853771146285568,-2.37023115380912,
13.1065752970797));
#94021=CARTESIAN_POINT('Ctrl Pts',(0.0760599064882378,-2.3705484303326,
13.1059544696866));
#94022=CARTESIAN_POINT('Ctrl Pts',(0.0581648179826237,-2.37105219866113,
13.1047589550329));
#94023=CARTESIAN_POINT('Ctrl Pts',(0.049587305344609,-2.37124709185295,
13.1041845411506));
#94024=CARTESIAN_POINT('Ctrl Pts',(0.0293710595065186,-2.37159669547986,
13.1028273782122));
#94025=CARTESIAN_POINT('Ctrl Pts',(0.0177319593183965,-2.37171227477861,
13.1020434152136));
#94026=CARTESIAN_POINT('Ctrl Pts',(-0.0228617688647179,-2.37181655412525,
13.0992998250801));
#94027=CARTESIAN_POINT('Ctrl Pts',(-0.0518139514957971,-2.37136070888297,
13.0973263999324));
#94028=CARTESIAN_POINT('Ctrl Pts',(-0.241040516821711,-2.36491449632116,
13.0843140434364));
#94029=CARTESIAN_POINT('Ctrl Pts',(-0.400334955452189,-2.34321045976057,
13.0727806591625));
#94030=CARTESIAN_POINT('Ctrl Pts',(-0.669784856626021,-2.27820990407324,
13.052554386564));
#94031=CARTESIAN_POINT('Ctrl Pts',(-0.781201358754205,-2.24244933832728,
13.0439784405596));
#94032=CARTESIAN_POINT('Ctrl Pts',(-0.92007656222129,-2.18626230494038,
13.0333008313638));
#94033=CARTESIAN_POINT('Ctrl Pts',(-0.9503619175815,-2.17326855383347,13.030973767359));
#94034=CARTESIAN_POINT('Ctrl Pts',(-0.999972096075376,-2.15074809679995,
13.0271751001228));
#94035=CARTESIAN_POINT('Ctrl Pts',(-1.01945477092564,-2.1415820370905,13.0256867764275));
#94036=CARTESIAN_POINT('Ctrl Pts',(-1.04589023996994,-2.12870234749524,
13.0236747215502));
#94037=CARTESIAN_POINT('Ctrl Pts',(-1.05295260907856,-2.12521784432056,
13.0231379219405));
#94038=CARTESIAN_POINT('Ctrl Pts',(-1.06476858703089,-2.11931459725055,
13.022241199171));
#94039=CARTESIAN_POINT('Ctrl Pts',(-1.069531575646,-2.11691490535367,13.0218801141194));
#94040=CARTESIAN_POINT('Ctrl Pts',(-1.07854663896613,-2.11233473754071,
13.0211974580525));
#94041=CARTESIAN_POINT('Ctrl Pts',(-1.08280027203294,-2.11015745094376,
13.0208756856676));
#94042=CARTESIAN_POINT('Ctrl Pts',(-1.09392957073957,-2.10441823733817,
13.0200345812468));
#94043=CARTESIAN_POINT('Ctrl Pts',(-1.10079449670808,-2.10083542992669,
13.019516550485));
#94044=CARTESIAN_POINT('Ctrl Pts',(-1.12458202122282,-2.08827209810911,
13.0177238526742));
#94045=CARTESIAN_POINT('Ctrl Pts',(-1.14141381595901,-2.07911991884032,
13.0164594578887));
#94046=CARTESIAN_POINT('Ctrl Pts',(-1.26823101907485,-2.00815954686025,
13.0069499990694));
#94047=CARTESIAN_POINT('Ctrl Pts',(-1.37325339274456,-1.93785925955151,
12.9991664562669));
#94048=CARTESIAN_POINT('Ctrl Pts',(-1.56431801403496,-1.78659266026616,
12.9842144659192));
#94049=CARTESIAN_POINT('Ctrl Pts',(-1.65089020684405,-1.70691658922275,
12.9770593143163));
#94050=CARTESIAN_POINT('Ctrl Pts',(-1.77037226865347,-1.57932403804773,
12.9661180872572));
#94051=CARTESIAN_POINT('Ctrl Pts',(-1.8080130880724,-1.53608929902158,12.9624892104753));
#94052=CARTESIAN_POINT('Ctrl Pts',(-1.8680597955052,-1.46185100805962,12.9563429133728));
#94053=CARTESIAN_POINT('Ctrl Pts',(-1.89134874720401,-1.43159191742304,
12.9538598124634));
#94054=CARTESIAN_POINT('Ctrl Pts',(-1.9221760123903,-1.38947255175145,12.9504256706073));
#94055=CARTESIAN_POINT('Ctrl Pts',(-1.9303551883669,-1.37808687216407,12.949499525053));
#94056=CARTESIAN_POINT('Ctrl Pts',(-1.94394282141897,-1.35881411932749,
12.9479350902317));
#94057=CARTESIAN_POINT('Ctrl Pts',(-1.94940545477528,-1.350965533288,12.9472988930998));
#94058=CARTESIAN_POINT('Ctrl Pts',(-1.96010500023052,-1.33539265302934,
12.9460382262195));
#94059=CARTESIAN_POINT('Ctrl Pts',(-1.96534408426394,-1.3276700553339,12.9454138542165));
#94060=CARTESIAN_POINT('Ctrl Pts',(-1.9767954142291,-1.31057407375535,12.944033278357));
#94061=CARTESIAN_POINT('Ctrl Pts',(-1.98298681722395,-1.30118706865472,
12.9432763079086));
#94062=CARTESIAN_POINT('Ctrl Pts',(-2.00460351973117,-1.26790059181442,
12.9405955817588));
#94063=CARTESIAN_POINT('Ctrl Pts',(-2.01966486030204,-1.24376883345289,
12.9386584164834));
#94064=CARTESIAN_POINT('Ctrl Pts',(-2.13099442350199,-1.05803697931263,
12.9237898750362));
#94065=CARTESIAN_POINT('Ctrl Pts',(-2.20814630307436,-0.885800042265752,
12.91015439604));
#94066=CARTESIAN_POINT('Ctrl Pts',(-2.28862930786293,-0.627802748084554,
12.8904118233233));
#94067=CARTESIAN_POINT('Ctrl Pts',(-2.3090201925046,-0.54807610780382,12.8844110439632));
#94068=CARTESIAN_POINT('Ctrl Pts',(-2.33649802229436,-0.411393016004873,
12.8744296156882));
#94069=CARTESIAN_POINT('Ctrl Pts',(-2.34573737410859,-0.354943166158775,
12.8703943731318));
#94070=CARTESIAN_POINT('Ctrl Pts',(-2.35429878281118,-0.287392065166123,
12.8657096037321));
#94071=CARTESIAN_POINT('Ctrl Pts',(-2.35559519422827,-0.276565092461932,
12.8649631253587));
#94072=CARTESIAN_POINT('Ctrl Pts',(-2.35748886198653,-0.259769698963854,
12.86381233909));
#94073=CARTESIAN_POINT('Ctrl Pts',(-2.35813820516683,-0.253807482666157,
12.8634052226132));
#94074=CARTESIAN_POINT('Ctrl Pts',(-2.35929976534582,-0.242752702777633,
12.8626530498243));
#94075=CARTESIAN_POINT('Ctrl Pts',(-2.35981811096488,-0.237660980140859,
12.8623076673249));
#94076=CARTESIAN_POINT('Ctrl Pts',(-2.36096019249512,-0.226070029910925,
12.8615238080385));
#94077=CARTESIAN_POINT('Ctrl Pts',(-2.36157357650475,-0.219569884800047,
12.8610859154861));
#94078=CARTESIAN_POINT('Ctrl Pts',(-2.36310107688707,-0.202635318454724,
12.8599493010245));
#94079=CARTESIAN_POINT('Ctrl Pts',(-2.36397294002247,-0.192197088300605,
12.8592528659236));
#94080=CARTESIAN_POINT('Ctrl Pts',(-2.36938498223819,-0.121781455892595,
12.8545806993733));
#94081=CARTESIAN_POINT('Ctrl Pts',(-2.37171174752863,-0.0616500417224155,
12.8507175434041));
#94082=CARTESIAN_POINT('Ctrl Pts',(-2.37178614178588,0.056799813610108,
12.8432429961234));
#94083=CARTESIAN_POINT('Ctrl Pts',(-2.36967389599326,0.115027955686387,
12.8396328989325));
#94084=CARTESIAN_POINT('Ctrl Pts',(-2.36542647041237,0.173077079858942,
12.8360489723835));
#94085=CARTESIAN_POINT('',(-2.37174897232385,-0.00158322021055804,12.6497084150621));
#94086=CARTESIAN_POINT('Ctrl Pts',(-2.36542649456986,0.173076749700613,
12.6375766332401));
#94087=CARTESIAN_POINT('Ctrl Pts',(-2.36658602748831,0.157229503369983,
12.6386617202425));
#94088=CARTESIAN_POINT('Ctrl Pts',(-2.36758627251794,0.141371074232541,
12.6397517332812));
#94089=CARTESIAN_POINT('Ctrl Pts',(-2.37067010211813,0.083175043826123,
12.6437674062594));
#94090=CARTESIAN_POINT('Ctrl Pts',(-2.37177781513596,0.0407965685027263,
12.6467221209576));
#94091=CARTESIAN_POINT('Ctrl Pts',(-2.37174946956768,-0.00158622363318729,
12.6497077602747));
#94092=CARTESIAN_POINT('Ctrl Pts',(-2.37174947153371,-0.00158328125955357,
12.6497075530004));
#94093=CARTESIAN_POINT('Ctrl Pts',(-2.37160653311771,-0.215704499816572,
12.6647912319001));
#94094=CARTESIAN_POINT('Ctrl Pts',(-2.34246509598743,-0.428823103194869,
12.6807104451231));
#94095=CARTESIAN_POINT('Ctrl Pts',(-2.2736546331288,-0.676410862535811,
12.6991701563721));
#94096=CARTESIAN_POINT('Ctrl Pts',(-2.26105235453986,-0.717411845906221,
12.7022211463399));
#94097=CARTESIAN_POINT('Ctrl Pts',(-2.23898449953131,-0.782834982600065,
12.7070571680125));
#94098=CARTESIAN_POINT('Ctrl Pts',(-2.23021474331369,-0.807480366208175,
12.7088713744339));
#94099=CARTESIAN_POINT('Ctrl Pts',(-2.21803786776668,-0.839987652639569,
12.7112496634414));
#94100=CARTESIAN_POINT('Ctrl Pts',(-2.21499374392475,-0.84798228726436,
12.7118333755295));
#94101=CARTESIAN_POINT('Ctrl Pts',(-2.20991014190329,-0.861118936225222,
12.7127903557539));
#94102=CARTESIAN_POINT('Ctrl Pts',(-2.20789584492145,-0.866270510409055,
12.7131650872419));
#94103=CARTESIAN_POINT('Ctrl Pts',(-2.20390796817783,-0.87636525428476,
12.7138982417253));
#94104=CARTESIAN_POINT('Ctrl Pts',(-2.20193574563793,-0.881308892588369,
12.7142567383546));
#94105=CARTESIAN_POINT('Ctrl Pts',(-2.19702441069505,-0.893500402927079,
12.7151395732966));
#94106=CARTESIAN_POINT('Ctrl Pts',(-2.1940660232248,-0.900740540506177,
12.7156627626911));
#94107=CARTESIAN_POINT('Ctrl Pts',(-2.18370695453858,-0.925738681962946,
12.7174658277318));
#94108=CARTESIAN_POINT('Ctrl Pts',(-2.17612582538652,-0.943421762126264,
12.7187353858324));
#94109=CARTESIAN_POINT('Ctrl Pts',(-2.1186300402621,-1.07314951455895,12.7280196492916));
#94110=CARTESIAN_POINT('Ctrl Pts',(-2.06029871015184,-1.1812791592184,12.7355998405026));
#94111=CARTESIAN_POINT('Ctrl Pts',(-1.9376385713577,-1.371688989503,12.7495048894272));
#94112=CARTESIAN_POINT('Ctrl Pts',(-1.87575394168097,-1.4551702141512,12.7558286043168));
#94113=CARTESIAN_POINT('Ctrl Pts',(-1.76490856660018,-1.585830236816,12.766485120645));
#94114=CARTESIAN_POINT('Ctrl Pts',(-1.7190383557578,-1.63544056213426,12.7707353018693));
#94115=CARTESIAN_POINT('Ctrl Pts',(-1.6506335766004,-1.70336139418507,12.7769186595485));
#94116=CARTESIAN_POINT('Ctrl Pts',(-1.62978185650955,-1.72332302019158,
12.778784371085));
#94117=CARTESIAN_POINT('Ctrl Pts',(-1.59212183531959,-1.75808054917181,
12.7821251325903));
#94118=CARTESIAN_POINT('Ctrl Pts',(-1.57545833218542,-1.77302852294085,
12.7835936985877));
#94119=CARTESIAN_POINT('Ctrl Pts',(-1.5499884698018,-1.79523366506084,12.7858254879866));
#94120=CARTESIAN_POINT('Ctrl Pts',(-1.54133690593353,-1.80266710831129,
12.7865813862619));
#94121=CARTESIAN_POINT('Ctrl Pts',(-1.52583649139523,-1.81579193636671,
12.7879319902799));
#94122=CARTESIAN_POINT('Ctrl Pts',(-1.5190085266129,-1.82150774003464,12.7885256795905));
#94123=CARTESIAN_POINT('Ctrl Pts',(-1.50417176808201,-1.83378640103706,
12.7898131294515));
#94124=CARTESIAN_POINT('Ctrl Pts',(-1.49615188833904,-1.84033551116142,
12.7905074305846));
#94125=CARTESIAN_POINT('Ctrl Pts',(-1.47466246398457,-1.8576506702423,12.7923637023425));
#94126=CARTESIAN_POINT('Ctrl Pts',(-1.46111817089196,-1.86832252531532,
12.7935294055202));
#94127=CARTESIAN_POINT('Ctrl Pts',(-1.40034548057679,-1.91514169098847,
12.7987421215399));
#94128=CARTESIAN_POINT('Ctrl Pts',(-1.35188740520355,-1.94964984294688,
12.8028522795967));
#94129=CARTESIAN_POINT('Ctrl Pts',(-1.11759999595871,-2.10355510124951,
12.8225273307876));
#94130=CARTESIAN_POINT('Ctrl Pts',(-0.916988769309791,-2.19842589424856,
12.8389486691159));
#94131=CARTESIAN_POINT('Ctrl Pts',(-0.66479954454223,-2.2770862780313,12.8579320995649));
#94132=CARTESIAN_POINT('Ctrl Pts',(-0.623032761525838,-2.28886675115751,
12.8610198450748));
#94133=CARTESIAN_POINT('Ctrl Pts',(-0.555393178803588,-2.30595578311835,
12.8659073020546));
#94134=CARTESIAN_POINT('Ctrl Pts',(-0.529715174909093,-2.31198954099091,
12.8677369074191));
#94135=CARTESIAN_POINT('Ctrl Pts',(-0.495555684710337,-2.3194172233172,
12.8701320799261));
#94136=CARTESIAN_POINT('Ctrl Pts',(-0.487160828402515,-2.32119495637415,
12.8707176205607));
#94137=CARTESIAN_POINT('Ctrl Pts',(-0.473333259457575,-2.32404482467859,
12.8716768182493));
#94138=CARTESIAN_POINT('Ctrl Pts',(-0.467906203561732,-2.325143545657,12.8720519517167));
#94139=CARTESIAN_POINT('Ctrl Pts',(-0.457259059871297,-2.32726029894397,
12.8727852340639));
#94140=CARTESIAN_POINT('Ctrl Pts',(-0.452039328622863,-2.32827979271884,
12.8731434601125));
#94141=CARTESIAN_POINT('Ctrl Pts',(-0.439155929227791,-2.33075116020108,
12.8740246205334));
#94142=CARTESIAN_POINT('Ctrl Pts',(-0.431488354137501,-2.33218281991877,
12.874546415896));
#94143=CARTESIAN_POINT('Ctrl Pts',(-0.405010085574822,-2.33699168423568,
12.876339698901));
#94144=CARTESIAN_POINT('Ctrl Pts',(-0.386165119596994,-2.34017945027589,
12.8776010176428));
#94145=CARTESIAN_POINT('Ctrl Pts',(-0.232265581378858,-2.36430293206934,
12.8877950788121));
#94146=CARTESIAN_POINT('Ctrl Pts',(-0.0956515269750207,-2.3737600966249,
12.896185326393));
#94147=CARTESIAN_POINT('Ctrl Pts',(0.169420606660706,-2.36917351240096,
12.9124373076921));
#94148=CARTESIAN_POINT('Ctrl Pts',(0.297407414053778,-2.35652973621305,
12.9202765722158));
#94149=CARTESIAN_POINT('Ctrl Pts',(0.489999451807937,-2.32155853063592,
12.9326476911491));
#94150=CARTESIAN_POINT('Ctrl Pts',(0.555713278921655,-2.30671083762182,
12.9369710547778));
#94151=CARTESIAN_POINT('Ctrl Pts',(0.637355911334626,-2.28457288130548,
12.9425152962927));
#94152=CARTESIAN_POINT('Ctrl Pts',(0.653959662099677,-2.27987555403383,
12.9436518941431));
#94153=CARTESIAN_POINT('Ctrl Pts',(0.680444685230702,-2.27206961982427,
12.9454801107687));
#94154=CARTESIAN_POINT('Ctrl Pts',(0.690359625870287,-2.26907666423019,
12.9461679550795));
#94155=CARTESIAN_POINT('Ctrl Pts',(0.709130695247628,-2.26327595090908,
12.9474768605706));
#94156=CARTESIAN_POINT('Ctrl Pts',(0.717990573207929,-2.26048090136846,
12.9480974948316));
#94157=CARTESIAN_POINT('Ctrl Pts',(0.738097734960632,-2.25400750343949,
12.9495125730766));
#94158=CARTESIAN_POINT('Ctrl Pts',(0.749334297451787,-2.25029691235278,
12.9503080656128));
#94159=CARTESIAN_POINT('Ctrl Pts',(0.778411428116668,-2.24045299157937,
12.9523790312647));
#94160=CARTESIAN_POINT('Ctrl Pts',(0.796207129189219,-2.23419071039242,
12.9536587315121));
#94161=CARTESIAN_POINT('Ctrl Pts',(0.960320668021123,-2.17422966302381,
12.9655765794031));
#94162=CARTESIAN_POINT('Ctrl Pts',(1.10105794426764,-2.10645305080535,12.9766966511729));
#94163=CARTESIAN_POINT('Ctrl Pts',(1.33046335943887,-1.96667142281494,12.9962491212371));
#94164=CARTESIAN_POINT('Ctrl Pts',(1.4225061700333,-1.90115915901359,13.0045418739486));
#94165=CARTESIAN_POINT('Ctrl Pts',(1.56281094009702,-1.78538250479204,13.017640331429));
#94166=CARTESIAN_POINT('Ctrl Pts',(1.61414520362341,-1.73911070267697,13.0225427884958));
#94167=CARTESIAN_POINT('Ctrl Pts',(1.67161564073098,-1.68256718587607,13.0280949961018));
#94168=CARTESIAN_POINT('Ctrl Pts',(1.6797812696329,-1.67441514718958,13.0288854421533));
#94169=CARTESIAN_POINT('Ctrl Pts',(1.69223278752939,-1.66180158764746,13.030092729751));
#94170=CARTESIAN_POINT('Ctrl Pts',(1.69656111158187,-1.65738249079377,13.0305127694367));
#94171=CARTESIAN_POINT('Ctrl Pts',(1.70448564918962,-1.64922818826259,13.0312823969629));
#94172=CARTESIAN_POINT('Ctrl Pts',(1.70808689163478,-1.64549813641519,13.0316323674027));
#94173=CARTESIAN_POINT('Ctrl Pts',(1.71617657479548,-1.63706392642015,13.0324190478163));
#94174=CARTESIAN_POINT('Ctrl Pts',(1.72065791500058,-1.63235311044019,13.0328552110986));
#94175=CARTESIAN_POINT('Ctrl Pts',(1.73380283699778,-1.61842079654651,13.0341359195323));
#94176=CARTESIAN_POINT('Ctrl Pts',(1.74241223492008,-1.60914815148283,13.0349764487167));
#94177=CARTESIAN_POINT('Ctrl Pts',(1.81512604620786,-1.52956476187093,13.0420948306693));
#94178=CARTESIAN_POINT('Ctrl Pts',(1.87502864835406,-1.45551476617364,13.0480902466388));
#94179=CARTESIAN_POINT('Ctrl Pts',(1.99556106951763,-1.28667778983721,13.0609487725575));
#94180=CARTESIAN_POINT('Ctrl Pts',(2.05422611566453,-1.19078116991798,13.0677614080987));
#94181=CARTESIAN_POINT('Ctrl Pts',(2.1456581979111,-1.01431068431526,13.080015267604));
#94182=CARTESIAN_POINT('Ctrl Pts',(2.18120626342059,-0.935421090181152,
13.0854009400213));
#94183=CARTESIAN_POINT('Ctrl Pts',(2.23082609414845,-0.806992321232268,
13.0941855389465));
#94184=CARTESIAN_POINT('Ctrl Pts',(2.24773222211429,-0.758630941669378,
13.0974964167411));
#94185=CARTESIAN_POINT('Ctrl Pts',(2.26777309820446,-0.694731182493242,
13.1018932967783));
#94186=CARTESIAN_POINT('Ctrl Pts',(2.27233751666291,-0.679653169803669,
13.1029323539921));
#94187=CARTESIAN_POINT('Ctrl Pts',(2.2795608014815,-0.654905459723067,13.1046408108678));
#94188=CARTESIAN_POINT('Ctrl Pts',(2.28230919584446,-0.645262224305075,
13.1053072807735));
#94189=CARTESIAN_POINT('Ctrl Pts',(2.28751159021908,-0.626559557436064,
13.1066014554102));
#94190=CARTESIAN_POINT('Ctrl Pts',(2.28997312925566,-0.617502402677312,
13.1072289014604));
#94191=CARTESIAN_POINT('Ctrl Pts',(2.29553977270727,-0.59652900238041,13.1086836282938));
#94192=CARTESIAN_POINT('Ctrl Pts',(2.2986059382747,-0.584602796202754,13.1095121512591));
#94193=CARTESIAN_POINT('Ctrl Pts',(2.30824328893264,-0.545868856115087,
13.1122075989894));
#94194=CARTESIAN_POINT('Ctrl Pts',(2.31443921213001,-0.518971010775866,
13.1140864887592));
#94195=CARTESIAN_POINT('Ctrl Pts',(2.36130122268905,-0.297967524982086,
13.1295883644198));
#94196=CARTESIAN_POINT('Ctrl Pts',(2.37793496214227,-0.0996058784028845,
13.1440044303405));
#94197=CARTESIAN_POINT('Ctrl Pts',(2.36884002499085,0.119287552253391,13.1600001153947));
#94198=CARTESIAN_POINT('Ctrl Pts',(2.36770012031077,0.140102590333102,13.1615209745401));
#94199=CARTESIAN_POINT('Ctrl Pts',(2.35968690899317,0.257949369536178,13.1701234460742));
#94200=CARTESIAN_POINT('Ctrl Pts',(2.34712282899186,0.354511968694002,13.1771450855675));
#94201=CARTESIAN_POINT('Ctrl Pts',(2.32508783213836,0.468528844570008,13.1852182507133));
#94202=CARTESIAN_POINT('Ctrl Pts',(2.32129423747973,0.486976205396619,13.1865174074998));
#94203=CARTESIAN_POINT('Ctrl Pts',(2.31567560534015,0.512739045552493,13.1883200600941));
#94204=CARTESIAN_POINT('Ctrl Pts',(2.31403494138933,0.520093387744145,13.188833309881));
#94205=CARTESIAN_POINT('Ctrl Pts',(2.31117598739048,0.532627381666701,13.1897056055392));
#94206=CARTESIAN_POINT('Ctrl Pts',(2.30997527318363,0.53781094440367,13.1900656389182));
#94207=CARTESIAN_POINT('Ctrl Pts',(2.30762506290797,0.547803871124166,13.1907582859238));
#94208=CARTESIAN_POINT('Ctrl Pts',(2.30647796480332,0.55261370884598,13.1910910395974));
#94209=CARTESIAN_POINT('Ctrl Pts',(2.30367764894772,0.564194945021064,13.1918908004721));
#94210=CARTESIAN_POINT('Ctrl Pts',(2.30200959446868,0.57096276262445,13.1923569656265));
#94211=CARTESIAN_POINT('Ctrl Pts',(2.29574764300367,0.59589587826222,13.1940702653053));
#94212=CARTESIAN_POINT('Ctrl Pts',(2.29096821941692,0.614014503102291,13.1953072888866));
#94213=CARTESIAN_POINT('Ctrl Pts',(2.24637990683325,0.775273366269205,13.2062610024248));
#94214=CARTESIAN_POINT('Ctrl Pts',(2.19341154052799,0.914456268135927,13.2153324695488));
#94215=CARTESIAN_POINT('Ctrl Pts',(2.04922777007196,1.20725371510017,13.2353321239612));
#94216=CARTESIAN_POINT('Ctrl Pts',(1.95303291388866,1.35736762112661,13.2462423194179));
#94217=CARTESIAN_POINT('Ctrl Pts',(1.82771824553745,1.51165031431606,13.2592186109098));
#94218=CARTESIAN_POINT('Ctrl Pts',(1.8142380990348,1.52780258244728,13.2606003600199));
#94219=CARTESIAN_POINT('Ctrl Pts',(1.79327365962642,1.55225398931975,13.2627292126041));
#94220=CARTESIAN_POINT('Ctrl Pts',(1.78594238108493,1.56068339834222,13.2634700344818));
#94221=CARTESIAN_POINT('Ctrl Pts',(1.77303409324476,1.57531512165759,13.2647682813023));
#94222=CARTESIAN_POINT('Ctrl Pts',(1.7674833646384,1.58154044557804,13.2653246033569));
#94223=CARTESIAN_POINT('Ctrl Pts',(1.75487377164345,1.59553322364326,13.2665841280606));
#94224=CARTESIAN_POINT('Ctrl Pts',(1.74779598968229,1.60328331696349,13.2672881230355));
#94225=CARTESIAN_POINT('Ctrl Pts',(1.72851699179423,1.62411423408215,13.2691979010369));
#94226=CARTESIAN_POINT('Ctrl Pts',(1.71621905558487,1.63710419915523,13.2704078034361));
#94227=CARTESIAN_POINT('Ctrl Pts',(1.65802551091313,1.69719604038684,13.2760957583057));
#94228=CARTESIAN_POINT('Ctrl Pts',(1.6103345845051,1.74251084646752,13.2806518487746));
#94229=CARTESIAN_POINT('Ctrl Pts',(1.416811230463,1.91165598472959,13.2987581489705));
#94230=CARTESIAN_POINT('Ctrl Pts',(1.25810836555815,2.01963541740983,13.3128840143935));
#94231=CARTESIAN_POINT('Ctrl Pts',(1.01894128090298,2.14313622572454,13.3323844957816));
#94232=CARTESIAN_POINT('Ctrl Pts',(0.947951928265619,2.17546866316755,13.337963725656));
#94233=CARTESIAN_POINT('Ctrl Pts',(0.859802384673073,2.2104802475581,13.3445426836938));
#94234=CARTESIAN_POINT('Ctrl Pts',(0.844045961541004,2.21654450020161,13.3457054101287));
#94235=CARTESIAN_POINT('Ctrl Pts',(0.821467496859058,2.22495870265292,13.34735140577));
#94236=CARTESIAN_POINT('Ctrl Pts',(0.814697856314741,2.22744640413542,13.347842353289));
#94237=CARTESIAN_POINT('Ctrl Pts',(0.802966870101622,2.23169666102543,13.3486885451363));
#94238=CARTESIAN_POINT('Ctrl Pts',(0.798010847093563,2.23347363349604,13.3490446328898));
#94239=CARTESIAN_POINT('Ctrl Pts',(0.78762372501528,2.23715892746806,13.3497879594987));
#94240=CARTESIAN_POINT('Ctrl Pts',(0.782191569376079,2.23906398960705,13.3501750066713));
#94241=CARTESIAN_POINT('Ctrl Pts',(0.767708607622437,2.24408403902726,13.3512025743881));
#94242=CARTESIAN_POINT('Ctrl Pts',(0.758645670351082,2.24716408727175,13.3518410700863));
#94243=CARTESIAN_POINT('Ctrl Pts',(0.719161164335299,2.26031683425736,13.3546042131311));
#94244=CARTESIAN_POINT('Ctrl Pts',(0.688554189797122,2.2698278236675,13.3566982821296));
#94245=CARTESIAN_POINT('Ctrl Pts',(0.417116847700562,2.34817947780277,13.3749282247614));
#94246=CARTESIAN_POINT('Ctrl Pts',(0.166965150983491,2.37909465177184,13.3895358083447));
#94247=CARTESIAN_POINT('Ctrl Pts',(-0.149283218388116,2.3679644941074,13.409551387553));
#94248=CARTESIAN_POINT('Ctrl Pts',(-0.215015205268351,2.36290256392582,
13.4137846972655));
#94249=CARTESIAN_POINT('Ctrl Pts',(-0.297464937205378,2.35308444332483,
13.419227497168));
#94250=CARTESIAN_POINT('Ctrl Pts',(-0.314460225316486,2.35087356685176,
13.4203565044592));
#94251=CARTESIAN_POINT('Ctrl Pts',(-0.341659475637941,2.34703506531036,
13.4221753924901));
#94252=CARTESIAN_POINT('Ctrl Pts',(-0.351879571878366,2.34552458017929,
13.4228615675343));
#94253=CARTESIAN_POINT('Ctrl Pts',(-0.371275884753336,2.34252826801927,
13.4241691677416));
#94254=CARTESIAN_POINT('Ctrl Pts',(-0.380453895290972,2.34105516773536,
13.4247901784174));
#94255=CARTESIAN_POINT('Ctrl Pts',(-0.401340443466845,2.33757674096446,
13.4262087255005));
#94256=CARTESIAN_POINT('Ctrl Pts',(-0.413042973831832,2.33553733951994,
13.4270073298483));
#94257=CARTESIAN_POINT('Ctrl Pts',(-0.443438897598897,2.33000464491128,
13.4290917544037));
#94258=CARTESIAN_POINT('Ctrl Pts',(-0.46210616025162,2.32637433812214,13.4303818929892));
#94259=CARTESIAN_POINT('Ctrl Pts',(-0.622927142581399,2.29308677420926,
13.4415857490044));
#94260=CARTESIAN_POINT('Ctrl Pts',(-0.762096568076674,2.25066207411848,
13.4519136922315));
#94261=CARTESIAN_POINT('Ctrl Pts',(-0.988181772134961,2.15835660844579,
13.4696516152788));
#94262=CARTESIAN_POINT('Ctrl Pts',(-1.07743547803684,2.11521605504404,13.4769212064894));
#94263=CARTESIAN_POINT('Ctrl Pts',(-1.23694037536483,2.02539768702431,13.4902090297533));
#94264=CARTESIAN_POINT('Ctrl Pts',(-1.30791634917458,1.98030682670697,13.4962393583677));
#94265=CARTESIAN_POINT('Ctrl Pts',(-1.39062866117043,1.92136856050259,13.5032894703318));
#94266=CARTESIAN_POINT('Ctrl Pts',(-1.40478899155932,1.91103980949199,13.5044972099905));
#94267=CARTESIAN_POINT('Ctrl Pts',(-1.424700977243,1.89617477892827,13.5061951158166));
#94268=CARTESIAN_POINT('Ctrl Pts',(-1.43054769967514,1.89176767849098,13.5066936196878));
#94269=CARTESIAN_POINT('Ctrl Pts',(-1.44057788464989,1.8841341059943,13.5075485954226));
#94270=CARTESIAN_POINT('Ctrl Pts',(-1.44477111738726,1.88092062346485,13.507905959358));
#94271=CARTESIAN_POINT('Ctrl Pts',(-1.45347490386056,1.87420419913461,13.5086475395512));
#94272=CARTESIAN_POINT('Ctrl Pts',(-1.45798357040366,1.87069895664694,13.5090315893851));
#94273=CARTESIAN_POINT('Ctrl Pts',(-1.4698535142068,1.86140174127125,13.51004254892));
#94274=CARTESIAN_POINT('Ctrl Pts',(-1.47719331110825,1.85558231415524,13.510667547924));
#94275=CARTESIAN_POINT('Ctrl Pts',(-1.50809006935702,1.83078601625937,13.5132988556975));
#94276=CARTESIAN_POINT('Ctrl Pts',(-1.53131854773121,1.81140189146337,13.5152780554275));
#94277=CARTESIAN_POINT('Ctrl Pts',(-1.74491179341248,1.62611242206457,13.53355577674));
#94278=CARTESIAN_POINT('Ctrl Pts',(-1.90802639374918,1.43123425867429,13.5482687024767));
#94279=CARTESIAN_POINT('Ctrl Pts',(-2.05967506020098,1.17679212077054,13.5670027289252));
#94280=CARTESIAN_POINT('Ctrl Pts',(-2.08096963471221,1.13871246435083,13.5697901062475));
#94281=CARTESIAN_POINT('Ctrl Pts',(-2.11566382405464,1.07244437286819,13.5746305118822));
#94282=CARTESIAN_POINT('Ctrl Pts',(-2.12957972161713,1.04453837175365,13.5766657565784));
#94283=CARTESIAN_POINT('Ctrl Pts',(-2.14854084804998,1.00456012869067,13.5795811064392));
#94284=CARTESIAN_POINT('Ctrl Pts',(-2.15404299289103,0.992707208167887,
13.5804454101347));
#94285=CARTESIAN_POINT('Ctrl Pts',(-2.16336581961056,0.972181157002413,
13.5819423516776));
#94286=CARTESIAN_POINT('Ctrl Pts',(-2.16723302394512,0.963529390802686,
13.5825733758317));
#94287=CARTESIAN_POINT('Ctrl Pts',(-2.17454358820276,0.946907399920196,
13.5837859397255));
#94288=CARTESIAN_POINT('Ctrl Pts',(-2.17799524484547,0.938940973105493,
13.5843671835787));
#94289=CARTESIAN_POINT('Ctrl Pts',(-2.1860033222167,0.920176555789852,13.5857365877449));
#94290=CARTESIAN_POINT('Ctrl Pts',(-2.19052356560152,0.909363468870273,
13.5865259623491));
#94291=CARTESIAN_POINT('Ctrl Pts',(-2.20589849194404,0.871804488526548,
13.5892689786342));
#94292=CARTESIAN_POINT('Ctrl Pts',(-2.21634456726761,0.844895173250619,
13.5912362625293));
#94293=CARTESIAN_POINT('Ctrl Pts',(-2.28496930534364,0.658078748583226,
13.6049137389491));
#94294=CARTESIAN_POINT('Ctrl Pts',(-2.32627207435697,0.492534002123081,
13.6171861893278));
#94295=CARTESIAN_POINT('Ctrl Pts',(-2.3564272854985,0.273881811246033,13.633303083632));
#94296=CARTESIAN_POINT('Ctrl Pts',(-2.3617342843641,0.22353792809192,13.6370032909136));
#94297=CARTESIAN_POINT('Ctrl Pts',(-2.3654265016339,0.173076653156924,13.6406850658798));
#94298=CARTESIAN_POINT('Origin',(0.,0.,-1.84858989190503));
#94299=CARTESIAN_POINT('',(-2.36542649432832,0.173076753001719,14.8389825814723));
#94300=CARTESIAN_POINT('',(-2.3654265029177,0.173076635611311,14.6411792785331));
#94301=CARTESIAN_POINT('',(-2.36542649454111,0.173076750093529,-1.84858989190503));
#94302=CARTESIAN_POINT('',(-2.37174914129228,0.00201823668619566,13.8479759907678));
#94303=CARTESIAN_POINT('Ctrl Pts',(-2.36542649432832,0.173076753001719,
14.8389825814723));
#94304=CARTESIAN_POINT('Ctrl Pts',(-2.3614020125275,0.228079032120752,14.8351425342295));
#94305=CARTESIAN_POINT('Ctrl Pts',(-2.35546045181701,0.282922847275077,
14.8312473450475));
#94306=CARTESIAN_POINT('Ctrl Pts',(-2.32776585976983,0.475558337415043,
14.8173422565782));
#94307=CARTESIAN_POINT('Ctrl Pts',(-2.29578163802699,0.61158049665499,14.8070970944981));
#94308=CARTESIAN_POINT('Ctrl Pts',(-2.21939821692657,0.842790865555311,
14.7893681751657));
#94309=CARTESIAN_POINT('Ctrl Pts',(-2.18028755787251,0.939348953397733,
14.7818688675747));
#94310=CARTESIAN_POINT('Ctrl Pts',(-2.12945263491179,1.04440852039878,14.7738162003158));
#94311=CARTESIAN_POINT('Ctrl Pts',(-2.12385882784374,1.0557373626657,14.7729493760261));
#94312=CARTESIAN_POINT('Ctrl Pts',(-2.11527540425551,1.07277656358541,14.7716485190868));
#94313=CARTESIAN_POINT('Ctrl Pts',(-2.11235271387947,1.07852009990428,14.7712105298397));
#94314=CARTESIAN_POINT('Ctrl Pts',(-2.10706947699421,1.08879861216497,14.7704277086525));
#94315=CARTESIAN_POINT('Ctrl Pts',(-2.10471765450586,1.09333791444461,14.7700823474971));
#94316=CARTESIAN_POINT('Ctrl Pts',(-2.0995449760829,1.10324326656844,14.7693295106624));
#94317=CARTESIAN_POINT('Ctrl Pts',(-2.09671822246143,1.10860611107363,14.7689224125096));
#94318=CARTESIAN_POINT('Ctrl Pts',(-2.0886079695387,1.12385068988137,14.7677664238005));
#94319=CARTESIAN_POINT('Ctrl Pts',(-2.08327487097476,1.13370606768764,14.767020586303));
#94320=CARTESIAN_POINT('Ctrl Pts',(-2.04717315776957,1.19930571430767,14.7620635953376));
#94321=CARTESIAN_POINT('Ctrl Pts',(-2.01423723317738,1.25383498793287,14.7579791816982));
#94322=CARTESIAN_POINT('Ctrl Pts',(-1.86232455973589,1.48387481152358,14.7406124006808));
#94323=CARTESIAN_POINT('Ctrl Pts',(-1.72231641754659,1.64431575023663,14.7280561531223));
#94324=CARTESIAN_POINT('Ctrl Pts',(-1.51146028422509,1.82903024844436,14.7103594773067));
#94325=CARTESIAN_POINT('Ctrl Pts',(-1.45816436874979,1.8717956963686,14.7059791279234));
#94326=CARTESIAN_POINT('Ctrl Pts',(-1.38882917100014,1.9226713065059,14.7003469749911));
#94327=CARTESIAN_POINT('Ctrl Pts',(-1.37444074962452,1.932983190984,14.6991817101431));
#94328=CARTESIAN_POINT('Ctrl Pts',(-1.35136637512529,1.94913223205842,14.6973178332736));
#94329=CARTESIAN_POINT('Ctrl Pts',(-1.34275469855957,1.95507476874487,14.696623262589));
#94330=CARTESIAN_POINT('Ctrl Pts',(-1.32656291567021,1.96609055866013,14.6953191344407));
#94331=CARTESIAN_POINT('Ctrl Pts',(-1.3189922916831,1.97117746145599,14.6947101094603));
#94332=CARTESIAN_POINT('Ctrl Pts',(-1.30200267756705,1.98245153446869,14.6933448911927));
#94333=CARTESIAN_POINT('Ctrl Pts',(-1.29256860427577,1.9886154617011,14.6925878433771));
#94334=CARTESIAN_POINT('Ctrl Pts',(-1.26460542229226,2.00660267640408,14.6903467207935));
#94335=CARTESIAN_POINT('Ctrl Pts',(-1.24595590779675,2.01823561409474,14.6888556472716));
#94336=CARTESIAN_POINT('Ctrl Pts',(-1.09905939912294,2.10705266996693,14.6771353604057));
#94337=CARTESIAN_POINT('Ctrl Pts',(-0.963951845381477,2.17218413718589,
14.6664668985994));
#94338=CARTESIAN_POINT('Ctrl Pts',(-0.667864472189908,2.28182970133326,
14.6435029238538));
#94339=CARTESIAN_POINT('Ctrl Pts',(-0.506459933749803,2.32299241982373,
14.6312182235382));
#94340=CARTESIAN_POINT('Ctrl Pts',(-0.336837498890614,2.34771517576119,
14.6192116560624));
#94341=CARTESIAN_POINT('Ctrl Pts',(-0.331600166535559,2.34846064003882,
14.618841846049));
#94342=CARTESIAN_POINT('Ctrl Pts',(-0.304918044152087,2.35216744604212,
14.6169625838682));
#94343=CARTESIAN_POINT('Ctrl Pts',(-0.283435003853626,2.35485273216162,
14.6154651823659));
#94344=CARTESIAN_POINT('Ctrl Pts',(-0.25382435813423,2.35814282043155,14.6134255161708));
#94345=CARTESIAN_POINT('Ctrl Pts',(-0.245726716122556,2.35900037139999,
14.6128702160168));
#94346=CARTESIAN_POINT('Ctrl Pts',(-0.232795285031159,2.36030251815304,
14.6119875767147));
#94347=CARTESIAN_POINT('Ctrl Pts',(-0.227964364108627,2.36077399844215,
14.6116587617775));
#94348=CARTESIAN_POINT('Ctrl Pts',(-0.217896631833942,2.36172538071267,
14.6109754714222));
#94349=CARTESIAN_POINT('Ctrl Pts',(-0.212659636586564,2.36220269996234,
14.610621153585));
#94350=CARTESIAN_POINT('Ctrl Pts',(-0.199949823355986,2.36331851009633,
14.6097638618266));
#94351=CARTESIAN_POINT('Ctrl Pts',(-0.192475393937949,2.36393898792157,
14.6092618906104));
#94352=CARTESIAN_POINT('Ctrl Pts',(-0.166041669104612,2.36600713639777,
14.6074939730283));
#94353=CARTESIAN_POINT('Ctrl Pts',(-0.147067420757558,2.36726230825546,
14.6062382757939));
#94354=CARTESIAN_POINT('Ctrl Pts',(-0.100211970523747,2.36979629669898,
14.6031657232352));
#94355=CARTESIAN_POINT('Ctrl Pts',(-0.0723187815931293,2.3708114790126,
14.6013612984657));
#94356=CARTESIAN_POINT('Ctrl Pts',(0.164682695112942,2.37525029564411,14.5861898389889));
#94357=CARTESIAN_POINT('Ctrl Pts',(0.373395163448005,2.35149516409628,14.5738139188356));
#94358=CARTESIAN_POINT('Ctrl Pts',(0.66579311152404,2.27825117407371,14.5550034499326));
#94359=CARTESIAN_POINT('Ctrl Pts',(0.753888379076735,2.25063504354883,14.5491441322446));
#94360=CARTESIAN_POINT('Ctrl Pts',(0.856599263480938,2.21172904269297,14.5419632546389));
#94361=CARTESIAN_POINT('Ctrl Pts',(0.872983393215745,2.20531349792047,14.5408070339504));
#94362=CARTESIAN_POINT('Ctrl Pts',(0.899827365795049,2.19445616723867,14.5388941507435));
#94363=CARTESIAN_POINT('Ctrl Pts',(0.910329555800329,2.19012037348924,14.5381410604948));
#94364=CARTESIAN_POINT('Ctrl Pts',(0.929211988542956,2.18216554422235,14.5367783278065));
#94365=CARTESIAN_POINT('Ctrl Pts',(0.93760331234588,2.17857325025094,14.5361696040151));
#94366=CARTESIAN_POINT('Ctrl Pts',(0.955507824629391,2.17078579265972,14.5348639633414));
#94367=CARTESIAN_POINT('Ctrl Pts',(0.965014553459373,2.16657634672054,14.5341665678627));
#94368=CARTESIAN_POINT('Ctrl Pts',(0.990779656584828,2.15496470000367,14.5322650262955));
#94369=CARTESIAN_POINT('Ctrl Pts',(1.00698229716312,2.14744122360354,14.5310567316241));
#94370=CARTESIAN_POINT('Ctrl Pts',(1.09344492277928,2.10609978824017,14.5245401301736));
#94371=CARTESIAN_POINT('Ctrl Pts',(1.16208241806356,2.06901912609388,14.5191191829032));
#94372=CARTESIAN_POINT('Ctrl Pts',(1.38520005734614,1.93387433498121,14.5006373631487));
#94373=CARTESIAN_POINT('Ctrl Pts',(1.53014170349035,1.82134602101831,14.4871187880885));
#94374=CARTESIAN_POINT('Ctrl Pts',(1.68503945359044,1.66943194150703,14.4714173817469));
#94375=CARTESIAN_POINT('Ctrl Pts',(1.70886925854408,1.64503100251655,14.4689632777369));
#94376=CARTESIAN_POINT('Ctrl Pts',(1.76589338603999,1.58406330280113,14.4630103526347));
#94377=CARTESIAN_POINT('Ctrl Pts',(1.79849009039522,1.54695514945682,14.45953704692));
#94378=CARTESIAN_POINT('Ctrl Pts',(1.83620691712339,1.50121293735987,14.4554575092086));
#94379=CARTESIAN_POINT('Ctrl Pts',(1.84245901027645,1.49353303608209,14.4547791679922));
#94380=CARTESIAN_POINT('Ctrl Pts',(1.85264435230421,1.48086034350073,14.4536709138133));
#94381=CARTESIAN_POINT('Ctrl Pts',(1.85660588268961,1.47589059616435,14.4532390653167));
#94382=CARTESIAN_POINT('Ctrl Pts',(1.86371546914683,1.46689768110117,14.4524626882875));
#94383=CARTESIAN_POINT('Ctrl Pts',(1.8668705254502,1.46288024097705,14.4521176701031));
#94384=CARTESIAN_POINT('Ctrl Pts',(1.87378732991716,1.45401401772847,14.4513602243834));
#94385=CARTESIAN_POINT('Ctrl Pts',(1.87754324314238,1.44916082399513,14.4509482083382));
#94386=CARTESIAN_POINT('Ctrl Pts',(1.88831762339303,1.43512653239419,14.4497640346406));
#94387=CARTESIAN_POINT('Ctrl Pts',(1.89528800461799,1.42590848369943,14.4489951684103));
#94388=CARTESIAN_POINT('Ctrl Pts',(1.94564823884009,1.35828734841707,14.4434167151619));
#94389=CARTESIAN_POINT('Ctrl Pts',(1.98640255118573,1.29795950757444,14.4387731377725));
#94390=CARTESIAN_POINT('Ctrl Pts',(2.08193205575991,1.14148175315283,14.4272853826972));
#94391=CARTESIAN_POINT('Ctrl Pts',(2.13287567818831,1.04319960590128,14.4205608433446));
#94392=CARTESIAN_POINT('Ctrl Pts',(2.23828765215156,0.799540074808669,14.4042725433401));
#94393=CARTESIAN_POINT('Ctrl Pts',(2.28571067915955,0.651699933567038,14.3946716787535));
#94394=CARTESIAN_POINT('Ctrl Pts',(2.32232527186871,0.482029973092071,14.3833370262321));
#94395=CARTESIAN_POINT('Ctrl Pts',(2.32605254044154,0.463710156781885,14.3821096695008));
#94396=CARTESIAN_POINT('Ctrl Pts',(2.33175882300326,0.433861308176566,14.3801033048129));
#94397=CARTESIAN_POINT('Ctrl Pts',(2.33386984982371,0.42235809351864,14.3793285022335));
#94398=CARTESIAN_POINT('Ctrl Pts',(2.33748254485082,0.401817541018991,14.3779419550727));
#94399=CARTESIAN_POINT('Ctrl Pts',(2.33901710283989,0.39278616615475,14.3773312694123));
#94400=CARTESIAN_POINT('Ctrl Pts',(2.34214792138358,0.373691051012584,14.3760377881741));
#94401=CARTESIAN_POINT('Ctrl Pts',(2.3437317226846,0.363625485493788,14.3753546103965));
#94402=CARTESIAN_POINT('Ctrl Pts',(2.34777256758438,0.336820819772042,14.3735315604107));
#94403=CARTESIAN_POINT('Ctrl Pts',(2.3501154081109,0.320065362640248,14.3723881025388));
#94404=CARTESIAN_POINT('Ctrl Pts',(2.36060566184537,0.238703386839367,14.3668157760449));
#94405=CARTESIAN_POINT('Ctrl Pts',(2.36626854351113,0.173810654741295,14.3623096528739));
#94406=CARTESIAN_POINT('Ctrl Pts',(2.38032334842894,-0.132327988621367,
14.340744983751));
#94407=CARTESIAN_POINT('Ctrl Pts',(2.35452810697936,-0.37365024381514,14.3226635346676));
#94408=CARTESIAN_POINT('Ctrl Pts',(2.28228604974796,-0.646569493660247,
14.3026407962111));
#94409=CARTESIAN_POINT('Ctrl Pts',(2.27075790852634,-0.685959730104411,
14.299767256913));
#94410=CARTESIAN_POINT('Ctrl Pts',(2.25508161952206,-0.734785582349324,
14.2962421800859));
#94411=CARTESIAN_POINT('Ctrl Pts',(2.25188745200605,-0.744517209917209,
14.2955414405841));
#94412=CARTESIAN_POINT('Ctrl Pts',(2.2467498075832,-0.759834410856349,14.2944417686379));
#94413=CARTESIAN_POINT('Ctrl Pts',(2.24484835788753,-0.765433786711405,
14.2940404625193));
#94414=CARTESIAN_POINT('Ctrl Pts',(2.24142571780832,-0.77539029607059,14.2933281873422));
#94415=CARTESIAN_POINT('Ctrl Pts',(2.23991276206047,-0.779750074491153,
14.2930167486488));
#94416=CARTESIAN_POINT('Ctrl Pts',(2.23627877140925,-0.790124032176763,
14.2922767459517));
#94417=CARTESIAN_POINT('Ctrl Pts',(2.23414619835565,-0.796134094526861,
14.2918488712038));
#94418=CARTESIAN_POINT('Ctrl Pts',(2.22768785060494,-0.81410482678005,14.2905717882783));
#94419=CARTESIAN_POINT('Ctrl Pts',(2.22328999363442,-0.826039618172592,
14.2897267179865));
#94420=CARTESIAN_POINT('Ctrl Pts',(2.21293871573412,-0.853448990776743,
14.2877917561236));
#94421=CARTESIAN_POINT('Ctrl Pts',(2.20691855158682,-0.86889785440863,14.2867054516841));
#94422=CARTESIAN_POINT('Ctrl Pts',(2.18600202948953,-0.920953324840884,
14.2830556117379));
#94423=CARTESIAN_POINT('Ctrl Pts',(2.17035222050802,-0.957252062871989,
14.2805282152508));
#94424=CARTESIAN_POINT('Ctrl Pts',(2.08239057215326,-1.14801170044348,14.2672544360006));
#94425=CARTESIAN_POINT('Ctrl Pts',(1.99448105722603,-1.294733522514,14.2570414815074));
#94426=CARTESIAN_POINT('Ctrl Pts',(1.82491817790297,-1.51890948996825,14.2396220593414));
#94427=CARTESIAN_POINT('Ctrl Pts',(1.75217675144003,-1.60227468719246,14.2326524475735));
#94428=CARTESIAN_POINT('Ctrl Pts',(1.66095843026834,-1.69314755491943,14.2242404474436));
#94429=CARTESIAN_POINT('Ctrl Pts',(1.64787291576171,-1.70588580291266,14.2230411114145));
#94430=CARTESIAN_POINT('Ctrl Pts',(1.62626260432966,-1.72644193256843,14.2210715326259));
#94431=CARTESIAN_POINT('Ctrl Pts',(1.61782524817451,-1.73435096307022,14.2203052403666));
#94432=CARTESIAN_POINT('Ctrl Pts',(1.60261172925364,-1.7484042350013,14.2189281171644));
#94433=CARTESIAN_POINT('Ctrl Pts',(1.595857182125,-1.75457162120467,14.2183182901236));
#94434=CARTESIAN_POINT('Ctrl Pts',(1.58144630540479,-1.7675777298281,14.2170204762423));
#94435=CARTESIAN_POINT('Ctrl Pts',(1.57378093152755,-1.77440610393022,14.2163320711971));
#94436=CARTESIAN_POINT('Ctrl Pts',(1.55310532298312,-1.79258472859395,14.2144802153294));
#94437=CARTESIAN_POINT('Ctrl Pts',(1.54001528509315,-1.80384285556825,14.2133129762345));
#94438=CARTESIAN_POINT('Ctrl Pts',(1.47361671150651,-1.85969960857639,14.2074168990212));
#94439=CARTESIAN_POINT('Ctrl Pts',(1.4184939116039,-1.90207837219248,14.2025994923366));
#94440=CARTESIAN_POINT('Ctrl Pts',(1.25002887732396,-2.02019596502572,14.188086594073));
#94441=CARTESIAN_POINT('Ctrl Pts',(1.13194137124756,-2.08865138613334,14.1781615053262));
#94442=CARTESIAN_POINT('Ctrl Pts',(0.893907777729786,-2.20049967436686,
14.1589489649872));
#94443=CARTESIAN_POINT('Ctrl Pts',(0.775018034314984,-2.24513333449316,
14.1497002682192));
#94444=CARTESIAN_POINT('Ctrl Pts',(0.634684710045782,-2.2853317256098,14.1395438220636));
#94445=CARTESIAN_POINT('Ctrl Pts',(0.616186102927349,-2.29038872746865,
14.1382199980675));
#94446=CARTESIAN_POINT('Ctrl Pts',(0.590130937384832,-2.29717294675024,
14.1363782966847));
#94447=CARTESIAN_POINT('Ctrl Pts',(0.582624754501801,-2.29908818235827,
14.1358503773092));
#94448=CARTESIAN_POINT('Ctrl Pts',(0.570472835117067,-2.30212546259906,
14.1350001504593));
#94449=CARTESIAN_POINT('Ctrl Pts',(0.565832935305995,-2.30327028190814,
14.1346765551882));
#94450=CARTESIAN_POINT('Ctrl Pts',(0.556008371373249,-2.30566285266996,
14.133993621224));
#94451=CARTESIAN_POINT('Ctrl Pts',(0.550822897572116,-2.3069071580499,14.1336344890514));
#94452=CARTESIAN_POINT('Ctrl Pts',(0.537972579863874,-2.30994491941135,
14.1327476887345));
#94453=CARTESIAN_POINT('Ctrl Pts',(0.530302835566549,-2.31171774540812,
14.132221194423));
#94454=CARTESIAN_POINT('Ctrl Pts',(0.501646433458125,-2.31819141710669,
14.1302639873015));
#94455=CARTESIAN_POINT('Ctrl Pts',(0.480604186342854,-2.32264510584657,
14.1288466546656));
#94456=CARTESIAN_POINT('Ctrl Pts',(0.427224006931558,-2.33318672682754,
14.1252944326726));
#94457=CARTESIAN_POINT('Ctrl Pts',(0.39481375911396,-2.33888926214865,14.1231775836762));
#94458=CARTESIAN_POINT('Ctrl Pts',(0.247124019929762,-2.36171732498843,
14.1136690406334));
#94459=CARTESIAN_POINT('Ctrl Pts',(0.130789282120243,-2.37100772415138,
14.1065523347632));
#94460=CARTESIAN_POINT('Ctrl Pts',(-0.146525832010526,-2.3726721650846,
14.089560617621));
#94461=CARTESIAN_POINT('Ctrl Pts',(-0.306946807904424,-2.3572903870215,
14.0796850104309));
#94462=CARTESIAN_POINT('Ctrl Pts',(-0.492959690905339,-2.32013511567851,
14.0673940742713));
#94463=CARTESIAN_POINT('Ctrl Pts',(-0.521242403944802,-2.31394521298482,
14.065502999199));
#94464=CARTESIAN_POINT('Ctrl Pts',(-0.560726259194147,-2.3045432504025,
14.0628285185071));
#94465=CARTESIAN_POINT('Ctrl Pts',(-0.572028589097567,-2.30176384884208,
14.0620589591454));
#94466=CARTESIAN_POINT('Ctrl Pts',(-0.591625920194157,-2.29679133634868,
14.060717464676));
#94467=CARTESIAN_POINT('Ctrl Pts',(-0.599930398558999,-2.29463617720601,
14.0601467614224));
#94468=CARTESIAN_POINT('Ctrl Pts',(-0.617233910138552,-2.29004525646018,
14.0589528590178));
#94469=CARTESIAN_POINT('Ctrl Pts',(-0.62623062424451,-2.28760140265372,
14.0583294063964));
#94470=CARTESIAN_POINT('Ctrl Pts',(-0.647522737391686,-2.2816826284064,
14.0568473824666));
#94471=CARTESIAN_POINT('Ctrl Pts',(-0.659804820587774,-2.27816129801967,
14.0559873146583));
#94472=CARTESIAN_POINT('Ctrl Pts',(-0.699932460915938,-2.2663048012793,
14.0531599676609));
#94473=CARTESIAN_POINT('Ctrl Pts',(-0.727652378417647,-2.25755726109058,
14.051179315727));
#94474=CARTESIAN_POINT('Ctrl Pts',(-0.793600692890124,-2.23540526412616,
14.0463988198523));
#94475=CARTESIAN_POINT('Ctrl Pts',(-0.831659048533409,-2.22152687153939,
14.0435841469416));
#94476=CARTESIAN_POINT('Ctrl Pts',(-1.06563532935693,-2.12934986788801,
14.0259271422914));
#94477=CARTESIAN_POINT('Ctrl Pts',(-1.2507185170132,-2.02617540701597,14.0102831756595));
#94478=CARTESIAN_POINT('Ctrl Pts',(-1.43172899683686,-1.89091949464764,
13.9939812907566));
#94479=CARTESIAN_POINT('Ctrl Pts',(-1.44369633829074,-1.88179843590999,
13.9928988888703));
#94480=CARTESIAN_POINT('Ctrl Pts',(-1.50182145098892,-1.83661678339207,
13.987621698453));
#94481=CARTESIAN_POINT('Ctrl Pts',(-1.54672378788611,-1.79896518351512,
13.9834822457971));
#94482=CARTESIAN_POINT('Ctrl Pts',(-1.59792210108302,-1.75269838740008,
13.9787296496769));
#94483=CARTESIAN_POINT('Ctrl Pts',(-1.60560851278842,-1.74565975837149,
13.9780152454683));
#94484=CARTESIAN_POINT('Ctrl Pts',(-1.61802278778451,-1.73414034654459,
13.9768603116519));
#94485=CARTESIAN_POINT('Ctrl Pts',(-1.6227789263163,-1.72969044692717,13.9764175682375));
#94486=CARTESIAN_POINT('Ctrl Pts',(-1.6312387741586,-1.72170970447448,13.9756296703288));
#94487=CARTESIAN_POINT('Ctrl Pts',(-1.63494943602169,-1.71818642416049,
13.9752839561611));
#94488=CARTESIAN_POINT('Ctrl Pts',(-1.6421509175494,-1.71130414982235,13.9746127737307));
#94489=CARTESIAN_POINT('Ctrl Pts',(-1.64564283062835,-1.70794648753418,
13.9742872080722));
#94490=CARTESIAN_POINT('Ctrl Pts',(-1.65566521381503,-1.6982501543112,13.9733523529318));
#94491=CARTESIAN_POINT('Ctrl Pts',(-1.66216961300225,-1.69188447336643,
13.9727451194643));
#94492=CARTESIAN_POINT('Ctrl Pts',(-1.69213134149449,-1.66222217062738,
13.9699445903256));
#94493=CARTESIAN_POINT('Ctrl Pts',(-1.71513794421006,-1.63847280366575,
13.9677844641144));
#94494=CARTESIAN_POINT('Ctrl Pts',(-1.7789945197234,-1.56973503185522,13.961733322715));
#94495=CARTESIAN_POINT('Ctrl Pts',(-1.81862460942257,-1.52364536535424,
13.9579100832205));
#94496=CARTESIAN_POINT('Ctrl Pts',(-1.91222348598784,-1.40592757866267,
13.9485616066458));
#94497=CARTESIAN_POINT('Ctrl Pts',(-1.96398375717597,-1.33266642323371,
13.9430964747904));
#94498=CARTESIAN_POINT('Ctrl Pts',(-2.09559796324398,-1.12199622193867,
13.9278625780495));
#94499=CARTESIAN_POINT('Ctrl Pts',(-2.16597593315566,-0.979257059794558,
13.9180382995999));
#94500=CARTESIAN_POINT('Ctrl Pts',(-2.2281211920225,-0.813034130090632,
13.906450319185));
#94501=CARTESIAN_POINT('Ctrl Pts',(-2.23446918232746,-0.79542189007037,
13.9052212695859));
#94502=CARTESIAN_POINT('Ctrl Pts',(-2.24444554133774,-0.766680663226114,
13.9032126840807));
#94503=CARTESIAN_POINT('Ctrl Pts',(-2.2482012725681,-0.755596490921561,
13.9024373691801));
#94504=CARTESIAN_POINT('Ctrl Pts',(-2.25475060810512,-0.735786446979471,
13.9010502513684));
#94505=CARTESIAN_POINT('Ctrl Pts',(-2.25757599386896,-0.727071267594697,
13.9004395106939));
#94506=CARTESIAN_POINT('Ctrl Pts',(-2.26343555747647,-0.70863338523543,
13.8991462741429));
#94507=CARTESIAN_POINT('Ctrl Pts',(-2.26645773538514,-0.698907093689615,
13.8984633981684));
#94508=CARTESIAN_POINT('Ctrl Pts',(-2.2743273041869,-0.672992518790541,
13.8966420101112));
#94509=CARTESIAN_POINT('Ctrl Pts',(-2.27906441647683,-0.656771632021285,
13.8954999239152));
#94510=CARTESIAN_POINT('Ctrl Pts',(-2.28905978403994,-0.621134424448397,
13.8929858820058));
#94511=CARTESIAN_POINT('Ctrl Pts',(-2.29424512680767,-0.601699196310096,
13.8916116620672));
#94512=CARTESIAN_POINT('Ctrl Pts',(-2.34755169363489,-0.391185040414472,
13.8766899946634));
#94513=CARTESIAN_POINT('Ctrl Pts',(-2.37191673355796,-0.194929333901108,
13.8623564033571));
#94514=CARTESIAN_POINT('Ctrl Pts',(-2.37174914129228,0.00201823668619566,
13.8479759907678));
#94515=CARTESIAN_POINT('Ctrl Pts',(-2.3717491398467,0.00201993475696598,
13.8479758667807));
#94516=CARTESIAN_POINT('Ctrl Pts',(-2.37170051413794,0.0591148396921598,
13.8438069996322));
#94517=CARTESIAN_POINT('Ctrl Pts',(-2.36959025382119,0.116171024686506,
13.8396487900764));
#94518=CARTESIAN_POINT('Ctrl Pts',(-2.36542648366643,0.173076898716907,
13.8355365560746));
#94519=CARTESIAN_POINT('Ctrl Pts',(-2.3654265016339,0.173076653156924,13.6406850658798));
#94520=CARTESIAN_POINT('Ctrl Pts',(-2.36966457379971,0.115155217573458,
13.644911151959));
#94521=CARTESIAN_POINT('Ctrl Pts',(-2.37177512500354,0.0570791205575195,
13.6491130294797));
#94522=CARTESIAN_POINT('Ctrl Pts',(-2.37172935718148,-0.0478396125883249,
13.6565829838009));
#94523=CARTESIAN_POINT('Ctrl Pts',(-2.37032343645748,-0.0946377349083146,
13.6598712536482));
#94524=CARTESIAN_POINT('Ctrl Pts',(-2.36689050219465,-0.152130446883851,
13.6638337330577));
#94525=CARTESIAN_POINT('Ctrl Pts',(-2.36617441736504,-0.162889410416478,
13.6645719125626));
#94526=CARTESIAN_POINT('Ctrl Pts',(-2.36493924025131,-0.179715099442791,
13.6657207145778));
#94527=CARTESIAN_POINT('Ctrl Pts',(-2.3644701304286,-0.185785175629894,
13.6661340136292));
#94528=CARTESIAN_POINT('Ctrl Pts',(-2.36355760519669,-0.197029117735796,
13.6668973842094));
#94529=CARTESIAN_POINT('Ctrl Pts',(-2.36312057520462,-0.202203299316896,
13.6672477923236));
#94530=CARTESIAN_POINT('Ctrl Pts',(-2.36208715259719,-0.213977231921002,
13.6680431921905));
#94531=CARTESIAN_POINT('Ctrl Pts',(-2.3614800929295,-0.220575940759209,
13.6684875822957));
#94532=CARTESIAN_POINT('Ctrl Pts',(-2.35953359855696,-0.240804533255232,
13.6698458449916));
#94533=CARTESIAN_POINT('Ctrl Pts',(-2.35810372875169,-0.254425730819577,
13.6707548317141));
#94534=CARTESIAN_POINT('Ctrl Pts',(-2.34195580645491,-0.396398228956341,
13.6801776474902));
#94535=CARTESIAN_POINT('Ctrl Pts',(-2.31688950310181,-0.523375281919996,
13.6881719460958));
#94536=CARTESIAN_POINT('Ctrl Pts',(-2.2285869977464,-0.834434008675452,
13.7080289441977));
#94537=CARTESIAN_POINT('Ctrl Pts',(-2.15285929837325,-1.01393675689906,
13.7197985919894));
#94538=CARTESIAN_POINT('Ctrl Pts',(-2.04214817680727,-1.20648818887445,
13.7342085859765));
#94539=CARTESIAN_POINT('Ctrl Pts',(-2.02775514984024,-1.23052503816858,
13.7360404491905));
#94540=CARTESIAN_POINT('Ctrl Pts',(-2.00638914573541,-1.264813862083,13.7387045862844));
#94541=CARTESIAN_POINT('Ctrl Pts',(-1.99975591654114,-1.27527556797241,
13.739524408507));
#94542=CARTESIAN_POINT('Ctrl Pts',(-1.98794671867997,-1.29358193641776,
13.7409715542617));
#94543=CARTESIAN_POINT('Ctrl Pts',(-1.98280546421823,-1.30144875782308,
13.7415975772099));
#94544=CARTESIAN_POINT('Ctrl Pts',(-1.97209829610196,-1.3176214698184,13.7428932510633));
#94545=CARTESIAN_POINT('Ctrl Pts',(-1.96652635202759,-1.32592312321959,
13.7435631200061));
#94546=CARTESIAN_POINT('Ctrl Pts',(-1.95211521315318,-1.3471036525959,13.7452846556922));
#94547=CARTESIAN_POINT('Ctrl Pts',(-1.9432010906199,-1.35993071783013,13.7463391489692));
#94548=CARTESIAN_POINT('Ctrl Pts',(-1.90522215232671,-1.41344501007247,
13.750789659394));
#94549=CARTESIAN_POINT('Ctrl Pts',(-1.87500303290319,-1.45329323090714,
13.7542297327448));
#94550=CARTESIAN_POINT('Ctrl Pts',(-1.79105035094229,-1.55701635136388,
13.7635355813404));
#94551=CARTESIAN_POINT('Ctrl Pts',(-1.73517031334781,-1.61905612310837,
13.769479917436));
#94552=CARTESIAN_POINT('Ctrl Pts',(-1.57640700866631,-1.77764206181256,
13.785688000691));
#94553=CARTESIAN_POINT('Ctrl Pts',(-1.46799220459803,-1.86817222551871,
13.7960863576813));
#94554=CARTESIAN_POINT('Ctrl Pts',(-1.34017759356799,-1.95686882643037,
13.8073067641497));
#94555=CARTESIAN_POINT('Ctrl Pts',(-1.32809564159908,-1.96508869180668,
13.8083576929742));
#94556=CARTESIAN_POINT('Ctrl Pts',(-1.26740415344156,-2.00556426229297,
13.8135861126565));
#94557=CARTESIAN_POINT('Ctrl Pts',(-1.21768743619563,-2.03613357035258,
13.8177085258715));
#94558=CARTESIAN_POINT('Ctrl Pts',(-1.15776327057873,-2.06999810524921,
13.8224493601109));
#94559=CARTESIAN_POINT('Ctrl Pts',(-1.14860287686701,-2.0750950310417,13.8231679579305));
#94560=CARTESIAN_POINT('Ctrl Pts',(-1.13363832825468,-2.08329198435553,
13.8243315822279));
#94561=CARTESIAN_POINT('Ctrl Pts',(-1.12785465845747,-2.08642882059846,
13.8247788324008));
#94562=CARTESIAN_POINT('Ctrl Pts',(-1.11748611907309,-2.09199659765284,
13.8255761013129));
#94563=CARTESIAN_POINT('Ctrl Pts',(-1.11290626928374,-2.09443658974088,
13.825926682421));
#94564=CARTESIAN_POINT('Ctrl Pts',(-1.10290463074564,-2.09972306119919,
13.8266888512001));
#94565=CARTESIAN_POINT('Ctrl Pts',(-1.0974798205337,-2.10256357904415,13.8271000636115));
#94566=CARTESIAN_POINT('Ctrl Pts',(-1.08206051738724,-2.11056143815232,
13.8282628780939));
#94567=CARTESIAN_POINT('Ctrl Pts',(-1.07204008918079,-2.11566883211694,
13.8290114247087));
#94568=CARTESIAN_POINT('Ctrl Pts',(-1.00647277428633,-2.14850291705219,
13.8338656536168));
#94569=CARTESIAN_POINT('Ctrl Pts',(-0.949886281574112,-2.17411357609958,
13.8378512926677));
#94570=CARTESIAN_POINT('Ctrl Pts',(-0.712166110121094,-2.27064733874149,
13.8540305809719));
#94571=CARTESIAN_POINT('Ctrl Pts',(-0.523656570790738,-2.32138177587498,
13.8656016084419));
#94572=CARTESIAN_POINT('Ctrl Pts',(-0.247210885606719,-2.36035056584702,
13.8830816645218));
#94573=CARTESIAN_POINT('Ctrl Pts',(-0.162800041479565,-2.36767009865302,
13.8884753678646));
#94574=CARTESIAN_POINT('Ctrl Pts',(-0.059160299622568,-2.37108845385537,
13.8952572092189));
#94575=CARTESIAN_POINT('Ctrl Pts',(-0.040129167633956,-2.37148687790052,
13.8965089538415));
#94576=CARTESIAN_POINT('Ctrl Pts',(-0.0102364215921659,-2.37175277221655,
13.898486066871));
#94577=CARTESIAN_POINT('Ctrl Pts',(0.000623285463821417,-2.37177477887079,
13.8992066001961));
#94578=CARTESIAN_POINT('Ctrl Pts',(0.0197974813912066,-2.3716819476805,
13.9004829619631));
#94579=CARTESIAN_POINT('Ctrl Pts',(0.0281119919635066,-2.37159796637159,
13.9010378148921));
#94580=CARTESIAN_POINT('Ctrl Pts',(0.047180535766741,-2.37130507341475,
13.9023135755977));
#94581=CARTESIAN_POINT('Ctrl Pts',(0.0579338676865814,-2.37106672502296,
13.9030353934356));
#94582=CARTESIAN_POINT('Ctrl Pts',(0.0877606907639155,-2.37020258817421,
13.9050443099736));
#94583=CARTESIAN_POINT('Ctrl Pts',(0.106828458096183,-2.36941973723284,
13.9063362875109));
#94584=CARTESIAN_POINT('Ctrl Pts',(0.222176638545932,-2.36328881586511,
13.9142005031177));
#94585=CARTESIAN_POINT('Ctrl Pts',(0.318054111611235,-2.35230389036165,
13.9209477537216));
#94586=CARTESIAN_POINT('Ctrl Pts',(0.531147861862907,-2.31462279841012,
13.9364134428607));
#94587=CARTESIAN_POINT('Ctrl Pts',(0.647545781603016,-2.28479260502635,
13.945192635216));
#94588=CARTESIAN_POINT('Ctrl Pts',(0.802775677621637,-2.23219139276793,
13.9571550318187));
#94589=CARTESIAN_POINT('Ctrl Pts',(0.84397564744979,-2.21694214842574,13.9603540510164));
#94590=CARTESIAN_POINT('Ctrl Pts',(0.910913774851806,-2.19002982029117,
13.9655713055385));
#94591=CARTESIAN_POINT('Ctrl Pts',(0.936909144820054,-2.17903553689865,
13.9676023942615));
#94592=CARTESIAN_POINT('Ctrl Pts',(1.01089740585605,-2.14617459354204,13.9733869774753));
#94593=CARTESIAN_POINT('Ctrl Pts',(1.05836916996301,-2.12316618589423,13.9771031277693));
#94594=CARTESIAN_POINT('Ctrl Pts',(1.11405345074896,-2.09384497518342,13.9814355002175));
#94595=CARTESIAN_POINT('Ctrl Pts',(1.12303818682076,-2.08903975824558,13.9821336770231));
#94596=CARTESIAN_POINT('Ctrl Pts',(1.13769516450775,-2.08107902255819,13.9832708783125));
#94597=CARTESIAN_POINT('Ctrl Pts',(1.14338579832841,-2.07795791685341,13.9837119666306));
#94598=CARTESIAN_POINT('Ctrl Pts',(1.15359886543818,-2.07230176302125,13.9845027128586));
#94599=CARTESIAN_POINT('Ctrl Pts',(1.15812583862474,-2.06977522520621,13.9848528930264));
#94600=CARTESIAN_POINT('Ctrl Pts',(1.16804444653797,-2.06419684486427,13.9856194312944));
#94601=CARTESIAN_POINT('Ctrl Pts',(1.17343241463426,-2.06113871778308,13.9860353807317));
#94602=CARTESIAN_POINT('Ctrl Pts',(1.18885974669095,-2.0523023021538,13.9872252603883));
#94603=CARTESIAN_POINT('Ctrl Pts',(1.19886902156877,-2.04647143138223,13.9879959063456));
#94604=CARTESIAN_POINT('Ctrl Pts',(1.26929495451525,-2.00475099307711,13.9934115952644));
#94605=CARTESIAN_POINT('Ctrl Pts',(1.32813966426015,-1.96626128218342,13.9979023549912));
#94606=CARTESIAN_POINT('Ctrl Pts',(1.47607317349681,-1.85982275403718,14.0093377579817));
#94607=CARTESIAN_POINT('Ctrl Pts',(1.56221309223093,-1.78807873119548,14.0161484865857));
#94608=CARTESIAN_POINT('Ctrl Pts',(1.75498516215986,-1.60291926916756,14.0325483822515));
#94609=CARTESIAN_POINT('Ctrl Pts',(1.85614783840731,-1.48459708184752,14.0421717709329));
#94610=CARTESIAN_POINT('Ctrl Pts',(1.95584498697376,-1.34172526429564,14.0535457806605));
#94611=CARTESIAN_POINT('Ctrl Pts',(1.96648967377802,-1.32607489484814,14.0547881670264));
#94612=CARTESIAN_POINT('Ctrl Pts',(1.98349343488059,-1.30042005766958,14.0568199828052));
#94613=CARTESIAN_POINT('Ctrl Pts',(1.98996696023742,-1.29049216236725,14.0576051122212));
#94614=CARTESIAN_POINT('Ctrl Pts',(2.00138272293743,-1.2726946248536,14.0590107891905));
#94615=CARTESIAN_POINT('Ctrl Pts',(2.00635366715774,-1.26484361478456,14.0596302535283));
#94616=CARTESIAN_POINT('Ctrl Pts',(2.01676152848103,-1.24818990740811,14.060943076362));
#94617=CARTESIAN_POINT('Ctrl Pts',(2.02218722478593,-1.23938046206231,14.0616368317503));
#94618=CARTESIAN_POINT('Ctrl Pts',(2.03648261687629,-1.21582593288236,14.0634900964053));
#94619=CARTESIAN_POINT('Ctrl Pts',(2.04524964132078,-1.20101957741495,14.064653316954));
#94620=CARTESIAN_POINT('Ctrl Pts',(2.08723526069181,-1.12831833712147,14.0703576034991));
#94621=CARTESIAN_POINT('Ctrl Pts',(2.11815785997799,-1.06913939433806,14.0749798181684));
#94622=CARTESIAN_POINT('Ctrl Pts',(2.25892586895362,-0.769593095637562,
14.0982922301832));
#94623=CARTESIAN_POINT('Ctrl Pts',(2.33053601419852,-0.513404003847887,
14.118239039586));
#94624=CARTESIAN_POINT('Ctrl Pts',(2.36063813866413,-0.230238550375794,
14.1380825608457));
#94625=CARTESIAN_POINT('Ctrl Pts',(2.36254848089642,-0.209730683584838,
14.139505995642));
#94626=CARTESIAN_POINT('Ctrl Pts',(2.36483339902296,-0.181178922373827,
14.1414663644167));
#94627=CARTESIAN_POINT('Ctrl Pts',(2.3654344688001,-0.173154802515619,14.1420149567927));
#94628=CARTESIAN_POINT('Ctrl Pts',(2.3663346520844,-0.16025672573131,14.1428928391608));
#94629=CARTESIAN_POINT('Ctrl Pts',(2.36665956412127,-0.155384724031287,
14.1432235416347));
#94630=CARTESIAN_POINT('Ctrl Pts',(2.36731047923859,-0.145148335667127,
14.1439164281146));
#94631=CARTESIAN_POINT('Ctrl Pts',(2.36763329863732,-0.139783792202878,
14.14427842293));
#94632=CARTESIAN_POINT('Ctrl Pts',(2.36838064539985,-0.126618377415897,
14.1451641573322));
#94633=CARTESIAN_POINT('Ctrl Pts',(2.36878487420083,-0.118816325087629,
14.1456867722255));
#94634=CARTESIAN_POINT('Ctrl Pts',(2.37011642340545,-0.0903992837354115,
14.1475824090917));
#94635=CARTESIAN_POINT('Ctrl Pts',(2.37081327721885,-0.0697736875681348,
14.1489432445272));
#94636=CARTESIAN_POINT('Ctrl Pts',(2.37188331454646,-0.0181400520376521,
14.1523181759893));
#94637=CARTESIAN_POINT('Ctrl Pts',(2.37191779587942,0.0128718786578912,
14.1543165864761));
#94638=CARTESIAN_POINT('Ctrl Pts',(2.36941773202961,0.147988169915104,14.162933242687));
#94639=CARTESIAN_POINT('Ctrl Pts',(2.36063695498753,0.251868279889686,14.1693278314723));
#94640=CARTESIAN_POINT('Ctrl Pts',(2.31866693835288,0.52923672758063,14.1865246601909));
#94641=CARTESIAN_POINT('Ctrl Pts',(2.2729120859637,0.70012086871169,14.1972930113968));
#94642=CARTESIAN_POINT('Ctrl Pts',(2.19821194557041,0.891000306396194,14.2105780377398));
#94643=CARTESIAN_POINT('Ctrl Pts',(2.18729972532151,0.917462315212398,14.212447972789));
#94644=CARTESIAN_POINT('Ctrl Pts',(2.17126484298643,0.954433564496448,14.2151035558771));
#94645=CARTESIAN_POINT('Ctrl Pts',(2.16653900995932,0.965113028371262,14.2158757639341));
#94646=CARTESIAN_POINT('Ctrl Pts',(2.15816690414544,0.983660956411467,14.2172260833561));
#94647=CARTESIAN_POINT('Ctrl Pts',(2.15455595845984,0.991545199052107,14.2178029771567));
#94648=CARTESIAN_POINT('Ctrl Pts',(2.14690485117357,1.00801170579069,14.2190140357177));
#94649=CARTESIAN_POINT('Ctrl Pts',(2.14285628664316,1.01658987270027,14.2196484823327));
#94650=CARTESIAN_POINT('Ctrl Pts',(2.1330869789981,1.03697157651888,14.2211645314235));
#94651=CARTESIAN_POINT('Ctrl Pts',(2.12731961226386,1.04875228996633,14.2220477411484));
#94652=CARTESIAN_POINT('Ctrl Pts',(2.10738008880033,1.08864047880309,14.2250622293253));
#94653=CARTESIAN_POINT('Ctrl Pts',(2.09274673920698,1.11651235998425,14.2272095485095));
#94654=CARTESIAN_POINT('Ctrl Pts',(2.05625844217895,1.18277216527265,14.2324162665376));
#94655=CARTESIAN_POINT('Ctrl Pts',(2.03387799618965,1.22085569833873,14.2354934070591));
#94656=CARTESIAN_POINT('Ctrl Pts',(1.87647056231414,1.47235536034209,14.2563930289056));
#94657=CARTESIAN_POINT('Ctrl Pts',(1.70919853806817,1.66360390189591,14.2753854692238));
#94658=CARTESIAN_POINT('Ctrl Pts',(1.49224228499878,1.8437141140417,14.2952045663636));
#94659=CARTESIAN_POINT('Ctrl Pts',(1.46918737457923,1.86213786585103,14.2972569078472));
#94660=CARTESIAN_POINT('Ctrl Pts',(1.43843797136571,1.88578375186439,14.2999181776973));
#94661=CARTESIAN_POINT('Ctrl Pts',(1.43104932214785,1.8913968386014,14.3005520059972));
#94662=CARTESIAN_POINT('Ctrl Pts',(1.41907576647131,1.90038270420443,14.3015698368535));
#94663=CARTESIAN_POINT('Ctrl Pts',(1.41451142132369,1.90378252280043,14.3019556750205));
#94664=CARTESIAN_POINT('Ctrl Pts',(1.40567983835459,1.91031155952172,14.30269800569));
#94665=CARTESIAN_POINT('Ctrl Pts',(1.40141433651535,1.91344294933466,14.3030546405708));
#94666=CARTESIAN_POINT('Ctrl Pts',(1.39118165717928,1.92090239138944,14.3039057371428));
#94667=CARTESIAN_POINT('Ctrl Pts',(1.38520464911514,1.92521699666826,14.3043992754068));
#94668=CARTESIAN_POINT('Ctrl Pts',(1.36470591753941,1.93986947140268,14.3060800313433));
#94669=CARTESIAN_POINT('Ctrl Pts',(1.35008737526894,1.95007177658532,14.3072583950441));
#94670=CARTESIAN_POINT('Ctrl Pts',(1.26350144619314,2.00905979365591,14.3141286784368));
#94671=CARTESIAN_POINT('Ctrl Pts',(1.18900227582438,2.0540287801548,14.319602481301));
#94672=CARTESIAN_POINT('Ctrl Pts',(0.995076054717052,2.15698973129651,14.3332156831375));
#94673=CARTESIAN_POINT('Ctrl Pts',(0.872949852459632,2.20923986455133,14.3412319294453));
#94674=CARTESIAN_POINT('Ctrl Pts',(0.643215935716809,2.28548700906873,14.3562384353388));
#94675=CARTESIAN_POINT('Ctrl Pts',(0.537087793350325,2.31272773709725,14.36314295956));
#94676=CARTESIAN_POINT('Ctrl Pts',(0.411379412146523,2.33587313487773,14.3714927976255));
#94677=CARTESIAN_POINT('Ctrl Pts',(0.393253895013062,2.33899287422973,14.3727005816301));
#94678=CARTESIAN_POINT('Ctrl Pts',(0.363550954485634,2.34375029259329,14.3746869603661));
#94679=CARTESIAN_POINT('Ctrl Pts',(0.351994236397848,2.34551375604328,14.3754615723831));
#94680=CARTESIAN_POINT('Ctrl Pts',(0.331245860438416,2.34852299834729,14.3768556327467));
#94681=CARTESIAN_POINT('Ctrl Pts',(0.322058977913698,2.34980043926408,14.3774740667892));
#94682=CARTESIAN_POINT('Ctrl Pts',(0.302513957564566,2.35240141311723,14.3787923912539));
#94683=CARTESIAN_POINT('Ctrl Pts',(0.292154127870092,2.35371048824434,14.3794927242597));
#94684=CARTESIAN_POINT('Ctrl Pts',(0.264267093188859,2.35704736420197,14.381382265363));
#94685=CARTESIAN_POINT('Ctrl Pts',(0.246725633312908,2.35894802954989,14.3825754446634));
#94686=CARTESIAN_POINT('Ctrl Pts',(0.15707990474941,2.36765056481396,14.3886980409045));
#94687=CARTESIAN_POINT('Ctrl Pts',(0.0847196167827616,2.37134222044782,
14.3937237446156));
#94688=CARTESIAN_POINT('Ctrl Pts',(-0.134262270104153,2.37247881922378,
14.4091955977359));
#94689=CARTESIAN_POINT('Ctrl Pts',(-0.280575212756807,2.35965048353693,
14.419910802823));
#94690=CARTESIAN_POINT('Ctrl Pts',(-0.468946857367222,2.32536128257686,
14.4338853130459));
#94691=CARTESIAN_POINT('Ctrl Pts',(-0.512908408510258,2.3160616159789,14.4371572283274));
#94692=CARTESIAN_POINT('Ctrl Pts',(-0.581529844257104,2.29949556719929,
14.4422605982404));
#94693=CARTESIAN_POINT('Ctrl Pts',(-0.606380742568676,2.29306765961788,
14.4441078930283));
#94694=CARTESIAN_POINT('Ctrl Pts',(-0.683384407995395,2.27181055486915,
14.4498205558896));
#94695=CARTESIAN_POINT('Ctrl Pts',(-0.735140690732121,2.25559453136196,
14.4536439835678));
#94696=CARTESIAN_POINT('Ctrl Pts',(-0.795990193165919,2.23421197956844,
14.4580847105894));
#94697=CARTESIAN_POINT('Ctrl Pts',(-0.805658383572585,2.23074385258039,
14.4587886124511));
#94698=CARTESIAN_POINT('Ctrl Pts',(-0.821422215508404,2.22497327076715,
14.4599332274704));
#94699=CARTESIAN_POINT('Ctrl Pts',(-0.827531313759111,2.22270835673344,
14.4603760487772));
#94700=CARTESIAN_POINT('Ctrl Pts',(-0.838485721216621,2.21859564751026,
14.4611686165873));
#94701=CARTESIAN_POINT('Ctrl Pts',(-0.843334351121684,2.21675711923979,
14.4615188966555));
#94702=CARTESIAN_POINT('Ctrl Pts',(-0.853943095538841,2.21269459587971,
14.4622841480391));
#94703=CARTESIAN_POINT('Ctrl Pts',(-0.859700562199524,2.21046400798772,
14.4626987203466));
#94704=CARTESIAN_POINT('Ctrl Pts',(-0.875460544566788,2.20428730354226,
14.4638316840239));
#94705=CARTESIAN_POINT('Ctrl Pts',(-0.885445192195174,2.2002955492857,14.4645474170893));
#94706=CARTESIAN_POINT('Ctrl Pts',(-0.947733503854984,2.17490068427505,
14.4690016842843));
#94707=CARTESIAN_POINT('Ctrl Pts',(-0.999290213896659,2.15169980659951,
14.4726409659885));
#94708=CARTESIAN_POINT('Ctrl Pts',(-1.18811724292918,2.05847297487345,14.4859683619522));
#94709=CARTESIAN_POINT('Ctrl Pts',(-1.31929619942623,1.97696690645317,14.4952443636338));
#94710=CARTESIAN_POINT('Ctrl Pts',(-1.54326762172838,1.80551938044957,14.5126353675754));
#94711=CARTESIAN_POINT('Ctrl Pts',(-1.63840951236473,1.71964609756744,14.5206497801449));
#94712=CARTESIAN_POINT('Ctrl Pts',(-1.73910170620789,1.61278633154561,14.5302359856086));
#94713=CARTESIAN_POINT('Ctrl Pts',(-1.75188422874247,1.59889215114501,14.5314752911328));
#94714=CARTESIAN_POINT('Ctrl Pts',(-1.77240937881996,1.57604035072261,14.5335030644104));
#94715=CARTESIAN_POINT('Ctrl Pts',(-1.78025336842764,1.5671745687165,14.5342872608593));
#94716=CARTESIAN_POINT('Ctrl Pts',(-1.79413465132423,1.55124634881878,14.5356919008291));
#94717=CARTESIAN_POINT('Ctrl Pts',(-1.80019747645138,1.54420640568578,14.5363112672532));
#94718=CARTESIAN_POINT('Ctrl Pts',(-1.81292940103184,1.52924565167884,14.5376245465101));
#94719=CARTESIAN_POINT('Ctrl Pts',(-1.81958828912588,1.52131644587139,14.5383188601581));
#94720=CARTESIAN_POINT('Ctrl Pts',(-1.83302885559845,1.505097334645,14.5397357113136));
#94721=CARTESIAN_POINT('Ctrl Pts',(-1.83980672100949,1.49680459478574,14.5404583815303));
#94722=CARTESIAN_POINT('Ctrl Pts',(-1.86937641212722,1.46012169275235,14.543647684254));
#94723=CARTESIAN_POINT('Ctrl Pts',(-1.89156788338949,1.43125616641486,14.5461380332027));
#94724=CARTESIAN_POINT('Ctrl Pts',(-1.97444070443029,1.31816422367882,14.5558275416721));
#94725=CARTESIAN_POINT('Ctrl Pts',(-2.03022535633471,1.23050922521842,14.5632045645012));
#94726=CARTESIAN_POINT('Ctrl Pts',(-2.12246910352673,1.06212311878316,14.5770860797305));
#94727=CARTESIAN_POINT('Ctrl Pts',(-2.16050237637178,0.982450584953549,
14.5835433171297));
#94728=CARTESIAN_POINT('Ctrl Pts',(-2.19603182186104,0.895918909124036,
14.5903691788301));
#94729=CARTESIAN_POINT('Ctrl Pts',(-2.19803906419902,0.890983011506573,
14.5907578938943));
#94730=CARTESIAN_POINT('Ctrl Pts',(-2.24290862879087,0.779572318830626,
14.599516865991));
#94731=CARTESIAN_POINT('Ctrl Pts',(-2.27800801630554,0.670118036919324,
14.6078232415036));
#94732=CARTESIAN_POINT('Ctrl Pts',(-2.30805192076658,0.54612952360223,14.6166270141927));
#94733=CARTESIAN_POINT('Ctrl Pts',(-2.3109589341186,0.533694621089315,14.6175032510949));
#94734=CARTESIAN_POINT('Ctrl Pts',(-2.31519982540412,0.514869332193258,
14.6188190701366));
#94735=CARTESIAN_POINT('Ctrl Pts',(-2.31660793141405,0.50849617057809,14.6192626807328));
#94736=CARTESIAN_POINT('Ctrl Pts',(-2.31908766683348,0.497048641077518,
14.6200560816172));
#94737=CARTESIAN_POINT('Ctrl Pts',(-2.32016897311292,0.491976519688363,
14.6204064106129));
#94738=CARTESIAN_POINT('Ctrl Pts',(-2.32249929460377,0.480867025753907,
14.6211710913307));
#94739=CARTESIAN_POINT('Ctrl Pts',(-2.32374140893419,0.474828323174784,
14.6215850483729));
#94740=CARTESIAN_POINT('Ctrl Pts',(-2.32626218594874,0.462326411442523,
14.622438689942));
#94741=CARTESIAN_POINT('Ctrl Pts',(-2.32753749432764,0.455862570897453,
14.6228781862929));
#94742=CARTESIAN_POINT('Ctrl Pts',(-2.33075883786171,0.439169359076368,
14.624008610313));
#94743=CARTESIAN_POINT('Ctrl Pts',(-2.3326644972697,0.428932207759946,14.6246973978613));
#94744=CARTESIAN_POINT('Ctrl Pts',(-2.3490847332647,0.33737577802246,14.6308206249047));
#94745=CARTESIAN_POINT('Ctrl Pts',(-2.359403337115,0.255394829345939,14.6360441351265));
#94746=CARTESIAN_POINT('Ctrl Pts',(-2.3654265029177,0.173076635611311,14.6411792785331));
#94747=CARTESIAN_POINT('Origin',(0.,0.,-1.84858989190503));
#94748=CARTESIAN_POINT('',(-2.3654264678378,0.1730771150452,15.8377719611872));
#94749=CARTESIAN_POINT('',(-2.36542649459319,0.173076749381846,15.6377659025437));
#94750=CARTESIAN_POINT('',(-2.36542649454111,0.173076750093529,-1.84858989190503));
#94751=CARTESIAN_POINT('Ctrl Pts',(-2.3654264678378,0.173077115045235,15.8377719611872));
#94752=CARTESIAN_POINT('Ctrl Pts',(-2.35693967585688,0.289065195696194,
15.8305839026341));
#94753=CARTESIAN_POINT('Ctrl Pts',(-2.33992823301383,0.404345136771074,
15.8232718114111));
#94754=CARTESIAN_POINT('Ctrl Pts',(-2.31108949090406,0.53320410740175,15.8146601565345));
#94755=CARTESIAN_POINT('Ctrl Pts',(-2.30753370920037,0.548388016895403,
15.8136385787627));
#94756=CARTESIAN_POINT('Ctrl Pts',(-2.30133322390988,0.573736651875055,
15.8119210921138));
#94757=CARTESIAN_POINT('Ctrl Pts',(-2.29877023651474,0.583921010869794,
15.8112277894557));
#94758=CARTESIAN_POINT('Ctrl Pts',(-2.29359273599811,0.603931963977296,
15.8098589241349));
#94759=CARTESIAN_POINT('Ctrl Pts',(-2.29098249745076,0.613759437086357,
15.8091835117595));
#94760=CARTESIAN_POINT('Ctrl Pts',(-2.28589948284066,0.632412538950499,
15.8078953905436));
#94761=CARTESIAN_POINT('Ctrl Pts',(-2.28343857822489,0.641241234226451,
15.8072830775913));
#94762=CARTESIAN_POINT('Ctrl Pts',(-2.27771063661152,0.661339545219483,
15.8058830408649));
#94763=CARTESIAN_POINT('Ctrl Pts',(-2.2744110386623,0.672599551586081,15.8050942677294));
#94764=CARTESIAN_POINT('Ctrl Pts',(-2.26560116083366,0.701857335075098,
15.8030330069283));
#94765=CARTESIAN_POINT('Ctrl Pts',(-2.25996003422465,0.719814522468014,
15.8017562720134));
#94766=CARTESIAN_POINT('Ctrl Pts',(-2.21024647093929,0.871718140942521,
15.7908547256863));
#94767=CARTESIAN_POINT('Ctrl Pts',(-2.15453125049659,1.00153079454575,15.7808399903655));
#94768=CARTESIAN_POINT('Ctrl Pts',(-2.04450575896787,1.20559174738188,15.7640162710425));
#94769=CARTESIAN_POINT('Ctrl Pts',(-1.99681957150012,1.28303014012067,15.7573529274218));
#94770=CARTESIAN_POINT('Ctrl Pts',(-1.88674710256206,1.44071984064076,15.7433513047515));
#94771=CARTESIAN_POINT('Ctrl Pts',(-1.8234004910064,1.52009995544995,15.7360382966012));
#94772=CARTESIAN_POINT('Ctrl Pts',(-1.75095360765454,1.59981204851793,15.7285892357328));
#94773=CARTESIAN_POINT('Ctrl Pts',(-1.74673157937264,1.6044207423317,15.7281581727187));
#94774=CARTESIAN_POINT('Ctrl Pts',(-1.73566036220545,1.61641039241845,15.7270358711188));
#94775=CARTESIAN_POINT('Ctrl Pts',(-1.72878220297823,1.62376462377793,15.7263465951686));
#94776=CARTESIAN_POINT('Ctrl Pts',(-1.7176602860957,1.63550556362733,15.7252450803992));
#94777=CARTESIAN_POINT('Ctrl Pts',(-1.71344616346962,1.63991998405933,15.7248306753802));
#94778=CARTESIAN_POINT('Ctrl Pts',(-1.70567236417713,1.64800059440189,15.7240717245548));
#94779=CARTESIAN_POINT('Ctrl Pts',(-1.70211789127296,1.65167153463199,15.7237268034905));
#94780=CARTESIAN_POINT('Ctrl Pts',(-1.69408838784669,1.65991068693467,15.7229523206187));
#94781=CARTESIAN_POINT('Ctrl Pts',(-1.68960673712148,1.66447229798099,15.7225232846837));
#94782=CARTESIAN_POINT('Ctrl Pts',(-1.67804747571868,1.67614300117668,15.721424805646));
#94783=CARTESIAN_POINT('Ctrl Pts',(-1.67094302487153,1.68322550706881,15.7207574039355));
#94784=CARTESIAN_POINT('Ctrl Pts',(-1.62705657986959,1.72642469899635,15.7166801761862));
#94785=CARTESIAN_POINT('Ctrl Pts',(-1.58914698497829,1.76138245492169,15.7133527406003));
#94786=CARTESIAN_POINT('Ctrl Pts',(-1.54436194322092,1.80005617340974,15.7095964739088));
#94787=CARTESIAN_POINT('Ctrl Pts',(-1.53857505434597,1.80500494278887,15.7091143350526));
#94788=CARTESIAN_POINT('Ctrl Pts',(-1.52140360789928,1.81954685459245,15.7076928393277));
#94789=CARTESIAN_POINT('Ctrl Pts',(-1.50995231200316,1.82906088592689,15.7067566661975));
#94790=CARTESIAN_POINT('Ctrl Pts',(-1.33517647980236,1.97150905594866,15.6926326741816));
#94791=CARTESIAN_POINT('Ctrl Pts',(-1.15495184694935,2.08221938959674,15.6801328847443));
#94792=CARTESIAN_POINT('Ctrl Pts',(-0.925112102712844,2.18427022318138,
15.6641893985041));
#94793=CARTESIAN_POINT('Ctrl Pts',(-0.887333449476023,2.19988814815114,
15.6615723000295));
#94794=CARTESIAN_POINT('Ctrl Pts',(-0.821753787069529,2.22503506808374,
15.6570213946533));
#94795=CARTESIAN_POINT('Ctrl Pts',(-0.794144014606266,2.23503814287156,
15.6551031045542));
#94796=CARTESIAN_POINT('Ctrl Pts',(-0.754265995440895,2.24865384066947,
15.6523258184863));
#94797=CARTESIAN_POINT('Ctrl Pts',(-0.74214242667253,2.25268415335576,15.6514806185523));
#94798=CARTESIAN_POINT('Ctrl Pts',(-0.72111704641421,2.25948560044177,15.650013071375));
#94799=CARTESIAN_POINT('Ctrl Pts',(-0.712230277849712,2.26230258813555,
15.6493922472451));
#94800=CARTESIAN_POINT('Ctrl Pts',(-0.695133338765421,2.26761136822035,
15.6481967313869));
#94801=CARTESIAN_POINT('Ctrl Pts',(-0.686925786584785,2.27011115065228,
15.6476223129959));
#94802=CARTESIAN_POINT('Ctrl Pts',(-0.667551751197329,2.27589723201266,
15.6462651278366));
#94803=CARTESIAN_POINT('Ctrl Pts',(-0.656374365842741,2.27914594412967,
15.6454811470284));
#94804=CARTESIAN_POINT('Ctrl Pts',(-0.617309551288481,2.29018895157638,
15.6427374341107));
#94805=CARTESIAN_POINT('Ctrl Pts',(-0.58930463531729,2.29755444616941,15.6407639023634));
#94806=CARTESIAN_POINT('Ctrl Pts',(-0.405510698896786,2.34231228123675,
15.627763290267));
#94807=CARTESIAN_POINT('Ctrl Pts',(-0.246436695430811,2.36434282350857,
15.6162429224672));
#94808=CARTESIAN_POINT('Ctrl Pts',(0.0305223052916856,2.37443727383841,
15.5960196491619));
#94809=CARTESIAN_POINT('Ctrl Pts',(0.147591400314387,2.37004287545471,15.5874334085726));
#94810=CARTESIAN_POINT('Ctrl Pts',(0.296628233311328,2.35335862152401,15.5767444166407));
#94811=CARTESIAN_POINT('Ctrl Pts',(0.329315742653128,2.34900755372275,15.5744158525005));
#94812=CARTESIAN_POINT('Ctrl Pts',(0.383190566855927,2.34068942612889,15.5706150045806));
#94813=CARTESIAN_POINT('Ctrl Pts',(0.404432752252761,2.33711279827662,15.5691259774135));
#94814=CARTESIAN_POINT('Ctrl Pts',(0.433372756292473,2.33183364646898,15.5671131337406));
#94815=CARTESIAN_POINT('Ctrl Pts',(0.44111437564362,2.33038155948592,15.5665762358444));
#94816=CARTESIAN_POINT('Ctrl Pts',(0.45408591986779,2.32788154478926,15.565679394864));
#94817=CARTESIAN_POINT('Ctrl Pts',(0.459319743927618,2.32685450421688,15.5653182892404));
#94818=CARTESIAN_POINT('Ctrl Pts',(0.469235769770708,2.32487390752343,15.5646356286755));
#94819=CARTESIAN_POINT('Ctrl Pts',(0.47391861331523,2.32392384610825,15.5643138721748));
#94820=CARTESIAN_POINT('Ctrl Pts',(0.486181443842185,2.32139733917417,15.5634728725083));
#94821=CARTESIAN_POINT('Ctrl Pts',(0.493756719417407,2.31979790260435,15.5629549299859));
#94822=CARTESIAN_POINT('Ctrl Pts',(0.520041119446728,2.31411365432948,15.5611628501551));
#94823=CARTESIAN_POINT('Ctrl Pts',(0.538709110459365,2.30983924187163,15.5598989757146));
#94824=CARTESIAN_POINT('Ctrl Pts',(0.680273982986816,2.27561542413877,15.5503683030772));
#94825=CARTESIAN_POINT('Ctrl Pts',(0.800666791653876,2.23609921589381,15.5425655466694));
#94826=CARTESIAN_POINT('Ctrl Pts',(1.04320994128863,2.13437101562512,15.5264289460545));
#94827=CARTESIAN_POINT('Ctrl Pts',(1.16427438951561,2.07081843612407,15.5181243358305));
#94828=CARTESIAN_POINT('Ctrl Pts',(1.33778254877248,1.95968770741986,15.5051170235499));
#94829=CARTESIAN_POINT('Ctrl Pts',(1.39468193375601,1.91960904777053,15.500654515259));
#94830=CARTESIAN_POINT('Ctrl Pts',(1.46340236473173,1.86653418080533,15.4949639155562));
#94831=CARTESIAN_POINT('Ctrl Pts',(1.47695477547199,1.85582889678899,15.4938263909079));
#94832=CARTESIAN_POINT('Ctrl Pts',(1.49837532876951,1.83852518203905,15.4920032234204));
#94833=CARTESIAN_POINT('Ctrl Pts',(1.50631979928641,1.83202186872252,15.4913214056588));
#94834=CARTESIAN_POINT('Ctrl Pts',(1.52126145608069,1.81962779229639,15.4900282051661));
#94835=CARTESIAN_POINT('Ctrl Pts',(1.52826729767062,1.81374771759362,15.4894172650885));
#94836=CARTESIAN_POINT('Ctrl Pts',(1.54405246594036,1.80034267421544,15.4880301916087));
#94837=CARTESIAN_POINT('Ctrl Pts',(1.55281107256781,1.79279377699712,15.4872530805268));
#94838=CARTESIAN_POINT('Ctrl Pts',(1.57525468649004,1.77316214730051,15.4852421489502));
#94839=CARTESIAN_POINT('Ctrl Pts',(1.58885580325391,1.76098510266316,15.4840044150705));
#94840=CARTESIAN_POINT('Ctrl Pts',(1.68365841238046,1.67411615265017,15.4752395649969));
#94841=CARTESIAN_POINT('Ctrl Pts',(1.75968969943949,1.59400631607207,15.4674795033223));
#94842=CARTESIAN_POINT('Ctrl Pts',(1.93848425021609,1.37718103543882,15.447273532252));
#94843=CARTESIAN_POINT('Ctrl Pts',(2.03255791093118,1.23412022731677,15.4346208836244));
#94844=CARTESIAN_POINT('Ctrl Pts',(2.12849746078623,1.04702426137897,15.4195530831733));
#94845=CARTESIAN_POINT('Ctrl Pts',(2.14565642940838,1.01139512967129,15.4167468026605));
#94846=CARTESIAN_POINT('Ctrl Pts',(2.16873761004793,0.960234493183907,15.4128214764018));
#94847=CARTESIAN_POINT('Ctrl Pts',(2.17539918975181,0.945045768411009,15.4116689010702));
#94848=CARTESIAN_POINT('Ctrl Pts',(2.18688835756502,0.918084536443186,15.4096470209919));
#94849=CARTESIAN_POINT('Ctrl Pts',(2.19178149874506,0.906340876482218,15.4087743062491));
#94850=CARTESIAN_POINT('Ctrl Pts',(2.19898552911719,0.888651439036968,15.4074722669136));
#94851=CARTESIAN_POINT('Ctrl Pts',(2.20136721612126,0.882735022295279,15.4070388764785));
#94852=CARTESIAN_POINT('Ctrl Pts',(2.20543112019826,0.872521022017261,15.4062943644555));
#94853=CARTESIAN_POINT('Ctrl Pts',(2.20712468107788,0.868228082511681,15.4059825684169));
#94854=CARTESIAN_POINT('Ctrl Pts',(2.21095956240096,0.858423460763895,15.4052730257796));
#94855=CARTESIAN_POINT('Ctrl Pts',(2.21309280646223,0.852908703491206,15.4048757666451));
#94856=CARTESIAN_POINT('Ctrl Pts',(2.2188640681435,0.837821681758359,15.4037938141284));
#94857=CARTESIAN_POINT('Ctrl Pts',(2.22246080558044,0.828233602615362,15.4031115313396));
#94858=CARTESIAN_POINT('Ctrl Pts',(2.24015012524344,0.78013285601442,15.3997138139706));
#94859=CARTESIAN_POINT('Ctrl Pts',(2.25330524414738,0.741279861033008,15.3970495710709));
#94860=CARTESIAN_POINT('Ctrl Pts',(2.33688252521683,0.471604252435205,15.3789779048374));
#94861=CARTESIAN_POINT('Ctrl Pts',(2.37272984031019,0.231539202901166,15.3648481760502));
#94862=CARTESIAN_POINT('Ctrl Pts',(2.3714597914905,-0.0749467387794673,
15.345452960439));
#94863=CARTESIAN_POINT('Ctrl Pts',(2.36850826509816,-0.140021188520125,
15.3412683038638));
#94864=CARTESIAN_POINT('Ctrl Pts',(2.36142212425107,-0.22174275603374,15.3358902921084));
#94865=CARTESIAN_POINT('Ctrl Pts',(2.35978031332053,-0.238581530923435,
15.3347756163957));
#94866=CARTESIAN_POINT('Ctrl Pts',(2.35686127844497,-0.265531169756604,
15.3329805306024));
#94867=CARTESIAN_POINT('Ctrl Pts',(2.35569877301529,-0.275654082551759,
15.3323037394639));
#94868=CARTESIAN_POINT('Ctrl Pts',(2.35336731041903,-0.294863164662963,
15.3310145515511));
#94869=CARTESIAN_POINT('Ctrl Pts',(2.35221086601096,-0.303950689051917,
15.3304025608439));
#94870=CARTESIAN_POINT('Ctrl Pts',(2.34945823726129,-0.324624141647093,
15.3290054440933));
#94871=CARTESIAN_POINT('Ctrl Pts',(2.34782895433662,-0.33620534590711,15.3282192847716));
#94872=CARTESIAN_POINT('Ctrl Pts',(2.34337286498678,-0.366266531218341,
15.3261693370552));
#94873=CARTESIAN_POINT('Ctrl Pts',(2.34041314168541,-0.384725678207977,
15.3249013775674));
#94874=CARTESIAN_POINT('Ctrl Pts',(2.31088147635433,-0.555934644427472,
15.3130530028221));
#94875=CARTESIAN_POINT('Ctrl Pts',(2.26961478330569,-0.705739404518133,
15.3019951946732));
#94876=CARTESIAN_POINT('Ctrl Pts',(2.17429511959932,-0.953900677607855,
15.2826483166463));
#94877=CARTESIAN_POINT('Ctrl Pts',(2.12734274542635,-1.05446628587405,15.2745012187566));
#94878=CARTESIAN_POINT('Ctrl Pts',(2.03839427384134,-1.21465422554761,15.2612889834184));
#94879=CARTESIAN_POINT('Ctrl Pts',(2.00037781755153,-1.27629424839385,15.2561445052538));
#94880=CARTESIAN_POINT('Ctrl Pts',(1.95309470854254,-1.34564198902912,15.250364051202));
#94881=CARTESIAN_POINT('Ctrl Pts',(1.94652235843236,-1.35513173712203,15.2495732264203));
#94882=CARTESIAN_POINT('Ctrl Pts',(1.93635172628529,-1.36959033258048,15.2483690787595));
#94883=CARTESIAN_POINT('Ctrl Pts',(1.93280313161056,-1.3745936649038,15.2479525287097));
#94884=CARTESIAN_POINT('Ctrl Pts',(1.92626370166427,-1.38373852653173,15.2471915187425));
#94885=CARTESIAN_POINT('Ctrl Pts',(1.92327890387963,-1.38788415119684,15.2468466692938));
#94886=CARTESIAN_POINT('Ctrl Pts',(1.916548692219,-1.3971684236928,15.246074657047));
#94887=CARTESIAN_POINT('Ctrl Pts',(1.91279600122218,-1.40230166295096,15.2456480043178));
#94888=CARTESIAN_POINT('Ctrl Pts',(1.90314008920739,-1.41539893107691,15.2445597265373));
#94889=CARTESIAN_POINT('Ctrl Pts',(1.8972074269294,-1.42334125247638,15.2439000793855));
#94890=CARTESIAN_POINT('Ctrl Pts',(1.86132323863089,-1.47075802047232,15.2399621069503));
#94891=CARTESIAN_POINT('Ctrl Pts',(1.8301879752349,-1.50932639601643,15.2367598279655));
#94892=CARTESIAN_POINT('Ctrl Pts',(1.77592660046604,-1.57239122103343,15.2314707189579));
#94893=CARTESIAN_POINT('Ctrl Pts',(1.7534478908879,-1.59741982839115,15.2293567201913));
#94894=CARTESIAN_POINT('Ctrl Pts',(1.60522495697014,-1.75555627735332,15.2158391307444));
#94895=CARTESIAN_POINT('Ctrl Pts',(1.46495873073014,-1.87419972936961,15.2048926119263));
#94896=CARTESIAN_POINT('Ctrl Pts',(1.24745570586754,-2.01869718451607,15.1884798855032));
#94897=CARTESIAN_POINT('Ctrl Pts',(1.1803915742276,-2.05863007613359,15.1834928906512));
#94898=CARTESIAN_POINT('Ctrl Pts',(1.095703862192,-2.10355658925593,15.1772141357848));
#94899=CARTESIAN_POINT('Ctrl Pts',(1.07982692638187,-2.11175070921024,15.1760379137506));
#94900=CARTESIAN_POINT('Ctrl Pts',(1.05456638609734,-2.12442837242452,15.1741671925049));
#94901=CARTESIAN_POINT('Ctrl Pts',(1.04524304884126,-2.12903103200157,15.1734768783272));
#94902=CARTESIAN_POINT('Ctrl Pts',(1.0276786342104,-2.13755888939294,15.172176504498));
#94903=CARTESIAN_POINT('Ctrl Pts',(1.01944454905733,-2.14149811772279,15.1715669477575));
#94904=CARTESIAN_POINT('Ctrl Pts',(1.00091113221028,-2.15023348617479,15.1701949526509));
#94905=CARTESIAN_POINT('Ctrl Pts',(0.990599723483981,-2.15500332242454,
15.169431621171));
#94906=CARTESIAN_POINT('Ctrl Pts',(0.964234874947978,-2.16696992802376,
15.1674796928669));
#94907=CARTESIAN_POINT('Ctrl Pts',(0.948135137597761,-2.17406239439141,
15.1662875579813));
#94908=CARTESIAN_POINT('Ctrl Pts',(0.847200648254077,-2.21719298687842,
15.1588110608896));
#94909=CARTESIAN_POINT('Ctrl Pts',(0.760414893120203,-2.24843477666683,
15.152366476678));
#94910=CARTESIAN_POINT('Ctrl Pts',(0.471568132331998,-2.33377793781825,
15.1308690329009));
#94911=CARTESIAN_POINT('Ctrl Pts',(0.264169319705671,-2.36624147709204,
15.1152706012825));
#94912=CARTESIAN_POINT('Ctrl Pts',(0.0271842661256244,-2.37175992832376,
15.0984551707561));
#94913=CARTESIAN_POINT('Ctrl Pts',(-0.000856008987816744,-2.37191558918204,
15.0964832946151));
#94914=CARTESIAN_POINT('Ctrl Pts',(-0.0479729056820139,-2.37134154656322,
15.0932065738879));
#94915=CARTESIAN_POINT('Ctrl Pts',(-0.0670493228838324,-2.37087886171445,
15.0918900282509));
#94916=CARTESIAN_POINT('Ctrl Pts',(-0.0936242064805073,-2.36991328438927,
15.0900719607503));
#94917=CARTESIAN_POINT('Ctrl Pts',(-0.101128377379546,-2.36960492967955,
15.0895603552497));
#94918=CARTESIAN_POINT('Ctrl Pts',(-0.113886129406169,-2.36901998420539,
15.0886937464375));
#94919=CARTESIAN_POINT('Ctrl Pts',(-0.119140447466716,-2.36876155235646,
15.0883377453047));
#94920=CARTESIAN_POINT('Ctrl Pts',(-0.129238693264588,-2.368231187772,15.0876553577104));
#94921=CARTESIAN_POINT('Ctrl Pts',(-0.134082678871221,-2.36796187361332,
15.0873288214136));
#94922=CARTESIAN_POINT('Ctrl Pts',(-0.145698819661519,-2.36728028491948,
15.0865476041563));
#94923=CARTESIAN_POINT('Ctrl Pts',(-0.152470147879234,-2.36685380838694,
15.0860937099072));
#94924=CARTESIAN_POINT('Ctrl Pts',(-0.177019475663254,-2.36520183518045,
15.0844532475073));
#94925=CARTESIAN_POINT('Ctrl Pts',(-0.194785905700682,-2.36380500759528,
15.0832757867304));
#94926=CARTESIAN_POINT('Ctrl Pts',(-0.377394729226437,-2.34737509638493,
15.0712582266444));
#94927=CARTESIAN_POINT('Ctrl Pts',(-0.54027473902114,-2.31532219922393,
15.0612293375868));
#94928=CARTESIAN_POINT('Ctrl Pts',(-0.852703847329381,-2.2190378164147,
15.0411867072496));
#94929=CARTESIAN_POINT('Ctrl Pts',(-1.00162540526861,-2.15591487324638,
15.0312200923291));
#94930=CARTESIAN_POINT('Ctrl Pts',(-1.16191713918939,-2.06775574899828,
15.0192840198992));
#94931=CARTESIAN_POINT('Ctrl Pts',(-1.18071289607803,-2.05708101007848,
15.0178649534504));
#94932=CARTESIAN_POINT('Ctrl Pts',(-1.20901750025377,-2.04049015384406,
15.0156969316168));
#94933=CARTESIAN_POINT('Ctrl Pts',(-1.21863502530075,-2.03476093231182,
15.0149547394725));
#94934=CARTESIAN_POINT('Ctrl Pts',(-1.23601005038821,-2.02424314771093,
15.01360364118));
#94935=CARTESIAN_POINT('Ctrl Pts',(-1.24378123132898,-2.01947750923621,
15.0129955832088));
#94936=CARTESIAN_POINT('Ctrl Pts',(-1.26046007721091,-2.00911649956961,
15.0116823034575));
#94937=CARTESIAN_POINT('Ctrl Pts',(-1.26935834755861,-2.00350644979484,
15.0109765483053));
#94938=CARTESIAN_POINT('Ctrl Pts',(-1.29333607259869,-1.98816547169633,
15.0090607170913));
#94939=CARTESIAN_POINT('Ctrl Pts',(-1.3083426233917,-1.97832244297608,15.0078464854185));
#94940=CARTESIAN_POINT('Ctrl Pts',(-1.3824295380888,-1.92851604366728,15.0017743972143));
#94941=CARTESIAN_POINT('Ctrl Pts',(-1.43979210807213,-1.88607592021797,
14.9968235318599));
#94942=CARTESIAN_POINT('Ctrl Pts',(-1.64251208369558,-1.72144952395835,
14.9783728372181));
#94943=CARTESIAN_POINT('Ctrl Pts',(-1.7749627041595,-1.58452669437551,14.9643354820092));
#94944=CARTESIAN_POINT('Ctrl Pts',(-1.92300311826264,-1.38935301425882,
14.9466118471814));
#94945=CARTESIAN_POINT('Ctrl Pts',(-1.95480744672241,-1.34423639495542,
14.9426564949999));
#94946=CARTESIAN_POINT('Ctrl Pts',(-1.99639817419316,-1.28063472531,14.9373105589053));
#94947=CARTESIAN_POINT('Ctrl Pts',(-2.00755625147056,-1.26307123099609,
14.9358575255901));
#94948=CARTESIAN_POINT('Ctrl Pts',(-2.02645648535382,-1.2324377526826,14.9333660203053));
#94949=CARTESIAN_POINT('Ctrl Pts',(-2.03430673444773,-1.21943628030228,
14.932321651587));
#94950=CARTESIAN_POINT('Ctrl Pts',(-2.04551705796916,-1.20046031996867,
14.9308172312614));
#94951=CARTESIAN_POINT('Ctrl Pts',(-2.04897678099046,-1.19454559068206,
14.9303510796189));
#94952=CARTESIAN_POINT('Ctrl Pts',(-2.05499295541223,-1.18415732121081,
14.9295373119134));
#94953=CARTESIAN_POINT('Ctrl Pts',(-2.05756052616757,-1.17969033708224,
14.9291889874651));
#94954=CARTESIAN_POINT('Ctrl Pts',(-2.06298457192879,-1.17018216077645,
14.928450983254));
#94955=CARTESIAN_POINT('Ctrl Pts',(-2.06583713819187,-1.16513885598103,
14.9280615528165));
#94956=CARTESIAN_POINT('Ctrl Pts',(-2.07354948623876,-1.15138614695593,
14.9270049494077));
#94957=CARTESIAN_POINT('Ctrl Pts',(-2.07837292957114,-1.14265633754892,
14.9263400550907));
#94958=CARTESIAN_POINT('Ctrl Pts',(-2.10070846950034,-1.10162252310833,
14.9232406237444));
#94959=CARTESIAN_POINT('Ctrl Pts',(-2.1175244933606,-1.06894276966595,14.9208468483219));
#94960=CARTESIAN_POINT('Ctrl Pts',(-2.23095214681353,-0.835319485329479,
14.904161479299));
#94961=CARTESIAN_POINT('Ctrl Pts',(-2.29957270271285,-0.62200949898686,
14.8910312443448));
#94962=CARTESIAN_POINT('Ctrl Pts',(-2.3519311619069,-0.317751784463505,
14.8716979076568));
#94963=CARTESIAN_POINT('Ctrl Pts',(-2.36187689590785,-0.232553953821026,
14.8662349030271));
#94964=CARTESIAN_POINT('Ctrl Pts',(-2.3683262126787,-0.12870653940678,14.8594237829296));
#94965=CARTESIAN_POINT('Ctrl Pts',(-2.36925062837203,-0.110389544538584,
14.8582168395338));
#94966=CARTESIAN_POINT('Ctrl Pts',(-2.37037011560242,-0.0815711117898674,
14.8563083837736));
#94967=CARTESIAN_POINT('Ctrl Pts',(-2.37070803168282,-0.0710756898555659,
14.855611352009));
#94968=CARTESIAN_POINT('Ctrl Pts',(-2.37120911297899,-0.0514639198755605,
14.8543050095035));
#94969=CARTESIAN_POINT('Ctrl Pts',(-2.37138942833516,-0.0423481722896496,
14.8536962481865));
#94970=CARTESIAN_POINT('Ctrl Pts',(-2.37167436448929,-0.0220142570688781,
14.8523347376869));
#94971=CARTESIAN_POINT('Ctrl Pts',(-2.37175195957292,-0.0107959910226772,
14.8515811552777));
#94972=CARTESIAN_POINT('Ctrl Pts',(-2.37174609359546,0.0221537695712086,
14.8493603935021));
#94973=CARTESIAN_POINT('Ctrl Pts',(-2.37144354767738,0.0438835641855433,
14.8478864060153));
#94974=CARTESIAN_POINT('Ctrl Pts',(-2.37007987530885,0.0931637545855088,
14.8445212369417));
#94975=CARTESIAN_POINT('Ctrl Pts',(-2.36883687920081,0.120705549485069,
14.8426246159026));
#94976=CARTESIAN_POINT('Ctrl Pts',(-2.36659508990106,0.156507915565579,
14.8401378662955));
#94977=CARTESIAN_POINT('Ctrl Pts',(-2.36603252855054,0.164794130518723,
14.8395608422669));
#94978=CARTESIAN_POINT('Ctrl Pts',(-2.36542649432832,0.173076753001719,
14.8389825814723));
#94979=CARTESIAN_POINT('',(-2.37174911292529,0.00215604138794719,14.6517284628086));
#94980=CARTESIAN_POINT('Ctrl Pts',(-2.3654265029177,0.173076635611311,14.6411792785331));
#94981=CARTESIAN_POINT('Ctrl Pts',(-2.36958616881481,0.116226767218978,
14.6447256661978));
#94982=CARTESIAN_POINT('Ctrl Pts',(-2.37169717082288,0.0592160450641252,
14.6482297751778));
#94983=CARTESIAN_POINT('Ctrl Pts',(-2.37174902082752,0.00215515746287692,
14.6517286780464));
#94984=CARTESIAN_POINT('Ctrl Pts',(-2.37174902001529,0.00215605114073682,
14.6517286232472));
#94985=CARTESIAN_POINT('Ctrl Pts',(-2.37188407915844,-0.146414817317101,
14.6608388048995));
#94986=CARTESIAN_POINT('Ctrl Pts',(-2.35805940655107,-0.294662613876634,
14.6698964317843));
#94987=CARTESIAN_POINT('Ctrl Pts',(-2.3220300978616,-0.485213149403807,
14.6822539492024));
#94988=CARTESIAN_POINT('Ctrl Pts',(-2.31232638921229,-0.529529811924109,
14.6851775598427));
#94989=CARTESIAN_POINT('Ctrl Pts',(-2.29786298848713,-0.587565061965923,
14.6890853884549));
#94990=CARTESIAN_POINT('Ctrl Pts',(-2.29423932220956,-0.60155875287674,
14.6900337775809));
#94991=CARTESIAN_POINT('Ctrl Pts',(-2.28710858702346,-0.628093896280901,
14.6918442832747));
#94992=CARTESIAN_POINT('Ctrl Pts',(-2.28362569159036,-0.640641335449396,
14.6927056006159));
#94993=CARTESIAN_POINT('Ctrl Pts',(-2.27743214611189,-0.662261682418899,
14.6941990134174));
#94994=CARTESIAN_POINT('Ctrl Pts',(-2.27477013505126,-0.671348303314509,
14.6948295157564));
#94995=CARTESIAN_POINT('Ctrl Pts',(-2.26956024319579,-0.688745173680708,
14.6960422318557));
#94996=CARTESIAN_POINT('Ctrl Pts',(-2.26702094418615,-0.697057850469502,
14.6966241561753));
#94997=CARTESIAN_POINT('Ctrl Pts',(-2.26093876765243,-0.716583726961803,
14.6979969364017));
#94998=CARTESIAN_POINT('Ctrl Pts',(-2.25735810031847,-0.727784821951238,
14.698789021556));
#94999=CARTESIAN_POINT('Ctrl Pts',(-2.24462872751488,-0.766607177342344,
14.7015505961192));
#95000=CARTESIAN_POINT('Ctrl Pts',(-2.23505546399521,-0.794085404825248,
14.7035339726358));
#95001=CARTESIAN_POINT('Ctrl Pts',(-2.17032504499603,-0.969429260526127,
14.7163815708037));
#95002=CARTESIAN_POINT('Ctrl Pts',(-2.10104049577333,-1.11162753573527,
14.7277221522006));
#95003=CARTESIAN_POINT('Ctrl Pts',(-1.9560492464894,-1.3464969102428,14.7478565478278));
#95004=CARTESIAN_POINT('Ctrl Pts',(-1.88648850009718,-1.4423405060646,14.7565380655361));
#95005=CARTESIAN_POINT('Ctrl Pts',(-1.77790422004556,-1.57058328601222,
14.7685182191503));
#95006=CARTESIAN_POINT('Ctrl Pts',(-1.74455175217438,-1.6075494773613,14.7720181372453));
#95007=CARTESIAN_POINT('Ctrl Pts',(-1.70297446455836,-1.6508120830478,14.7761443206911));
#95008=CARTESIAN_POINT('Ctrl Pts',(-1.69584336508935,-1.65813686138779,
14.7768440009937));
#95009=CARTESIAN_POINT('Ctrl Pts',(-1.6843803995946,-1.66975985194065,14.7779556530799));
#95010=CARTESIAN_POINT('Ctrl Pts',(-1.68007901968961,-1.67408774663358,
14.7783698972478));
#95011=CARTESIAN_POINT('Ctrl Pts',(-1.67208723920401,-1.68206696552753,
14.7791341264748));
#95012=CARTESIAN_POINT('Ctrl Pts',(-1.66840157627194,-1.68572275099926,
14.779484454621));
#95013=CARTESIAN_POINT('Ctrl Pts',(-1.65999704766947,-1.69400458369598,
14.7802785481569));
#95014=CARTESIAN_POINT('Ctrl Pts',(-1.65527083748654,-1.69862302618862,
14.7807217200125));
#95015=CARTESIAN_POINT('Ctrl Pts',(-1.64292956654227,-1.71058246740024,
14.7818703966056));
#95016=CARTESIAN_POINT('Ctrl Pts',(-1.63528448928846,-1.71789248435492,
14.782573579838));
#95017=CARTESIAN_POINT('Ctrl Pts',(-1.58372774149858,-1.76653359688116,
14.7872619577807));
#95018=CARTESIAN_POINT('Ctrl Pts',(-1.53829817834778,-1.80623217010358,
14.7911343230446));
#95019=CARTESIAN_POINT('Ctrl Pts',(-1.3604906255676,-1.95002790562508,14.80556257972));
#95020=CARTESIAN_POINT('Ctrl Pts',(-1.21867405519078,-2.04166221802933,
14.8156523286273));
#95021=CARTESIAN_POINT('Ctrl Pts',(-1.00255946174628,-2.15069783848545,
14.8306582334018));
#95022=CARTESIAN_POINT('Ctrl Pts',(-0.935272425592493,-2.18080050035398,
14.8352785916219));
#95023=CARTESIAN_POINT('Ctrl Pts',(-0.838201431012205,-2.21890819725326,
14.8419553869037));
#95024=CARTESIAN_POINT('Ctrl Pts',(-0.809492620791687,-2.22954183449925,
14.8439311522988));
#95025=CARTESIAN_POINT('Ctrl Pts',(-0.758572156691437,-2.24728945046012,
14.8474429145604));
#95026=CARTESIAN_POINT('Ctrl Pts',(-0.73644602866137,-2.25463717138054,
14.8489712544664));
#95027=CARTESIAN_POINT('Ctrl Pts',(-0.702935621056583,-2.26521952734965,
14.8512912096976));
#95028=CARTESIAN_POINT('Ctrl Pts',(-0.691629118248512,-2.26869723600131,
14.8520748591022));
#95029=CARTESIAN_POINT('Ctrl Pts',(-0.67139772026644,-2.27475481439072,
14.8534788915955));
#95030=CARTESIAN_POINT('Ctrl Pts',(-0.662482728436488,-2.27736711899384,
14.8540982011746));
#95031=CARTESIAN_POINT('Ctrl Pts',(-0.64359457038248,-2.28278150615841,
14.8554117508069));
#95032=CARTESIAN_POINT('Ctrl Pts',(-0.633617958003769,-2.28557075000316,
14.8561063939867));
#95033=CARTESIAN_POINT('Ctrl Pts',(-0.606965035238863,-2.29283440845556,
14.857964550659));
#95034=CARTESIAN_POINT('Ctrl Pts',(-0.590257860485844,-2.29719215765701,
14.8591318100629));
#95035=CARTESIAN_POINT('Ctrl Pts',(-0.515584650582316,-2.31580086160872,
14.8643610256478));
#95036=CARTESIAN_POINT('Ctrl Pts',(-0.457145031694033,-2.32804176844397,
14.8684866177011));
#95037=CARTESIAN_POINT('Ctrl Pts',(-0.185879074554081,-2.37425434998922,
14.8878032272628));
#95038=CARTESIAN_POINT('Ctrl Pts',(0.0304803080597236,-2.3813186274865,
14.9038006607889));
#95039=CARTESIAN_POINT('Ctrl Pts',(0.313699421184216,-2.35193425649568,
14.9243059976412));
#95040=CARTESIAN_POINT('Ctrl Pts',(0.382301447171688,-2.34176210302865,
14.9292261053387));
#95041=CARTESIAN_POINT('Ctrl Pts',(0.461703040152434,-2.32640531740401,
14.9347956294977));
#95042=CARTESIAN_POINT('Ctrl Pts',(0.473024183568396,-2.32412984438194,
14.9355867155604));
#95043=CARTESIAN_POINT('Ctrl Pts',(0.49038569553102,-2.32050818092702,14.9367947723344));
#95044=CARTESIAN_POINT('Ctrl Pts',(0.496437968678867,-2.31922092384733,
14.9372149473856));
#95045=CARTESIAN_POINT('Ctrl Pts',(0.507552272119802,-2.31681152344353,
14.9379847035603));
#95046=CARTESIAN_POINT('Ctrl Pts',(0.512615644213608,-2.3156964711449,14.9383346681992));
#95047=CARTESIAN_POINT('Ctrl Pts',(0.524018163837556,-2.31314618399231,
14.9391211869554));
#95048=CARTESIAN_POINT('Ctrl Pts',(0.530355083448118,-2.31170149296202,
14.9395571954198));
#95049=CARTESIAN_POINT('Ctrl Pts',(0.546639768905023,-2.30791842323976,
14.9406750193388));
#95050=CARTESIAN_POINT('Ctrl Pts',(0.556578632375637,-2.30554174123821,
14.941354714291));
#95051=CARTESIAN_POINT('Ctrl Pts',(0.618234443303363,-2.29037603839949,
14.9455572123572));
#95052=CARTESIAN_POINT('Ctrl Pts',(0.669528167059367,-2.27591064849159,
14.9489922011807));
#95053=CARTESIAN_POINT('Ctrl Pts',(0.746125572671108,-2.25149498684292,
14.9540890844331));
#95054=CARTESIAN_POINT('Ctrl Pts',(0.77181339914516,-2.24281903226161,14.9557927132238));
#95055=CARTESIAN_POINT('Ctrl Pts',(0.97105013081545,-2.17169908891392,14.9690015845943));
#95056=CARTESIAN_POINT('Ctrl Pts',(1.13692704357163,-2.08964504591076,14.9800233120382));
#95057=CARTESIAN_POINT('Ctrl Pts',(1.35737603429716,-1.94650308303175,14.9965402697932));
#95058=CARTESIAN_POINT('Ctrl Pts',(1.42096334074232,-1.90058020396791,15.0015504883894));
#95059=CARTESIAN_POINT('Ctrl Pts',(1.49625450140992,-1.84031156746689,15.0078659166613));
#95060=CARTESIAN_POINT('Ctrl Pts',(1.51022343750123,-1.82886558752378,15.0090546846172));
#95061=CARTESIAN_POINT('Ctrl Pts',(1.53213066004606,-1.81049293060851,15.0109470146997));
#95062=CARTESIAN_POINT('Ctrl Pts',(1.54015603950557,-1.80367080674768,15.0116463155656));
#95063=CARTESIAN_POINT('Ctrl Pts',(1.55515275794233,-1.79074949592438,15.0129647065017));
#95064=CARTESIAN_POINT('Ctrl Pts',(1.56213434973657,-1.78466246860957,15.0135832865284));
#95065=CARTESIAN_POINT('Ctrl Pts',(1.57774183428862,-1.77089304866532,15.0149771190655));
#95066=CARTESIAN_POINT('Ctrl Pts',(1.58634756972254,-1.76318826711683,15.0157533000154));
#95067=CARTESIAN_POINT('Ctrl Pts',(1.60816923232508,-1.7433620866982,15.0177413173231));
#95068=CARTESIAN_POINT('Ctrl Pts',(1.62130439243005,-1.73115328072409,15.018956838408));
#95069=CARTESIAN_POINT('Ctrl Pts',(1.70440942380411,-1.65213375990979,15.0267708210299));
#95070=CARTESIAN_POINT('Ctrl Pts',(1.77036532926587,-1.58125252367993,15.0335461051405));
#95071=CARTESIAN_POINT('Ctrl Pts',(1.947877243474,-1.36541726744294,15.0535322448719));
#95072=CARTESIAN_POINT('Ctrl Pts',(2.04724073255277,-1.2113575385468,15.067088396166));
#95073=CARTESIAN_POINT('Ctrl Pts',(2.15474540495974,-0.992953590609145,
15.0845484657005));
#95074=CARTESIAN_POINT('Ctrl Pts',(2.17946062796281,-0.937463297247468,
15.0888411724001));
#95075=CARTESIAN_POINT('Ctrl Pts',(2.20617544200097,-0.870696881086827,
15.0937908285052));
#95076=CARTESIAN_POINT('Ctrl Pts',(2.21025671114814,-0.860283919930739,
15.0945566964036));
#95077=CARTESIAN_POINT('Ctrl Pts',(2.21645356154783,-0.844138023600395,
15.0957344089074));
#95078=CARTESIAN_POINT('Ctrl Pts',(2.21862083421389,-0.838425303485623,
15.0961492174612));
#95079=CARTESIAN_POINT('Ctrl Pts',(2.22258839060707,-0.827844097587817,
15.0969139624857));
#95080=CARTESIAN_POINT('Ctrl Pts',(2.22439475842074,-0.822978106399219,
15.0972642459179));
#95081=CARTESIAN_POINT('Ctrl Pts',(2.22846078673267,-0.811913854020796,
15.0980575730636));
#95082=CARTESIAN_POINT('Ctrl Pts',(2.23071056789279,-0.805712075937854,
15.0985000280209));
#95083=CARTESIAN_POINT('Ctrl Pts',(2.23648781269638,-0.789576748061331,
15.0996456061896));
#95084=CARTESIAN_POINT('Ctrl Pts',(2.23997502951377,-0.779628792942433,
15.1003464284599));
#95085=CARTESIAN_POINT('Ctrl Pts',(2.26272031862458,-0.713330893769666,
15.1049828851964));
#95086=CARTESIAN_POINT('Ctrl Pts',(2.27991845296082,-0.656290662968781,
15.1088085193969));
#95087=CARTESIAN_POINT('Ctrl Pts',(2.31228212858095,-0.53222471196045,15.1169023755771));
#95088=CARTESIAN_POINT('Ctrl Pts',(2.32672001592493,-0.465066407494585,
15.121145356429));
#95089=CARTESIAN_POINT('Ctrl Pts',(2.35892814836613,-0.275547189256023,
15.1329590184188));
#95090=CARTESIAN_POINT('Ctrl Pts',(2.37007882267018,-0.152294011403453,
15.1404676034347));
#95091=CARTESIAN_POINT('Ctrl Pts',(2.37229237931211,0.0303956330879317,
15.1518890829129));
#95092=CARTESIAN_POINT('Ctrl Pts',(2.37079708877883,0.0895288105885493,
15.1556290710958));
#95093=CARTESIAN_POINT('Ctrl Pts',(2.36544366523301,0.174838825398544,15.1611272287962));
#95094=CARTESIAN_POINT('Ctrl Pts',(2.36335535873658,0.20110621679509,15.1628341394351));
#95095=CARTESIAN_POINT('Ctrl Pts',(2.35881515900443,0.248255814529363,15.1659265974966));
#95096=CARTESIAN_POINT('Ctrl Pts',(2.35652237844452,0.269150769800251,15.1673071865638));
#95097=CARTESIAN_POINT('Ctrl Pts',(2.35258666572137,0.301095935328145,15.1694346221225));
#95098=CARTESIAN_POINT('Ctrl Pts',(2.35114284616125,0.312169972451478,15.1701752002129));
#95099=CARTESIAN_POINT('Ctrl Pts',(2.34848424031921,0.331495694677993,15.1714731816141));
#95100=CARTESIAN_POINT('Ctrl Pts',(2.34730402716108,0.33975200313287,15.172029483578));
#95101=CARTESIAN_POINT('Ctrl Pts',(2.34453988231379,0.358386692141769,15.173289178486));
#95102=CARTESIAN_POINT('Ctrl Pts',(2.34293054712228,0.368761069083972,15.1739933650291));
#95103=CARTESIAN_POINT('Ctrl Pts',(2.33839100185604,0.396794676942097,15.1759042026645));
#95104=CARTESIAN_POINT('Ctrl Pts',(2.33532970803214,0.41443167989719,15.1771149809511));
#95105=CARTESIAN_POINT('Ctrl Pts',(2.32006243002613,0.496843061129686,15.1828140615002));
#95106=CARTESIAN_POINT('Ctrl Pts',(2.30536033336788,0.561119381146274,15.187380776995));
#95107=CARTESIAN_POINT('Ctrl Pts',(2.23169526248906,0.830924396912919,15.2070847821052));
#95108=CARTESIAN_POINT('Ctrl Pts',(2.1477637219239,1.02858446220783,15.2229767452182));
#95109=CARTESIAN_POINT('Ctrl Pts',(2.01655841703121,1.24921453156977,15.241417722844));
#95110=CARTESIAN_POINT('Ctrl Pts',(1.99359196459685,1.28554904115497,15.2444753204328));
#95111=CARTESIAN_POINT('Ctrl Pts',(1.95505671005739,1.34299572489189,15.2493205954363));
#95112=CARTESIAN_POINT('Ctrl Pts',(1.94010378572815,1.36450786066598,15.2511375763042));
#95113=CARTESIAN_POINT('Ctrl Pts',(1.91979580876341,1.39271510865154,15.2535189084736));
#95114=CARTESIAN_POINT('Ctrl Pts',(1.91475720757121,1.39963429615781,15.2541029510482));
#95115=CARTESIAN_POINT('Ctrl Pts',(1.90640030776704,1.41098069998046,15.2550603320241));
#95116=CARTESIAN_POINT('Ctrl Pts',(1.90310383411348,1.41542377660126,15.255435136135));
#95117=CARTESIAN_POINT('Ctrl Pts',(1.89660594535028,1.42411806782916,15.2561683133144));
#95118=CARTESIAN_POINT('Ctrl Pts',(1.8934057270203,1.42837009801208,15.256526760657));
#95119=CARTESIAN_POINT('Ctrl Pts',(1.88546936141968,1.43884135966132,15.2574092911295));
#95120=CARTESIAN_POINT('Ctrl Pts',(1.88071667119692,1.4450480885286,15.2579322271438));
#95121=CARTESIAN_POINT('Ctrl Pts',(1.86417590617694,1.46642949857931,15.2597335147248));
#95122=CARTESIAN_POINT('Ctrl Pts',(1.85223378870077,1.48148484091234,15.2610015758265));
#95123=CARTESIAN_POINT('Ctrl Pts',(1.76158619417707,1.59295381731406,15.2704023289056));
#95124=CARTESIAN_POINT('Ctrl Pts',(1.67557291078516,1.68319683948664,15.278087237919));
#95125=CARTESIAN_POINT('Ctrl Pts',(1.48050011699526,1.85801245203081,15.2941643012499));
#95126=CARTESIAN_POINT('Ctrl Pts',(1.37036413288083,1.94066749617801,15.3025244507063));
#95127=CARTESIAN_POINT('Ctrl Pts',(1.21448141570072,2.03773569614314,15.3141139268554));
#95128=CARTESIAN_POINT('Ctrl Pts',(1.17456625541696,2.06100111043549,15.3170601976165));
#95129=CARTESIAN_POINT('Ctrl Pts',(1.10539073973818,2.09865918166663,15.3221513434685));
#95130=CARTESIAN_POINT('Ctrl Pts',(1.07646579789997,2.1136414704478,15.3242757940824));
#95131=CARTESIAN_POINT('Ctrl Pts',(1.03531410950908,2.13389303998039,15.3272967576469));
#95132=CARTESIAN_POINT('Ctrl Pts',(1.0233366742371,2.13966278896058,15.3281758400736));
#95133=CARTESIAN_POINT('Ctrl Pts',(1.00270190958164,2.14939003939643,15.3296903130966));
#95134=CARTESIAN_POINT('Ctrl Pts',(0.994068008356898,2.15339672405444,15.330323987384));
#95135=CARTESIAN_POINT('Ctrl Pts',(0.977554320270775,2.16093965828936,15.3315360900953));
#95136=CARTESIAN_POINT('Ctrl Pts',(0.969678859997232,2.1644850567527,15.3321141915063));
#95137=CARTESIAN_POINT('Ctrl Pts',(0.949260759971957,2.17354313926609,15.3336132021712));
#95138=CARTESIAN_POINT('Ctrl Pts',(0.936689549640122,2.17899023461167,15.3345363341513));
#95139=CARTESIAN_POINT('Ctrl Pts',(0.900633508450888,2.19424361265366,15.33718497023));
#95140=CARTESIAN_POINT('Ctrl Pts',(0.877037693912088,2.20378096545064,15.338919467926));
#95141=CARTESIAN_POINT('Ctrl Pts',(0.674657946939588,2.28181726577387,15.3538109982713));
#95142=CARTESIAN_POINT('Ctrl Pts',(0.488372604105772,2.3288015298481,15.367702749917));
#95143=CARTESIAN_POINT('Ctrl Pts',(0.178264514818422,2.36814540170152,15.3905327926856));
#95144=CARTESIAN_POINT('Ctrl Pts',(0.05700911703828,2.37416235216484,15.3993643359055));
#95145=CARTESIAN_POINT('Ctrl Pts',(-0.0850730743664251,2.37031585521377,
15.4092678461821));
#95146=CARTESIAN_POINT('Ctrl Pts',(-0.105953385329535,2.36947433778072,
15.4107117039305));
#95147=CARTESIAN_POINT('Ctrl Pts',(-0.134660229625759,2.36793714422441,
15.4126784252293));
#95148=CARTESIAN_POINT('Ctrl Pts',(-0.142497736268541,2.36747842567647,
15.4132134941106));
#95149=CARTESIAN_POINT('Ctrl Pts',(-0.155703984657882,2.3666396633045,15.4141117525515));
#95150=CARTESIAN_POINT('Ctrl Pts',(-0.161073921805298,2.36628024977837,
15.4144760726008));
#95151=CARTESIAN_POINT('Ctrl Pts',(-0.17130588959036,2.36556042461378,15.4151684223748));
#95152=CARTESIAN_POINT('Ctrl Pts',(-0.176168083728361,2.36520329732695,
15.4154966390823));
#95153=CARTESIAN_POINT('Ctrl Pts',(-0.187716036577664,2.36431929483684,
15.416274377685));
#95154=CARTESIAN_POINT('Ctrl Pts',(-0.194400775885755,2.36377904623439,
15.4167231575918));
#95155=CARTESIAN_POINT('Ctrl Pts',(-0.217976359209992,2.36177302320012,
15.4183011499951));
#95156=CARTESIAN_POINT('Ctrl Pts',(-0.234854183731834,2.36015445668455,
15.4194222245435));
#95157=CARTESIAN_POINT('Ctrl Pts',(-0.425286930044106,2.3398290395197,15.4319886928342));
#95158=CARTESIAN_POINT('Ctrl Pts',(-0.596312956175944,2.30219446218493,
15.4425248252931));
#95159=CARTESIAN_POINT('Ctrl Pts',(-0.843344323952578,2.21842390892055,
15.4585313339605));
#95160=CARTESIAN_POINT('Ctrl Pts',(-0.923434994510418,2.18629840932515,
15.4638488995471));
#95161=CARTESIAN_POINT('Ctrl Pts',(-1.06843643381551,2.11874472183461,15.4739246455523));
#95162=CARTESIAN_POINT('Ctrl Pts',(-1.13378347644475,2.08450687777171,15.4786461563837));
#95163=CARTESIAN_POINT('Ctrl Pts',(-1.21273769158019,2.03832775471391,15.4846379006));
#95164=CARTESIAN_POINT('Ctrl Pts',(-1.22794883147133,2.02920042950557,15.48580590956));
#95165=CARTESIAN_POINT('Ctrl Pts',(-1.25196676623674,2.01441970703472,15.4876727305471));
#95166=CARTESIAN_POINT('Ctrl Pts',(-1.26084120320339,2.0088770480488,15.4883674779864));
#95167=CARTESIAN_POINT('Ctrl Pts',(-1.27751014367972,1.99831225465248,15.4896819961845));
#95168=CARTESIAN_POINT('Ctrl Pts',(-1.28531246004263,1.99330276429487,15.4903012895199));
#95169=CARTESIAN_POINT('Ctrl Pts',(-1.30285751027588,1.98189209196657,15.491703067741));
#95170=CARTESIAN_POINT('Ctrl Pts',(-1.31258276794445,1.97546460994222,15.4924865263094));
#95171=CARTESIAN_POINT('Ctrl Pts',(-1.33743778065287,1.9587732120232,15.4945056899544));
#95172=CARTESIAN_POINT('Ctrl Pts',(-1.35249671857184,1.9484057346483,15.495745279423));
#95173=CARTESIAN_POINT('Ctrl Pts',(-1.45414015891353,1.87668213295483,15.5042252346625));
#95174=CARTESIAN_POINT('Ctrl Pts',(-1.53662954343993,1.80975777666961,15.511679967145));
#95175=CARTESIAN_POINT('Ctrl Pts',(-1.76947049451228,1.59342535986851,15.5344960603421));
#95176=CARTESIAN_POINT('Ctrl Pts',(-1.90458076916447,1.42919465779465,15.5503199148087));
#95177=CARTESIAN_POINT('Ctrl Pts',(-2.03012248219144,1.2265846022667,15.5670218090217));
#95178=CARTESIAN_POINT('Ctrl Pts',(-2.04376591912257,1.20371429273349,15.5688692978379));
#95179=CARTESIAN_POINT('Ctrl Pts',(-2.06130853139191,1.17314933167095,15.5712840569237));
#95180=CARTESIAN_POINT('Ctrl Pts',(-2.06555444311969,1.16565735287634,15.5718717036749));
#95181=CARTESIAN_POINT('Ctrl Pts',(-2.07246658434096,1.1533044057457,15.5728334558691));
#95182=CARTESIAN_POINT('Ctrl Pts',(-2.07515669584047,1.14845700174375,15.5732090528179));
#95183=CARTESIAN_POINT('Ctrl Pts',(-2.08039191624003,1.13894502581081,15.5739424892654));
#95184=CARTESIAN_POINT('Ctrl Pts',(-2.08293837817727,1.13428127490075,15.5743004099822));
#95185=CARTESIAN_POINT('Ctrl Pts',(-2.08917264981897,1.12277164484894,15.5751796717716));
#95186=CARTESIAN_POINT('Ctrl Pts',(-2.09284255060222,1.11591603174464,15.5756998850522));
#95187=CARTESIAN_POINT('Ctrl Pts',(-2.10534779883016,1.09227673029467,15.5774820563793));
#95188=CARTESIAN_POINT('Ctrl Pts',(-2.11401577944215,1.07540464481927,15.5787340132242));
#95189=CARTESIAN_POINT('Ctrl Pts',(-2.18612238692098,0.930808474258009,
15.5893094541972));
#95190=CARTESIAN_POINT('Ctrl Pts',(-2.23813340819028,0.797687955272024,
15.5980405478792));
#95191=CARTESIAN_POINT('Ctrl Pts',(-2.29648430277262,0.596508853296747,
15.6108779156309));
#95192=CARTESIAN_POINT('Ctrl Pts',(-2.31237730707812,0.531576793309128,
15.6149674495067));
#95193=CARTESIAN_POINT('Ctrl Pts',(-2.340985853288,0.388828751946018,15.6239711531178));
#95194=CARTESIAN_POINT('Ctrl Pts',(-2.35260612703856,0.310878471967256,
15.6288969703466));
#95195=CARTESIAN_POINT('Ctrl Pts',(-2.36227572960904,0.212712792373175,
15.6352034205374));
#95196=CARTESIAN_POINT('Ctrl Pts',(-2.36397576033377,0.19290382185746,15.6364810911436));
#95197=CARTESIAN_POINT('Ctrl Pts',(-2.36542649459319,0.173076749381846,
15.6377659025437));
#95198=CARTESIAN_POINT('Origin',(0.,0.,-1.84858989190503));
#95199=CARTESIAN_POINT('',(-2.36542649454112,0.173076750093503,16.8347081153257));
#95200=CARTESIAN_POINT('',(-2.36542650336594,0.173076629485306,16.639047070016));
#95201=CARTESIAN_POINT('',(-2.36542649454111,0.173076750093529,-1.84858989190503));
#95202=CARTESIAN_POINT('',(-2.37174901238863,-0.00218034299483271,15.8485516738248));
#95203=CARTESIAN_POINT('Ctrl Pts',(-2.36542649454112,0.173076750093436,
16.8347081153257));
#95204=CARTESIAN_POINT('Ctrl Pts',(-2.36533617570272,0.174311130639557,
16.8346254070491));
#95205=CARTESIAN_POINT('Ctrl Pts',(-2.36524489032645,0.175545444712604,
16.8345427506042));
#95206=CARTESIAN_POINT('Ctrl Pts',(-2.36391281400652,0.193367423027911,
16.8333499699269));
#95207=CARTESIAN_POINT('Ctrl Pts',(-2.36249847603169,0.209942235006699,
16.8322491253632));
#95208=CARTESIAN_POINT('Ctrl Pts',(-2.35359957088513,0.302698903603241,
16.8261290782948));
#95209=CARTESIAN_POINT('Ctrl Pts',(-2.34260389197387,0.378506420972745,
16.8212801743013));
#95210=CARTESIAN_POINT('Ctrl Pts',(-2.29067130219724,0.645000732237099,
16.804363538187));
#95211=CARTESIAN_POINT('Ctrl Pts',(-2.22993731004444,0.831013748684088,
16.7927308734518));
#95212=CARTESIAN_POINT('Ctrl Pts',(-2.11971056829759,1.0659219185898,16.7763160834327));
#95213=CARTESIAN_POINT('Ctrl Pts',(-2.08992726287125,1.12319423164069,16.7721714559497));
#95214=CARTESIAN_POINT('Ctrl Pts',(-2.04908633141048,1.19446801615383,16.7667899210928));
#95215=CARTESIAN_POINT('Ctrl Pts',(-2.04015461308784,1.20966018451698,16.7656295031259));
#95216=CARTESIAN_POINT('Ctrl Pts',(-2.02571293365896,1.23360941008247,16.7637782008537));
#95217=CARTESIAN_POINT('Ctrl Pts',(-2.02031342522013,1.242432583414,16.7630913529259));
#95218=CARTESIAN_POINT('Ctrl Pts',(-2.01051938240359,1.25820406223153,16.7618548078621));
#95219=CARTESIAN_POINT('Ctrl Pts',(-2.00614608595954,1.26516541530651,16.7613059012589));
#95220=CARTESIAN_POINT('Ctrl Pts',(-1.99583076141785,1.28139723836003,16.7600186334271));
#95221=CARTESIAN_POINT('Ctrl Pts',(-1.9898602311561,1.29064928003093,16.7592792202131));
#95222=CARTESIAN_POINT('Ctrl Pts',(-1.97246445608558,1.31719844896596,16.7571407864881));
#95223=CARTESIAN_POINT('Ctrl Pts',(-1.96087682681101,1.33438742756422,16.7557357025098));
#95224=CARTESIAN_POINT('Ctrl Pts',(-1.85406522923017,1.48843467876153,16.742952261787));
#95225=CARTESIAN_POINT('Ctrl Pts',(-1.74490208264013,1.61502055063036,16.7310176564493));
#95226=CARTESIAN_POINT('Ctrl Pts',(-1.50581348109747,1.83949381046031,16.7071068823235));
#95227=CARTESIAN_POINT('Ctrl Pts',(-1.37726570381673,1.93761693322448,16.6952162024716));
#95228=CARTESIAN_POINT('Ctrl Pts',(-1.22431931440361,2.03139549522977,16.6827489309086));
#95229=CARTESIAN_POINT('Ctrl Pts',(-1.20878602382077,2.04067680936544,16.6815009110854));
#95230=CARTESIAN_POINT('Ctrl Pts',(-1.1872528034207,2.05321098849625,16.6797972495607));
#95231=CARTESIAN_POINT('Ctrl Pts',(-1.18134328461928,2.05661679204363,16.6793324095788));
#95232=CARTESIAN_POINT('Ctrl Pts',(-1.1711970383492,2.06240616487493,16.6785390452809));
#95233=CARTESIAN_POINT('Ctrl Pts',(-1.1669675675838,2.0648022638635,16.6782097313688));
#95234=CARTESIAN_POINT('Ctrl Pts',(-1.15815231821045,2.06976058125513,16.6775263176511));
#95235=CARTESIAN_POINT('Ctrl Pts',(-1.15356536516053,2.07232058447675,16.6771723711277));
#95236=CARTESIAN_POINT('Ctrl Pts',(-1.14243531716525,2.07848391947978,16.6763174676491));
#95237=CARTESIAN_POINT('Ctrl Pts',(-1.13588355611618,2.08207166260082,16.6758174997181));
#95238=CARTESIAN_POINT('Ctrl Pts',(-1.11276433339208,2.09459013458696,16.674064366193));
#95239=CARTESIAN_POINT('Ctrl Pts',(-1.09610708943823,2.10335484343125,16.6728212237736));
#95240=CARTESIAN_POINT('Ctrl Pts',(-0.991861081030645,2.15663221289448,
16.6651536253653));
#95241=CARTESIAN_POINT('Ctrl Pts',(-0.901670595950356,2.19587015915884,
16.6590071197204));
#95242=CARTESIAN_POINT('Ctrl Pts',(-0.658672096993869,2.28408106635424,
16.6430487977259));
#95243=CARTESIAN_POINT('Ctrl Pts',(-0.502901181207463,2.32335203886898,
16.6333870689937));
#95244=CARTESIAN_POINT('Ctrl Pts',(-0.271985804316576,2.3572383787849,16.6186908837538));
#95245=CARTESIAN_POINT('Ctrl Pts',(-0.199164422236027,2.3645043696942,16.6140091751904));
#95246=CARTESIAN_POINT('Ctrl Pts',(-0.10807750245448,2.3693552060209,16.6080377281787));
#95247=CARTESIAN_POINT('Ctrl Pts',(-0.0900161544375763,2.37011010308593,
16.6068481338259));
#95248=CARTESIAN_POINT('Ctrl Pts',(-0.0614041847593705,2.37097846265692,
16.6049541071176));
#95249=CARTESIAN_POINT('Ctrl Pts',(-0.0508581517034558,2.37122811778336,
16.6042539450632));
#95250=CARTESIAN_POINT('Ctrl Pts',(-0.0311983581266371,2.37156230958205,
16.6029447430095));
#95251=CARTESIAN_POINT('Ctrl Pts',(-0.0220850632155012,2.37166468366853,
16.6023362738307));
#95252=CARTESIAN_POINT('Ctrl Pts',(-0.00181518510370797,2.37177554481518,
16.600979271786));
#95253=CARTESIAN_POINT('Ctrl Pts',(0.00934126530847542,2.37175784245316,
16.6002299318039));
#95254=CARTESIAN_POINT('Ctrl Pts',(0.0419255783884655,2.3714762335178,16.598033972593));
#95255=CARTESIAN_POINT('Ctrl Pts',(0.0633500117264997,2.37100063339745,
16.5965807739839));
#95256=CARTESIAN_POINT('Ctrl Pts',(0.252211877356171,2.36424654562392,16.5836844607207));
#95257=CARTESIAN_POINT('Ctrl Pts',(0.418519295769792,2.34053262250061,16.5716804045725));
#95258=CARTESIAN_POINT('Ctrl Pts',(0.735236340058118,2.26052261831971,16.5478571236935));
#95259=CARTESIAN_POINT('Ctrl Pts',(0.885259017458775,2.20609608089654,16.5361293189005));
#95260=CARTESIAN_POINT('Ctrl Pts',(1.04508637725509,2.12916015845876,16.5238017350609));
#95261=CARTESIAN_POINT('Ctrl Pts',(1.06137530294645,2.12108722905776,16.5225477855257));
#95262=CARTESIAN_POINT('Ctrl Pts',(1.08365631243148,2.10972361492944,16.5208375164233));
#95263=CARTESIAN_POINT('Ctrl Pts',(1.08972887215594,2.10659339289433,16.5203719050675));
#95264=CARTESIAN_POINT('Ctrl Pts',(1.10010161639664,2.10118969970303,16.519577566067));
#95265=CARTESIAN_POINT('Ctrl Pts',(1.10440844346936,2.09892918213749,16.51924804467));
#95266=CARTESIAN_POINT('Ctrl Pts',(1.11334994336599,2.09420092996764,16.5185645759924));
#95267=CARTESIAN_POINT('Ctrl Pts',(1.11798340429571,2.09173103907508,16.5182107802222));
#95268=CARTESIAN_POINT('Ctrl Pts',(1.12917760214604,2.0857160916241,16.5173568524488));
#95269=CARTESIAN_POINT('Ctrl Pts',(1.1357299710987,2.08215539972302,16.5168577038867));
#95270=CARTESIAN_POINT('Ctrl Pts',(1.15869109753201,2.06953721419665,16.5151105892596));
#95271=CARTESIAN_POINT('Ctrl Pts',(1.17500971292941,2.06031589073837,16.5138725551421));
#95272=CARTESIAN_POINT('Ctrl Pts',(1.27544571060828,2.00198000894331,16.5062646627697));
#95273=CARTESIAN_POINT('Ctrl Pts',(1.35659050829796,1.94790978384181,16.5001681086439));
#95274=CARTESIAN_POINT('Ctrl Pts',(1.46044632887465,1.86905899972199,16.4921162388261));
#95275=CARTESIAN_POINT('Ctrl Pts',(1.48628657622867,1.84857709975849,16.4900907974325));
#95276=CARTESIAN_POINT('Ctrl Pts',(1.6541571684501,1.70972082054441,16.4767290701639));
#95277=CARTESIAN_POINT('Ctrl Pts',(1.78233742009686,1.57564116773329,16.4654791236031));
#95278=CARTESIAN_POINT('Ctrl Pts',(1.91054789826366,1.40562904757918,16.4516716397998));
#95279=CARTESIAN_POINT('Ctrl Pts',(1.9270523009774,1.38291561962534,16.4498368080758));
#95280=CARTESIAN_POINT('Ctrl Pts',(1.94973692362416,1.35050212860594,16.4472292216274));
#95281=CARTESIAN_POINT('Ctrl Pts',(1.95625618206859,1.34104131666104,16.4464693995572));
#95282=CARTESIAN_POINT('Ctrl Pts',(1.9675022376664,1.32446441323959,16.4451400815902));
#95283=CARTESIAN_POINT('Ctrl Pts',(1.97225984601859,1.3173693990945,16.4445717617784));
#95284=CARTESIAN_POINT('Ctrl Pts',(1.98214641608798,1.30245197321451,16.4433780963415));
#95285=CARTESIAN_POINT('Ctrl Pts',(1.98726762861412,1.29462462716546,16.442752473146));
#95286=CARTESIAN_POINT('Ctrl Pts',(1.999368548526,1.27588839152302,16.4412564862635));
#95287=CARTESIAN_POINT('Ctrl Pts',(2.00630540839049,1.26495232207124,16.4403845494136));
#95288=CARTESIAN_POINT('Ctrl Pts',(2.02961681583138,1.227527359973,16.4374044913445));
#95289=CARTESIAN_POINT('Ctrl Pts',(2.04555847719562,1.20077399776745,16.4352806365019));
#95290=CARTESIAN_POINT('Ctrl Pts',(2.08259546773821,1.1357394546441,16.4301306219768));
#95291=CARTESIAN_POINT('Ctrl Pts',(2.10316771981346,1.09717505862559,16.4270870393097));
#95292=CARTESIAN_POINT('Ctrl Pts',(2.23679871427543,0.829088480404798,16.4059963486313));
#95293=CARTESIAN_POINT('Ctrl Pts',(2.31311270784828,0.583206262588846,16.3867357693863));
#95294=CARTESIAN_POINT('Ctrl Pts',(2.35257849925455,0.302246837219172,16.3668222853823));
#95295=CARTESIAN_POINT('Ctrl Pts',(2.35597609363102,0.274509681348841,16.364881024595));
#95296=CARTESIAN_POINT('Ctrl Pts',(2.35982011674732,0.237756709145371,16.3623468315939));
#95297=CARTESIAN_POINT('Ctrl Pts',(2.36070628259687,0.228790493897491,16.3617315805551));
#95298=CARTESIAN_POINT('Ctrl Pts',(2.36205853424685,0.214263113001964,16.3607397987397));
#95299=CARTESIAN_POINT('Ctrl Pts',(2.3625561141146,0.208705079273164,16.3603615529729));
#95300=CARTESIAN_POINT('Ctrl Pts',(2.3634818965698,0.197936157527195,16.3596310772723));
#95301=CARTESIAN_POINT('Ctrl Pts',(2.36391248840145,0.192725570722194,16.3592787243643));
#95302=CARTESIAN_POINT('Ctrl Pts',(2.36490578697394,0.180201241814655,16.358434336287));
#95303=CARTESIAN_POINT('Ctrl Pts',(2.36545180706015,0.172886150146965,16.3579432301242));
#95304=CARTESIAN_POINT('Ctrl Pts',(2.36721929880935,0.14762880262042,16.3562543497708));
#95305=CARTESIAN_POINT('Ctrl Pts',(2.36827067489717,0.129674712189231,16.3550656476386));
#95306=CARTESIAN_POINT('Ctrl Pts',(2.37872711325141,-0.0920833506401716,
16.3405102065191));
#95307=CARTESIAN_POINT('Ctrl Pts',(2.36200287983935,-0.296297986119699,
16.3283711887797));
#95308=CARTESIAN_POINT('Ctrl Pts',(2.29326099487223,-0.617820652472512,
16.3080826352234));
#95309=CARTESIAN_POINT('Ctrl Pts',(2.25761633218332,-0.737502838405029,
16.3002624276322));
#95310=CARTESIAN_POINT('Ctrl Pts',(2.20601910657216,-0.871220796122533,
16.2909025801712));
#95311=CARTESIAN_POINT('Ctrl Pts',(2.19909944774937,-0.888542379610534,
16.289677974538));
#95312=CARTESIAN_POINT('Ctrl Pts',(2.18751475642649,-0.916577184348615,
16.2876752193181));
#95313=CARTESIAN_POINT('Ctrl Pts',(2.18297350301448,-0.927340941243415,
16.2869012497671));
#95314=CARTESIAN_POINT('Ctrl Pts',(2.1747302721878,-0.946483069195635,16.2855156296985));
#95315=CARTESIAN_POINT('Ctrl Pts',(2.17105890594106,-0.95487443149719,16.2849050327117));
#95316=CARTESIAN_POINT('Ctrl Pts',(2.16319788135841,-0.972562059829648,
16.2836111498312));
#95317=CARTESIAN_POINT('Ctrl Pts',(2.15899670476978,-0.981852971317604,
16.2829274783043));
#95318=CARTESIAN_POINT('Ctrl Pts',(2.14765220402877,-1.00651647446432,16.2811017091746));
#95319=CARTESIAN_POINT('Ctrl Pts',(2.140403874461,-1.02183982646383,16.2799560069773));
#95320=CARTESIAN_POINT('Ctrl Pts',(2.10434358847059,-1.09600577371286,16.2743541112912));
#95321=CARTESIAN_POINT('Ctrl Pts',(2.0732686402692,-1.15370979010063,16.2698196648299));
#95322=CARTESIAN_POINT('Ctrl Pts',(1.91417641015858,-1.42190050384566,16.2478724385789));
#95323=CARTESIAN_POINT('Ctrl Pts',(1.75630270374976,-1.61283575755307,16.229388119014));
#95324=CARTESIAN_POINT('Ctrl Pts',(1.54464106643181,-1.80016866782357,16.2094094376548));
#95325=CARTESIAN_POINT('Ctrl Pts',(1.5168273976501,-1.8236661609592,16.2068668467367));
#95326=CARTESIAN_POINT('Ctrl Pts',(1.48074295088946,-1.85275394635916,16.2036830757187));
#95327=CARTESIAN_POINT('Ctrl Pts',(1.47296464575211,-1.85894379516006,16.2030033923139));
#95328=CARTESIAN_POINT('Ctrl Pts',(1.46059694040858,-1.86865944635325,16.2019333830018));
#95329=CARTESIAN_POINT('Ctrl Pts',(1.45603326880744,-1.87221758103514,16.2015408320305));
#95330=CARTESIAN_POINT('Ctrl Pts',(1.44738027045671,-1.87891324451396,16.2008009058681));
#95331=CARTESIAN_POINT('Ctrl Pts',(1.44329378598774,-1.88205411069947,16.2004533060632));
#95332=CARTESIAN_POINT('Ctrl Pts',(1.4337397347113,-1.88934792305906,16.1996448523224));
#95333=CARTESIAN_POINT('Ctrl Pts',(1.4282643392905,-1.89349047564534,16.1991847280566));
#95334=CARTESIAN_POINT('Ctrl Pts',(1.41056043560559,-1.906764335725,16.197706975059));
#95335=CARTESIAN_POINT('Ctrl Pts',(1.39826144800889,-1.91580164102501,16.1966956418841));
#95336=CARTESIAN_POINT('Ctrl Pts',(1.36888366370195,-1.93695482659693,16.1943136344407));
#95337=CARTESIAN_POINT('Ctrl Pts',(1.35172970773243,-1.94896468665653,16.1929493091814));
#95338=CARTESIAN_POINT('Ctrl Pts',(1.28836573615744,-1.99208808581077,16.1879970125502));
#95339=CARTESIAN_POINT('Ctrl Pts',(1.24121986128674,-2.02180002900068,16.1844793434659));
#95340=CARTESIAN_POINT('Ctrl Pts',(1.02688626074101,-2.14654944682609,16.1690142813773));
#95341=CARTESIAN_POINT('Ctrl Pts',(0.849562055822769,-2.22270511311299,
16.1575391100184));
#95342=CARTESIAN_POINT('Ctrl Pts',(0.599215427544226,-2.29582959502444,
16.1410761667402));
#95343=CARTESIAN_POINT('Ctrl Pts',(0.532650579853703,-2.31217962553114,
16.1366826892701));
#95344=CARTESIAN_POINT('Ctrl Pts',(0.448102133597615,-2.32910207647693,
16.1310357650741));
#95345=CARTESIAN_POINT('Ctrl Pts',(0.430690284209022,-2.3323845856906,16.1298694274504));
#95346=CARTESIAN_POINT('Ctrl Pts',(0.402936932366686,-2.33729532705455,
16.1280042209181));
#95347=CARTESIAN_POINT('Ctrl Pts',(0.392618373174155,-2.33905075284699,
16.1273094033278));
#95348=CARTESIAN_POINT('Ctrl Pts',(0.373287346545925,-2.34220789095282,
16.1260050544224));
#95349=CARTESIAN_POINT('Ctrl Pts',(0.364277726658014,-2.34362603274966,
16.1253960572953));
#95350=CARTESIAN_POINT('Ctrl Pts',(0.344123236211176,-2.34667938602927,
16.1240312177397));
#95351=CARTESIAN_POINT('Ctrl Pts',(0.332974506141521,-2.34828722969584,
16.123274522952));
#95352=CARTESIAN_POINT('Ctrl Pts',(0.300063484305986,-2.35279450153916,
16.1210354787866));
#95353=CARTESIAN_POINT('Ctrl Pts',(0.278272408952129,-2.35547117809369,
16.1195461502331));
#95354=CARTESIAN_POINT('Ctrl Pts',(0.108378267009901,-2.37394949405787,
16.1078782791159));
#95355=CARTESIAN_POINT('Ctrl Pts',(-0.0408509129551264,-2.37606776643412,
16.0972650740089));
#95356=CARTESIAN_POINT('Ctrl Pts',(-0.273901578097779,-2.35741060508209,
16.08026335504));
#95357=CARTESIAN_POINT('Ctrl Pts',(-0.358109371584906,-2.34609554568976,
16.0740386865986));
#95358=CARTESIAN_POINT('Ctrl Pts',(-0.540205367386482,-2.31159315547355,
16.0605545377084));
#95359=CARTESIAN_POINT('Ctrl Pts',(-0.637607967696352,-2.28664510532846,
16.0533264306466));
#95360=CARTESIAN_POINT('Ctrl Pts',(-0.745128999687133,-2.25169705193351,
16.0455262453547));
#95361=CARTESIAN_POINT('Ctrl Pts',(-0.75708166587365,-2.24770643293271,
16.0446617413604));
#95362=CARTESIAN_POINT('Ctrl Pts',(-0.775091696695292,-2.24153348431924,
16.0433636713543));
#95363=CARTESIAN_POINT('Ctrl Pts',(-0.781172676876621,-2.23942152151149,
16.0429261732525));
#95364=CARTESIAN_POINT('Ctrl Pts',(-0.792067212753133,-2.23558800432949,
16.042143872362));
#95365=CARTESIAN_POINT('Ctrl Pts',(-0.796883848702104,-2.23387562946221,
16.0417985435126));
#95366=CARTESIAN_POINT('Ctrl Pts',(-0.807405736566323,-2.23009660275287,
16.0410453600294));
#95367=CARTESIAN_POINT('Ctrl Pts',(-0.813108599435453,-2.22802362839086,
16.0406378855409));
#95368=CARTESIAN_POINT('Ctrl Pts',(-0.828687360842096,-2.22229301159185,
16.0395266625553));
#95369=CARTESIAN_POINT('Ctrl Pts',(-0.83854710093816,-2.21859138671503,
16.0388254609616));
#95370=CARTESIAN_POINT('Ctrl Pts',(-0.899640904612517,-2.19518957885801,
16.0344916623222));
#95371=CARTESIAN_POINT('Ctrl Pts',(-0.950207518037905,-2.17377962025859,
16.0309529724007));
#95372=CARTESIAN_POINT('Ctrl Pts',(-1.13140032553404,-2.08952950890807,
16.0182914772698));
#95373=CARTESIAN_POINT('Ctrl Pts',(-1.25694335468402,-2.01650691556494,
16.0095392689006));
#95374=CARTESIAN_POINT('Ctrl Pts',(-1.48867711433565,-1.8516180171476,15.9920485441622));
#95375=CARTESIAN_POINT('Ctrl Pts',(-1.59494300794087,-1.76090815367774,
15.9833527433846));
#95376=CARTESIAN_POINT('Ctrl Pts',(-1.70579422406851,-1.64797389206909,
15.9730203504685));
#95377=CARTESIAN_POINT('Ctrl Pts',(-1.71881013690306,-1.63439394381048,
15.9717855463248));
#95378=CARTESIAN_POINT('Ctrl Pts',(-1.73967811049984,-1.61209668602616,
15.9697694130094));
#95379=CARTESIAN_POINT('Ctrl Pts',(-1.74762960622435,-1.60347323155543,
15.9689923581639));
#95380=CARTESIAN_POINT('Ctrl Pts',(-1.76167924631987,-1.58800764807777,
15.9676032996199));
#95381=CARTESIAN_POINT('Ctrl Pts',(-1.76780235768211,-1.58118843829046,
15.966992369422));
#95382=CARTESIAN_POINT('Ctrl Pts',(-1.78063657639965,-1.56672744246382,
15.9656999508173));
#95383=CARTESIAN_POINT('Ctrl Pts',(-1.78733834508678,-1.55907765386027,
15.9650180893987));
#95384=CARTESIAN_POINT('Ctrl Pts',(-1.8008619095087,-1.54343927518922,15.9636277258134));
#95385=CARTESIAN_POINT('Ctrl Pts',(-1.8076802387571,-1.53544800026534,15.9629191013909));
#95386=CARTESIAN_POINT('Ctrl Pts',(-1.83714539922911,-1.50044570574904,
15.9598230750714));
#95387=CARTESIAN_POINT('Ctrl Pts',(-1.85924053461064,-1.47297825340967,
15.957413462809));
#95388=CARTESIAN_POINT('Ctrl Pts',(-1.93973270080922,-1.36821725339418,
15.9482915147709));
#95389=CARTESIAN_POINT('Ctrl Pts',(-1.99398244553544,-1.28787080424194,
15.9414256504957));
#95390=CARTESIAN_POINT('Ctrl Pts',(-2.08667011980185,-1.13063943018615,
15.9282625183686));
#95391=CARTESIAN_POINT('Ctrl Pts',(-2.12614426868707,-1.054536450132,15.9220016201069));
#95392=CARTESIAN_POINT('Ctrl Pts',(-2.21575877287421,-0.85617471462228,
15.9061033935888));
#95393=CARTESIAN_POINT('Ctrl Pts',(-2.25997385379626,-0.731538661048981,
15.8964908511269));
#95394=CARTESIAN_POINT('Ctrl Pts',(-2.29676236927959,-0.591807356432421,
15.8865239123712));
#95395=CARTESIAN_POINT('Ctrl Pts',(-2.29983995670252,-0.579732281874622,
15.8856691522359));
#95396=CARTESIAN_POINT('Ctrl Pts',(-2.30435575927281,-0.561412192081109,
15.8843827933144));
#95397=CARTESIAN_POINT('Ctrl Pts',(-2.30586400863065,-0.555184915930167,
15.8839473646129));
#95398=CARTESIAN_POINT('Ctrl Pts',(-2.30852985023345,-0.54397987947777,
15.8831672468825));
#95399=CARTESIAN_POINT('Ctrl Pts',(-2.30969660047925,-0.539004447097838,
15.8828220451017));
#95400=CARTESIAN_POINT('Ctrl Pts',(-2.31221905592662,-0.528089212803355,
15.8820673602205));
#95401=CARTESIAN_POINT('Ctrl Pts',(-2.31356795803539,-0.522147953112554,
15.8816582684804));
#95402=CARTESIAN_POINT('Ctrl Pts',(-2.31631188806069,-0.509842860325071,
15.880814356802));
#95403=CARTESIAN_POINT('Ctrl Pts',(-2.31770362059747,-0.503478335719643,
15.8803797226988));
#95404=CARTESIAN_POINT('Ctrl Pts',(-2.32123047074438,-0.487025154039982,
15.8792607402974));
#95405=CARTESIAN_POINT('Ctrl Pts',(-2.32332607620465,-0.476928036305058,
15.8785784992669));
#95406=CARTESIAN_POINT('Ctrl Pts',(-2.3293147153752,-0.447096847026955,
15.8765751560402));
#95407=CARTESIAN_POINT('Ctrl Pts',(-2.33302275033609,-0.427326035668191,
15.8752632486081));
#95408=CARTESIAN_POINT('Ctrl Pts',(-2.35982196460956,-0.273671294235081,
15.8651728829661));
#95409=CARTESIAN_POINT('Ctrl Pts',(-2.3716240877574,-0.138062488030204,
15.8568770509635));
#95410=CARTESIAN_POINT('Ctrl Pts',(-2.37174899790563,-0.00218023705663272,
15.8485516447737));
#95411=CARTESIAN_POINT('Ctrl Pts',(-2.37174899780696,-0.00218034439917192,
15.8485516513505));
#95412=CARTESIAN_POINT('Ctrl Pts',(-2.37180279384753,0.0563382572370928,
15.8449662594045));
#95413=CARTESIAN_POINT('Ctrl Pts',(-2.36969079452154,0.114797017167598,
15.8413837181339));
#95414=CARTESIAN_POINT('Ctrl Pts',(-2.3654264678378,0.173077115045234,15.8377719611872));
#95415=CARTESIAN_POINT('Ctrl Pts',(-2.36542649459319,0.173076749381846,
15.6377659025437));
#95416=CARTESIAN_POINT('Ctrl Pts',(-2.36631134326739,0.160983591258964,
15.6385495496222));
#95417=CARTESIAN_POINT('Ctrl Pts',(-2.36710344948036,0.148883698754822,
15.6393358508964));
#95418=CARTESIAN_POINT('Ctrl Pts',(-2.36921667602307,0.112301069719473,
15.6417203895829));
#95419=CARTESIAN_POINT('Ctrl Pts',(-2.37025093872748,0.087804339989173,
15.6433269601623));
#95420=CARTESIAN_POINT('Ctrl Pts',(-2.37122207081869,0.0514286380925134,
15.6457290649617));
#95421=CARTESIAN_POINT('Ctrl Pts',(-2.37144979429577,0.0395585440656365,
15.6465155157445));
#95422=CARTESIAN_POINT('Ctrl Pts',(-2.37169689066206,0.0183933053218808,
15.6479226634835));
#95423=CARTESIAN_POINT('Ctrl Pts',(-2.37175075912594,0.00909874794829185,
15.648542268556));
#95424=CARTESIAN_POINT('Ctrl Pts',(-2.37174913884153,-0.010530621915938,
15.6498544549616));
#95425=CARTESIAN_POINT('Ctrl Pts',(-2.3716807349954,-0.0208652097371478,
15.6505474276722));
#95426=CARTESIAN_POINT('Ctrl Pts',(-2.37131912426492,-0.0483526079760888,
15.652396380362));
#95427=CARTESIAN_POINT('Ctrl Pts',(-2.37090735729391,-0.0655029764717682,
15.6535560412081));
#95428=CARTESIAN_POINT('Ctrl Pts',(-2.36800590946871,-0.148716293252062,
15.6592131153046));
#95429=CARTESIAN_POINT('Ctrl Pts',(-2.36294109887037,-0.214654117274369,
15.6637900571563));
#95430=CARTESIAN_POINT('Ctrl Pts',(-2.32516883836494,-0.532035648390992,
15.6862948703533));
#95431=CARTESIAN_POINT('Ctrl Pts',(-2.25505024466011,-0.777293436356326,
15.7053643700398));
#95432=CARTESIAN_POINT('Ctrl Pts',(-2.13496872761573,-1.03342772216534,
15.7252461944924));
#95433=CARTESIAN_POINT('Ctrl Pts',(-2.12197935460644,-1.05984345240878,
15.7272931885206));
#95434=CARTESIAN_POINT('Ctrl Pts',(-2.10425637371343,-1.09425275966583,
15.7299486161534));
#95435=CARTESIAN_POINT('Ctrl Pts',(-2.09996349835073,-1.10246873023807,
15.730581817809));
#95436=CARTESIAN_POINT('Ctrl Pts',(-2.09295825398374,-1.11568641544864,
15.7315988874223));
#95437=CARTESIAN_POINT('Ctrl Pts',(-2.09027591817234,-1.12070380484424,
15.7319845861501));
#95438=CARTESIAN_POINT('Ctrl Pts',(-2.0850635669779,-1.13036984819048,15.7327268371551));
#95439=CARTESIAN_POINT('Ctrl Pts',(-2.08253602848405,-1.13501971905999,
15.7330835307112));
#95440=CARTESIAN_POINT('Ctrl Pts',(-2.07644831807439,-1.14613038540311,
15.7339350347479));
#95441=CARTESIAN_POINT('Ctrl Pts',(-2.07287348946835,-1.15258317631219,
15.7344289194539));
#95442=CARTESIAN_POINT('Ctrl Pts',(-2.06054219413112,-1.17459899763979,
15.7361121193993));
#95443=CARTESIAN_POINT('Ctrl Pts',(-2.05163983692345,-1.19008023514798,
15.7372925459132));
#95444=CARTESIAN_POINT('Ctrl Pts',(-1.94441592511465,-1.37176325021753,
15.7511259403435));
#95445=CARTESIAN_POINT('Ctrl Pts',(-1.82630988652712,-1.52548501698307,
15.7626764463837));
#95446=CARTESIAN_POINT('Ctrl Pts',(-1.59621020903865,-1.7594102709425,15.7828753777435));
#95447=CARTESIAN_POINT('Ctrl Pts',(-1.49354547756389,-1.84735645835428,
15.7913042326119));
#95448=CARTESIAN_POINT('Ctrl Pts',(-1.36858058133164,-1.93714851196461,
15.801350165109));
#95449=CARTESIAN_POINT('Ctrl Pts',(-1.35305975293344,-1.94802115896561,
15.8025940309628));
#95450=CARTESIAN_POINT('Ctrl Pts',(-1.32761702485824,-1.9653935308073,15.8046277878265));
#95451=CARTESIAN_POINT('Ctrl Pts',(-1.31777351977363,-1.97200700748384,
15.8054133650298));
#95452=CARTESIAN_POINT('Ctrl Pts',(-1.30012845483306,-1.9836709473229,15.8068195401472));
#95453=CARTESIAN_POINT('Ctrl Pts',(-1.29234597248754,-1.98874993638936,
15.8074390519087));
#95454=CARTESIAN_POINT('Ctrl Pts',(-1.27583973779702,-1.99938440296286,
15.808751657762));
#95455=CARTESIAN_POINT('Ctrl Pts',(-1.26710911587882,-2.00492880420458,
15.809445146872));
#95456=CARTESIAN_POINT('Ctrl Pts',(-1.2437719625559,-2.01953579949575,15.8112969444497));
#95457=CARTESIAN_POINT('Ctrl Pts',(-1.229102926197,-2.02849685972918,15.8124589538399));
#95458=CARTESIAN_POINT('Ctrl Pts',(-1.15719014017813,-2.07136072116984,
15.8181471208542));
#95459=CARTESIAN_POINT('Ctrl Pts',(-1.09863970524698,-2.10300107736592,
15.8227538720135));
#95460=CARTESIAN_POINT('Ctrl Pts',(-0.804860947462469,-2.24613902027037,
15.8457691102005));
#95461=CARTESIAN_POINT('Ctrl Pts',(-0.55376648330663,-2.32082903353083,
15.8653908050566));
#95462=CARTESIAN_POINT('Ctrl Pts',(-0.272029619000312,-2.35621769094964,
15.8852423421883));
#95463=CARTESIAN_POINT('Ctrl Pts',(-0.248424784876344,-2.35882325659125,
15.8868874403877));
#95464=CARTESIAN_POINT('Ctrl Pts',(-0.216295793451214,-2.3618820651424,
15.8890985143586));
#95465=CARTESIAN_POINT('Ctrl Pts',(-0.207803433990869,-2.36264438677919,
15.8896802848559));
#95466=CARTESIAN_POINT('Ctrl Pts',(-0.194348917044858,-2.36377903328643,
15.8905975809338));
#95467=CARTESIAN_POINT('Ctrl Pts',(-0.189389487173416,-2.36418155882362,
15.8909347553056));
#95468=CARTESIAN_POINT('Ctrl Pts',(-0.179145571107979,-2.36498055147068,
15.8916291967896));
#95469=CARTESIAN_POINT('Ctrl Pts',(-0.17386099911327,-2.36537491701392,
15.8919863313915));
#95470=CARTESIAN_POINT('Ctrl Pts',(-0.161178102738392,-2.36627865543115,
15.8928408711688));
#95471=CARTESIAN_POINT('Ctrl Pts',(-0.153778544067317,-2.36677105337061,
15.8933373330714));
#95472=CARTESIAN_POINT('Ctrl Pts',(-0.128316864190886,-2.36834546648013,
15.895038797576));
#95473=CARTESIAN_POINT('Ctrl Pts',(-0.110244186457916,-2.36925552334713,
15.8962346494589));
#95474=CARTESIAN_POINT('Ctrl Pts',(-0.00260461544937177,-2.37344137628158,
15.9032960410269));
#95475=CARTESIAN_POINT('Ctrl Pts',(0.0870893102498231,-2.37184526406578,
15.9089300712097));
#95476=CARTESIAN_POINT('Ctrl Pts',(0.262626872989535,-2.35874682502402,
15.919831644605));
#95477=CARTESIAN_POINT('Ctrl Pts',(0.348352970704382,-2.34761800585365,
15.9250973675146));
#95478=CARTESIAN_POINT('Ctrl Pts',(0.5822925405043,-2.30414932650543,15.9397031800274));
#95479=CARTESIAN_POINT('Ctrl Pts',(0.728283654516866,-2.2622471630529,15.9491074507989));
#95480=CARTESIAN_POINT('Ctrl Pts',(0.886913424052246,-2.19975959467743,
15.9602378773239));
#95481=CARTESIAN_POINT('Ctrl Pts',(0.904473376747888,-2.19259790490656,
15.961482648542));
#95482=CARTESIAN_POINT('Ctrl Pts',(0.932875283084999,-2.18061516587046,
15.963517593173));
#95483=CARTESIAN_POINT('Ctrl Pts',(0.943770491125504,-2.17592188435986,
15.9643034443188));
#95484=CARTESIAN_POINT('Ctrl Pts',(0.963137497869736,-2.16740642137893,
15.9657099243245));
#95485=CARTESIAN_POINT('Ctrl Pts',(0.971622963394734,-2.16361578105142,
15.9663294652346));
#95486=CARTESIAN_POINT('Ctrl Pts',(0.989501704740244,-2.15550257589281,
15.9676419390078));
#95487=CARTESIAN_POINT('Ctrl Pts',(0.998889406674494,-2.15116826996895,
15.9683352657454));
#95488=CARTESIAN_POINT('Ctrl Pts',(1.02379751441148,-2.13946998566868,15.9701861687651));
#95489=CARTESIAN_POINT('Ctrl Pts',(1.03926652070592,-2.13199864960447,15.9713474396586));
#95490=CARTESIAN_POINT('Ctrl Pts',(1.11412415492165,-2.09483508093924,15.977025806264));
#95491=CARTESIAN_POINT('Ctrl Pts',(1.17232393371998,-2.06282857451295,15.9816231590127));
#95492=CARTESIAN_POINT('Ctrl Pts',(1.44978472303103,-1.89470457806378,16.0044697084451));
#95493=CARTESIAN_POINT('Ctrl Pts',(1.6471212070856,-1.72590164929287,16.023908047607));
#95494=CARTESIAN_POINT('Ctrl Pts',(1.82988567228383,-1.5090962922528,16.0437678882579));
#95495=CARTESIAN_POINT('Ctrl Pts',(1.84606576412765,-1.48925972287497,16.0455434557501));
#95496=CARTESIAN_POINT('Ctrl Pts',(1.86736132667646,-1.46227112185837,16.0478998672218));
#95497=CARTESIAN_POINT('Ctrl Pts',(1.87276208353858,-1.45534784254626,16.0484992159628));
#95498=CARTESIAN_POINT('Ctrl Pts',(1.88119363931474,-1.44441469594736,16.0494374537593));
#95499=CARTESIAN_POINT('Ctrl Pts',(1.8842502826396,-1.44042500535293,16.0497781220154));
#95500=CARTESIAN_POINT('Ctrl Pts',(1.89048600929064,-1.43223199399843,16.0504741520808));
#95501=CARTESIAN_POINT('Ctrl Pts',(1.89366377337741,-1.42802778329928,16.0508294088157));
#95502=CARTESIAN_POINT('Ctrl Pts',(1.90117613402937,-1.41801969040789,16.0516706506771));
#95503=CARTESIAN_POINT('Ctrl Pts',(1.90549824681049,-1.41220641900579,16.0521557690981));
#95504=CARTESIAN_POINT('Ctrl Pts',(1.91991382147241,-1.39263069660829,16.0537779257677));
#95505=CARTESIAN_POINT('Ctrl Pts',(1.92988564566857,-1.37877872602922,16.0549069219039));
#95506=CARTESIAN_POINT('Ctrl Pts',(1.98554862906991,-1.29966945456524,16.0612561868064));
#95507=CARTESIAN_POINT('Ctrl Pts',(2.02808358047842,-1.23224341729562,16.0662927950689));
#95508=CARTESIAN_POINT('Ctrl Pts',(2.16535194256524,-0.988216354172134,
16.0837104603745));
#95509=CARTESIAN_POINT('Ctrl Pts',(2.24104234669843,-0.801905214317238,
16.0956646999749));
#95510=CARTESIAN_POINT('Ctrl Pts',(2.30692333880819,-0.553626026889995,
16.1119899127481));
#95511=CARTESIAN_POINT('Ctrl Pts',(2.31946831013191,-0.498460639596935,
16.1156347928399));
#95512=CARTESIAN_POINT('Ctrl Pts',(2.33319204266687,-0.426262662596877,
16.1204532279965));
#95513=CARTESIAN_POINT('Ctrl Pts',(2.33617668133387,-0.409589372785323,
16.1215692392768));
#95514=CARTESIAN_POINT('Ctrl Pts',(2.34068649944891,-0.38274090274353,16.1233721569007));
#95515=CARTESIAN_POINT('Ctrl Pts',(2.34232453975285,-0.372585066957693,
16.1240554740859));
#95516=CARTESIAN_POINT('Ctrl Pts',(2.34531832248156,-0.353223179002146,
16.1253608912502));
#95517=CARTESIAN_POINT('Ctrl Pts',(2.34668606026206,-0.3440191539199,16.1259825982509));
#95518=CARTESIAN_POINT('Ctrl Pts',(2.34968788895487,-0.322967373467029,
16.1274073361614));
#95519=CARTESIAN_POINT('Ctrl Pts',(2.35128658491925,-0.311114908487316,
16.1282114695021));
#95520=CARTESIAN_POINT('Ctrl Pts',(2.35594635326863,-0.274478504451135,
16.1307034797173));
#95521=CARTESIAN_POINT('Ctrl Pts',(2.35870561189589,-0.24965861100176,16.1324007841839));
#95522=CARTESIAN_POINT('Ctrl Pts',(2.37009713187918,-0.130013889384252,
16.1406290551175));
#95523=CARTESIAN_POINT('Ctrl Pts',(2.3734047312238,-0.0347822048791796,
16.1473234187161));
#95524=CARTESIAN_POINT('Ctrl Pts',(2.36700753309429,0.216419937859404,16.1653406258765));
#95525=CARTESIAN_POINT('Ctrl Pts',(2.34763891667966,0.371683116098985,16.1768638115163));
#95526=CARTESIAN_POINT('Ctrl Pts',(2.30730454719941,0.549770269147731,16.1900657858004));
#95527=CARTESIAN_POINT('Ctrl Pts',(2.30101171848522,0.575540419663705,16.1919748281507));
#95528=CARTESIAN_POINT('Ctrl Pts',(2.28066973482631,0.653169064556107,16.1977120649367));
#95529=CARTESIAN_POINT('Ctrl Pts',(2.26528860714011,0.704665059014168,16.201499815575));
#95530=CARTESIAN_POINT('Ctrl Pts',(2.24490643746561,0.765309152039998,16.2059045759265));
#95531=CARTESIAN_POINT('Ctrl Pts',(2.24157977842134,0.774998785582229,16.2066066284557));
#95532=CARTESIAN_POINT('Ctrl Pts',(2.23603752744574,0.790807550649909,16.2077488491666));
#95533=CARTESIAN_POINT('Ctrl Pts',(2.23385939377354,0.796939532045251,16.2081911111398));
#95534=CARTESIAN_POINT('Ctrl Pts',(2.22990037324158,0.807941379709544,16.208983089878));
#95535=CARTESIAN_POINT('Ctrl Pts',(2.22812873812324,0.812814416464725,16.2093333365608));
#95536=CARTESIAN_POINT('Ctrl Pts',(2.2242101151525,0.823483837887346,16.2100989981503));
#95537=CARTESIAN_POINT('Ctrl Pts',(2.2220564472532,0.829277646531788,16.2105140109562));
#95538=CARTESIAN_POINT('Ctrl Pts',(2.21582531816323,0.84584209583743,16.2116985201911));
#95539=CARTESIAN_POINT('Ctrl Pts',(2.21169195540132,0.856591734435686,16.2124647783753));
#95540=CARTESIAN_POINT('Ctrl Pts',(2.18242541852354,0.931080928072647,16.21776038779));
#95541=CARTESIAN_POINT('Ctrl Pts',(2.15461617268167,0.993742210508296,16.2221431591681));
#95542=CARTESIAN_POINT('Ctrl Pts',(2.07375581623797,1.15652773882642,16.2335598488762));
#95543=CARTESIAN_POINT('Ctrl Pts',(2.01618207264991,1.25420581714142,16.2404479159748));
#95544=CARTESIAN_POINT('Ctrl Pts',(1.86325014110692,1.47574325160229,16.2569635762311));
#95545=CARTESIAN_POINT('Ctrl Pts',(1.76222459476682,1.59501530850938,16.2666236821927));
#95546=CARTESIAN_POINT('Ctrl Pts',(1.63665258877876,1.71666070253472,16.2780379353255));
#95547=CARTESIAN_POINT('Ctrl Pts',(1.622913736542,1.72965506206226,16.2792792388647));
#95548=CARTESIAN_POINT('Ctrl Pts',(1.60031752330987,1.75052056197424,16.2813096338896));
#95549=CARTESIAN_POINT('Ctrl Pts',(1.5915537976266,1.75849222743307,16.2820944354729));
#95550=CARTESIAN_POINT('Ctrl Pts',(1.57581058967376,1.7725984843435,16.2834997479155));
#95551=CARTESIAN_POINT('Ctrl Pts',(1.56885403650617,1.7787583897592,16.2841191777095));
#95552=CARTESIAN_POINT('Ctrl Pts',(1.55407324730291,1.79169235885959,16.2854321602534));
#95553=CARTESIAN_POINT('Ctrl Pts',(1.54624052995704,1.79845638935291,16.2861261112714));
#95554=CARTESIAN_POINT('Ctrl Pts',(1.52525745687911,1.81633815270661,16.2879804538177));
#95555=CARTESIAN_POINT('Ctrl Pts',(1.51203007067873,1.82736412156763,16.289144564247));
#95556=CARTESIAN_POINT('Ctrl Pts',(1.44682628597602,1.88052345777757,16.2948607314237));
#95557=CARTESIAN_POINT('Ctrl Pts',(1.39320766631885,1.92058470931037,16.2994943473301));
#95558=CARTESIAN_POINT('Ctrl Pts',(1.13833937031688,2.09471667176372,16.3212380101209));
#95559=CARTESIAN_POINT('Ctrl Pts',(0.919071448557426,2.19975693976898,16.3393601541189));
#95560=CARTESIAN_POINT('Ctrl Pts',(0.651006461277558,2.2809783485855,16.3591881085869));
#95561=CARTESIAN_POINT('Ctrl Pts',(0.61400105479112,2.29121687429302,16.3618725218722));
#95562=CARTESIAN_POINT('Ctrl Pts',(0.566849618394449,2.30303798923258,16.3652130777629));
#95563=CARTESIAN_POINT('Ctrl Pts',(0.556922180982075,2.30545877508622,16.3659119667044));
#95564=CARTESIAN_POINT('Ctrl Pts',(0.541238689485686,2.30917594563744,16.3670087499883));
#95565=CARTESIAN_POINT('Ctrl Pts',(0.535493058692275,2.31051510554239,16.3674090087311));
#95566=CARTESIAN_POINT('Ctrl Pts',(0.525161880149412,2.31288243217529,16.3681258614494));
#95567=CARTESIAN_POINT('Ctrl Pts',(0.520578312860992,2.31391840091876,16.3684428901693));
#95568=CARTESIAN_POINT('Ctrl Pts',(0.509526474841681,2.31638181395521,16.369204904818));
#95569=CARTESIAN_POINT('Ctrl Pts',(0.503055270548331,2.31779579213878,16.3696491173834));
#95570=CARTESIAN_POINT('Ctrl Pts',(0.483199717937665,2.32204721800046,16.3710062930981));
#95571=CARTESIAN_POINT('Ctrl Pts',(0.469796377252478,2.32479604180571,16.3719143817251));
#95572=CARTESIAN_POINT('Ctrl Pts',(0.438573974559455,2.33091822936595,16.3740126108513));
#95573=CARTESIAN_POINT('Ctrl Pts',(0.42073829119197,2.33420355982982,16.3751983089881));
#95574=CARTESIAN_POINT('Ctrl Pts',(0.194010155285068,2.37328356462553,16.3901278026231));
#95575=CARTESIAN_POINT('Ctrl Pts',(-0.0187557240737306,2.38113192331203,
16.402671331518));
#95576=CARTESIAN_POINT('Ctrl Pts',(-0.334738812670418,2.35037736255527,
16.4223808911361));
#95577=CARTESIAN_POINT('Ctrl Pts',(-0.438910140511386,2.33316895835173,
16.4290451302656));
#95578=CARTESIAN_POINT('Ctrl Pts',(-0.559361175096658,2.30491792067688,
16.437128193812));
#95579=CARTESIAN_POINT('Ctrl Pts',(-0.577091036013345,2.3005428600057,16.4383275482758));
#95580=CARTESIAN_POINT('Ctrl Pts',(-0.606046887676739,2.29304186128059,
16.4403028470243));
#95581=CARTESIAN_POINT('Ctrl Pts',(-0.617303710468162,2.29003710198756,
16.4410748842376));
#95582=CARTESIAN_POINT('Ctrl Pts',(-0.637477766645613,2.28449253010937,
16.4424661266822));
#95583=CARTESIAN_POINT('Ctrl Pts',(-0.646403168537081,2.28198312057731,
16.4430843344653));
#95584=CARTESIAN_POINT('Ctrl Pts',(-0.665373257611699,2.27652938769551,
16.4444041314596));
#95585=CARTESIAN_POINT('Ctrl Pts',(-0.675413597174228,2.27357077999345,
16.4451061749616));
#95586=CARTESIAN_POINT('Ctrl Pts',(-0.702433975455513,2.26541385029123,
16.447005164379));
#95587=CARTESIAN_POINT('Ctrl Pts',(-0.719375475673119,2.26009121453313,
16.4482061503907));
#95588=CARTESIAN_POINT('Ctrl Pts',(-0.805512092615517,2.23196244439509,
16.454366626511));
#95589=CARTESIAN_POINT('Ctrl Pts',(-0.87368283898543,2.20616916716439,16.4594235393733));
#95590=CARTESIAN_POINT('Ctrl Pts',(-1.08484824146486,2.11494893451944,16.4756803479646));
#95591=CARTESIAN_POINT('Ctrl Pts',(-1.22257632674005,2.03843100769523,16.4872042469043));
#95592=CARTESIAN_POINT('Ctrl Pts',(-1.44297470466723,1.88556605096541,16.5067547322551));
#95593=CARTESIAN_POINT('Ctrl Pts',(-1.52969607430036,1.81592164463275,16.5147817610046));
#95594=CARTESIAN_POINT('Ctrl Pts',(-1.62059621745061,1.73177049814813,16.5233298979126));
#95595=CARTESIAN_POINT('Ctrl Pts',(-1.62989784121626,1.72301892146699,16.5242062240611));
#95596=CARTESIAN_POINT('Ctrl Pts',(-1.64384600106517,1.70968154611866,16.5255221503006));
#95597=CARTESIAN_POINT('Ctrl Pts',(-1.64854485659463,1.70515117299054,16.5259657797996));
#95598=CARTESIAN_POINT('Ctrl Pts',(-1.65694358403618,1.69698642231767,16.5267592006612));
#95599=CARTESIAN_POINT('Ctrl Pts',(-1.66065027601395,1.69335927099031,16.5271095308544));
#95600=CARTESIAN_POINT('Ctrl Pts',(-1.6678577292978,1.68626005284801,16.5277910406233));
#95601=CARTESIAN_POINT('Ctrl Pts',(-1.67135954290541,1.68278924719491,16.5281223125147));
#95602=CARTESIAN_POINT('Ctrl Pts',(-1.68138178448826,1.67279360509633,16.5290709520292));
#95603=CARTESIAN_POINT('Ctrl Pts',(-1.68787509809914,1.66624152231348,16.5296862201383));
#95604=CARTESIAN_POINT('Ctrl Pts',(-1.71846549912924,1.63501193218469,16.5325889019886));
#95605=CARTESIAN_POINT('Ctrl Pts',(-1.74206207247801,1.60984711521785,16.5348401721584));
#95606=CARTESIAN_POINT('Ctrl Pts',(-1.80817422454824,1.53618432548653,16.5412150867873));
#95607=CARTESIAN_POINT('Ctrl Pts',(-1.849273920515,1.48645334095125,16.545262535052));
#95608=CARTESIAN_POINT('Ctrl Pts',(-1.94302570206359,1.36309562775726,16.5548732788437));
#95609=CARTESIAN_POINT('Ctrl Pts',(-1.99359047065856,1.28801258521187,16.5603847697278));
#95610=CARTESIAN_POINT('Ctrl Pts',(-2.11719378615471,1.07968811971746,16.5752535464667));
#95611=CARTESIAN_POINT('Ctrl Pts',(-2.18192304514981,0.94203946141935,16.5846709892642));
#95612=CARTESIAN_POINT('Ctrl Pts',(-2.23943589762864,0.781334409869855,
16.5958143438064));
#95613=CARTESIAN_POINT('Ctrl Pts',(-2.24560219951976,0.763431285058992,
16.5970572451884));
#95614=CARTESIAN_POINT('Ctrl Pts',(-2.2552792524472,0.734203025621577,16.5990897366829));
#95615=CARTESIAN_POINT('Ctrl Pts',(-2.25892068699309,0.722921787321626,
16.5998750219936));
#95616=CARTESIAN_POINT('Ctrl Pts',(-2.26526550212029,0.702749330666586,
16.6012808723589));
#95617=CARTESIAN_POINT('Ctrl Pts',(-2.26800150477372,0.693868566060845,
16.6019003531756));
#95618=CARTESIAN_POINT('Ctrl Pts',(-2.2736728708009,0.675067964194774,16.603213100316));
#95619=CARTESIAN_POINT('Ctrl Pts',(-2.27659565562608,0.665144566690179,
16.6039067628791));
#95620=CARTESIAN_POINT('Ctrl Pts',(-2.28420520425342,0.638670901854381,
16.6057595160973));
#95621=CARTESIAN_POINT('Ctrl Pts',(-2.2887769261295,0.622088491461285,16.6069223144217));
#95622=CARTESIAN_POINT('Ctrl Pts',(-2.29840021455703,0.585640368256932,
16.6094836446329));
#95623=CARTESIAN_POINT('Ctrl Pts',(-2.30337538619074,0.565756106135499,
16.6108845348272));
#95624=CARTESIAN_POINT('Ctrl Pts',(-2.33709238449061,0.423175572073484,
16.6209568971406));
#95625=CARTESIAN_POINT('Ctrl Pts',(-2.35624693458251,0.298533170639224,
16.6299219917352));
#95626=CARTESIAN_POINT('Ctrl Pts',(-2.36542650336594,0.17307662948527,16.639047070016));
#95627=CARTESIAN_POINT('Origin',(0.,0.,-1.84858989190503));
#95628=CARTESIAN_POINT('',(-2.36542646972628,0.173077089235633,17.8377309811821));
#95629=CARTESIAN_POINT('',(-2.3692863196969,0.173352773124932,17.639803316701));
#95630=CARTESIAN_POINT('',(-2.36542649454111,0.173076750093529,-1.84858989190503));
#95631=CARTESIAN_POINT('Ctrl Pts',(-2.36542646972629,0.173077089235462,
17.8377309811821));
#95632=CARTESIAN_POINT('Ctrl Pts',(-2.35433609142309,0.324648129131858,
17.8267093548572));
#95633=CARTESIAN_POINT('Ctrl Pts',(-2.3286947503669,0.474925913114985,17.8154678917761));
#95634=CARTESIAN_POINT('Ctrl Pts',(-2.28012575711333,0.653692848604288,
17.8022638581209));
#95635=CARTESIAN_POINT('Ctrl Pts',(-2.27080606778965,0.685366943566306,
17.7999323289627));
#95636=CARTESIAN_POINT('Ctrl Pts',(-2.25431165770714,0.737388501923027,
17.7961271714833));
#95637=CARTESIAN_POINT('Ctrl Pts',(-2.24751546673184,0.75785035640701,17.7946367544241));
#95638=CARTESIAN_POINT('Ctrl Pts',(-2.23785557246991,0.785660602118027,
17.7926223524087));
#95639=CARTESIAN_POINT('Ctrl Pts',(-2.23523311809341,0.7930908253336,17.7920852604333));
#95640=CARTESIAN_POINT('Ctrl Pts',(-2.23077327396355,0.80552909045965,17.7911881860162));
#95641=CARTESIAN_POINT('Ctrl Pts',(-2.22895594963453,0.810544194819505,
17.7908270397563));
#95642=CARTESIAN_POINT('Ctrl Pts',(-2.22547882620366,0.820039561875361,
17.7901443702398));
#95643=CARTESIAN_POINT('Ctrl Pts',(-2.22382238849385,0.824520996940868,
17.7898226450493));
#95644=CARTESIAN_POINT('Ctrl Pts',(-2.21944722740887,0.836248746821881,
17.7889818519484));
#95645=CARTESIAN_POINT('Ctrl Pts',(-2.21670652829653,0.843486889911999,
17.7884640834377));
#95646=CARTESIAN_POINT('Ctrl Pts',(-2.20706737918103,0.868572247713667,
17.7866732223519));
#95647=CARTESIAN_POINT('Ctrl Pts',(-2.19998820639566,0.886349883081612,
17.7854103741261));
#95648=CARTESIAN_POINT('Ctrl Pts',(-2.1453116973185,1.01896436464643,17.7760234310807));
#95649=CARTESIAN_POINT('Ctrl Pts',(-2.08896038534084,1.13000157716791,17.7683472537538));
#95650=CARTESIAN_POINT('Ctrl Pts',(-1.96871125148398,1.32691025881613,17.7541876848687));
#95651=CARTESIAN_POINT('Ctrl Pts',(-1.90722268800142,1.41386547461939,17.7477078053922));
#95652=CARTESIAN_POINT('Ctrl Pts',(-1.79888601085289,1.54708622654022,17.7370147231516));
#95653=CARTESIAN_POINT('Ctrl Pts',(-1.75559066508366,1.59604733071329,17.7328977553571));
#95654=CARTESIAN_POINT('Ctrl Pts',(-1.69084743149421,1.66343740401887,17.7268984897846));
#95655=CARTESIAN_POINT('Ctrl Pts',(-1.6710043622939,1.68336964181303,17.7250794317993));
#95656=CARTESIAN_POINT('Ctrl Pts',(-1.63512468469334,1.71815094986002,17.721820391858));
#95657=CARTESIAN_POINT('Ctrl Pts',(-1.61922825028689,1.73314028342154,17.7203865462583));
#95658=CARTESIAN_POINT('Ctrl Pts',(-1.59486518331644,1.75548534558101,17.718202696384));
#95659=CARTESIAN_POINT('Ctrl Pts',(-1.58654943297323,1.76300443587321,17.7174596446547));
#95660=CARTESIAN_POINT('Ctrl Pts',(-1.57807502812236,1.7705584678841,17.7167046801618));
#95661=CARTESIAN_POINT('Ctrl Pts',(-1.57796924195418,1.77065274800735,17.7166952562797));
#95662=CARTESIAN_POINT('Ctrl Pts',(-1.57775371135024,1.77084480133748,17.7166760566192));
#95663=CARTESIAN_POINT('Ctrl Pts',(-1.57764396627176,1.77094257382608,17.7166662808104));
#95664=CARTESIAN_POINT('Ctrl Pts',(-1.57742026114263,1.77114183664773,17.7166463545115));
#95665=CARTESIAN_POINT('Ctrl Pts',(-1.57730630039247,1.7712433261778,17.7166362039889));
#95666=CARTESIAN_POINT('Ctrl Pts',(-1.57707388492029,1.77145026719746,17.7166155035019));
#95667=CARTESIAN_POINT('Ctrl Pts',(-1.57695542941263,1.77155571780781,17.7166049535006));
#95668=CARTESIAN_POINT('Ctrl Pts',(-1.57671372063203,1.77177084660838,17.7165834270993));
#95669=CARTESIAN_POINT('Ctrl Pts',(-1.57659046649173,1.7718805238187,17.7165724506587));
#95670=CARTESIAN_POINT('Ctrl Pts',(-1.57633882911922,1.77210439529776,17.7165500419834));
#95671=CARTESIAN_POINT('Ctrl Pts',(-1.57621044492265,1.77221858847584,17.7165386097033));
#95672=CARTESIAN_POINT('Ctrl Pts',(-1.57594818542865,1.77245180792992,17.7165152572364));
#95673=CARTESIAN_POINT('Ctrl Pts',(-1.57581430905966,1.77257083298599,17.7165033369993));
#95674=CARTESIAN_POINT('Ctrl Pts',(-1.57554066900929,1.77281406181197,17.7164789734773));
#95675=CARTESIAN_POINT('Ctrl Pts',(-1.57540090411789,1.77293826422834,17.7164665301352));
#95676=CARTESIAN_POINT('Ctrl Pts',(-1.57511505250619,1.77319222647951,17.7164410818713));
#95677=CARTESIAN_POINT('Ctrl Pts',(-1.57496896443893,1.77332198478818,17.7164280768862));
#95678=CARTESIAN_POINT('Ctrl Pts',(-1.57466998907782,1.77358747452592,17.7164014630098));
#95679=CARTESIAN_POINT('Ctrl Pts',(-1.57451710027174,1.77372320423718,17.7163878540474));
#95680=CARTESIAN_POINT('Ctrl Pts',(-1.57428024895467,1.77393341838099,17.7163667725361));
#95681=CARTESIAN_POINT('Ctrl Pts',(-1.57419629867085,1.77400791665332,17.7163593005636));
#95682=CARTESIAN_POINT('Ctrl Pts',(-1.57400770356189,1.77417525380031,17.7163425152024));
#95683=CARTESIAN_POINT('Ctrl Pts',(-1.57390305583108,1.77426808935831,17.7163332016773));
#95684=CARTESIAN_POINT('Ctrl Pts',(-1.57366747479444,1.77447704180718,17.7163122360133));
#95685=CARTESIAN_POINT('Ctrl Pts',(-1.57353653685349,1.77459315346188,17.7163005836555));
#95686=CARTESIAN_POINT('Ctrl Pts',(-1.57324100163432,1.77485516638854,17.7162742847562));
#95687=CARTESIAN_POINT('Ctrl Pts',(-1.57307639692571,1.77500105924325,17.716259637864));
#95688=CARTESIAN_POINT('Ctrl Pts',(-1.57270364763563,1.77533134274638,17.71622647172));
#95689=CARTESIAN_POINT('Ctrl Pts',(-1.57249549094759,1.77551571966386,17.7162079518969));
#95690=CARTESIAN_POINT('Ctrl Pts',(-1.57202213970447,1.77593484683839,17.7161658406272));
#95691=CARTESIAN_POINT('Ctrl Pts',(-1.57175692502872,1.77616957426928,17.7161422482304));
#95692=CARTESIAN_POINT('Ctrl Pts',(-1.56463521320983,1.78246977917069,17.7155087889948));
#95693=CARTESIAN_POINT('Ctrl Pts',(-1.55774379341371,1.78849549456921,17.7148972734048));
#95694=CARTESIAN_POINT('Ctrl Pts',(-1.54201311578825,1.80209018448958,17.7135045891922));
#95695=CARTESIAN_POINT('Ctrl Pts',(-1.53315274472992,1.8096342545427,17.7127224117717));
#95696=CARTESIAN_POINT('Ctrl Pts',(-1.51006277652303,1.82900266905013,17.710689661714));
#95697=CARTESIAN_POINT('Ctrl Pts',(-1.49574992765401,1.84072607207892,17.7094350325183));
#95698=CARTESIAN_POINT('Ctrl Pts',(-1.39042105029566,1.92495945108253,17.7002393381218));
#95699=CARTESIAN_POINT('Ctrl Pts',(-1.29432948786212,1.990839803525,17.6920380063034));
#95700=CARTESIAN_POINT('Ctrl Pts',(-1.05114855366332,2.13249654360722,17.6717593279395));
#95701=CARTESIAN_POINT('Ctrl Pts',(-0.900212777535253,2.20047013307773,
17.6595330368863));
#95702=CARTESIAN_POINT('Ctrl Pts',(-0.688180678851421,2.27046084061658,
17.6435385405596));
#95703=CARTESIAN_POINT('Ctrl Pts',(-0.632257361532253,2.2866650437756,17.639429155624));
#95704=CARTESIAN_POINT('Ctrl Pts',(-0.56516258737836,2.30345595002304,17.6346702208398));
#95705=CARTESIAN_POINT('Ctrl Pts',(-0.55451723111309,2.30604178539709,17.6339202327329));
#95706=CARTESIAN_POINT('Ctrl Pts',(-0.538005900301467,2.30993156026769,
17.6327652148397));
#95707=CARTESIAN_POINT('Ctrl Pts',(-0.53215241988171,2.31128707994899,17.6323573442527));
#95708=CARTESIAN_POINT('Ctrl Pts',(-0.521304348141874,2.31375582607862,
17.6316044871929));
#95709=CARTESIAN_POINT('Ctrl Pts',(-0.516311338804347,2.31487512587566,
17.6312591694107));
#95710=CARTESIAN_POINT('Ctrl Pts',(-0.504953656398979,2.31738264019071,
17.6304763567351));
#95711=CARTESIAN_POINT('Ctrl Pts',(-0.498586867895889,2.31876079704201,
17.6300394396708));
#95712=CARTESIAN_POINT('Ctrl Pts',(-0.482016193407498,2.3222762832845,17.6289070436771));
#95713=CARTESIAN_POINT('Ctrl Pts',(-0.471803614392826,2.32437262631441,
17.6282138237781));
#95714=CARTESIAN_POINT('Ctrl Pts',(-0.40357841149047,2.33790907062999,17.6236119196753));
#95715=CARTESIAN_POINT('Ctrl Pts',(-0.34516368633506,2.3472447137581,17.6198119929584));
#95716=CARTESIAN_POINT('Ctrl Pts',(-0.216685226020823,2.36287654137471,
17.6116393278272));
#95717=CARTESIAN_POINT('Ctrl Pts',(-0.146567955237341,2.3682603226395,17.6072973634294));
#95718=CARTESIAN_POINT('Ctrl Pts',(0.0195230748374318,2.37360711387456,
17.5970883317019));
#95719=CARTESIAN_POINT('Ctrl Pts',(0.115455206019669,2.37087782733981,17.5912489224489));
#95720=CARTESIAN_POINT('Ctrl Pts',(0.325226749636935,2.35214521247095,17.5782097301718));
#95721=CARTESIAN_POINT('Ctrl Pts',(0.438589678738733,2.33366520341996,17.5709818005324));
#95722=CARTESIAN_POINT('Ctrl Pts',(0.569278799271721,2.30249993995939,17.5621987043796));
#95723=CARTESIAN_POINT('Ctrl Pts',(0.58833839366314,2.29770368431307,17.5609066166919));
#95724=CARTESIAN_POINT('Ctrl Pts',(0.617760143383031,2.28990977160232,17.5588937324179));
#95725=CARTESIAN_POINT('Ctrl Pts',(0.628165464648626,2.28707728319701,17.5581782815323));
#95726=CARTESIAN_POINT('Ctrl Pts',(0.646451802346504,2.28196525640271,17.5569144875278));
#95727=CARTESIAN_POINT('Ctrl Pts',(0.654341042082733,2.27971558794437,17.5563671244791));
#95728=CARTESIAN_POINT('Ctrl Pts',(0.672328591468121,2.27448525751791,17.5551141872217));
#95729=CARTESIAN_POINT('Ctrl Pts',(0.682418983410505,2.27147820734345,17.5544077607304));
#95730=CARTESIAN_POINT('Ctrl Pts',(0.709694355689285,2.26315169626541,17.5524883451438));
#95731=CARTESIAN_POINT('Ctrl Pts',(0.726839089474695,2.25770383036204,17.5512711742375));
#95732=CARTESIAN_POINT('Ctrl Pts',(0.812207946496449,2.22950407674143,17.5451557117674));
#95733=CARTESIAN_POINT('Ctrl Pts',(0.879427727219195,2.20385460875232,17.5401627867531));
#95734=CARTESIAN_POINT('Ctrl Pts',(1.11900388236409,2.09973110811302,17.5217007694263));
#95735=CARTESIAN_POINT('Ctrl Pts',(1.28296330421368,2.00375369913688,17.5077009430674));
#95736=CARTESIAN_POINT('Ctrl Pts',(1.47760950558301,1.85604441957882,17.4900231277926));
#95737=CARTESIAN_POINT('Ctrl Pts',(1.52030845028555,1.82123414166839,17.4860758532282));
#95738=CARTESIAN_POINT('Ctrl Pts',(1.57739753167688,1.77128395627919,17.4807397311835));
#95739=CARTESIAN_POINT('Ctrl Pts',(1.59285578607418,1.75739589706813,17.4792886599954));
#95740=CARTESIAN_POINT('Ctrl Pts',(1.61928142281692,1.73301930254124,17.476800182791));
#95741=CARTESIAN_POINT('Ctrl Pts',(1.63033414825874,1.72262556130442,17.4757568983895));
#95742=CARTESIAN_POINT('Ctrl Pts',(1.64623112028907,1.70738632824647,17.4742537447551));
#95743=CARTESIAN_POINT('Ctrl Pts',(1.65115503163474,1.70262504380405,17.4737877895056));
#95744=CARTESIAN_POINT('Ctrl Pts',(1.65974635176797,1.69424515703345,17.4729742438012));
#95745=CARTESIAN_POINT('Ctrl Pts',(1.66342268553847,1.69063584951031,17.4726259462045));
#95746=CARTESIAN_POINT('Ctrl Pts',(1.67120970125448,1.6829408146612,17.4718878669036));
#95747=CARTESIAN_POINT('Ctrl Pts',(1.67531717888695,1.67885198965874,17.471498335297));
#95748=CARTESIAN_POINT('Ctrl Pts',(1.68645704955735,1.66768111163502,17.4704411691226));
#95749=CARTESIAN_POINT('Ctrl Pts',(1.69345989505657,1.66056955975671,17.4697758173114));
#95750=CARTESIAN_POINT('Ctrl Pts',(1.7260841497601,1.62701784914539,17.4666711688291));
#95751=CARTESIAN_POINT('Ctrl Pts',(1.75113416368911,1.60002596348554,17.4642727995735));
#95752=CARTESIAN_POINT('Ctrl Pts',(1.87960477562636,1.45496304280099,17.4518241095926));
#95753=CARTESIAN_POINT('Ctrl Pts',(1.97175382898818,1.32741451748516,17.4423489501649));
#95754=CARTESIAN_POINT('Ctrl Pts',(2.12486389866136,1.06394511276895,17.4236333799158));
#95755=CARTESIAN_POINT('Ctrl Pts',(2.18698836566015,0.929569025539528,17.4144483322207));
#95756=CARTESIAN_POINT('Ctrl Pts',(2.24303577069241,0.770978917000507,17.403461607158));
#95757=CARTESIAN_POINT('Ctrl Pts',(2.24961292066846,0.751571435560694,17.4021152578435));
#95758=CARTESIAN_POINT('Ctrl Pts',(2.25932101719623,0.721655565094474,17.4000359799522));
#95759=CARTESIAN_POINT('Ctrl Pts',(2.26263205484322,0.711206292794496,17.3993089840294));
#95760=CARTESIAN_POINT('Ctrl Pts',(2.2685354212722,0.692117376723466,17.3979793989934));
#95761=CARTESIAN_POINT('Ctrl Pts',(2.27115113726744,0.683485134105364,17.3973775899567));
#95762=CARTESIAN_POINT('Ctrl Pts',(2.27675644308931,0.664599302680216,17.3960596266192));
#95763=CARTESIAN_POINT('Ctrl Pts',(2.27972612666063,0.654340060825932,17.3953428366152));
#95764=CARTESIAN_POINT('Ctrl Pts',(2.28769182018423,0.626108736586486,17.3933678873121));
#95765=CARTESIAN_POINT('Ctrl Pts',(2.29254516883256,0.6080975483065,17.3921051310474));
#95766=CARTESIAN_POINT('Ctrl Pts',(2.31745450270745,0.511117359469357,17.3852895531852));
#95767=CARTESIAN_POINT('Ctrl Pts',(2.3336414585999,0.431220501594079,17.3796138496288));
#95768=CARTESIAN_POINT('Ctrl Pts',(2.37502849286606,0.154366110544676,17.3597334684906));
#95769=CARTESIAN_POINT('Ctrl Pts',(2.37961487791347,-0.0448013889349336,
17.3449891624996));
#95770=CARTESIAN_POINT('Ctrl Pts',(2.35507670675476,-0.283837818392776,
17.3277399118691));
#95771=CARTESIAN_POINT('Ctrl Pts',(2.3497003325302,-0.325359777074311,17.3247640247835));
#95772=CARTESIAN_POINT('Ctrl Pts',(2.34056005924066,-0.383763281885125,
17.3206256455705));
#95773=CARTESIAN_POINT('Ctrl Pts',(2.33770680830536,-0.40077745205299,17.3194257889684));
#95774=CARTESIAN_POINT('Ctrl Pts',(2.33235686347936,-0.430675860652665,
17.3173291742773));
#95775=CARTESIAN_POINT('Ctrl Pts',(2.32993843519552,-0.443573154713716,
17.3164286586334));
#95776=CARTESIAN_POINT('Ctrl Pts',(2.32617018494521,-0.462787248677799,
17.3150935836234));
#95777=CARTESIAN_POINT('Ctrl Pts',(2.32490144887061,-0.46911941169255,17.3146546543047));
#95778=CARTESIAN_POINT('Ctrl Pts',(2.32258184942387,-0.480455783271049,
17.3138708350069));
#95779=CARTESIAN_POINT('Ctrl Pts',(2.32154065679897,-0.485461829003278,
17.3135254097795));
#95780=CARTESIAN_POINT('Ctrl Pts',(2.31923187143544,-0.496385140240768,
17.3127732263469));
#95781=CARTESIAN_POINT('Ctrl Pts',(2.31795782132636,-0.502300927296729,
17.3123668407005));
#95782=CARTESIAN_POINT('Ctrl Pts',(2.31433689237911,-0.518806770702629,
17.3112355363785));
#95783=CARTESIAN_POINT('Ctrl Pts',(2.31193994951072,-0.529385868586778,
17.3105134041528));
#95784=CARTESIAN_POINT('Ctrl Pts',(2.29827149657482,-0.587848655292425,
17.3065372027048));
#95785=CARTESIAN_POINT('Ctrl Pts',(2.28558404076224,-0.63539305195678,17.3033574358266));
#95786=CARTESIAN_POINT('Ctrl Pts',(2.26157897847777,-0.715282778716147,
17.2980527197474));
#95787=CARTESIAN_POINT('Ctrl Pts',(2.25102375161325,-0.747837669828325,
17.2959020890173));
#95788=CARTESIAN_POINT('Ctrl Pts',(2.17958815624332,-0.952924262141285,
17.2823588543075));
#95789=CARTESIAN_POINT('Ctrl Pts',(2.09962195591142,-1.11815047311524,17.2714208237175));
#95790=CARTESIAN_POINT('Ctrl Pts',(1.95961240145338,-1.33835688619862,17.2550191426764));
#95791=CARTESIAN_POINT('Ctrl Pts',(1.91455304692249,-1.40205725600445,17.2500337920764));
#95792=CARTESIAN_POINT('Ctrl Pts',(1.85541886409564,-1.47747692176913,17.2437568780338));
#95793=CARTESIAN_POINT('Ctrl Pts',(1.84423765095556,-1.49141029679071,17.2425807689984));
#95794=CARTESIAN_POINT('Ctrl Pts',(1.82630183417624,-1.51325073098052,17.2407101865838));
#95795=CARTESIAN_POINT('Ctrl Pts',(1.8196506441849,-1.52124215415385,17.2400198971673));
#95796=CARTESIAN_POINT('Ctrl Pts',(1.80706196498811,-1.53616679964939,17.2387195448843));
#95797=CARTESIAN_POINT('Ctrl Pts',(1.80113655824584,-1.54311000132188,17.2381099847555));
#95798=CARTESIAN_POINT('Ctrl Pts',(1.78774599347641,-1.5586184314928,17.2367379488071));
#95799=CARTESIAN_POINT('Ctrl Pts',(1.78025911305771,-1.56716452063316,17.2359745796424));
#95800=CARTESIAN_POINT('Ctrl Pts',(1.76102248615991,-1.58880692021838,17.2340224906222));
#95801=CARTESIAN_POINT('Ctrl Pts',(1.74918805649212,-1.60182668860903,17.2328302317064));
#95802=CARTESIAN_POINT('Ctrl Pts',(1.67442758937374,-1.68225870267956,17.2253504879774));
#95803=CARTESIAN_POINT('Ctrl Pts',(1.60776739376707,-1.74607622166779,17.2189026160298));
#95804=CARTESIAN_POINT('Ctrl Pts',(1.37835242948756,-1.94140935884335,17.197396409941));
#95805=CARTESIAN_POINT('Ctrl Pts',(1.20192720540499,-2.05530652664814,17.1817923076774));
#95806=CARTESIAN_POINT('Ctrl Pts',(0.987580518264483,-2.15654003360007,
17.1649780500708));
#95807=CARTESIAN_POINT('Ctrl Pts',(0.962081827807614,-2.16803572506896,
17.1630112525459));
#95808=CARTESIAN_POINT('Ctrl Pts',(0.918887297376993,-2.18659710169309,
17.1597420799682));
#95809=CARTESIAN_POINT('Ctrl Pts',(0.901299383690034,-2.19390524625424,
17.1584280696258));
#95810=CARTESIAN_POINT('Ctrl Pts',(0.876660263789917,-2.20379698805432,
17.1566128866317));
#95811=CARTESIAN_POINT('Ctrl Pts',(0.869682518015558,-2.20655992540975,
17.1561016716897));
#95812=CARTESIAN_POINT('Ctrl Pts',(0.857792429938606,-2.21120281111398,
17.1552355262774));
#95813=CARTESIAN_POINT('Ctrl Pts',(0.852886769861896,-2.21309961019504,
17.1548796005022));
#95814=CARTESIAN_POINT('Ctrl Pts',(0.843442786571962,-2.21671510958756,
17.1541972016762));
#95815=CARTESIAN_POINT('Ctrl Pts',(0.838905468569996,-2.21843621210642,
17.153870579638));
#95816=CARTESIAN_POINT('Ctrl Pts',(0.828007306321643,-2.22253190326943,
17.1530889496392));
#95817=CARTESIAN_POINT('Ctrl Pts',(0.821641439425255,-2.22489314535519,
17.1526347302468));
#95818=CARTESIAN_POINT('Ctrl Pts',(0.798496496010837,-2.23336523715348,
17.1509914919503));
#95819=CARTESIAN_POINT('Ctrl Pts',(0.781658158372099,-2.23931407075631,
17.1498116217844));
#95820=CARTESIAN_POINT('Ctrl Pts',(0.60851605554866,-2.29829259239294,17.137823106008));
#95821=CARTESIAN_POINT('Ctrl Pts',(0.447124653813533,-2.33506683080722,
17.127820727477));
#95822=CARTESIAN_POINT('Ctrl Pts',(0.121065654715695,-2.37428081666814,
17.1076880548794));
#95823=CARTESIAN_POINT('Ctrl Pts',(-0.0426254971908174,-2.37698100552649,
17.0976014020263));
#95824=CARTESIAN_POINT('Ctrl Pts',(-0.225905277401668,-2.36105766667142,
17.0855872106768));
#95825=CARTESIAN_POINT('Ctrl Pts',(-0.246501426800852,-2.35899629111795,
17.0842274386187));
#95826=CARTESIAN_POINT('Ctrl Pts',(-0.278002236623175,-2.35542648461675,
17.0821317588908));
#95827=CARTESIAN_POINT('Ctrl Pts',(-0.288928123614085,-2.35411123365992,
17.0814019333868));
#95828=CARTESIAN_POINT('Ctrl Pts',(-0.307998871968717,-2.3516807466931,
17.0801227237711));
#95829=CARTESIAN_POINT('Ctrl Pts',(-0.316147888811791,-2.35059910426449,
17.0795744095148));
#95830=CARTESIAN_POINT('Ctrl Pts',(-0.334542937624182,-2.34806009065543,
17.0783327531875));
#95831=CARTESIAN_POINT('Ctrl Pts',(-0.344785329478392,-2.3465779844528,
17.0776386385551));
#95832=CARTESIAN_POINT('Ctrl Pts',(-0.372463931280955,-2.34238767811711,
17.0757552544318));
#95833=CARTESIAN_POINT('Ctrl Pts',(-0.38987986468718,-2.3395518964928,17.0745619696391));
#95834=CARTESIAN_POINT('Ctrl Pts',(-0.471086991365619,-2.32539727442062,
17.0689582708733));
#95835=CARTESIAN_POINT('Ctrl Pts',(-0.534423281641454,-2.31166299096289,
17.0644720280644));
#95836=CARTESIAN_POINT('Ctrl Pts',(-0.805868774350716,-2.24104922422023,
17.0447256355332));
#95837=CARTESIAN_POINT('Ctrl Pts',(-1.00623010420782,-2.15851843572842,
17.028685532724));
#95838=CARTESIAN_POINT('Ctrl Pts',(-1.22979114553509,-2.02846253828057,
17.0101046096524));
#95839=CARTESIAN_POINT('Ctrl Pts',(-1.26636162998509,-2.00583529196605,
17.0070456527621));
#95840=CARTESIAN_POINT('Ctrl Pts',(-1.32413676887402,-1.9678776936457,17.0022039808885));
#95841=CARTESIAN_POINT('Ctrl Pts',(-1.34573725576179,-1.95316977811418,
17.0003917379912));
#95842=CARTESIAN_POINT('Ctrl Pts',(-1.3740180531115,-1.93322122462922,16.998020786177));
#95843=CARTESIAN_POINT('Ctrl Pts',(-1.38091863397588,-1.92829812153926,
16.9974424108545));
#95844=CARTESIAN_POINT('Ctrl Pts',(-1.39222248376649,-1.92014178025695,
16.9964954065984));
#95845=CARTESIAN_POINT('Ctrl Pts',(-1.39664116528902,-1.91693019110469,
16.9961253318837));
#95846=CARTESIAN_POINT('Ctrl Pts',(-1.40527449272274,-1.91060961224155,
16.9954025501633));
#95847=CARTESIAN_POINT('Ctrl Pts',(-1.40948998778683,-1.90750189134353,
16.9950497646464));
#95848=CARTESIAN_POINT('Ctrl Pts',(-1.41984591751478,-1.89981428358279,
16.9941833415555));
#95849=CARTESIAN_POINT('Ctrl Pts',(-1.42597459533989,-1.89521850960284,
16.9936707991329));
#95850=CARTESIAN_POINT('Ctrl Pts',(-1.44695423188662,-1.87932691456675,
16.9919165774579));
#95851=CARTESIAN_POINT('Ctrl Pts',(-1.46169456980216,-1.86788523184674,
16.9906845928065));
#95852=CARTESIAN_POINT('Ctrl Pts',(-1.59302151266226,-1.76344041181769,
16.9796975738021));
#95853=CARTESIAN_POINT('Ctrl Pts',(-1.70074619987023,-1.65979370056975,
16.9705944473841));
#95854=CARTESIAN_POINT('Ctrl Pts',(-1.91401455416183,-1.41187017630449,
16.9505575010884));
#95855=CARTESIAN_POINT('Ctrl Pts',(-2.01444731264387,-1.26444433988212,
16.9396415779262));
#95856=CARTESIAN_POINT('Ctrl Pts',(-2.10720081892097,-1.08873247820053,
16.9266682741967));
#95857=CARTESIAN_POINT('Ctrl Pts',(-2.116700003558,-1.07014706904861,16.9252972908358));
#95858=CARTESIAN_POINT('Ctrl Pts',(-2.1308470764969,-1.04154246286506,16.9231879185604));
#95859=CARTESIAN_POINT('Ctrl Pts',(-2.13567249460642,-1.03161182338023,
16.9224557380088));
#95860=CARTESIAN_POINT('Ctrl Pts',(-2.14397083083727,-1.01422619344112,
16.9211739599357));
#95861=CARTESIAN_POINT('Ctrl Pts',(-2.14747466637575,-1.00678609907083,
16.9206254469545));
#95862=CARTESIAN_POINT('Ctrl Pts',(-2.15528899086396,-0.989966655850969,
16.9193854105219));
#95863=CARTESIAN_POINT('Ctrl Pts',(-2.15957706202411,-0.980577136772298,
16.9186931265382));
#95864=CARTESIAN_POINT('Ctrl Pts',(-2.17097888841599,-0.955173174320616,
16.9168198601892));
#95865=CARTESIAN_POINT('Ctrl Pts',(-2.17797656337175,-0.939107654890715,
16.9156349359843));
#95866=CARTESIAN_POINT('Ctrl Pts',(-2.20966887322561,-0.864087361306736,
16.9100993817005));
#95867=CARTESIAN_POINT('Ctrl Pts',(-2.23214976807925,-0.80423227683552,
16.9056750172134));
#95868=CARTESIAN_POINT('Ctrl Pts',(-2.31339341021456,-0.55814743750153,
16.8874400430945));
#95869=CARTESIAN_POINT('Ctrl Pts',(-2.35146859172631,-0.365913477462063,
16.8730126545402));
#95870=CARTESIAN_POINT('Ctrl Pts',(-2.36970278055722,-0.114010354654363,
16.8547207567684));
#95871=CARTESIAN_POINT('Ctrl Pts',(-2.37176750132454,-0.0566522349982106,
16.8506032362722));
#95872=CARTESIAN_POINT('Ctrl Pts',(-2.37174026352844,0.032083723484378,
16.844356528475));
#95873=CARTESIAN_POINT('Ctrl Pts',(-2.37110883104935,0.063438111953284,
16.842173191473));
#95874=CARTESIAN_POINT('Ctrl Pts',(-2.36947960879403,0.104177965148921,
16.8393750394647));
#95875=CARTESIAN_POINT('Ctrl Pts',(-2.36904748386543,0.113581211687271,
16.83873188062));
#95876=CARTESIAN_POINT('Ctrl Pts',(-2.36826538448301,0.128643995826007,
16.8377061957126));
#95877=CARTESIAN_POINT('Ctrl Pts',(-2.36795108362451,0.134305161086325,
16.8373217400156));
#95878=CARTESIAN_POINT('Ctrl Pts',(-2.36731020592937,0.14514608704302,16.8365875747979));
#95879=CARTESIAN_POINT('Ctrl Pts',(-2.36698692713815,0.150325929018152,
16.8362376945008));
#95880=CARTESIAN_POINT('Ctrl Pts',(-2.36626168529946,0.16136347921972,16.8354940160912));
#95881=CARTESIAN_POINT('Ctrl Pts',(-2.36585496609515,0.16722086265911,16.83510048246));
#95882=CARTESIAN_POINT('Ctrl Pts',(-2.36542649454112,0.173076750093436,
16.8347081153257));
#95883=CARTESIAN_POINT('',(-2.37247048654875,-0.00211540104443233,16.651410108095));
#95884=CARTESIAN_POINT('Ctrl Pts',(-2.36542650336594,0.173076629485272,
16.639047070016));
#95885=CARTESIAN_POINT('Ctrl Pts',(-2.36968866402696,0.114825970114507,
16.643283930221));
#95886=CARTESIAN_POINT('Ctrl Pts',(-2.37180047394265,0.0563995970809621,
16.6475524590594));
#95887=CARTESIAN_POINT('Ctrl Pts',(-2.37174908437069,-0.00208405537486423,
16.6518242564532));
#95888=CARTESIAN_POINT('Ctrl Pts',(-2.37247048654875,-0.00211540104443233,
16.651410108095));
#95889=CARTESIAN_POINT('Ctrl Pts',(-2.37394798832961,-0.162106932516699,
16.6621578139988));
#95890=CARTESIAN_POINT('Ctrl Pts',(-2.28621603133195,-1.10891487060638,
16.7258694983972));
#95891=CARTESIAN_POINT('Ctrl Pts',(-1.013610398569,-2.61441006592229,16.8425451612904));
#95892=CARTESIAN_POINT('Ctrl Pts',(1.64854813367676,-2.2682228911273,17.0014370967742));
#95893=CARTESIAN_POINT('Ctrl Pts',(2.79962146477649,0.157053133829965,17.1603290322581));
#95894=CARTESIAN_POINT('Ctrl Pts',(1.38451763804013,2.43837178109468,17.3192209677419));
#95895=CARTESIAN_POINT('Ctrl Pts',(-1.29965687630912,2.48464042403432,17.4781129032258));
#95896=CARTESIAN_POINT('Ctrl Pts',(-2.30368038220262,0.984080211399787,
17.5849736862122));
#95897=CARTESIAN_POINT('Ctrl Pts',(-2.36829936334429,0.187155604555285,
17.6388704907039));
#95898=CARTESIAN_POINT('Ctrl Pts',(-2.3692863196969,0.173352773124932,17.639803316701));
#95899=CARTESIAN_POINT('Origin',(0.,0.,-1.84858989190503));
#95900=CARTESIAN_POINT('',(-2.36542649320577,0.173076768343595,18.8389943251842));
#95901=CARTESIAN_POINT('',(-2.36542649880512,0.173076691817703,18.6388842277111));
#95902=CARTESIAN_POINT('',(-2.36542649454111,0.173076750093529,-1.84858989190503));
#95903=CARTESIAN_POINT('',(-2.37174930964901,0.0018096075435597,17.8500526884225));
#95904=CARTESIAN_POINT('Ctrl Pts',(-2.36542649320577,0.173076768343595,
18.8389943251842));
#95905=CARTESIAN_POINT('Ctrl Pts',(-2.3638889171336,0.194090698816365,18.837632151699));
#95906=CARTESIAN_POINT('Ctrl Pts',(-2.36207122772979,0.215085357947287,
18.8362618402781));
#95907=CARTESIAN_POINT('Ctrl Pts',(-2.35813192756486,0.254468710188079,
18.8336719300932));
#95908=CARTESIAN_POINT('Ctrl Pts',(-2.35607472795328,0.272859590989085,
18.8324545545264));
#95909=CARTESIAN_POINT('Ctrl Pts',(-2.35249527673793,0.301790306904119,
18.8305261184804));
#95910=CARTESIAN_POINT('Ctrl Pts',(-2.35111685834559,0.312347448399746,
18.8298195964156));
#95911=CARTESIAN_POINT('Ctrl Pts',(-2.34843925734046,0.331832035124003,
18.8285102563322));
#95912=CARTESIAN_POINT('Ctrl Pts',(-2.34716012425922,0.340762075589015,
18.8279080832585));
#95913=CARTESIAN_POINT('Ctrl Pts',(-2.34420835805375,0.360563759872961,
18.8265680757639));
#95914=CARTESIAN_POINT('Ctrl Pts',(-2.3425109868226,0.371431447812002,18.8258294694569));
#95915=CARTESIAN_POINT('Ctrl Pts',(-2.3374059122059,0.402689768436501,18.8236956815773));
#95916=CARTESIAN_POINT('Ctrl Pts',(-2.33380719354624,0.423047732585077,
18.8222944773178));
#95917=CARTESIAN_POINT('Ctrl Pts',(-2.29987265693084,0.601382122486404,
18.8099154572715));
#95918=CARTESIAN_POINT('Ctrl Pts',(-2.25380989835203,0.755907807660723,
18.7984225642131));
#95919=CARTESIAN_POINT('Ctrl Pts',(-2.12844996080835,1.05975764006811,18.7744782758937));
#95920=CARTESIAN_POINT('Ctrl Pts',(-2.04811593198904,1.20773139538127,18.7620779589741));
#95921=CARTESIAN_POINT('Ctrl Pts',(-1.94282460118863,1.36049291083907,18.7491918731087));
#95922=CARTESIAN_POINT('Ctrl Pts',(-1.93266561689994,1.37488619564203,18.7479772443534));
#95923=CARTESIAN_POINT('Ctrl Pts',(-1.91838940737889,1.3946418162566,18.7463108772995));
#95924=CARTESIAN_POINT('Ctrl Pts',(-1.91440853841083,1.40010130522569,18.7458504588808));
#95925=CARTESIAN_POINT('Ctrl Pts',(-1.90753370488749,1.4094455261716,18.7450626765911));
#95926=CARTESIAN_POINT('Ctrl Pts',(-1.90465109834309,1.41333850198485,18.7447345468374));
#95927=CARTESIAN_POINT('Ctrl Pts',(-1.89860938679805,1.42144581271925,18.7440514048503));
#95928=CARTESIAN_POINT('Ctrl Pts',(-1.8954481478562,1.42565848702899,18.7436965561889));
#95929=CARTESIAN_POINT('Ctrl Pts',(-1.88772550197103,1.43587861131393,18.7428358848511));
#95930=CARTESIAN_POINT('Ctrl Pts',(-1.88314936582983,1.44187496931005,18.7423310842754));
#95931=CARTESIAN_POINT('Ctrl Pts',(-1.86676906325064,1.46312795822798,18.7405421190698));
#95932=CARTESIAN_POINT('Ctrl Pts',(-1.8548070791405,1.47826280349651,18.7392685298721));
#95933=CARTESIAN_POINT('Ctrl Pts',(-1.82475199537688,1.51535057634333,18.7361438005216));
#95934=CARTESIAN_POINT('Ctrl Pts',(-1.8064456849198,1.53712763212333,18.7343056446987));
#95935=CARTESIAN_POINT('Ctrl Pts',(-1.65067474003797,1.71580391305499,18.7191442541905));
#95936=CARTESIAN_POINT('Ctrl Pts',(-1.49344440301926,1.85427954792722,18.7067978965549));
#95937=CARTESIAN_POINT('Ctrl Pts',(-1.2437592428878,2.02156052828421,18.6880401838632));
#95938=CARTESIAN_POINT('Ctrl Pts',(-1.16450860998334,2.06822645262339,18.6822024412626));
#95939=CARTESIAN_POINT('Ctrl Pts',(-1.06711489221767,2.11820040894792,18.6750453824303));
#95940=CARTESIAN_POINT('Ctrl Pts',(-1.05138417137342,2.12605231882062,18.6738900648808));
#95941=CARTESIAN_POINT('Ctrl Pts',(-1.02535002174132,2.13868754009514,18.6719783704234));
#95942=CARTESIAN_POINT('Ctrl Pts',(-1.0150967544948,2.14357309943853,18.6712255580424));
#95943=CARTESIAN_POINT('Ctrl Pts',(-0.996540947123981,2.1522517316632,18.6698631249258));
#95944=CARTESIAN_POINT('Ctrl Pts',(-0.98825080000316,2.15607090050937,18.6692544210438));
#95945=CARTESIAN_POINT('Ctrl Pts',(-0.97046814486707,2.16413904398056,18.6679485996849));
#95946=CARTESIAN_POINT('Ctrl Pts',(-0.960969350282641,2.1683736125749,18.6672510022746));
#95947=CARTESIAN_POINT('Ctrl Pts',(-0.935067165364577,2.17971719827224,
18.6653483420286));
#95948=CARTESIAN_POINT('Ctrl Pts',(-0.918611029799717,2.1867033208726,18.6641391223376));
#95949=CARTESIAN_POINT('Ctrl Pts',(-0.829772870769042,2.22323801136056,
18.6576075080201));
#95950=CARTESIAN_POINT('Ctrl Pts',(-0.756049980422834,2.24937685903972,
18.6521718510515));
#95951=CARTESIAN_POINT('Ctrl Pts',(-0.504848549649827,2.32469640816963,
18.6335892802959));
#95952=CARTESIAN_POINT('Ctrl Pts',(-0.322972581486908,2.3568538006023,18.6199778618305));
#95953=CARTESIAN_POINT('Ctrl Pts',(-0.10956132734833,2.36940466513714,18.6045137407469));
#95954=CARTESIAN_POINT('Ctrl Pts',(-0.0798477853005942,2.37059203524411,
18.6023736754747));
#95955=CARTESIAN_POINT('Ctrl Pts',(0.00190205393253838,2.3723199255449,
18.5965335772806));
#95956=CARTESIAN_POINT('Ctrl Pts',(0.053949897088508,2.37170736490583,18.5928683812466));
#95957=CARTESIAN_POINT('Ctrl Pts',(0.115986763319578,2.36893357367933,18.5885941878057));
#95958=CARTESIAN_POINT('Ctrl Pts',(0.126030993296137,2.36842044483756,18.5879051313908));
#95959=CARTESIAN_POINT('Ctrl Pts',(0.142463822813691,2.36747610623312,18.5867829880303));
#95960=CARTESIAN_POINT('Ctrl Pts',(0.148854351064524,2.36708289652537,18.5863478844971));
#95961=CARTESIAN_POINT('Ctrl Pts',(0.160342521694305,2.36632932030617,18.5855681084475));
#95962=CARTESIAN_POINT('Ctrl Pts',(0.165440634765094,2.36597835457686,18.5852229252734));
#95963=CARTESIAN_POINT('Ctrl Pts',(0.176618234501882,2.36517255741627,18.5844679983444));
#95964=CARTESIAN_POINT('Ctrl Pts',(0.18269710750569,2.36471076373935,18.5840586477392));
#95965=CARTESIAN_POINT('Ctrl Pts',(0.200103776645388,2.3633209088671,18.5828897831624));
#95966=CARTESIAN_POINT('Ctrl Pts',(0.211426968363484,2.36233483860016,18.5821334300941));
#95967=CARTESIAN_POINT('Ctrl Pts',(0.2900251384133,2.35492052133287,18.5769084106021));
#95968=CARTESIAN_POINT('Ctrl Pts',(0.357012785027204,2.34570012523191,18.5725827377564));
#95969=CARTESIAN_POINT('Ctrl Pts',(0.53578938543403,2.31325462333385,18.5611635879967));
#95970=CARTESIAN_POINT('Ctrl Pts',(0.646446452166589,2.28480351850729,18.5542238170749));
#95971=CARTESIAN_POINT('Ctrl Pts',(0.903286424763167,2.19860397318873,18.5376057488124));
#95972=CARTESIAN_POINT('Ctrl Pts',(1.04660607922392,2.13410203459282,18.5278954450568));
#95973=CARTESIAN_POINT('Ctrl Pts',(1.19874285183673,2.04659829603238,18.5164351946238));
#95974=CARTESIAN_POINT('Ctrl Pts',(1.21487033885845,2.03706628188476,18.5152053387258));
#95975=CARTESIAN_POINT('Ctrl Pts',(1.24088980571409,2.02126881070514,18.5131956955289));
#95976=CARTESIAN_POINT('Ctrl Pts',(1.25085148999671,2.01511926612143,18.5124201366882));
#95977=CARTESIAN_POINT('Ctrl Pts',(1.26852755743489,2.00402590907782,18.5110327470355));
#95978=CARTESIAN_POINT('Ctrl Pts',(1.2762596430015,1.99911063421166,18.5104219800391));
#95979=CARTESIAN_POINT('Ctrl Pts',(1.29252471424234,1.98863813149318,18.5091288593763));
#95980=CARTESIAN_POINT('Ctrl Pts',(1.30105075748709,1.98307051709702,18.5084461266104));
#95981=CARTESIAN_POINT('Ctrl Pts',(1.32362166683324,1.96812321239009,18.5066255271191));
#95982=CARTESIAN_POINT('Ctrl Pts',(1.33760243198273,1.95864825944254,18.5054840917558));
#95983=CARTESIAN_POINT('Ctrl Pts',(1.40469829893898,1.91212307094796,18.4999382446258));
#95984=CARTESIAN_POINT('Ctrl Pts',(1.45637741706116,1.87306042551144,18.495457466478));
#95985=CARTESIAN_POINT('Ctrl Pts',(1.6896253317248,1.68126206337177,18.474212476597));
#95986=CARTESIAN_POINT('Ctrl Pts',(1.84917957844107,1.50398767360189,18.4564645970122));
#95987=CARTESIAN_POINT('Ctrl Pts',(2.00454905423034,1.26846572792676,18.4363998746689));
#95988=CARTESIAN_POINT('Ctrl Pts',(2.02825188050805,1.23021021637042,18.4332423289523));
#95989=CARTESIAN_POINT('Ctrl Pts',(2.05615300391422,1.18217773422587,18.4294219550703));
#95990=CARTESIAN_POINT('Ctrl Pts',(2.06139147108046,1.17301943046962,18.4286998462869));
#95991=CARTESIAN_POINT('Ctrl Pts',(2.06950510032962,1.15861232058548,18.4275741088186));
#95992=CARTESIAN_POINT('Ctrl Pts',(2.07242172642968,1.15338721145426,18.4271679222311));
#95993=CARTESIAN_POINT('Ctrl Pts',(2.07779693702528,1.14367135177573,18.4264165873547));
#95994=CARTESIAN_POINT('Ctrl Pts',(2.08026073878041,1.13918371297294,18.4260711192105));
#95995=CARTESIAN_POINT('Ctrl Pts',(2.08584247629389,1.12893848169294,18.4252859429967));
#95996=CARTESIAN_POINT('Ctrl Pts',(2.08895111175834,1.12317593753154,18.4248468271886));
#95997=CARTESIAN_POINT('Ctrl Pts',(2.09843168224074,1.10542608544135,18.4235017395438));
#95998=CARTESIAN_POINT('Ctrl Pts',(2.10472473368632,1.09339662171995,18.4226005855719));
#95999=CARTESIAN_POINT('Ctrl Pts',(2.16852226782995,0.968852595392169,18.4133709330852));
#96000=CARTESIAN_POINT('Ctrl Pts',(2.21705997920133,0.851950012875309,18.4055406039854));
#96001=CARTESIAN_POINT('Ctrl Pts',(2.31718140379656,0.543253732273883,18.3856039291076));
#96002=CARTESIAN_POINT('Ctrl Pts',(2.35444570973427,0.34789444499838,18.3736099783295));
#96003=CARTESIAN_POINT('Ctrl Pts',(2.36873467684687,0.12269059553261,18.3589640701756));
#96004=CARTESIAN_POINT('Ctrl Pts',(2.369999873543,0.0951706222629558,18.3571622495575));
#96005=CARTESIAN_POINT('Ctrl Pts',(2.37113333796937,0.0554401493765309,
18.3545408362035));
#96006=CARTESIAN_POINT('Ctrl Pts',(2.37138715036497,0.0432422278212077,
18.3537332885812));
#96007=CARTESIAN_POINT('Ctrl Pts',(2.37166805975997,0.0217820580899005,
18.3523075073959));
#96008=CARTESIAN_POINT('Ctrl Pts',(2.37173503498008,0.0125205194035137,
18.351690534684));
#96009=CARTESIAN_POINT('Ctrl Pts',(2.37176130605753,-0.00659870758624893,
18.3504133616833));
#96010=CARTESIAN_POINT('Ctrl Pts',(2.37171339413396,-0.0164562099832505,
18.3497529475765));
#96011=CARTESIAN_POINT('Ctrl Pts',(2.37143310872952,-0.0417184759970903,
18.3480553890985));
#96012=CARTESIAN_POINT('Ctrl Pts',(2.37111208597875,-0.0571215946107433,
18.3470154900759));
#96013=CARTESIAN_POINT('Ctrl Pts',(2.36913337438663,-0.121804484884013,
18.3426274909025));
#96014=CARTESIAN_POINT('Ctrl Pts',(2.36608931532903,-0.171026307851277,
18.3392364906479));
#96015=CARTESIAN_POINT('Ctrl Pts',(2.35389718838626,-0.301830408297821,
18.3300797053622));
#96016=CARTESIAN_POINT('Ctrl Pts',(2.34204502355489,-0.383087776122668,
18.3242378358102));
#96017=CARTESIAN_POINT('Ctrl Pts',(2.29645080086922,-0.611865866534978,
18.3073994295363));
#96018=CARTESIAN_POINT('Ctrl Pts',(2.25278015865569,-0.756997764949759,
18.2962254576282));
#96019=CARTESIAN_POINT('Ctrl Pts',(2.17103393654159,-0.957092532381801,
18.2806831696291));
#96020=CARTESIAN_POINT('Ctrl Pts',(2.1440154543891,-1.01617613565392,18.2760803028914));
#96021=CARTESIAN_POINT('Ctrl Pts',(2.10975771976275,-1.08362120020772,18.2708679566668));
#96022=CARTESIAN_POINT('Ctrl Pts',(2.1048476862521,-1.09312797518076,18.2701342590254));
#96023=CARTESIAN_POINT('Ctrl Pts',(2.09680673160502,-1.10844174700714,18.2689544304942));
#96024=CARTESIAN_POINT('Ctrl Pts',(2.09371569281862,-1.11426934649491,18.2685059305135));
#96025=CARTESIAN_POINT('Ctrl Pts',(2.08818062022305,-1.12460037877652,18.2677117951661));
#96026=CARTESIAN_POINT('Ctrl Pts',(2.08574626909357,-1.12910885985711,18.2673655634014));
#96027=CARTESIAN_POINT('Ctrl Pts',(2.08045361637527,-1.1388354617641,18.2666193344661));
#96028=CARTESIAN_POINT('Ctrl Pts',(2.07759028783736,-1.14405072296763,18.2662196623388));
#96029=CARTESIAN_POINT('Ctrl Pts',(2.06953088717731,-1.1586000564742,18.2651057606708));
#96030=CARTESIAN_POINT('Ctrl Pts',(2.06429124999805,-1.16791002641602,18.2643942438386));
#96031=CARTESIAN_POINT('Ctrl Pts',(2.03268795430826,-1.2231866895201,18.2601752815136));
#96032=CARTESIAN_POINT('Ctrl Pts',(2.00485041708913,-1.26829878994666,18.2567551273347));
#96033=CARTESIAN_POINT('Ctrl Pts',(1.90544539733524,-1.41792559909278,18.2453566725837));
#96034=CARTESIAN_POINT('Ctrl Pts',(1.8270274596388,-1.51763330635945,18.2376587423586));
#96035=CARTESIAN_POINT('Ctrl Pts',(1.63224009091363,-1.72819234997147,18.2200698351161));
#96036=CARTESIAN_POINT('Ctrl Pts',(1.51184855445607,-1.83443727092541,18.2101634984347));
#96037=CARTESIAN_POINT('Ctrl Pts',(1.36650586314567,-1.93860989705733,18.1984860934438));
#96038=CARTESIAN_POINT('Ctrl Pts',(1.35120409391995,-1.94930604851172,18.1972603915262));
#96039=CARTESIAN_POINT('Ctrl Pts',(1.3261202848848,-1.96640271907262,18.195256197912));
#96040=CARTESIAN_POINT('Ctrl Pts',(1.31641419575749,-1.97291366270145,18.1944818963411));
#96041=CARTESIAN_POINT('Ctrl Pts',(1.29901603430026,-1.98439897961288,18.1930959068778));
#96042=CARTESIAN_POINT('Ctrl Pts',(1.29134246635504,-1.98940106519379,18.1924852746644));
#96043=CARTESIAN_POINT('Ctrl Pts',(1.27506846347442,-1.99987559335461,18.1911915524305));
#96044=CARTESIAN_POINT('Ctrl Pts',(1.26646135940306,-2.00533727710442,18.1905080781475));
#96045=CARTESIAN_POINT('Ctrl Pts',(1.24345955273348,-2.01972604583219,18.1886833953017));
#96046=CARTESIAN_POINT('Ctrl Pts',(1.2290041969046,-2.02855456359102,18.1875385897122));
#96047=CARTESIAN_POINT('Ctrl Pts',(1.15831671403562,-2.07069361530912,18.1819485304966));
#96048=CARTESIAN_POINT('Ctrl Pts',(1.10082355078082,-2.10182199986388,18.1774254244031));
#96049=CARTESIAN_POINT('Ctrl Pts',(0.822685710882808,-2.23786949286002,
18.1556349719605));
#96050=CARTESIAN_POINT('Ctrl Pts',(0.588035363089336,-2.3106389887493,18.1373162435833));
#96051=CARTESIAN_POINT('Ctrl Pts',(0.308564686573695,-2.35190387428073,
18.1173202162493));
#96052=CARTESIAN_POINT('Ctrl Pts',(0.270555135296414,-2.3565789478467,18.1146430772318));
#96053=CARTESIAN_POINT('Ctrl Pts',(0.22249328839912,-2.36131209826872,18.1113246380363));
#96054=CARTESIAN_POINT('Ctrl Pts',(0.212533795847012,-2.36222934606758,
18.1106405863889));
#96055=CARTESIAN_POINT('Ctrl Pts',(0.196732161749504,-2.36358389592875,
18.1095612999533));
#96056=CARTESIAN_POINT('Ctrl Pts',(0.190893831297306,-2.36406258877249,
18.1091638313948));
#96057=CARTESIAN_POINT('Ctrl Pts',(0.180444484493849,-2.36488038293118,
18.1084548498376));
#96058=CARTESIAN_POINT('Ctrl Pts',(0.175834286165009,-2.36522763004027,
18.1081428932598));
#96059=CARTESIAN_POINT('Ctrl Pts',(0.164783901016678,-2.36602747392307,
18.1073971377854));
#96060=CARTESIAN_POINT('Ctrl Pts',(0.158342854408788,-2.3664672582468,18.1069640609123));
#96061=CARTESIAN_POINT('Ctrl Pts',(0.138815346633409,-2.36772048080911,
18.1056557455279));
#96062=CARTESIAN_POINT('Ctrl Pts',(0.125723587473741,-2.36845172523456,
18.1047849507712));
#96063=CARTESIAN_POINT('Ctrl Pts',(0.0954114528987166,-2.36989276759288,
18.1027820004851));
#96064=CARTESIAN_POINT('Ctrl Pts',(0.0781878569893333,-2.37052352310055,
18.1016537958135));
#96065=CARTESIAN_POINT('Ctrl Pts',(0.0191720720200844,-2.37204083893903,
18.0978172191023));
#96066=CARTESIAN_POINT('Ctrl Pts',(-0.0226379414105889,-2.37201038475446,
18.0951491900336));
#96067=CARTESIAN_POINT('Ctrl Pts',(-0.261989599228159,-2.3655060795045,
18.0800516682263));
#96068=CARTESIAN_POINT('Ctrl Pts',(-0.458111944455925,-2.33546590371927,
18.0683047789183));
#96069=CARTESIAN_POINT('Ctrl Pts',(-0.675253954785322,-2.27376746744674,
18.0541543923723));
#96070=CARTESIAN_POINT('Ctrl Pts',(-0.702123067630764,-2.26561460012877,
18.0523840125398));
#96071=CARTESIAN_POINT('Ctrl Pts',(-0.783901774435791,-2.23920610402609,
18.0469263892053));
#96072=CARTESIAN_POINT('Ctrl Pts',(-0.83828998853264,-2.21941771412418,
18.0431994509407));
#96073=CARTESIAN_POINT('Ctrl Pts',(-0.907584082453756,-2.19129546396012,
18.0382965027672));
#96074=CARTESIAN_POINT('Ctrl Pts',(-0.923202161365873,-2.18476141067499,
18.0371811011504));
#96075=CARTESIAN_POINT('Ctrl Pts',(-0.948108231690302,-2.17402684414751,
18.0353851232423));
#96076=CARTESIAN_POINT('Ctrl Pts',(-0.957441616189827,-2.16993259898191,
18.0347081723703));
#96077=CARTESIAN_POINT('Ctrl Pts',(-0.97488966673664,-2.16214423447773,
18.033435156353));
#96078=CARTESIAN_POINT('Ctrl Pts',(-0.983010480228202,-2.15846425613357,
18.0328395854654));
#96079=CARTESIAN_POINT('Ctrl Pts',(-1.00140600410227,-2.1500029085617,18.0314833819141));
#96080=CARTESIAN_POINT('Ctrl Pts',(-1.01166751802854,-2.14519353837276,
18.0307217924938));
#96081=CARTESIAN_POINT('Ctrl Pts',(-1.04227582173911,-2.13057956678148,
18.0284346657212));
#96082=CARTESIAN_POINT('Ctrl Pts',(-1.06251693991157,-2.12055791471812,
18.0269016278185));
#96083=CARTESIAN_POINT('Ctrl Pts',(-1.10861565377571,-2.09690810564084,
18.0233615794851));
#96084=CARTESIAN_POINT('Ctrl Pts',(-1.13437018156041,-2.08308819571863,
18.0213480693335));
#96085=CARTESIAN_POINT('Ctrl Pts',(-1.22015991875619,-2.03499054916931,
18.014517852893));
#96086=CARTESIAN_POINT('Ctrl Pts',(-1.27894590224819,-1.99856763822727,
18.0096295314601));
#96087=CARTESIAN_POINT('Ctrl Pts',(-1.46611273588913,-1.87095962741856,
17.9933882342957));
#96088=CARTESIAN_POINT('Ctrl Pts',(-1.58701861113946,-1.76956006539772,
17.9817634390738));
#96089=CARTESIAN_POINT('Ctrl Pts',(-1.71401158083338,-1.6394989872607,17.9686229045318));
#96090=CARTESIAN_POINT('Ctrl Pts',(-1.73077686959884,-1.62179040534361,
17.9668677016156));
#96091=CARTESIAN_POINT('Ctrl Pts',(-1.78454590749602,-1.56321245476488,
17.9611786321793));
#96092=CARTESIAN_POINT('Ctrl Pts',(-1.82040153714008,-1.52130754601497,
17.9572892771233));
#96093=CARTESIAN_POINT('Ctrl Pts',(-1.86114012488982,-1.4701904853683,17.9527889696058));
#96094=CARTESIAN_POINT('Ctrl Pts',(-1.86746163794254,-1.46215240930158,
17.9520881949362));
#96095=CARTESIAN_POINT('Ctrl Pts',(-1.87768780031794,-1.44897489227797,
17.9509508809542));
#96096=CARTESIAN_POINT('Ctrl Pts',(-1.88162372574966,-1.44386005939865,
17.9505122348381));
#96097=CARTESIAN_POINT('Ctrl Pts',(-1.88864033420739,-1.43466438320371,
17.9497287165349));
#96098=CARTESIAN_POINT('Ctrl Pts',(-1.89172873236783,-1.43058960194536,
17.9493833109162));
#96099=CARTESIAN_POINT('Ctrl Pts',(-1.89844557917788,-1.42166771892882,
17.9486309320261));
#96100=CARTESIAN_POINT('Ctrl Pts',(-1.90206864829719,-1.41681670634907,
17.948224332804));
#96101=CARTESIAN_POINT('Ctrl Pts',(-1.91232290099519,-1.40297681889011,
17.9470711888568));
#96102=CARTESIAN_POINT('Ctrl Pts',(-1.91890932670062,-1.39395474825456,
17.9463276736002));
#96103=CARTESIAN_POINT('Ctrl Pts',(-1.96213355606657,-1.33385933565691,
17.9414267936992));
#96104=CARTESIAN_POINT('Ctrl Pts',(-1.99679608626379,-1.28138824180711,
17.9373928967893));
#96105=CARTESIAN_POINT('Ctrl Pts',(-2.12094677869681,-1.07615515053145,
17.9222743256585));
#96106=CARTESIAN_POINT('Ctrl Pts',(-2.19532200024861,-0.914928626495204,
17.9116949573022));
#96107=CARTESIAN_POINT('Ctrl Pts',(-2.27011780511127,-0.689508531334165,
17.8969230004817));
#96108=CARTESIAN_POINT('Ctrl Pts',(-2.28696254467658,-0.631394023045678,
17.8931208814061));
#96109=CARTESIAN_POINT('Ctrl Pts',(-2.31307547043486,-0.526451772986574,
17.8862090073252));
#96110=CARTESIAN_POINT('Ctrl Pts',(-2.32318658685537,-0.479867876850167,
17.8831251567669));
#96111=CARTESIAN_POINT('Ctrl Pts',(-2.33476773899723,-0.417500442673414,
17.8789607948591));
#96112=CARTESIAN_POINT('Ctrl Pts',(-2.33749345522159,-0.401959377759127,
17.8779202098518));
#96113=CARTESIAN_POINT('Ctrl Pts',(-2.34168303334647,-0.376586529563042,
17.8762161150517));
#96114=CARTESIAN_POINT('Ctrl Pts',(-2.34324053799955,-0.366770526140564,
17.8755555878879));
#96115=CARTESIAN_POINT('Ctrl Pts',(-2.34605857081241,-0.348259156022767,
17.8743074368661));
#96116=CARTESIAN_POINT('Ctrl Pts',(-2.34733257035951,-0.339565984711979,
17.8737202513871));
#96117=CARTESIAN_POINT('Ctrl Pts',(-2.34980761584553,-0.321997579955538,
17.8725314040962));
#96118=CARTESIAN_POINT('Ctrl Pts',(-2.35100675039044,-0.313122226564666,
17.8719296919819));
#96119=CARTESIAN_POINT('Ctrl Pts',(-2.35364620836122,-0.292715943271395,
17.8705435689204));
#96120=CARTESIAN_POINT('Ctrl Pts',(-2.35505210281333,-0.281180870984554,
17.8697580847151));
#96121=CARTESIAN_POINT('Ctrl Pts',(-2.3600078577577,-0.237872102395406,
17.8668013824221));
#96122=CARTESIAN_POINT('Ctrl Pts',(-2.36299976056252,-0.206039276681309,
17.8646128046373));
#96123=CARTESIAN_POINT('Ctrl Pts',(-2.36965898024622,-0.115595792904657,
17.8583485300874));
#96124=CARTESIAN_POINT('Ctrl Pts',(-2.37179410419742,-0.0569000500529674,
17.8542278766152));
#96125=CARTESIAN_POINT('Ctrl Pts',(-2.37174930964901,0.0018096075435597,
17.8500526884225));
#96126=CARTESIAN_POINT('Ctrl Pts',(-2.37174931191249,0.00180663849497052,
17.8500528995689));
#96127=CARTESIAN_POINT('Ctrl Pts',(-2.37170574199841,0.0590050841321918,
17.8459851842573));
#96128=CARTESIAN_POINT('Ctrl Pts',(-2.36959309700692,0.11613223014051,17.8418717785171));
#96129=CARTESIAN_POINT('Ctrl Pts',(-2.36542646972629,0.173077089235465,
17.8377309811821));
#96130=CARTESIAN_POINT('',(-2.37484677778953,0.00124248804868218,17.651410108095));
#96131=CARTESIAN_POINT('Ctrl Pts',(-2.3692863196969,0.173352773124932,17.639803316701));
#96132=CARTESIAN_POINT('Ctrl Pts',(-2.3733797578211,0.116105017183839,17.6436722471657));
#96133=CARTESIAN_POINT('Ctrl Pts',(-2.37521206853831,0.0586860232060512,
17.6475411776303));
#96134=CARTESIAN_POINT('Ctrl Pts',(-2.37484677778953,0.00124248804868218,
17.651410108095));
#96135=CARTESIAN_POINT('Ctrl Pts',(-2.37174961402095,0.00135310438809495,
17.6531887653657));
#96136=CARTESIAN_POINT('Ctrl Pts',(-2.37183342235333,-0.145547889885166,
17.6625130572248));
#96137=CARTESIAN_POINT('Ctrl Pts',(-2.35826911062213,-0.292155716357493,
17.6713843938006));
#96138=CARTESIAN_POINT('Ctrl Pts',(-2.31386044907917,-0.529285915613408,
17.6862218858644));
#96139=CARTESIAN_POINT('Ctrl Pts',(-2.29098606075038,-0.620865847881408,
17.6920731806637));
#96140=CARTESIAN_POINT('Ctrl Pts',(-2.24645949220594,-0.762602140158466,
17.7015343051946));
#96141=CARTESIAN_POINT('Ctrl Pts',(-2.22842655443409,-0.813791517993269,
17.7050369695526));
#96142=CARTESIAN_POINT('Ctrl Pts',(-2.20279814763335,-0.879281929486418,
17.7096525478088));
#96143=CARTESIAN_POINT('Ctrl Pts',(-2.19678909558774,-0.894189039865554,
17.7107123310204));
#96144=CARTESIAN_POINT('Ctrl Pts',(-2.18675919578312,-0.918359532548057,
17.7124462012953));
#96145=CARTESIAN_POINT('Ctrl Pts',(-2.18282981197231,-0.927660507915268,
17.7131171861059));
#96146=CARTESIAN_POINT('Ctrl Pts',(-2.17514383762062,-0.945534213127708,
17.7144140579433));
#96147=CARTESIAN_POINT('Ctrl Pts',(-2.17139564863548,-0.95411036850187,
17.7150396487939));
#96148=CARTESIAN_POINT('Ctrl Pts',(-2.1626656503379,-0.973767399995322,
17.716481317084));
#96149=CARTESIAN_POINT('Ctrl Pts',(-2.15764929866002,-0.984832553722475,
17.7172985669006));
#96150=CARTESIAN_POINT('Ctrl Pts',(-2.14134410150622,-1.02007623873823,
17.7199202396106));
#96151=CARTESIAN_POINT('Ctrl Pts',(-2.12973248433963,-1.04410226392291,
17.7217357324254));
#96152=CARTESIAN_POINT('Ctrl Pts',(-2.02478481810144,-1.25221547680833,
17.737716554569));
#96153=CARTESIAN_POINT('Ctrl Pts',(-1.90821002238374,-1.42355035905783,
17.752751389025));
#96154=CARTESIAN_POINT('Ctrl Pts',(-1.71500453586684,-1.64043884609838,
17.7739469859592));
#96155=CARTESIAN_POINT('Ctrl Pts',(-1.65571874767782,-1.7002580823744,17.7800605222474));
#96156=CARTESIAN_POINT('Ctrl Pts',(-1.57311335202293,-1.77517905088021,
17.7879658319816));
#96157=CARTESIAN_POINT('Ctrl Pts',(-1.55253462797485,-1.79320457638353,
17.7898885203851));
#96158=CARTESIAN_POINT('Ctrl Pts',(-1.52182776696813,-1.81917666201578,
17.7926843028116));
#96159=CARTESIAN_POINT('Ctrl Pts',(-1.5119401572364,-1.82740265360929,17.7935737000445));
#96160=CARTESIAN_POINT('Ctrl Pts',(-1.49409517025223,-1.84200478761569,
17.7951588209297));
#96161=CARTESIAN_POINT('Ctrl Pts',(-1.48616274465999,-1.84841075555056,
17.7958564562207));
#96162=CARTESIAN_POINT('Ctrl Pts',(-1.47355541088184,-1.85845839926883,
17.7969539275869));
#96163=CARTESIAN_POINT('Ctrl Pts',(-1.46890785781613,-1.86213395811339,
17.7973560951031));
#96164=CARTESIAN_POINT('Ctrl Pts',(-1.46041023718247,-1.86880276720142,
17.7980869777507));
#96165=CARTESIAN_POINT('Ctrl Pts',(-1.45656473732404,-1.87180154137763,
17.7984160763638));
#96166=CARTESIAN_POINT('Ctrl Pts',(-1.44756073402735,-1.87877843748111,
17.7991828157463));
#96167=CARTESIAN_POINT('Ctrl Pts',(-1.44239507312713,-1.88274718202666,
17.7996197938765));
#96168=CARTESIAN_POINT('Ctrl Pts',(-1.42710211263575,-1.89439678432292,
17.8009051399312));
#96169=CARTESIAN_POINT('Ctrl Pts',(-1.41692914736248,-1.90201772480529,
17.8017494483677));
#96170=CARTESIAN_POINT('Ctrl Pts',(-1.31133273741533,-1.97980643553498,
17.8104092834261));
#96171=CARTESIAN_POINT('Ctrl Pts',(-1.21082709036922,-2.04282478133419,
17.817784221682));
#96172=CARTESIAN_POINT('Ctrl Pts',(-0.990213872334371,-2.15912303980801,
17.8331348945922));
#96173=CARTESIAN_POINT('Ctrl Pts',(-0.869556635652998,-2.21047645715894,
17.8410727381015));
#96174=CARTESIAN_POINT('Ctrl Pts',(-0.688828352355133,-2.27029722165716,
17.8529710236549));
#96175=CARTESIAN_POINT('Ctrl Pts',(-0.631697722750983,-2.28685180244383,
17.8567310193342));
#96176=CARTESIAN_POINT('Ctrl Pts',(-0.535842053508748,-2.31076148908148,
17.8630848959532));
#96177=CARTESIAN_POINT('Ctrl Pts',(-0.497446678921503,-2.31933004895306,
17.8656415833285));
#96178=CARTESIAN_POINT('Ctrl Pts',(-0.444826341892124,-2.32970644577635,
17.8691693663205));
#96179=CARTESIAN_POINT('Ctrl Pts',(-0.430770484689626,-2.33234632342885,
17.870113987718));
#96180=CARTESIAN_POINT('Ctrl Pts',(-0.407125635392751,-2.33656611439937,
17.8717072468124));
#96181=CARTESIAN_POINT('Ctrl Pts',(-0.397549126562619,-2.33821452760694,
17.8723536951134));
#96182=CARTESIAN_POINT('Ctrl Pts',(-0.378634806219472,-2.34135071085036,
17.8736328779299));
#96183=CARTESIAN_POINT('Ctrl Pts',(-0.36929768672698,-2.34284158273207,
17.8742655010687));
#96184=CARTESIAN_POINT('Ctrl Pts',(-0.348722073387177,-2.34600086592043,
17.8756622136121));
#96185=CARTESIAN_POINT('Ctrl Pts',(-0.337480057864742,-2.34764442581958,
17.8764270744855));
#96186=CARTESIAN_POINT('Ctrl Pts',(-0.297922266824205,-2.35313768899784,
17.8791247702891));
#96187=CARTESIAN_POINT('Ctrl Pts',(-0.269550109399032,-2.35655623195983,
17.8810710926302));
#96188=CARTESIAN_POINT('Ctrl Pts',(-0.0545725752773576,-2.3785257721283,
17.8959111435252));
#96189=CARTESIAN_POINT('Ctrl Pts',(0.133546535276466,-2.37539491084169,
17.909502949411));
#96190=CARTESIAN_POINT('Ctrl Pts',(0.453012312828874,-2.33199260329422,
17.9330514893249));
#96191=CARTESIAN_POINT('Ctrl Pts',(0.584955895348675,-2.30244322824763,
17.942894599277));
#96192=CARTESIAN_POINT('Ctrl Pts',(0.726757912645861,-2.25769993668585,
17.9531668044338));
#96193=CARTESIAN_POINT('Ctrl Pts',(0.739798290669297,-2.25346057860115,
17.9541083687691));
#96194=CARTESIAN_POINT('Ctrl Pts',(0.759088341637895,-2.24700398390668,
17.9554958426281));
#96195=CARTESIAN_POINT('Ctrl Pts',(0.765366376667241,-2.24487334303957,
17.9559465582791));
#96196=CARTESIAN_POINT('Ctrl Pts',(0.776545830315653,-2.24102690783438,
17.9567475484446));
#96197=CARTESIAN_POINT('Ctrl Pts',(0.781450617482266,-2.2393213173797,17.9570984077864));
#96198=CARTESIAN_POINT('Ctrl Pts',(0.792091450459432,-2.23558185558142,
17.9578583572558));
#96199=CARTESIAN_POINT('Ctrl Pts',(0.797825277406989,-2.23354201387355,
17.958267089846));
#96200=CARTESIAN_POINT('Ctrl Pts',(0.813686405496006,-2.2278304551381,17.9593957808565));
#96201=CARTESIAN_POINT('Ctrl Pts',(0.823796798630394,-2.22411172131955,
17.9601130244233));
#96202=CARTESIAN_POINT('Ctrl Pts',(0.877569478030481,-2.2039164467956,17.9639176446507));
#96203=CARTESIAN_POINT('Ctrl Pts',(0.920767056987352,-2.18622154216185,
17.9669385185713));
#96204=CARTESIAN_POINT('Ctrl Pts',(0.993242380450834,-2.1540039284578,17.9719917511904));
#96205=CARTESIAN_POINT('Ctrl Pts',(1.02279138673865,-2.14013113918767,17.9740476138423));
#96206=CARTESIAN_POINT('Ctrl Pts',(1.21873514837492,-2.04315300665441,17.9877106671746));
#96207=CARTESIAN_POINT('Ctrl Pts',(1.37514242682399,-1.94133397296124,17.9988185881367));
#96208=CARTESIAN_POINT('Ctrl Pts',(1.57848757018939,-1.77193741762053,18.0154474016746));
#96209=CARTESIAN_POINT('Ctrl Pts',(1.63637537325596,-1.71862119660974,18.0204738842507));
#96210=CARTESIAN_POINT('Ctrl Pts',(1.7041748967107,-1.64964018653987,18.0268075306637));
#96211=CARTESIAN_POINT('Ctrl Pts',(1.71669795448427,-1.63660408366716,18.0279974211188));
#96212=CARTESIAN_POINT('Ctrl Pts',(1.7362829143761,-1.6157446370699,18.0298911303832));
#96213=CARTESIAN_POINT('Ctrl Pts',(1.74344395930143,-1.60801500168566,18.0305906771843));
#96214=CARTESIAN_POINT('Ctrl Pts',(1.75680237689437,-1.5934017878899,18.0319092808099));
#96215=CARTESIAN_POINT('Ctrl Pts',(1.76301141502651,-1.58652910323158,18.0325278258428));
#96216=CARTESIAN_POINT('Ctrl Pts',(1.77686932545066,-1.57100819779399,18.0339212462599));
#96217=CARTESIAN_POINT('Ctrl Pts',(1.78449558105185,-1.56234019031363,18.0346970477239));
#96218=CARTESIAN_POINT('Ctrl Pts',(1.80379306368695,-1.5400810291993,18.0366834445101));
#96219=CARTESIAN_POINT('Ctrl Pts',(1.8153739681301,-1.52641289242954,18.0378977143016));
#96220=CARTESIAN_POINT('Ctrl Pts',(1.88821500934869,-1.43844212742857,18.0456800255062));
#96221=CARTESIAN_POINT('Ctrl Pts',(1.94504864105884,-1.36060759097457,18.0524232046689));
#96222=CARTESIAN_POINT('Ctrl Pts',(2.09580226144295,-1.12532579230039,18.0724041803507));
#96223=CARTESIAN_POINT('Ctrl Pts',(2.17640908872627,-0.96019800683005,18.0859923138909));
#96224=CARTESIAN_POINT('Ctrl Pts',(2.25738846686118,-0.730128915946238,
18.1034869742571));
#96225=CARTESIAN_POINT('Ctrl Pts',(2.27535609696793,-0.672046894754203,
18.107783472737));
#96226=CARTESIAN_POINT('Ctrl Pts',(2.29396679330645,-0.602527630298205,
18.1127369032897));
#96227=CARTESIAN_POINT('Ctrl Pts',(2.29678313412631,-0.591701310891322,
18.1135029400769));
#96228=CARTESIAN_POINT('Ctrl Pts',(2.30101931839607,-0.574930862057385,
18.1146808560458));
#96229=CARTESIAN_POINT('Ctrl Pts',(2.30249291764024,-0.569000673234998,
18.1150957007588));
#96230=CARTESIAN_POINT('Ctrl Pts',(2.3051758452213,-0.558022693155453,18.1158604789062));
#96231=CARTESIAN_POINT('Ctrl Pts',(2.3063915151016,-0.55297665725261,18.1162107595499));
#96232=CARTESIAN_POINT('Ctrl Pts',(2.3091145663072,-0.541508536305284,18.1170040379381));
#96233=CARTESIAN_POINT('Ctrl Pts',(2.31061172583991,-0.535084133850368,
18.1174464472306));
#96234=CARTESIAN_POINT('Ctrl Pts',(2.31443114413587,-0.51837979138383,18.1185918281201));
#96235=CARTESIAN_POINT('Ctrl Pts',(2.31671175428307,-0.508090333339361,
18.1192925000824));
#96236=CARTESIAN_POINT('Ctrl Pts',(2.33141200714864,-0.439609539128274,
18.1239256512753));
#96237=CARTESIAN_POINT('Ctrl Pts',(2.3417078219471,-0.380978148627399,18.127748309186));
#96238=CARTESIAN_POINT('Ctrl Pts',(2.37718430487489,-0.122102242138023,
18.1442433433969));
#96239=CARTESIAN_POINT('Ctrl Pts',(2.37895888052462,0.0804969451879324,
18.1562237784904));
#96240=CARTESIAN_POINT('Ctrl Pts',(2.34545712120427,0.361388724791912,18.1739767144192));
#96241=CARTESIAN_POINT('Ctrl Pts',(2.33173527595175,0.441338086820873,18.1791524934653));
#96242=CARTESIAN_POINT('Ctrl Pts',(2.3099482170731,0.538209718041095,18.185653306329));
#96243=CARTESIAN_POINT('Ctrl Pts',(2.30574279252618,0.55595018668948,18.1868532772087));
#96244=CARTESIAN_POINT('Ctrl Pts',(2.29877662231556,0.583897121489828,18.1887593710122));
#96245=CARTESIAN_POINT('Ctrl Pts',(2.29615138086196,0.59413688472647,18.1894611248946));
#96246=CARTESIAN_POINT('Ctrl Pts',(2.29109868314232,0.613311177485965,18.1907816525605));
#96247=CARTESIAN_POINT('Ctrl Pts',(2.28868718634904,0.622249736982913,18.1913998989234));
#96248=CARTESIAN_POINT('Ctrl Pts',(2.2831640110465,0.642255656224311,18.1927896949178));
#96249=CARTESIAN_POINT('Ctrl Pts',(2.28002409030713,0.653314907845404,18.1935621498184));
#96250=CARTESIAN_POINT('Ctrl Pts',(2.27183076997444,0.681394329195688,18.1955342706714));
#96251=CARTESIAN_POINT('Ctrl Pts',(2.26666650422937,0.698381133708327,18.1967375212846));
#96252=CARTESIAN_POINT('Ctrl Pts',(2.23344621786385,0.803400846316708,18.2042415325558));
#96253=CARTESIAN_POINT('Ctrl Pts',(2.20046018506622,0.889778600285362,18.210702981233));
#96254=CARTESIAN_POINT('Ctrl Pts',(2.08577219872466,1.14441384949323,18.2306388479346));
#96255=CARTESIAN_POINT('Ctrl Pts',(1.9891560321356,1.30513486989951,18.2445087855476));
#96256=CARTESIAN_POINT('Ctrl Pts',(1.83718610426479,1.50123049585591,18.2623076229358));
#96257=CARTESIAN_POINT('Ctrl Pts',(1.79782259572171,1.54815412636854,18.2666368495276));
#96258=CARTESIAN_POINT('Ctrl Pts',(1.74915373381788,1.60180675396093,18.2716228436165));
#96259=CARTESIAN_POINT('Ctrl Pts',(1.74156509915752,1.61005424737185,18.2723903291557));
#96260=CARTESIAN_POINT('Ctrl Pts',(1.72974589162321,1.62271827654194,18.2735699903415));
#96261=CARTESIAN_POINT('Ctrl Pts',(1.72555634870324,1.62717262274551,18.273985145115));
#96262=CARTESIAN_POINT('Ctrl Pts',(1.71777914061087,1.63537757820224,18.2747502076607));
#96263=CARTESIAN_POINT('Ctrl Pts',(1.71419641297866,1.63913259313402,18.275100464768));
#96264=CARTESIAN_POINT('Ctrl Pts',(1.70603613173496,1.64762927093074,18.275893326752));
#96265=CARTESIAN_POINT('Ctrl Pts',(1.7014511267994,1.65236362916364,18.2763353457791));
#96266=CARTESIAN_POINT('Ctrl Pts',(1.68949688152212,1.66460475899594,18.2774790410602));
#96267=CARTESIAN_POINT('Ctrl Pts',(1.68209723057876,1.67208182615978,18.2781784288283));
#96268=CARTESIAN_POINT('Ctrl Pts',(1.63280231121122,1.72123405153977,18.2827834234678));
#96269=CARTESIAN_POINT('Ctrl Pts',(1.58940780397776,1.76138418128598,18.2865807272622));
#96270=CARTESIAN_POINT('Ctrl Pts',(1.37892531860329,1.94200879360372,18.3040945560035));
#96271=CARTESIAN_POINT('Ctrl Pts',(1.19446733944039,2.06060523899123,18.3169967842246));
#96272=CARTESIAN_POINT('Ctrl Pts',(0.935589584378949,2.18044893106411,18.3350299043153));
#96273=CARTESIAN_POINT('Ctrl Pts',(0.873639993177372,2.20600028468821,18.3393309334958));
#96274=CARTESIAN_POINT('Ctrl Pts',(0.794507405411819,2.23478249496345,18.3448500248827));
#96275=CARTESIAN_POINT('Ctrl Pts',(0.778255130046074,2.2404940846964,18.3459847576857));
#96276=CARTESIAN_POINT('Ctrl Pts',(0.752140550800908,2.24935319325938,18.3478106821816));
#96277=CARTESIAN_POINT('Ctrl Pts',(0.74231714598531,2.25261413588092,18.3484981163552));
#96278=CARTESIAN_POINT('Ctrl Pts',(0.723635465395617,2.25868016974658,18.3498066991493));
#96279=CARTESIAN_POINT('Ctrl Pts',(0.714781412862605,2.26149771690584,18.3504274238967));
#96280=CARTESIAN_POINT('Ctrl Pts',(0.694603452924602,2.26778843750314,18.3518433447345));
#96281=CARTESIAN_POINT('Ctrl Pts',(0.683269698463124,2.27122893262466,18.3526395940912));
#96282=CARTESIAN_POINT('Ctrl Pts',(0.653783155120678,2.27993923954168,18.3547138306048));
#96283=CARTESIAN_POINT('Ctrl Pts',(0.635592591604018,2.28507710401309,18.3559960669848));
#96284=CARTESIAN_POINT('Ctrl Pts',(0.466303628291112,2.33071444078106,18.3679558813846));
#96285=CARTESIAN_POINT('Ctrl Pts',(0.311636353017043,2.35638157498201,18.3791191057528));
#96286=CARTESIAN_POINT('Ctrl Pts',(0.0439197365305154,2.37398294364994,
18.3986488458375));
#96287=CARTESIAN_POINT('Ctrl Pts',(-0.0681387684765478,2.37341142431974,
18.4068734872944));
#96288=CARTESIAN_POINT('Ctrl Pts',(-0.248866658219189,2.35967574986997,
18.4199261233835));
#96289=CARTESIAN_POINT('Ctrl Pts',(-0.317738240700849,2.3513929360394,18.4248473851097));
#96290=CARTESIAN_POINT('Ctrl Pts',(-0.397548285450235,2.33822299465723,
18.4304180412203));
#96291=CARTESIAN_POINT('Ctrl Pts',(-0.408928318019502,2.33625962949064,
18.4312091689987));
#96292=CARTESIAN_POINT('Ctrl Pts',(-0.426383580456419,2.33311666918466,
18.4324172759056));
#96293=CARTESIAN_POINT('Ctrl Pts',(-0.432469091013121,2.33199632016331,
18.4328374597782));
#96294=CARTESIAN_POINT('Ctrl Pts',(-0.443645570105871,2.32989346368997,
18.4336072243406));
#96295=CARTESIAN_POINT('Ctrl Pts',(-0.448737685132687,2.32891808250796,
18.4339571886052));
#96296=CARTESIAN_POINT('Ctrl Pts',(-0.460205870615151,2.32668237179374,
18.4347436968437));
#96297=CARTESIAN_POINT('Ctrl Pts',(-0.466579974275102,2.32541252957876,
18.4351796952322));
#96298=CARTESIAN_POINT('Ctrl Pts',(-0.482961898297004,2.3220788702843,18.436297475918));
#96299=CARTESIAN_POINT('Ctrl Pts',(-0.492961874081811,2.31997652467836,
18.4369771379888));
#96300=CARTESIAN_POINT('Ctrl Pts',(-0.555002103406856,2.30651423666919,
18.4411790069551));
#96301=CARTESIAN_POINT('Ctrl Pts',(-0.606665530876341,2.29346750884674,
18.4446134298115));
#96302=CARTESIAN_POINT('Ctrl Pts',(-0.673734309713538,2.2741049839767,18.449039157693));
#96303=CARTESIAN_POINT('Ctrl Pts',(-0.689570415980987,2.26935322526014,
18.450081707307));
#96304=CARTESIAN_POINT('Ctrl Pts',(-0.726049490018855,2.25799025185859,
18.4524802958612));
#96305=CARTESIAN_POINT('Ctrl Pts',(-0.74665422786761,2.25126083367592,18.453832899681));
#96306=CARTESIAN_POINT('Ctrl Pts',(-0.890536266017226,2.20207684674148,
18.4632805222851));
#96307=CARTESIAN_POINT('Ctrl Pts',(-1.01022240249457,2.14980222806255,18.471164457647));
#96308=CARTESIAN_POINT('Ctrl Pts',(-1.22879475123163,2.03203355707197,18.4865210031303));
#96309=CARTESIAN_POINT('Ctrl Pts',(-1.32825390427852,1.96845950007973,18.4939385685271));
#96310=CARTESIAN_POINT('Ctrl Pts',(-1.43853270528544,1.88579421903294,18.5029459785705));
#96311=CARTESIAN_POINT('Ctrl Pts',(-1.45434599510926,1.87362586101682,18.5042574889887));
#96312=CARTESIAN_POINT('Ctrl Pts',(-1.47859079955985,1.85447756786646,18.5063004259626));
#96313=CARTESIAN_POINT('Ctrl Pts',(-1.48713094802665,1.84763614893775,18.5070263467968));
#96314=CARTESIAN_POINT('Ctrl Pts',(-1.502082979576,1.83548741739263,18.5083086069133));
#96315=CARTESIAN_POINT('Ctrl Pts',(-1.50851488652366,1.83020495328633,18.508863937658));
#96316=CARTESIAN_POINT('Ctrl Pts',(-1.5231375929359,1.81806601494296,18.5101351258628));
#96317=CARTESIAN_POINT('Ctrl Pts',(-1.53131009555283,1.81118788271092,18.5108518592384));
#96318=CARTESIAN_POINT('Ctrl Pts',(-1.55332166559151,1.79240705627806,18.5127995725726));
#96319=CARTESIAN_POINT('Ctrl Pts',(-1.56707000074492,1.78039962716612,18.51403485321));
#96320=CARTESIAN_POINT('Ctrl Pts',(-1.6353543599066,1.71935820017017,18.5202665286874));
#96321=CARTESIAN_POINT('Ctrl Pts',(-1.6877285317892,1.66797688374222,18.525361263538));
#96322=CARTESIAN_POINT('Ctrl Pts',(-1.87786521957995,1.46330808262911,18.5451209721441));
#96323=CARTESIAN_POINT('Ctrl Pts',(-1.99782268371322,1.29473299503854,18.5604322621519));
#96324=CARTESIAN_POINT('Ctrl Pts',(-2.12415473253877,1.05696110572707,18.5797685628429));
#96325=CARTESIAN_POINT('Ctrl Pts',(-2.15159328520423,0.999924035898249,
18.5842466214546));
#96326=CARTESIAN_POINT('Ctrl Pts',(-2.1812075073074,0.931482444221716,18.5893803660805));
#96327=CARTESIAN_POINT('Ctrl Pts',(-2.18562050561715,0.921080209359811,
18.5901542416944));
#96328=CARTESIAN_POINT('Ctrl Pts',(-2.1923145389544,0.904982131750435,18.5913415977056));
#96329=CARTESIAN_POINT('Ctrl Pts',(-2.19464802215909,0.899308488508613,
18.5917581175134));
#96330=CARTESIAN_POINT('Ctrl Pts',(-2.19891436730815,0.88881977189486,18.5925244399729));
#96331=CARTESIAN_POINT('Ctrl Pts',(-2.20085343388057,0.884007435045523,
18.592874601297));
#96332=CARTESIAN_POINT('Ctrl Pts',(-2.20521029979314,0.873091457819205,
18.5936656653581));
#96333=CARTESIAN_POINT('Ctrl Pts',(-2.20761855625226,0.866984124853753,
18.5941059935295));
#96334=CARTESIAN_POINT('Ctrl Pts',(-2.21378881175248,0.851143957703621,
18.5952423940668));
#96335=CARTESIAN_POINT('Ctrl Pts',(-2.21751204585688,0.841396028139503,
18.5959362259058));
#96336=CARTESIAN_POINT('Ctrl Pts',(-2.24128487900333,0.777901528986282,
18.600421923511));
#96337=CARTESIAN_POINT('Ctrl Pts',(-2.25944515932818,0.723462175274785,
18.6041117966285));
#96338=CARTESIAN_POINT('Ctrl Pts',(-2.2795056542623,0.655166123527973,18.6086117407948));
#96339=CARTESIAN_POINT('Ctrl Pts',(-2.28328091117517,0.641885480345634,
18.6094808178627));
#96340=CARTESIAN_POINT('Ctrl Pts',(-2.32790527061401,0.479528318939938,
18.6200410194997));
#96341=CARTESIAN_POINT('Ctrl Pts',(-2.35416628279363,0.3269692411613,18.6293285405642));
#96342=CARTESIAN_POINT('Ctrl Pts',(-2.36542649880509,0.173076691818106,
18.6388842277111));
#96343=CARTESIAN_POINT('Origin',(0.,0.,-1.84858989190503));
#96344=CARTESIAN_POINT('',(-2.36542647001695,0.17307708526301,19.8356128877059));
#96345=CARTESIAN_POINT('',(-2.36542650053005,0.173076668243166,19.6378399312857));
#96346=CARTESIAN_POINT('',(-2.36542649454111,0.173076750093529,-1.84858989190503));
#96347=CARTESIAN_POINT('Ctrl Pts',(-2.3654264700169,0.173077085263749,19.8356128877059));
#96348=CARTESIAN_POINT('Ctrl Pts',(-2.35323422706518,0.33970719786897,19.8252325324572));
#96349=CARTESIAN_POINT('Ctrl Pts',(-2.323456168924,0.504766661904006,19.815190742496));
#96350=CARTESIAN_POINT('Ctrl Pts',(-2.26083942397636,0.718962231332386,
19.8012072448235));
#96351=CARTESIAN_POINT('Ctrl Pts',(-2.24332976957548,0.771862980924048,
19.7976761047838));
#96352=CARTESIAN_POINT('Ctrl Pts',(-2.21098346100693,0.859155500580385,
19.7916802044054));
#96353=CARTESIAN_POINT('Ctrl Pts',(-2.19716537539688,0.893901616588215,
19.78924755419));
#96354=CARTESIAN_POINT('Ctrl Pts',(-2.17708906651077,0.941102902069325,
19.7858722520732));
#96355=CARTESIAN_POINT('Ctrl Pts',(-2.17153337343339,0.953852331342261,
19.7849533765998));
#96356=CARTESIAN_POINT('Ctrl Pts',(-2.16197831514997,0.975263467969434,
19.7833977367547));
#96357=CARTESIAN_POINT('Ctrl Pts',(-2.15803818302342,0.983951352043978,
19.7827630115038));
#96358=CARTESIAN_POINT('Ctrl Pts',(-2.15013218985068,1.00110792256907,19.7815025070584));
#96359=CARTESIAN_POINT('Ctrl Pts',(-2.1461684422494,1.00957739654596,19.7808768098936));
#96360=CARTESIAN_POINT('Ctrl Pts',(-2.13638790779684,1.03015789058932,19.7793478669117));
#96361=CARTESIAN_POINT('Ctrl Pts',(-2.13051815385665,1.04224323228562,19.7784427942912));
#96362=CARTESIAN_POINT('Ctrl Pts',(-2.11042269333423,1.08273894564482,19.7753851844087));
#96363=CARTESIAN_POINT('Ctrl Pts',(-2.09572939555262,1.1109121020342,19.7732163972922));
#96364=CARTESIAN_POINT('Ctrl Pts',(-1.98336292460144,1.31619807793784,19.757096227552));
#96365=CARTESIAN_POINT('Ctrl Pts',(-1.86397128286467,1.48043384994926,19.7423295411214));
#96366=CARTESIAN_POINT('Ctrl Pts',(-1.71097780090446,1.64261525099771,19.7260650070205));
#96367=CARTESIAN_POINT('Ctrl Pts',(-1.69651988910732,1.65754341741345,19.7245510264689));
#96368=CARTESIAN_POINT('Ctrl Pts',(-1.63506840018614,1.71934722836924,19.7182165956811));
#96369=CARTESIAN_POINT('Ctrl Pts',(-1.58631056620238,1.76443294678743,19.7134311699763));
#96370=CARTESIAN_POINT('Ctrl Pts',(-1.51782271026867,1.82262557554497,19.7070879531499));
#96371=CARTESIAN_POINT('Ctrl Pts',(-1.49969739047633,1.83756839330913,19.7054430630328));
#96372=CARTESIAN_POINT('Ctrl Pts',(-1.4723661563832,1.8594268915841,19.7030161586475));
#96373=CARTESIAN_POINT('Ctrl Pts',(-1.46332759545993,1.86654837193496,19.7022220745988));
#96374=CARTESIAN_POINT('Ctrl Pts',(-1.44693101487991,1.87927492481491,19.7007973363327));
#96375=CARTESIAN_POINT('Ctrl Pts',(-1.43959141859806,1.88490322284688,19.7001652028588));
#96376=CARTESIAN_POINT('Ctrl Pts',(-1.42769341910421,1.89391705161524,19.6991497543746));
#96377=CARTESIAN_POINT('Ctrl Pts',(-1.42315554701653,1.89732933042263,19.6987646224744));
#96378=CARTESIAN_POINT('Ctrl Pts',(-1.41462592675644,1.90369540827246,19.698044811519));
#96379=CARTESIAN_POINT('Ctrl Pts',(-1.41063720057052,1.90665293355087,19.6977098826646));
#96380=CARTESIAN_POINT('Ctrl Pts',(-1.40130213395993,1.91352928646954,19.6969298878984));
#96381=CARTESIAN_POINT('Ctrl Pts',(-1.39594862480298,1.9174382494427,19.6964855065237));
#96382=CARTESIAN_POINT('Ctrl Pts',(-1.38162925115415,1.92780204449874,19.6953044800833));
#96383=CARTESIAN_POINT('Ctrl Pts',(-1.37263442467525,1.93421685917467,19.6945704895389));
#96384=CARTESIAN_POINT('Ctrl Pts',(-1.30177863356973,1.98400566207694,19.6888471842528));
#96385=CARTESIAN_POINT('Ctrl Pts',(-1.23791484721852,2.02446919527554,19.6840362285206));
#96386=CARTESIAN_POINT('Ctrl Pts',(-1.00899498516731,2.15461872577638,19.6675691896541));
#96387=CARTESIAN_POINT('Ctrl Pts',(-0.83532658605038,2.22770900132511,19.6563638300093));
#96388=CARTESIAN_POINT('Ctrl Pts',(-0.579110865355982,2.30131233274503,
19.6396149862796));
#96389=CARTESIAN_POINT('Ctrl Pts',(-0.502341968516801,2.31927970216971,
19.6345791240251));
#96390=CARTESIAN_POINT('Ctrl Pts',(-0.40719884366394,2.33660185294187,19.6282456666917));
#96391=CARTESIAN_POINT('Ctrl Pts',(-0.389535231438675,2.33961137619871,
19.6270661088356));
#96392=CARTESIAN_POINT('Ctrl Pts',(-0.361559503302609,2.34405228860277,
19.6251912892799));
#96393=CARTESIAN_POINT('Ctrl Pts',(-0.351268907604851,2.34561645517582,
19.6245002442858));
#96394=CARTESIAN_POINT('Ctrl Pts',(-0.331936701295934,2.34842487286597,
19.6231992329643));
#96395=CARTESIAN_POINT('Ctrl Pts',(-0.322897528017077,2.34968477450544,
19.6225897746515));
#96396=CARTESIAN_POINT('Ctrl Pts',(-0.302606160096279,2.35239373489734,
19.6212189773812));
#96397=CARTESIAN_POINT('Ctrl Pts',(-0.291350450806926,2.35381428306019,
19.6204567520999));
#96398=CARTESIAN_POINT('Ctrl Pts',(-0.262668181947738,2.35722530314698,
19.6185095399311));
#96399=CARTESIAN_POINT('Ctrl Pts',(-0.245229194411968,2.35910328661205,
19.6173210442405));
#96400=CARTESIAN_POINT('Ctrl Pts',(-0.137358437550926,2.36951077568546,
19.609939787628));
#96401=CARTESIAN_POINT('Ctrl Pts',(-0.0465307437459041,2.3730317704547,
19.6035916103679));
#96402=CARTESIAN_POINT('Ctrl Pts',(0.251430474564564,2.36746975878224,19.5823334496865));
#96403=CARTESIAN_POINT('Ctrl Pts',(0.457169261931409,2.33647476600093,19.5668819448654));
#96404=CARTESIAN_POINT('Ctrl Pts',(0.699444633034538,2.26671469785821,19.5489626290743));
#96405=CARTESIAN_POINT('Ctrl Pts',(0.742278385510339,2.25305165749233,19.5458102274945));
#96406=CARTESIAN_POINT('Ctrl Pts',(0.794313791440348,2.23480814019125,19.5420209193307));
#96407=CARTESIAN_POINT('Ctrl Pts',(0.803904809947787,2.23137600793186,19.5413241943613));
#96408=CARTESIAN_POINT('Ctrl Pts',(0.818960282448285,2.2258787556836,19.5402335360746));
#96409=CARTESIAN_POINT('Ctrl Pts',(0.824439586028089,2.22385510996247,19.5398372341574));
#96410=CARTESIAN_POINT('Ctrl Pts',(0.83472823035326,2.22001200056672,19.5390943538715));
#96411=CARTESIAN_POINT('Ctrl Pts',(0.839539078235053,2.21819715939314,19.5387475241839));
#96412=CARTESIAN_POINT('Ctrl Pts',(0.850562871952614,2.21399754938837,19.5379539554359));
#96413=CARTESIAN_POINT('Ctrl Pts',(0.856771713545251,2.21160226565256,19.5375078501455));
#96414=CARTESIAN_POINT('Ctrl Pts',(0.873344260857463,2.20512854519738,19.5363191770899));
#96415=CARTESIAN_POINT('Ctrl Pts',(0.883689614038453,2.20100312967401,19.535579318406));
#96416=CARTESIAN_POINT('Ctrl Pts',(0.966042088881135,2.16748918948094,19.5297041745093));
#96417=CARTESIAN_POINT('Ctrl Pts',(1.03660154027528,2.13464441296786,19.5247579032972));
#96418=CARTESIAN_POINT('Ctrl Pts',(1.26976673603639,2.0118134185979,19.5082970901789));
#96419=CARTESIAN_POINT('Ctrl Pts',(1.42336782128133,1.906234338101,19.4972034770522));
#96420=CARTESIAN_POINT('Ctrl Pts',(1.62209518680712,1.73209763430365,19.480599576103));
#96421=CARTESIAN_POINT('Ctrl Pts',(1.67850192112975,1.67749345068799,19.4755845088593));
#96422=CARTESIAN_POINT('Ctrl Pts',(1.74432053590521,1.60712918115199,19.4692743279309));
#96423=CARTESIAN_POINT('Ctrl Pts',(1.75639725739358,1.59392188702392,19.468096184289));
#96424=CARTESIAN_POINT('Ctrl Pts',(1.77525655535978,1.57282245330248,19.4662231021776));
#96425=CARTESIAN_POINT('Ctrl Pts',(1.78213880719684,1.5650199912335,19.4655323669739));
#96426=CARTESIAN_POINT('Ctrl Pts',(1.79496182886096,1.55028816677097,19.4642316262527));
#96427=CARTESIAN_POINT('Ctrl Pts',(1.80091438683262,1.54336927997675,19.4636221265878));
#96428=CARTESIAN_POINT('Ctrl Pts',(1.81418051243925,1.52776830562045,19.4622508233453));
#96429=CARTESIAN_POINT('Ctrl Pts',(1.821471939502,1.51906777109398,19.4614881305742));
#96430=CARTESIAN_POINT('Ctrl Pts',(1.83988392743178,1.49677440589022,19.4595389256816));
#96431=CARTESIAN_POINT('Ctrl Pts',(1.85091632151539,1.4831099859008,19.4583488924076));
#96432=CARTESIAN_POINT('Ctrl Pts',(1.91841767960669,1.39757835045672,19.4509274359899));
#96433=CARTESIAN_POINT('Ctrl Pts',(1.97083781475041,1.32262848766791,19.444538577251));
#96434=CARTESIAN_POINT('Ctrl Pts',(2.1279305802648,1.06786792929575,19.4231832461695));
#96435=CARTESIAN_POINT('Ctrl Pts',(2.21330423888941,0.877327039506695,19.4076739070152));
#96436=CARTESIAN_POINT('Ctrl Pts',(2.28108809074832,0.650143787249741,19.3908366525989));
#96437=CARTESIAN_POINT('Ctrl Pts',(2.28891590403338,0.622024096419955,19.3887819696381));
#96438=CARTESIAN_POINT('Ctrl Pts',(2.30114636235901,0.574726216142021,19.385382527452));
#96439=CARTESIAN_POINT('Ctrl Pts',(2.30583288043755,0.555625409614157,19.384024970706));
#96440=CARTESIAN_POINT('Ctrl Pts',(2.31200065555246,0.529064080399357,19.382160332651));
#96441=CARTESIAN_POINT('Ctrl Pts',(2.3136842836461,0.521652060381731,19.3816424879022));
#96442=CARTESIAN_POINT('Ctrl Pts',(2.3164766239762,0.509079532060504,19.3807684603905));
#96443=CARTESIAN_POINT('Ctrl Pts',(2.31760378524778,0.503923224353551,19.3804112395059));
#96444=CARTESIAN_POINT('Ctrl Pts',(2.31972972099569,0.494039902027675,19.3797289642144));
#96445=CARTESIAN_POINT('Ctrl Pts',(2.32073127351936,0.489313560459673,19.3794037466331));
#96446=CARTESIAN_POINT('Ctrl Pts',(2.3230889870294,0.478017386294966,19.3786289098032));
#96447=CARTESIAN_POINT('Ctrl Pts',(2.32443174008037,0.471444749385867,19.3781800486682));
#96448=CARTESIAN_POINT('Ctrl Pts',(2.32913603649639,0.447908952094694,19.3765795020276));
#96449=CARTESIAN_POINT('Ctrl Pts',(2.33234002527015,0.430914325105343,19.3754363476759));
#96450=CARTESIAN_POINT('Ctrl Pts',(2.36521876131017,0.24539536965729,19.3630787464496));
#96451=CARTESIAN_POINT('Ctrl Pts',(2.37676259289263,0.0741408232858691,
19.3527362204046));
#96452=CARTESIAN_POINT('Ctrl Pts',(2.36341513740825,-0.252327964506718,
19.332696214678));
#96453=CARTESIAN_POINT('Ctrl Pts',(2.34178353180174,-0.406744094267162,
19.3230683148398));
#96454=CARTESIAN_POINT('Ctrl Pts',(2.29997836458666,-0.579473342540759,
19.3114789476771));
#96455=CARTESIAN_POINT('Ctrl Pts',(2.2944599293526,-0.600952086304352,19.3100236207595));
#96456=CARTESIAN_POINT('Ctrl Pts',(2.28567375401478,-0.633262543399366,
19.3078114533882));
#96457=CARTESIAN_POINT('Ctrl Pts',(2.28262825904641,-0.644153849746004,
19.3070618093151));
#96458=CARTESIAN_POINT('Ctrl Pts',(2.27698524163552,-0.663791771619905,
19.3057027815364));
#96459=CARTESIAN_POINT('Ctrl Pts',(2.27441490293912,-0.672546022200261,
19.3050942942144));
#96460=CARTESIAN_POINT('Ctrl Pts',(2.26879692706143,-0.691279566124195,
19.3037863624069));
#96461=CARTESIAN_POINT('Ctrl Pts',(2.2657338280945,-0.701253983206915,19.3030864225291));
#96462=CARTESIAN_POINT('Ctrl Pts',(2.25733452090882,-0.727975170529574,
19.3012015829373));
#96463=CARTESIAN_POINT('Ctrl Pts',(2.25187789131268,-0.744683101544696,
19.3000127511698));
#96464=CARTESIAN_POINT('Ctrl Pts',(2.22483190791318,-0.824480022631643,
19.294284174069));
#96465=CARTESIAN_POINT('Ctrl Pts',(2.20077602588636,-0.886694804547859,
19.2896636893009));
#96466=CARTESIAN_POINT('Ctrl Pts',(2.09676334990071,-1.12528456208013,19.2713207105903));
#96467=CARTESIAN_POINT('Ctrl Pts',(1.99795744969515,-1.29260541247844,19.2570083941157));
#96468=CARTESIAN_POINT('Ctrl Pts',(1.84564809411906,-1.49061935623535,19.2389247049613));
#96469=CARTESIAN_POINT('Ctrl Pts',(1.80977044175354,-1.53398004786865,19.2348896480655));
#96470=CARTESIAN_POINT('Ctrl Pts',(1.75837717564129,-1.59177635755103,19.2294469920694));
#96471=CARTESIAN_POINT('Ctrl Pts',(1.74416224446116,-1.60733954083286,19.2279747010726));
#96472=CARTESIAN_POINT('Ctrl Pts',(1.71924647937187,-1.63389867852809,19.2254535015569));
#96473=CARTESIAN_POINT('Ctrl Pts',(1.70864313758474,-1.64498389295039,19.2243985145924));
#96474=CARTESIAN_POINT('Ctrl Pts',(1.69312908157624,-1.66089111879631,19.2228816977405));
#96475=CARTESIAN_POINT('Ctrl Pts',(1.68830402886305,-1.66579557705312,19.2224136297586));
#96476=CARTESIAN_POINT('Ctrl Pts',(1.67982574648213,-1.67433870755467,19.2215976921519));
#96477=CARTESIAN_POINT('Ctrl Pts',(1.67618190253589,-1.67798655473388,19.2212491020098));
#96478=CARTESIAN_POINT('Ctrl Pts',(1.66842847112013,-1.68569804503254,19.220511813399));
#96479=CARTESIAN_POINT('Ctrl Pts',(1.66431591594802,-1.68975856145586,19.2201233567907));
#96480=CARTESIAN_POINT('Ctrl Pts',(1.65311371666262,-1.70073843977101,19.219072167911));
#96481=CARTESIAN_POINT('Ctrl Pts',(1.64599539693776,-1.70762857865914,19.2184116749844));
#96482=CARTESIAN_POINT('Ctrl Pts',(1.61276929722372,-1.7393887910815,19.2153619560181));
#96483=CARTESIAN_POINT('Ctrl Pts',(1.58613810319798,-1.76370758314151,19.2130119297252));
#96484=CARTESIAN_POINT('Ctrl Pts',(1.37309442202791,-1.94952200625935,19.1948382814933));
#96485=CARTESIAN_POINT('Ctrl Pts',(1.16306635384933,-2.0816657986593,19.180431777314));
#96486=CARTESIAN_POINT('Ctrl Pts',(0.896647951783794,-2.19615434743124,
19.1620858363049));
#96487=CARTESIAN_POINT('Ctrl Pts',(0.856423127097393,-2.2121506614815,19.1593193701576));
#96488=CARTESIAN_POINT('Ctrl Pts',(0.786758936108575,-2.23766932286812,
19.1545173117106));
#96489=CARTESIAN_POINT('Ctrl Pts',(0.757528998682597,-2.24773292300983,
19.1524992912835));
#96490=CARTESIAN_POINT('Ctrl Pts',(0.715822501933081,-2.26118618199805,
19.149611583108));
#96491=CARTESIAN_POINT('Ctrl Pts',(0.703501243442268,-2.26504984344146,
19.1487574656509));
#96492=CARTESIAN_POINT('Ctrl Pts',(0.682207905543772,-2.27153644102507,
19.1472793851924));
#96493=CARTESIAN_POINT('Ctrl Pts',(0.673250647471314,-2.27420733238551,
19.1466570058537));
#96494=CARTESIAN_POINT('Ctrl Pts',(0.656069858292932,-2.2792199347792,19.1454619593861));
#96495=CARTESIAN_POINT('Ctrl Pts',(0.647848976926148,-2.2815702640576,19.1448895846303));
#96496=CARTESIAN_POINT('Ctrl Pts',(0.628521422363691,-2.28698308253088,
19.1435425282315));
#96497=CARTESIAN_POINT('Ctrl Pts',(0.61740486850121,-2.29000917428923,19.1427666768551));
#96498=CARTESIAN_POINT('Ctrl Pts',(0.578946718868338,-2.30017767361133,
19.1400786300085));
#96499=CARTESIAN_POINT('Ctrl Pts',(0.551500726367081,-2.30691210532085,
19.1381533613131));
#96500=CARTESIAN_POINT('Ctrl Pts',(0.346650282882144,-2.35331183911892,
19.1237264707463));
#96501=CARTESIAN_POINT('Ctrl Pts',(0.165363106866224,-2.37294604550088,
19.1105722474374));
#96502=CARTESIAN_POINT('Ctrl Pts',(-0.158489839592776,-2.37071398866252,
19.0869132045793));
#96503=CARTESIAN_POINT('Ctrl Pts',(-0.300274715566463,-2.35695745070675,
19.0765235020582));
#96504=CARTESIAN_POINT('Ctrl Pts',(-0.452482285816575,-2.32822239836764,
19.0658374058627));
#96505=CARTESIAN_POINT('Ctrl Pts',(-0.464958590656073,-2.32576294628314,
19.0649650991082));
#96506=CARTESIAN_POINT('Ctrl Pts',(-0.483660835030993,-2.32191966245373,
19.0636635453347));
#96507=CARTESIAN_POINT('Ctrl Pts',(-0.48990170641114,-2.3206109201495,19.0632302368633));
#96508=CARTESIAN_POINT('Ctrl Pts',(-0.500650000530844,-2.31831165628882,
19.0624858150292));
#96509=CARTESIAN_POINT('Ctrl Pts',(-0.505159866614682,-2.31733313728532,
19.0621740277182));
#96510=CARTESIAN_POINT('Ctrl Pts',(-0.515442562472784,-2.31507062519926,
19.0614644359696));
#96511=CARTESIAN_POINT('Ctrl Pts',(-0.521213457382012,-2.3137782021312,
19.0610671194011));
#96512=CARTESIAN_POINT('Ctrl Pts',(-0.536967421617674,-2.31018808522019,
19.0599848580806));
#96513=CARTESIAN_POINT('Ctrl Pts',(-0.546940680980112,-2.30784724407641,
19.0593023261981));
#96514=CARTESIAN_POINT('Ctrl Pts',(-0.596805472431441,-2.29580198803152,
19.0559014046275));
#96515=CARTESIAN_POINT('Ctrl Pts',(-0.636458236015943,-2.2851269011834,
19.053234321735));
#96516=CARTESIAN_POINT('Ctrl Pts',(-0.907081331865152,-2.20467935926936,
19.0351635044363));
#96517=CARTESIAN_POINT('Ctrl Pts',(-1.12651865824161,-2.10104499769973,
19.0210362521405));
#96518=CARTESIAN_POINT('Ctrl Pts',(-1.38054059284589,-1.92964911561629,
19.0016442512426));
#96519=CARTESIAN_POINT('Ctrl Pts',(-1.43299081159047,-1.89102462986639,
18.9974598435712));
#96520=CARTESIAN_POINT('Ctrl Pts',(-1.49698083985673,-1.83970993713107,
18.9920821122248));
#96521=CARTESIAN_POINT('Ctrl Pts',(-1.51006545585992,-1.82898512349717,
18.9909674577762));
#96522=CARTESIAN_POINT('Ctrl Pts',(-1.53084486924783,-1.81157828226521,
18.9891723981157));
#96523=CARTESIAN_POINT('Ctrl Pts',(-1.5386134475841,-1.80498491402518,18.9884956116562));
#96524=CARTESIAN_POINT('Ctrl Pts',(-1.55328527459743,-1.79236905787066,
18.9872064273893));
#96525=CARTESIAN_POINT('Ctrl Pts',(-1.56019660449998,-1.78635621731257,
18.9865944356143));
#96526=CARTESIAN_POINT('Ctrl Pts',(-1.57585174922727,-1.7725761223244,18.9851973090798));
#96527=CARTESIAN_POINT('Ctrl Pts',(-1.5845732374067,-1.76478397877312,18.984411140988));
#96528=CARTESIAN_POINT('Ctrl Pts',(-1.60708548293363,-1.74436917616835,
18.9823611553451));
#96529=CARTESIAN_POINT('Ctrl Pts',(-1.62078503102436,-1.73164760284145,
18.9810931664466));
#96530=CARTESIAN_POINT('Ctrl Pts',(-1.74669958483512,-1.61191852321592,
18.9692438249788));
#96531=CARTESIAN_POINT('Ctrl Pts',(-1.84829611080618,-1.49433098502667,
18.9581849903403));
#96532=CARTESIAN_POINT('Ctrl Pts',(-2.00162157045803,-1.27710773386986,
18.9388346698566));
#96533=CARTESIAN_POINT('Ctrl Pts',(-2.05913226282864,-1.18214548026865,
18.9306851298374));
#96534=CARTESIAN_POINT('Ctrl Pts',(-2.14283194294092,-1.01916676607044,
18.9174739851719));
#96535=CARTESIAN_POINT('Ctrl Pts',(-2.17291820085267,-0.953340673476525,
18.9123327896251));
#96536=CARTESIAN_POINT('Ctrl Pts',(-2.20426368555865,-0.875530051789763,
18.9065555376872));
#96537=CARTESIAN_POINT('Ctrl Pts',(-2.20849820304283,-0.864793020247135,
18.9057648215134));
#96538=CARTESIAN_POINT('Ctrl Pts',(-2.21486286283677,-0.84830311903016,
18.904560804249));
#96539=CARTESIAN_POINT('Ctrl Pts',(-2.21704927240024,-0.842572376030845,
18.9041442770434));
#96540=CARTESIAN_POINT('Ctrl Pts',(-2.22101587408609,-0.83205327074183,
18.9033832891466));
#96541=CARTESIAN_POINT('Ctrl Pts',(-2.22280282413186,-0.827267649808519,
18.9030384390758));
#96542=CARTESIAN_POINT('Ctrl Pts',(-2.22677950991498,-0.816511795892212,
18.9022664011495));
#96543=CARTESIAN_POINT('Ctrl Pts',(-2.22896070176143,-0.810538519138946,
18.9018397235281));
#96544=CARTESIAN_POINT('Ctrl Pts',(-2.234481083762,-0.79522993152708,18.9007513393234));
#96545=CARTESIAN_POINT('Ctrl Pts',(-2.23778585189174,-0.785882209569662,
18.9000916112971));
#96546=CARTESIAN_POINT('Ctrl Pts',(-2.25726177810717,-0.729674359324691,
18.8961521952245));
#96547=CARTESIAN_POINT('Ctrl Pts',(-2.27202052389178,-0.682333486275215,
18.892948617959));
#96548=CARTESIAN_POINT('Ctrl Pts',(-2.28912447805736,-0.620735896634144,
18.8888844770757));
#96549=CARTESIAN_POINT('Ctrl Pts',(-2.29283783531148,-0.606876103692446,
18.8879767352116));
#96550=CARTESIAN_POINT('Ctrl Pts',(-2.34630924864452,-0.399799242755879,
18.8745026788418));
#96551=CARTESIAN_POINT('Ctrl Pts',(-2.37161967530902,-0.201087963350939,
18.8626479715626));
#96552=CARTESIAN_POINT('Ctrl Pts',(-2.37178741181482,0.0567324659326155,
18.846463663737));
#96553=CARTESIAN_POINT('Ctrl Pts',(-2.36967752226244,0.114978290712743,
18.8427604081577));
#96554=CARTESIAN_POINT('Ctrl Pts',(-2.36542649320577,0.173076768343595,
18.8389943251842));
#96555=CARTESIAN_POINT('Ctrl Pts',(-2.36542649880509,0.173076691818108,
18.6388842277111));
#96556=CARTESIAN_POINT('Ctrl Pts',(-2.36960585386229,0.115957751674473,
18.6424309278243));
#96557=CARTESIAN_POINT('Ctrl Pts',(-2.37171871494586,0.0586549215548028,
18.6460114842864));
#96558=CARTESIAN_POINT('Ctrl Pts',(-2.37178256024484,-0.0597406771378477,
18.6535160827396));
#96559=CARTESIAN_POINT('Ctrl Pts',(-2.36946063533492,-0.120734203229363,
18.6574407824453));
#96560=CARTESIAN_POINT('Ctrl Pts',(-2.36345772608295,-0.198918322189068,
18.6625793557217));
#96561=CARTESIAN_POINT('Ctrl Pts',(-2.36193456230257,-0.216254522369614,
18.6637255319754));
#96562=CARTESIAN_POINT('Ctrl Pts',(-2.35919764343389,-0.243910801448145,
18.6655655206083));
#96563=CARTESIAN_POINT('Ctrl Pts',(-2.35810658974592,-0.254242611277065,
18.666255471001));
#96564=CARTESIAN_POINT('Ctrl Pts',(-2.35601563001911,-0.272870357030803,
18.6675041972383));
#96565=CARTESIAN_POINT('Ctrl Pts',(-2.35503969215494,-0.281168856620004,
18.6680622086428));
#96566=CARTESIAN_POINT('Ctrl Pts',(-2.35263813537177,-0.300699274452836,
18.6693796079774));
#96567=CARTESIAN_POINT('Ctrl Pts',(-2.35117591036786,-0.311926402276078,
18.6701401391712));
#96568=CARTESIAN_POINT('Ctrl Pts',(-2.34666817821891,-0.344703022866579,
18.6723700923827));
#96569=CARTESIAN_POINT('Ctrl Pts',(-2.34340644515367,-0.366221094842173,
18.6738462953658));
#96570=CARTESIAN_POINT('Ctrl Pts',(-2.31108293187759,-0.561304856341472,
18.687344773823));
#96571=CARTESIAN_POINT('Ctrl Pts',(-2.26308943834641,-0.731142571251129,
18.6999894688802));
#96572=CARTESIAN_POINT('Ctrl Pts',(-2.14053998927671,-1.03225041046977,
18.7237172458917));
#96573=CARTESIAN_POINT('Ctrl Pts',(-2.07138847780926,-1.16482197330694,
18.7346757068148));
#96574=CARTESIAN_POINT('Ctrl Pts',(-1.98005013023606,-1.30573736461901,
18.7463535578338));
#96575=CARTESIAN_POINT('Ctrl Pts',(-1.96968079490732,-1.32132744044284,
18.747645614633));
#96576=CARTESIAN_POINT('Ctrl Pts',(-1.9552001193874,-1.34254948116033,18.7494028038583));
#96577=CARTESIAN_POINT('Ctrl Pts',(-1.95124729590324,-1.34828802915066,
18.749877790829));
#96578=CARTESIAN_POINT('Ctrl Pts',(-1.94444664697418,-1.35806838691302,
18.7506869246753));
#96579=CARTESIAN_POINT('Ctrl Pts',(-1.94161139842078,-1.36211882195922,
18.7510219013372));
#96580=CARTESIAN_POINT('Ctrl Pts',(-1.93569838185847,-1.37051017954972,
18.7517155832062));
#96581=CARTESIAN_POINT('Ctrl Pts',(-1.93261865242142,-1.37484963640894,
18.7520741376405));
#96582=CARTESIAN_POINT('Ctrl Pts',(-1.92514136975313,-1.38531064372476,
18.7529381674868));
#96583=CARTESIAN_POINT('Ctrl Pts',(-1.92072913869028,-1.39142173795563,
18.7534426447906));
#96584=CARTESIAN_POINT('Ctrl Pts',(-1.90518273612611,-1.41273918312857,
18.7552018758767));
#96585=CARTESIAN_POINT('Ctrl Pts',(-1.89389615638716,-1.4278342557352,18.7564466238072));
#96586=CARTESIAN_POINT('Ctrl Pts',(-1.82316225612422,-1.52012162712957,
18.7640616808848));
#96587=CARTESIAN_POINT('Ctrl Pts',(-1.75917805844449,-1.59373383438171,
18.770159399917));
#96588=CARTESIAN_POINT('Ctrl Pts',(-1.68030220458323,-1.6739200493627,18.7771050937606));
#96589=CARTESIAN_POINT('Ctrl Pts',(-1.66966376996903,-1.68453160617613,
18.7780308315554));
#96590=CARTESIAN_POINT('Ctrl Pts',(-1.51234417014642,-1.83849919379218,
18.7915717218202));
#96591=CARTESIAN_POINT('Ctrl Pts',(-1.34779376538526,-1.96232197187314,
18.8039547586385));
#96592=CARTESIAN_POINT('Ctrl Pts',(-1.14602435727059,-2.07666716795414,
18.8190159738905));
#96593=CARTESIAN_POINT('Ctrl Pts',(-1.12245284164,-2.08950182492433,18.8207720839803));
#96594=CARTESIAN_POINT('Ctrl Pts',(-1.0878775203179,-2.10757416154482,18.8233456088109));
#96595=CARTESIAN_POINT('Ctrl Pts',(-1.07704256239913,-2.11313171739394,
18.8241517408364));
#96596=CARTESIAN_POINT('Ctrl Pts',(-1.05780105502936,-2.12281479923587,
18.8255829665949));
#96597=CARTESIAN_POINT('Ctrl Pts',(-1.04941190390112,-2.12697446987693,
18.8262068492024));
#96598=CARTESIAN_POINT('Ctrl Pts',(-1.03193706308321,-2.13551063245499,
18.8275062759891));
#96599=CARTESIAN_POINT('Ctrl Pts',(-1.02284766825667,-2.13987906330876,
18.8281820851467));
#96600=CARTESIAN_POINT('Ctrl Pts',(-0.999251037581454,-2.15103508910312,
18.8299364826471));
#96601=CARTESIAN_POINT('Ctrl Pts',(-0.9847026112443,-2.15773384273846,18.8310181098449));
#96602=CARTESIAN_POINT('Ctrl Pts',(-0.921073066539403,-2.18625423359942,
18.8357494281989));
#96603=CARTESIAN_POINT('Ctrl Pts',(-0.871329977319599,-2.20655079836367,
18.8394504281182));
#96604=CARTESIAN_POINT('Ctrl Pts',(-0.733812991353957,-2.2572863752599,
18.8496962696139));
#96605=CARTESIAN_POINT('Ctrl Pts',(-0.644878152731193,-2.28428372151262,
18.8563411367774));
#96606=CARTESIAN_POINT('Ctrl Pts',(-0.449086783957416,-2.33137207037752,
18.8709415087171));
#96607=CARTESIAN_POINT('Ctrl Pts',(-0.341960694182375,-2.34947587670341,
18.8789139601156));
#96608=CARTESIAN_POINT('Ctrl Pts',(-0.211356979913292,-2.36242307796204,
18.8884367504633));
#96609=CARTESIAN_POINT('Ctrl Pts',(-0.188709467621251,-2.36433993965945,
18.8900806435221));
#96610=CARTESIAN_POINT('Ctrl Pts',(-0.144643633172765,-2.36743241347858,
18.8932611980413));
#96611=CARTESIAN_POINT('Ctrl Pts',(-0.123229842556786,-2.36864359223355,
18.8947985445297));
#96612=CARTESIAN_POINT('Ctrl Pts',(-0.0535526134322616,-2.37163708928384,
18.89976859173));
#96613=CARTESIAN_POINT('Ctrl Pts',(-0.00524690536728323,-2.3722359971031,
18.9031641156925));
#96614=CARTESIAN_POINT('Ctrl Pts',(0.0539314152003348,-2.37116173408091,
18.9072368714703));
#96615=CARTESIAN_POINT('Ctrl Pts',(0.0648143623579783,-2.37088921644014,
18.9079822380623));
#96616=CARTESIAN_POINT('Ctrl Pts',(0.081803807107464,-2.37034671545087,
18.9091397905149));
#96617=CARTESIAN_POINT('Ctrl Pts',(0.0879116174798878,-2.37012804801061,
18.9095547174014));
#96618=CARTESIAN_POINT('Ctrl Pts',(0.0992048811247318,-2.36968001930408,
18.9103195708558));
#96619=CARTESIAN_POINT('Ctrl Pts',(0.104390396130632,-2.36945724765325,
18.9106698451967));
#96620=CARTESIAN_POINT('Ctrl Pts',(0.116163107028454,-2.36891276476409,
18.9114630129342));
#96621=CARTESIAN_POINT('Ctrl Pts',(0.122749712598003,-2.36858060137621,
18.9119053185701));
#96622=CARTESIAN_POINT('Ctrl Pts',(0.142849447040167,-2.36748290055367,
18.9132508501642));
#96623=CARTESIAN_POINT('Ctrl Pts',(0.156357775466462,-2.36662914634799,
18.9141493223036));
#96624=CARTESIAN_POINT('Ctrl Pts',(0.300900624114397,-2.3562507208666,18.9237080823717));
#96625=CARTESIAN_POINT('Ctrl Pts',(0.430955604850893,-2.33596799301929,
18.9318298448764));
#96626=CARTESIAN_POINT('Ctrl Pts',(0.745155705811506,-2.25981372510544,
18.9516778417322));
#96627=CARTESIAN_POINT('Ctrl Pts',(0.925437117947199,-2.19216148062066,
18.9633216823021));
#96628=CARTESIAN_POINT('Ctrl Pts',(1.120297736124,-2.09067138269913,18.9775732889336));
#96629=CARTESIAN_POINT('Ctrl Pts',(1.14477142330908,-2.07737144721192,18.9793941266265));
#96630=CARTESIAN_POINT('Ctrl Pts',(1.17895076413854,-2.05800967793005,18.9819838009365));
#96631=CARTESIAN_POINT('Ctrl Pts',(1.18885610893811,-2.05230355533512,18.9827399340325));
#96632=CARTESIAN_POINT('Ctrl Pts',(1.20689403523592,-2.04173813095045,18.9841274225775));
#96633=CARTESIAN_POINT('Ctrl Pts',(1.21503953459712,-2.03690125744204,18.9847579574094));
#96634=CARTESIAN_POINT('Ctrl Pts',(1.23146198743714,-2.02701589253636,18.9860373950893));
#96635=CARTESIAN_POINT('Ctrl Pts',(1.23973739360127,-2.0219651938576,18.9866863699388));
#96636=CARTESIAN_POINT('Ctrl Pts',(1.26005055058218,-2.00939595543441,18.9882900287777));
#96637=CARTESIAN_POINT('Ctrl Pts',(1.27205209400526,-2.00181990963255,18.9892468194956));
#96638=CARTESIAN_POINT('Ctrl Pts',(1.3164001960882,-1.97326505529228,18.9928176640518));
#96639=CARTESIAN_POINT('Ctrl Pts',(1.34830018952424,-1.95160722210424,18.9954568533656));
#96640=CARTESIAN_POINT('Ctrl Pts',(1.42672009400098,-1.89552515993178,19.0021283868771));
#96641=CARTESIAN_POINT('Ctrl Pts',(1.4725325732193,-1.86015933209813,19.0061945277994));
#96642=CARTESIAN_POINT('Ctrl Pts',(1.60863985601224,-1.74690783626517,19.0187990021559));
#96643=CARTESIAN_POINT('Ctrl Pts',(1.69439032680061,-1.66386479894757,19.0274988529642));
#96644=CARTESIAN_POINT('Ctrl Pts',(1.85513170142364,-1.4828317884799,19.0451801493841));
#96645=CARTESIAN_POINT('Ctrl Pts',(1.92947686536043,-1.38471265401808,19.0541345733921));
#96646=CARTESIAN_POINT('Ctrl Pts',(2.00627662577104,-1.26507789468366,19.0640264443602));
#96647=CARTESIAN_POINT('Ctrl Pts',(2.01646992189924,-1.2487662280536,19.0653543167582));
#96648=CARTESIAN_POINT('Ctrl Pts',(2.03052734570979,-1.2256499975811,19.0672050916567));
#96649=CARTESIAN_POINT('Ctrl Pts',(2.03455763301484,-1.21894809593416,19.0677380517976));
#96650=CARTESIAN_POINT('Ctrl Pts',(2.04127502980425,-1.20765170541397,19.0686301578468));
#96651=CARTESIAN_POINT('Ctrl Pts',(2.04397992874673,-1.20306792896309,19.0689904401363));
#96652=CARTESIAN_POINT('Ctrl Pts',(2.04946456349759,-1.19370166418243,19.0697230816299));
#96653=CARTESIAN_POINT('Ctrl Pts',(2.05224303413521,-1.18891849617883,19.0700953592895));
#96654=CARTESIAN_POINT('Ctrl Pts',(2.05927616241807,-1.17671277037519,19.071040708387));
#96655=CARTESIAN_POINT('Ctrl Pts',(2.06350748505046,-1.16927675161346,19.071612295602));
#96656=CARTESIAN_POINT('Ctrl Pts',(2.08051541374976,-1.13900757518601,19.0739221230864));
#96657=CARTESIAN_POINT('Ctrl Pts',(2.09295460169205,-1.11598558235589,19.0756401315038));
#96658=CARTESIAN_POINT('Ctrl Pts',(2.12477794819871,-1.05468354674276,19.0801259700997));
#96659=CARTESIAN_POINT('Ctrl Pts',(2.1435094401328,-1.01607403925689,19.0828616548797));
#96660=CARTESIAN_POINT('Ctrl Pts',(2.24875445073026,-0.783259698496598,
19.0989549504641));
#96661=CARTESIAN_POINT('Ctrl Pts',(2.30988531194409,-0.578647529580843,
19.1115481072305));
#96662=CARTESIAN_POINT('Ctrl Pts',(2.35334942230048,-0.302389102565685,
19.1292140576278));
#96663=CARTESIAN_POINT('Ctrl Pts',(2.36095547297555,-0.235755413113114,
19.1335151208604));
#96664=CARTESIAN_POINT('Ctrl Pts',(2.36700870509727,-0.150966454101397,
19.1390821079322));
#96665=CARTESIAN_POINT('Ctrl Pts',(2.36808470633828,-0.133025840973636,
19.140265262001));
#96666=CARTESIAN_POINT('Ctrl Pts',(2.3694668286772,-0.104573230352077,19.1421506941763));
#96667=CARTESIAN_POINT('Ctrl Pts',(2.36990712491347,-0.0940681982777818,
19.1428487645939));
#96668=CARTESIAN_POINT('Ctrl Pts',(2.37057132597695,-0.0752275191216445,
19.1441043841442));
#96669=CARTESIAN_POINT('Ctrl Pts',(2.37082115024523,-0.0668929119218101,
19.1446611114527));
#96670=CARTESIAN_POINT('Ctrl Pts',(2.37130222529585,-0.0474138224384436,
19.1459653218307));
#96671=CARTESIAN_POINT('Ctrl Pts',(2.37149886862469,-0.0362687604916444,
19.1467138762243));
#96672=CARTESIAN_POINT('Ctrl Pts',(2.37183853270492,-0.00420425298295702,
19.1488744386249));
#96673=CARTESIAN_POINT('Ctrl Pts',(2.37178334471784,0.0167157921117499,
19.150292598664));
#96674=CARTESIAN_POINT('Ctrl Pts',(2.3688273780653,0.202992601673781,19.1629996234797));
#96675=CARTESIAN_POINT('Ctrl Pts',(2.34891567886943,0.367591883083198,19.174834131301));
#96676=CARTESIAN_POINT('Ctrl Pts',(2.27593733976225,0.686702966076191,19.1986951394924));
#96677=CARTESIAN_POINT('Ctrl Pts',(2.22372148604837,0.840549176717783,19.2106419894999));
#96678=CARTESIAN_POINT('Ctrl Pts',(2.14868564190265,1.00432836779843,19.2231611152709));
#96679=CARTESIAN_POINT('Ctrl Pts',(2.14096083079876,1.02069203435124,19.2244092094301));
#96680=CARTESIAN_POINT('Ctrl Pts',(2.1300394736735,1.0431573663133,19.2261173166618));
#96681=CARTESIAN_POINT('Ctrl Pts',(2.12700274607811,1.04933539513049,19.2265864839681));
#96682=CARTESIAN_POINT('Ctrl Pts',(2.12174885205832,1.05990758724572,19.2273882645834));
#96683=CARTESIAN_POINT('Ctrl Pts',(2.11954484977422,1.0643081864028,19.2277216759355));
#96684=CARTESIAN_POINT('Ctrl Pts',(2.11492146784913,1.07346809490425,19.2284149500984));
#96685=CARTESIAN_POINT('Ctrl Pts',(2.11249969904126,1.07822613037188,19.2287746485647));
#96686=CARTESIAN_POINT('Ctrl Pts',(2.10657728251937,1.08976531998421,19.2296460683405));
#96687=CARTESIAN_POINT('Ctrl Pts',(2.10305989129882,1.0965379143184,19.2301567486535));
#96688=CARTESIAN_POINT('Ctrl Pts',(2.09046457048215,1.12050615022578,19.231961717272));
#96689=CARTESIAN_POINT('Ctrl Pts',(2.08120763434184,1.13760757581048,19.2332452939246));
#96690=CARTESIAN_POINT('Ctrl Pts',(2.05779695554892,1.17961443592142,19.2363924265068));
#96691=CARTESIAN_POINT('Ctrl Pts',(2.04340005809985,1.20438153795247,19.2382428803413));
#96692=CARTESIAN_POINT('Ctrl Pts',(1.9202798697087,1.4076200712671,19.2534368949746));
#96693=CARTESIAN_POINT('Ctrl Pts',(1.7888471003349,1.57127770350817,19.2658063500539));
#96694=CARTESIAN_POINT('Ctrl Pts',(1.57206888208808,1.77820637888635,19.284520110327));
#96695=CARTESIAN_POINT('Ctrl Pts',(1.50295663019337,1.83699126730792,19.2902815955152));
#96696=CARTESIAN_POINT('Ctrl Pts',(1.4165512462419,1.90233891104908,19.297364011117));
#96697=CARTESIAN_POINT('Ctrl Pts',(1.40232869095856,1.91284734893101,19.2985259672059));
#96698=CARTESIAN_POINT('Ctrl Pts',(1.3786857315032,1.92991071927386,19.3004520596908));
#96699=CARTESIAN_POINT('Ctrl Pts',(1.36933272425729,1.9365581873643,19.3012126168562));
#96700=CARTESIAN_POINT('Ctrl Pts',(1.35234826184569,1.94844500163773,19.3025914346006));
#96701=CARTESIAN_POINT('Ctrl Pts',(1.34473362532725,1.95370806889323,19.3032087728965));
#96702=CARTESIAN_POINT('Ctrl Pts',(1.32834474694658,1.96489449257834,19.3045358068088));
#96703=CARTESIAN_POINT('Ctrl Pts',(1.31956129249625,1.97080392803043,19.3052460117351));
#96704=CARTESIAN_POINT('Ctrl Pts',(1.29548507654745,1.98676910116397,19.3071901969432));
#96705=CARTESIAN_POINT('Ctrl Pts',(1.2801152756355,1.99670676194119,19.3084285538078));
#96706=CARTESIAN_POINT('Ctrl Pts',(1.1950882629761,2.05029747795338,19.3152656418944));
#96707=CARTESIAN_POINT('Ctrl Pts',(1.12332058878302,2.09047930759519,19.320989837225));
#96708=CARTESIAN_POINT('Ctrl Pts',(0.860833226062364,2.22001905152122,19.3417736551214));
#96709=CARTESIAN_POINT('Ctrl Pts',(0.660513824287204,2.28762388462553,19.3574606796617));
#96710=CARTESIAN_POINT('Ctrl Pts',(0.404380602763094,2.3375675237912,19.3760821309725));
#96711=CARTESIAN_POINT('Ctrl Pts',(0.354540247288059,2.34564441116114,19.3796348894492));
#96712=CARTESIAN_POINT('Ctrl Pts',(0.294495923733967,2.35341698054325,19.3838020314702));
#96713=CARTESIAN_POINT('Ctrl Pts',(0.284507502669724,2.35464537103996,19.384491503903));
#96714=CARTESIAN_POINT('Ctrl Pts',(0.268102744439084,2.35655693942311,19.3856174245552));
#96715=CARTESIAN_POINT('Ctrl Pts',(0.261691026148367,2.3572775610152,19.3860558699821));
#96716=CARTESIAN_POINT('Ctrl Pts',(0.250123689809365,2.35852985213008,19.3868438589733));
#96717=CARTESIAN_POINT('Ctrl Pts',(0.244969232779565,2.35907079167362,19.3871939075083));
#96718=CARTESIAN_POINT('Ctrl Pts',(0.23361661373494,2.360224593243,19.3879625016301));
#96719=CARTESIAN_POINT('Ctrl Pts',(0.227417803490441,2.36082993832145,19.388380623408));
#96720=CARTESIAN_POINT('Ctrl Pts',(0.209528703472811,2.36250578633685,19.3895829963485));
#96721=CARTESIAN_POINT('Ctrl Pts',(0.197832548232664,2.36351394433449,19.390363855012));
#96722=CARTESIAN_POINT('Ctrl Pts',(0.111694493764132,2.37029475925463,19.3960790336162));
#96723=CARTESIAN_POINT('Ctrl Pts',(0.0370159239255071,2.37263677720445,
19.4008389510381));
#96724=CARTESIAN_POINT('Ctrl Pts',(-0.202184964010994,2.36883847254191,
19.4158134530331));
#96725=CARTESIAN_POINT('Ctrl Pts',(-0.365998432568143,2.34911136622944,
19.4256854104883));
#96726=CARTESIAN_POINT('Ctrl Pts',(-0.623700839572435,2.2904457886415,19.4421285496156));
#96727=CARTESIAN_POINT('Ctrl Pts',(-0.719441000451815,2.26219926962089,
19.448443855865));
#96728=CARTESIAN_POINT('Ctrl Pts',(-0.830070648555137,2.22182508104026,
19.4561397668617));
#96729=CARTESIAN_POINT('Ctrl Pts',(-0.846957936076613,2.21544266393317,
19.4573256330484));
#96730=CARTESIAN_POINT('Ctrl Pts',(-0.874562108324556,2.20464814710041,
19.4592831938697));
#96731=CARTESIAN_POINT('Ctrl Pts',(-0.885322637395361,2.20034909809023,
19.460051101131));
#96732=CARTESIAN_POINT('Ctrl Pts',(-0.904630071332128,2.19247083218566,
19.4614378467492));
#96733=CARTESIAN_POINT('Ctrl Pts',(-0.913188376840121,2.188920030553,19.4620557146923));
#96734=CARTESIAN_POINT('Ctrl Pts',(-0.921884193083915,2.18525230275268,
19.4626868015243));
#96735=CARTESIAN_POINT('Ctrl Pts',(-0.92204282604314,2.18518537407842,19.4626983152102));
#96736=CARTESIAN_POINT('Ctrl Pts',(-0.922346631466237,2.18505715686209,
19.4627203677528));
#96737=CARTESIAN_POINT('Ctrl Pts',(-0.922491805121438,2.18499587112084,
19.4627309065144));
#96738=CARTESIAN_POINT('Ctrl Pts',(-0.9227698706679,2.18487845179058,19.4627510942486));
#96739=CARTESIAN_POINT('Ctrl Pts',(-0.922902763550764,2.1848223205427,19.4627607431415));
#96740=CARTESIAN_POINT('Ctrl Pts',(-0.923157339105347,2.18471476564036,
19.4627792284981));
#96741=CARTESIAN_POINT('Ctrl Pts',(-0.923279022605258,2.18466334394298,
19.4627880648951));
#96742=CARTESIAN_POINT('Ctrl Pts',(-0.923512153708541,2.18456480313434,
19.4628049956431));
#96743=CARTESIAN_POINT('Ctrl Pts',(-0.923623602006379,2.18451768565913,
19.4628130899383));
#96744=CARTESIAN_POINT('Ctrl Pts',(-0.923837148880787,2.18442738426728,
19.4628286005348));
#96745=CARTESIAN_POINT('Ctrl Pts',(-0.923939248037813,2.18438420172008,
19.4628360167893));
#96746=CARTESIAN_POINT('Ctrl Pts',(-0.924134902921061,2.18430143387371,
19.4628502296128));
#96747=CARTESIAN_POINT('Ctrl Pts',(-0.924228459140427,2.18426184971825,
19.462857026143));
#96748=CARTESIAN_POINT('Ctrl Pts',(-0.924407762068903,2.18418597207209,
19.4628700526178));
#96749=CARTESIAN_POINT('Ctrl Pts',(-0.924493509197177,2.1841496795371,19.4628762825303));
#96750=CARTESIAN_POINT('Ctrl Pts',(-0.924657862316789,2.18408010554611,
19.4628882241481));
#96751=CARTESIAN_POINT('Ctrl Pts',(-0.924736468648707,2.18404682489586,
19.4628939358259));
#96752=CARTESIAN_POINT('Ctrl Pts',(-0.924887149132199,2.18398301962184,
19.4629048850696));
#96753=CARTESIAN_POINT('Ctrl Pts',(-0.924959223556996,2.18395249567917,
19.4629101226115));
#96754=CARTESIAN_POINT('Ctrl Pts',(-0.925097395246018,2.1838939710897,19.4629201637881));
#96755=CARTESIAN_POINT('Ctrl Pts',(-0.925163492758077,2.18386597100659,
19.462924967404));
#96756=CARTESIAN_POINT('Ctrl Pts',(-0.925330229361803,2.18379532948391,
19.462937085426));
#96757=CARTESIAN_POINT('Ctrl Pts',(-0.925430866752822,2.18375268409855,
19.4629443999654));
#96758=CARTESIAN_POINT('Ctrl Pts',(-0.925630249183668,2.1836681789592,19.4629588923997));
#96759=CARTESIAN_POINT('Ctrl Pts',(-0.925728994335965,2.18362631946232,
19.462966070286));
#96760=CARTESIAN_POINT('Ctrl Pts',(-0.925924639110301,2.18354336715959,
19.4629802927676));
#96761=CARTESIAN_POINT('Ctrl Pts',(-0.926021538843426,2.18350227459836,
19.4629873373549));
#96762=CARTESIAN_POINT('Ctrl Pts',(-0.926213538302597,2.18342083773069,
19.4630012965003));
#96763=CARTESIAN_POINT('Ctrl Pts',(-0.926308638126264,2.18338049366213,
19.4630082110502));
#96764=CARTESIAN_POINT('Ctrl Pts',(-0.926497081956118,2.18330053586517,
19.4630219132879));
#96765=CARTESIAN_POINT('Ctrl Pts',(-0.926590426071098,2.18326092235805,
19.463028700969));
#96766=CARTESIAN_POINT('Ctrl Pts',(-0.936804601029095,2.17892544334773,
19.463771485232));
#96767=CARTESIAN_POINT('Ctrl Pts',(-0.946895289193552,2.17455932372564,
19.4645098683679));
#96768=CARTESIAN_POINT('Ctrl Pts',(-0.975676854756248,2.16186757175691,
19.4666292988969));
#96769=CARTESIAN_POINT('Ctrl Pts',(-0.994290451729112,2.1533701898398,19.4680161922149));
#96770=CARTESIAN_POINT('Ctrl Pts',(-1.03609773427408,2.13362693034339,19.4711689141561));
#96771=CARTESIAN_POINT('Ctrl Pts',(-1.05922239361368,2.12224179187999,19.472939394091));
#96772=CARTESIAN_POINT('Ctrl Pts',(-1.13312783338187,2.08434655753697,19.4786855659897));
#96773=CARTESIAN_POINT('Ctrl Pts',(-1.18313208579832,2.05637467735449,19.4827096826433));
#96774=CARTESIAN_POINT('Ctrl Pts',(-1.34789701557225,1.9562069269485,19.496430628623));
#96775=CARTESIAN_POINT('Ctrl Pts',(-1.45746398793284,1.87599691445871,19.5063566201135));
#96776=CARTESIAN_POINT('Ctrl Pts',(-1.64794564657305,1.70974644259325,19.5248002727797));
#96777=CARTESIAN_POINT('Ctrl Pts',(-1.73048844658271,1.6261532402266,19.5332973220643));
#96778=CARTESIAN_POINT('Ctrl Pts',(-1.81479087967416,1.52705445754513,19.5422756807723));
#96779=CARTESIAN_POINT('Ctrl Pts',(-1.82298972662788,1.51725730452842,19.5431522655787));
#96780=CARTESIAN_POINT('Ctrl Pts',(-1.83525806332084,1.50235432429424,19.5444685024982));
#96781=CARTESIAN_POINT('Ctrl Pts',(-1.83938612578529,1.49729735108902,19.5449121867768));
#96782=CARTESIAN_POINT('Ctrl Pts',(-1.84675626641251,1.48819227625998,19.5457056655387));
#96783=CARTESIAN_POINT('Ctrl Pts',(-1.85000597951484,1.4841505436037,19.5460559992093));
#96784=CARTESIAN_POINT('Ctrl Pts',(-1.857089269066,1.47528150057555,19.5468206271378));
#96785=CARTESIAN_POINT('Ctrl Pts',(-1.86091728860406,1.47044989931184,19.5472345271177));
#96786=CARTESIAN_POINT('Ctrl Pts',(-1.87179400487539,1.45661116132722,19.5484126680337));
#96787=CARTESIAN_POINT('Ctrl Pts',(-1.87879656764788,1.44756773330525,19.5491737248964));
#96788=CARTESIAN_POINT('Ctrl Pts',(-1.92607970393777,1.38558300980043,19.5543329012951));
#96789=CARTESIAN_POINT('Ctrl Pts',(-1.96418711655136,1.33101245336678,19.5585929418024));
#96790=CARTESIAN_POINT('Ctrl Pts',(-2.07840825189903,1.15183306441105,19.5719554566838));
#96791=CARTESIAN_POINT('Ctrl Pts',(-2.14533942665075,1.02177488207393,19.5807552380452));
#96792=CARTESIAN_POINT('Ctrl Pts',(-2.22354038883136,0.827689724622768,
19.5936650268779));
#96793=CARTESIAN_POINT('Ctrl Pts',(-2.24482944561364,0.768076948163438,
19.5975994103254));
#96794=CARTESIAN_POINT('Ctrl Pts',(-2.28379299174548,0.643442580024122,
19.6058471351649));
#96795=CARTESIAN_POINT('Ctrl Pts',(-2.30113161261755,0.578377694243966,
19.6101649591812));
#96796=CARTESIAN_POINT('Ctrl Pts',(-2.31956902568924,0.495097419101356,
19.6157509306108));
#96797=CARTESIAN_POINT('Ctrl Pts',(-2.32325877702115,0.477483554385752,
19.6169355980639));
#96798=CARTESIAN_POINT('Ctrl Pts',(-2.32878712481555,0.449510008111972,
19.6188228898157));
#96799=CARTESIAN_POINT('Ctrl Pts',(-2.3307578939416,0.439176904965135,19.6195212920108));
#96800=CARTESIAN_POINT('Ctrl Pts',(-2.33416737018052,0.420630799270693,
19.6207772011715));
#96801=CARTESIAN_POINT('Ctrl Pts',(-2.33563163988689,0.412422624268697,
19.6213338839945));
#96802=CARTESIAN_POINT('Ctrl Pts',(-2.33855590238336,0.395515061029755,
19.6224823656931));
#96803=CARTESIAN_POINT('Ctrl Pts',(-2.34001070242373,0.386814918227326,
19.6230743202251));
#96804=CARTESIAN_POINT('Ctrl Pts',(-2.34315544535991,0.367341184528241,
19.6244015793265));
#96805=CARTESIAN_POINT('Ctrl Pts',(-2.34481967442248,0.35656370325153,19.6251376861328));
#96806=CARTESIAN_POINT('Ctrl Pts',(-2.34880486843972,0.329520425336842,
19.6269887985295));
#96807=CARTESIAN_POINT('Ctrl Pts',(-2.35103121423866,0.31324148301411,19.628106753869));
#96808=CARTESIAN_POINT('Ctrl Pts',(-2.35828550765783,0.25575535628729,19.6320680853066));
#96809=CARTESIAN_POINT('Ctrl Pts',(-2.36239902303451,0.214452987595711,
19.6349387342668));
#96810=CARTESIAN_POINT('Ctrl Pts',(-2.36542650053005,0.173076668243166,
19.6378399312857));
#96811=CARTESIAN_POINT('Origin',(0.,0.,-1.84858989190503));
#96812=CARTESIAN_POINT('',(-2.3654264754702,0.173077010733998,20.8359749974364));
#96813=CARTESIAN_POINT('',(-2.36542650966497,0.173076543396847,20.6413652673669));
#96814=CARTESIAN_POINT('',(-2.36542649454111,0.173076750093529,-1.84858989190503));
#96815=CARTESIAN_POINT('',(-2.37174975346702,-0.0010814014724484,19.8466119453452));
#96816=CARTESIAN_POINT('Ctrl Pts',(-2.3654264754702,0.173077010733998,20.8359749974364));
#96817=CARTESIAN_POINT('Ctrl Pts',(-2.35906927455258,0.259960250146641,
20.8296422157243));
#96818=CARTESIAN_POINT('Ctrl Pts',(-2.34792654946133,0.346475014108061,
20.8233719415871));
#96819=CARTESIAN_POINT('Ctrl Pts',(-2.32859917105788,0.450753822994609,
20.8159958757342));
#96820=CARTESIAN_POINT('Ctrl Pts',(-2.32494449007119,0.469240111977688,
20.8146954084924));
#96821=CARTESIAN_POINT('Ctrl Pts',(-2.31948832425912,0.495208164514945,
20.8128805280791));
#96822=CARTESIAN_POINT('Ctrl Pts',(-2.31787028340761,0.502727128830011,
20.8123564483484));
#96823=CARTESIAN_POINT('Ctrl Pts',(-2.31508770824918,0.515358570198658,
20.8114785537713));
#96824=CARTESIAN_POINT('Ctrl Pts',(-2.31394275441837,0.520475248111737,
20.8111236410527));
#96825=CARTESIAN_POINT('Ctrl Pts',(-2.31157221070702,0.530906510228892,
20.8104015748021));
#96826=CARTESIAN_POINT('Ctrl Pts',(-2.31034524259327,0.536220728326226,
20.810034502292));
#96827=CARTESIAN_POINT('Ctrl Pts',(-2.30717339198383,0.549745574775442,
20.8091021816128));
#96828=CARTESIAN_POINT('Ctrl Pts',(-2.30520298505307,0.557950231474603,
20.8085383798383));
#96829=CARTESIAN_POINT('Ctrl Pts',(-2.29702814398103,0.591207124766822,
20.8062596244083));
#96830=CARTESIAN_POINT('Ctrl Pts',(-2.2904584936035,0.616168957468834,20.8045644019244));
#96831=CARTESIAN_POINT('Ctrl Pts',(-2.22920453016805,0.83437179189627,20.7898388695554));
#96832=CARTESIAN_POINT('Ctrl Pts',(-2.15058191588978,1.02007361119127,20.7778968074392));
#96833=CARTESIAN_POINT('Ctrl Pts',(-1.99014054526828,1.29554627669857,20.758187094471));
#96834=CARTESIAN_POINT('Ctrl Pts',(-1.9232945957011,1.39285024101216,20.7507732273953));
#96835=CARTESIAN_POINT('Ctrl Pts',(-1.83792938887508,1.49918482565912,20.7418666647132));
#96836=CARTESIAN_POINT('Ctrl Pts',(-1.82619257781649,1.51345968459105,20.7406531936883));
#96837=CARTESIAN_POINT('Ctrl Pts',(-1.80679931842709,1.53649261593003,20.73866505213));
#96838=CARTESIAN_POINT('Ctrl Pts',(-1.79924298996926,1.54533426505339,20.7378944597733));
#96839=CARTESIAN_POINT('Ctrl Pts',(-1.78562401180971,1.56103450953162,20.7365125881501));
#96840=CARTESIAN_POINT('Ctrl Pts',(-1.77958606911388,1.56791430571702,20.7359023405736));
#96841=CARTESIAN_POINT('Ctrl Pts',(-1.76671853144158,1.58240584967211,20.7346067804124));
#96842=CARTESIAN_POINT('Ctrl Pts',(-1.75987924614014,1.59000870303565,20.7339210680778));
#96843=CARTESIAN_POINT('Ctrl Pts',(-1.74148193689602,1.61019584987692,20.7320840564289));
#96844=CARTESIAN_POINT('Ctrl Pts',(-1.72983691286378,1.62269967636549,20.7309290738201));
#96845=CARTESIAN_POINT('Ctrl Pts',(-1.67173016327922,1.68375540155034,20.7252027804125));
#96846=CARTESIAN_POINT('Ctrl Pts',(-1.62335880857015,1.73043884528232,20.7205489395811));
#96847=CARTESIAN_POINT('Ctrl Pts',(-1.45060856863031,1.88353672878001,20.7042874639698));
#96848=CARTESIAN_POINT('Ctrl Pts',(-1.31725079592528,1.97909402131459,20.6922926552741));
#96849=CARTESIAN_POINT('Ctrl Pts',(-1.07793968154945,2.11560094712487,20.6722069828031));
#96850=CARTESIAN_POINT('Ctrl Pts',(-0.976919177969611,2.16410640602832,
20.6641171364737));
#96851=CARTESIAN_POINT('Ctrl Pts',(-0.861075649258256,2.20995630069271,
20.6555209075231));
#96852=CARTESIAN_POINT('Ctrl Pts',(-0.849274572321439,2.21451819665596,
20.6546528650766));
#96853=CARTESIAN_POINT('Ctrl Pts',(-0.831404539800097,2.22126228314383,
20.6533505452796));
#96854=CARTESIAN_POINT('Ctrl Pts',(-0.825362496542031,2.22351442341369,
20.6529122984383));
#96855=CARTESIAN_POINT('Ctrl Pts',(-0.81451341350607,2.22750804715898,20.6521292040489));
#96856=CARTESIAN_POINT('Ctrl Pts',(-0.809709878643328,2.22925864694746,
20.6517838256317));
#96857=CARTESIAN_POINT('Ctrl Pts',(-0.799201015227734,2.23305004713406,
20.6510311691658));
#96858=CARTESIAN_POINT('Ctrl Pts',(-0.793493521826344,2.23508451935296,
20.6506242672763));
#96859=CARTESIAN_POINT('Ctrl Pts',(-0.777222111719395,2.24081438339896,
20.6494693979082));
#96860=CARTESIAN_POINT('Ctrl Pts',(-0.766639571371292,2.2444569703462,20.6487244741959));
#96861=CARTESIAN_POINT('Ctrl Pts',(-0.695987644065285,2.26821786440349,
20.6437896873907));
#96862=CARTESIAN_POINT('Ctrl Pts',(-0.635152638383065,2.28599953161763,
20.6397252639053));
#96863=CARTESIAN_POINT('Ctrl Pts',(-0.37141131917774,2.35174476863999,20.6225982372617));
#96864=CARTESIAN_POINT('Ctrl Pts',(-0.163381961725513,2.37528247478567,
20.6102413128642));
#96865=CARTESIAN_POINT('Ctrl Pts',(0.11672035919401,2.36996032203786,20.5925869933682));
#96866=CARTESIAN_POINT('Ctrl Pts',(0.188278919168975,2.36535093343878,20.5879969017559));
#96867=CARTESIAN_POINT('Ctrl Pts',(0.277378099973835,2.35554291938324,20.5821281350748));
#96868=CARTESIAN_POINT('Ctrl Pts',(0.295218844093893,2.35337350626273,20.5809453477241));
#96869=CARTESIAN_POINT('Ctrl Pts',(0.323465733506921,2.3496124695966,20.5790597551683));
#96870=CARTESIAN_POINT('Ctrl Pts',(0.3338891467691,2.34815392800814,20.578361155657));
#96871=CARTESIAN_POINT('Ctrl Pts',(0.352419489143528,2.34543511363328,20.5771140876956));
#96872=CARTESIAN_POINT('Ctrl Pts',(0.36053028958553,2.34420205527712,20.5765664899889));
#96873=CARTESIAN_POINT('Ctrl Pts',(0.379291805892951,2.34125013179166,20.575295674811));
#96874=CARTESIAN_POINT('Ctrl Pts',(0.389937448119666,2.339500637635,20.5745714957796));
#96875=CARTESIAN_POINT('Ctrl Pts',(0.41996260869426,2.3343557055748,20.5725200644883));
#96876=CARTESIAN_POINT('Ctrl Pts',(0.439311957437699,2.3307917358935,20.5711874907284));
#96877=CARTESIAN_POINT('Ctrl Pts',(0.571773642710384,2.30468553098584,20.5619901144981));
#96878=CARTESIAN_POINT('Ctrl Pts',(0.683137386115929,2.2741627751318,20.5538703865256));
#96879=CARTESIAN_POINT('Ctrl Pts',(0.905400110717562,2.19544210067263,20.5368944548262));
#96880=CARTESIAN_POINT('Ctrl Pts',(1.01574079824913,2.14662140507074,20.5280453296828));
#96881=CARTESIAN_POINT('Ctrl Pts',(1.21195892616301,2.04127533204025,20.5118360253846));
#96882=CARTESIAN_POINT('Ctrl Pts',(1.29882140538037,1.98713803687843,20.5044731720221));
#96883=CARTESIAN_POINT('Ctrl Pts',(1.39218300474642,1.92020409852209,20.4965473446824));
#96884=CARTESIAN_POINT('Ctrl Pts',(1.40238000334442,1.91276962610964,20.4956815754885));
#96885=CARTESIAN_POINT('Ctrl Pts',(1.41769162355744,1.90141789464161,20.4943819857503));
#96886=CARTESIAN_POINT('Ctrl Pts',(1.42285021956747,1.89756075126635,20.4939442197611));
#96887=CARTESIAN_POINT('Ctrl Pts',(1.43207484402695,1.8906046223241,20.4931616351831));
#96888=CARTESIAN_POINT('Ctrl Pts',(1.43614660729585,1.8875134756641,20.4928162888128));
#96889=CARTESIAN_POINT('Ctrl Pts',(1.44502702284024,1.88072638798975,20.4920632948543));
#96890=CARTESIAN_POINT('Ctrl Pts',(1.44983149845559,1.87702516536037,20.491656025981));
#96891=CARTESIAN_POINT('Ctrl Pts',(1.46348184788285,1.86642566852043,20.4904990632767));
#96892=CARTESIAN_POINT('Ctrl Pts',(1.47229320199399,1.85948289450991,20.4897524306007));
#96893=CARTESIAN_POINT('Ctrl Pts',(1.53100774530896,1.81254064043229,20.484775983401));
#96894=CARTESIAN_POINT('Ctrl Pts',(1.57932980252574,1.77059519894959,20.4806740538275));
#96895=CARTESIAN_POINT('Ctrl Pts',(1.7825895915519,1.57920576902224,20.4630891451906));
#96896=CARTESIAN_POINT('Ctrl Pts',(1.91847068255332,1.41102724016807,20.4503510646682));
#96897=CARTESIAN_POINT('Ctrl Pts',(2.06353987079851,1.17100553976515,20.4326163050924));
#96898=CARTESIAN_POINT('Ctrl Pts',(2.09495308212083,1.11383173663211,20.4284291288387));
#96899=CARTESIAN_POINT('Ctrl Pts',(2.1318374261876,1.03960564498066,20.4229994969871));
#96900=CARTESIAN_POINT('Ctrl Pts',(2.1395284123607,1.0236839616395,20.4218352670797));
#96901=CARTESIAN_POINT('Ctrl Pts',(2.15144089151315,0.998302270361539,20.4199792806134));
#96902=CARTESIAN_POINT('Ctrl Pts',(2.15577977170574,0.988897822215872,20.4192915960795));
#96903=CARTESIAN_POINT('Ctrl Pts',(2.16345130160985,0.971979469540694,20.4180543250497));
#96904=CARTESIAN_POINT('Ctrl Pts',(2.16680677065702,0.964476043945466,20.417505534867));
#96905=CARTESIAN_POINT('Ctrl Pts',(2.17455904611944,0.946895922492694,20.4162195496063));
#96906=CARTESIAN_POINT('Ctrl Pts',(2.17892489492178,0.936805864786943,20.4154813094975));
#96907=CARTESIAN_POINT('Ctrl Pts',(2.1912878093185,0.907679528996994,20.413349628599));
#96908=CARTESIAN_POINT('Ctrl Pts',(2.19910647662195,0.88856910139725,20.4119501835738));
#96909=CARTESIAN_POINT('Ctrl Pts',(2.26481621799933,0.721779644783481,20.399726110056));
#96910=CARTESIAN_POINT('Ctrl Pts',(2.30799520922596,0.568768999435616,20.3884016590865));
#96911=CARTESIAN_POINT('Ctrl Pts',(2.36525079026029,0.244685088851014,20.3644364943913));
#96912=CARTESIAN_POINT('Ctrl Pts',(2.37672272697818,0.0740247741490599,
20.3518315184729));
#96913=CARTESIAN_POINT('Ctrl Pts',(2.36908472454218,-0.113740156497965,
20.3387835171047));
#96914=CARTESIAN_POINT('Ctrl Pts',(2.36818900036583,-0.131073102270997,
20.3375871595422));
#96915=CARTESIAN_POINT('Ctrl Pts',(2.36668273439652,-0.155100057815818,
20.3359414593089));
#96916=CARTESIAN_POINT('Ctrl Pts',(2.36623391596791,-0.16180312401547,20.3354837121452));
#96917=CARTESIAN_POINT('Ctrl Pts',(2.3654131937711,-0.173325850829405,20.3346992974161));
#96918=CARTESIAN_POINT('Ctrl Pts',(2.36505502871858,-0.17814640059247,20.3343718782056));
#96919=CARTESIAN_POINT('Ctrl Pts',(2.36427513419983,-0.188225890041623,
20.333688862687));
#96920=CARTESIAN_POINT('Ctrl Pts',(2.36385059213733,-0.193484559306545,
20.3333334362796));
#96921=CARTESIAN_POINT('Ctrl Pts',(2.36277258846945,-0.206304021010512,
20.3324691292034));
#96922=CARTESIAN_POINT('Ctrl Pts',(2.36210037067516,-0.213863266508053,
20.3319612915524));
#96923=CARTESIAN_POINT('Ctrl Pts',(2.35956311497801,-0.24092258496678,20.3301495121948));
#96924=CARTESIAN_POINT('Ctrl Pts',(2.35749273268513,-0.260403269760521,
20.3288565057438));
#96925=CARTESIAN_POINT('Ctrl Pts',(2.35175534908219,-0.308687161605983,
20.3256748958064));
#96926=CARTESIAN_POINT('Ctrl Pts',(2.34780029798639,-0.337453569321867,
20.3237998958705));
#96927=CARTESIAN_POINT('Ctrl Pts',(2.3112031329413,-0.571676667139665,20.3086480735083));
#96928=CARTESIAN_POINT('Ctrl Pts',(2.25218535280696,-0.772109749905612,
20.2963329124854));
#96929=CARTESIAN_POINT('Ctrl Pts',(2.13063902886255,-1.0459197527264,20.2776323969683));
#96930=CARTESIAN_POINT('Ctrl Pts',(2.08870920028371,-1.12732499737327,20.2718191207217));
#96931=CARTESIAN_POINT('Ctrl Pts',(2.03325350200847,-1.22122348757576,20.2646890642057));
#96932=CARTESIAN_POINT('Ctrl Pts',(2.0241534182703,-1.2362481635703,20.2635347699027));
#96933=CARTESIAN_POINT('Ctrl Pts',(2.00889847146728,-1.26081476942052,20.2616244223404));
#96934=CARTESIAN_POINT('Ctrl Pts',(2.00284037568124,-1.27041622052866,20.2608719248443));
#96935=CARTESIAN_POINT('Ctrl Pts',(1.99178793756484,-1.28765763323158,20.2595098310332));
#96936=CARTESIAN_POINT('Ctrl Pts',(1.98681795296427,-1.29531300712061,20.2589011495377));
#96937=CARTESIAN_POINT('Ctrl Pts',(1.97608881722333,-1.31163229529747,20.2575951225793));
#96938=CARTESIAN_POINT('Ctrl Pts',(1.97031661808154,-1.32028735892578,20.2568972956639));
#96939=CARTESIAN_POINT('Ctrl Pts',(1.95446228495629,-1.34372444840439,20.2549933638179));
#96940=CARTESIAN_POINT('Ctrl Pts',(1.94426968524244,-1.35843055653313,20.25378309262));
#96941=CARTESIAN_POINT('Ctrl Pts',(1.88851668075994,-1.43695922447999,20.247234351778));
#96942=CARTESIAN_POINT('Ctrl Pts',(1.83998356905705,-1.49860103601939,20.2417819080904));
#96943=CARTESIAN_POINT('Ctrl Pts',(1.66668429209244,-1.69757401982479,20.2230829528693));
#96944=CARTESIAN_POINT('Ctrl Pts',(1.52889849982726,-1.8226488896822,20.2093639836792));
#96945=CARTESIAN_POINT('Ctrl Pts',(1.35750560841799,-1.94499602308788,20.1941397102244));
#96946=CARTESIAN_POINT('Ctrl Pts',(1.336797225773,-1.95928666939635,20.1923287640153));
#96947=CARTESIAN_POINT('Ctrl Pts',(1.27035869997588,-2.00359140540216,20.1866165934868));
#96948=CARTESIAN_POINT('Ctrl Pts',(1.22381204774047,-2.03235698783164,20.1827585995803));
#96949=CARTESIAN_POINT('Ctrl Pts',(1.16744848050704,-2.06454988057956,20.1782898329272));
#96950=CARTESIAN_POINT('Ctrl Pts',(1.15855601276231,-2.06955312537316,20.1775906349952));
#96951=CARTESIAN_POINT('Ctrl Pts',(1.14399242168159,-2.07762387457363,20.176455361126));
#96952=CARTESIAN_POINT('Ctrl Pts',(1.13834070442529,-2.08072585128843,20.17601719062));
#96953=CARTESIAN_POINT('Ctrl Pts',(1.12818450280728,-2.08624637277283,20.1752341772116));
#96954=CARTESIAN_POINT('Ctrl Pts',(1.12368480130221,-2.08867342330638,20.1748888039305));
#96955=CARTESIAN_POINT('Ctrl Pts',(1.11383423901974,-2.09394557579926,20.17413609411));
#96956=CARTESIAN_POINT('Ctrl Pts',(1.1084803173339,-2.09678472299646,20.1737291341348));
#96957=CARTESIAN_POINT('Ctrl Pts',(1.09320453468374,-2.10481050200625,20.1725739335356));
#96958=CARTESIAN_POINT('Ctrl Pts',(1.0832565831071,-2.10994753288132,20.1718287394263));
#96959=CARTESIAN_POINT('Ctrl Pts',(1.01669624306915,-2.14372384502187,20.1668873993031));
#96960=CARTESIAN_POINT('Ctrl Pts',(0.958984929635194,-2.17015500306125,
20.1628170759069));
#96961=CARTESIAN_POINT('Ctrl Pts',(0.706475735500689,-2.2737572008258,20.1456202483129));
#96962=CARTESIAN_POINT('Ctrl Pts',(0.50299071127396,-2.32724963424059,20.133205352057));
#96963=CARTESIAN_POINT('Ctrl Pts',(0.224954368997793,-2.36211628032176,
20.1155380103127));
#96964=CARTESIAN_POINT('Ctrl Pts',(0.154442925865272,-2.36777187445222,
20.1110080427819));
#96965=CARTESIAN_POINT('Ctrl Pts',(0.0659145624144746,-2.37090135402565,
20.1052077250694));
#96966=CARTESIAN_POINT('Ctrl Pts',(0.0480338915409297,-2.37133099254882,
20.104030536922));
#96967=CARTESIAN_POINT('Ctrl Pts',(0.0196461015713497,-2.37169189668111,
20.1021518827972));
#96968=CARTESIAN_POINT('Ctrl Pts',(0.00914110871235234,-2.37175564849506,
20.1014545696869));
#96969=CARTESIAN_POINT('Ctrl Pts',(-0.0104810265275968,-2.37174436524865,
20.1001479721044));
#96970=CARTESIAN_POINT('Ctrl Pts',(-0.01959801657848,-2.37168655174857,
20.0995392389858));
#96971=CARTESIAN_POINT('Ctrl Pts',(-0.0399263932461271,-2.3714404218185,
20.0981781430179));
#96972=CARTESIAN_POINT('Ctrl Pts',(-0.0511371737527683,-2.37122516287566,
20.0974249493329));
#96973=CARTESIAN_POINT('Ctrl Pts',(-0.0840421049860365,-2.37035989682129,
20.095206465772));
#96974=CARTESIAN_POINT('Ctrl Pts',(-0.105728859911678,-2.36949160566055,
20.0937343889457));
#96975=CARTESIAN_POINT('Ctrl Pts',(-0.307051995570714,-2.35866177259903,
20.0799725003353));
#96976=CARTESIAN_POINT('Ctrl Pts',(-0.484983840982608,-2.32858995708623,
20.0670287493638));
#96977=CARTESIAN_POINT('Ctrl Pts',(-0.797578245764926,-2.23835703353013,
20.0432718636491));
#96978=CARTESIAN_POINT('Ctrl Pts',(-0.933389327795246,-2.18521523082703,
20.0325932447577));
#96979=CARTESIAN_POINT('Ctrl Pts',(-1.08029044275168,-2.11152178335929,
20.0211633130528));
#96980=CARTESIAN_POINT('Ctrl Pts',(-1.09699861610564,-2.10288986265206,
20.019865500233));
#96981=CARTESIAN_POINT('Ctrl Pts',(-1.1203878652371,-2.09045166099273,20.0180536680637));
#96982=CARTESIAN_POINT('Ctrl Pts',(-1.12715527504981,-2.08681051023429,
20.0175300244356));
#96983=CARTESIAN_POINT('Ctrl Pts',(-1.13850898893608,-2.08063039049961,
20.0166526498844));
#96984=CARTESIAN_POINT('Ctrl Pts',(-1.14310474561318,-2.07810901595188,
20.0162978239329));
#96985=CARTESIAN_POINT('Ctrl Pts',(-1.15237068977889,-2.07298539231441,
20.0155831248039));
#96986=CARTESIAN_POINT('Ctrl Pts',(-1.1570404929592,-2.07038255946035,20.015223291175));
#96987=CARTESIAN_POINT('Ctrl Pts',(-1.1688137279455,-2.06376817532079,20.0143168989306));
#96988=CARTESIAN_POINT('Ctrl Pts',(-1.17590540991095,-2.05973568303437,
20.013771666033));
#96989=CARTESIAN_POINT('Ctrl Pts',(-1.19131162786577,-2.05086985319753,
20.01258847824));
#96990=CARTESIAN_POINT('Ctrl Pts',(-1.19961789868764,-2.04602234937336,
20.0119513903899));
#96991=CARTESIAN_POINT('Ctrl Pts',(-1.22357324515061,-2.03184607732286,
20.0101157392803));
#96992=CARTESIAN_POINT('Ctrl Pts',(-1.23914498680597,-2.02238713301143,
20.0089246404658));
#96993=CARTESIAN_POINT('Ctrl Pts',(-1.29307089353859,-1.98877350686875,
20.0048016369158));
#96994=CARTESIAN_POINT('Ctrl Pts',(-1.33084242878452,-1.96369838785343,
20.0019169766822));
#96995=CARTESIAN_POINT('Ctrl Pts',(-1.4612361776655,-1.87164303417996,19.9918841940544));
#96996=CARTESIAN_POINT('Ctrl Pts',(-1.54971705749849,-1.79906609074472,
19.9849333703448));
#96997=CARTESIAN_POINT('Ctrl Pts',(-1.74642457542066,-1.61239349936576,
19.9682992231747));
#96998=CARTESIAN_POINT('Ctrl Pts',(-1.84921241213584,-1.49339044585526,
19.958584140688));
#96999=CARTESIAN_POINT('Ctrl Pts',(-1.9502762685528,-1.3498042216479,19.9471185908959));
#97000=CARTESIAN_POINT('Ctrl Pts',(-1.96087599576264,-1.334359118298,19.9458888207482));
#97001=CARTESIAN_POINT('Ctrl Pts',(-1.9778007370199,-1.30906048384905,19.9438792900351));
#97002=CARTESIAN_POINT('Ctrl Pts',(-1.98423782947643,-1.29928262263194,
19.943103757135));
#97003=CARTESIAN_POINT('Ctrl Pts',(-1.99558339030224,-1.28176789620188,
19.9417163963934));
#97004=CARTESIAN_POINT('Ctrl Pts',(-2.00051994371233,-1.27404943316137,
19.9411056321996));
#97005=CARTESIAN_POINT('Ctrl Pts',(-2.01084849603477,-1.25769236519591,
19.939812499231));
#97006=CARTESIAN_POINT('Ctrl Pts',(-2.01622981576902,-1.24904727046751,
19.9391297512506));
#97007=CARTESIAN_POINT('Ctrl Pts',(-2.0303882163845,-1.22597186790908,19.9373090679843));
#97008=CARTESIAN_POINT('Ctrl Pts',(-2.03906697404138,-1.21148222426534,
19.9361675634791));
#97009=CARTESIAN_POINT('Ctrl Pts',(-2.08027738414806,-1.14098182861809,
19.9306208137242));
#97010=CARTESIAN_POINT('Ctrl Pts',(-2.11065723825525,-1.08375188078543,
19.9261391719099));
#97011=CARTESIAN_POINT('Ctrl Pts',(-2.2412729061114,-0.81131763799426,19.9048835935862));
#97012=CARTESIAN_POINT('Ctrl Pts',(-2.31115947940311,-0.583138513754106,
19.8871247096919));
#97013=CARTESIAN_POINT('Ctrl Pts',(-2.35169250939148,-0.31021276020117,
19.8675049846224));
#97014=CARTESIAN_POINT('Ctrl Pts',(-2.35643240577609,-0.271875588474613,
19.8647896616793));
#97015=CARTESIAN_POINT('Ctrl Pts',(-2.36166248848164,-0.218995348799627,
19.8611147194343));
#97016=CARTESIAN_POINT('Ctrl Pts',(-2.36295832113581,-0.20454014620526,
19.8601173638172));
#97017=CARTESIAN_POINT('Ctrl Pts',(-2.36465478774715,-0.183439609711855,
19.8586728946492));
#97018=CARTESIAN_POINT('Ctrl Pts',(-2.36516023135868,-0.17680338903282,
19.8582202431059));
#97019=CARTESIAN_POINT('Ctrl Pts',(-2.36599573028966,-0.165188265492498,
19.85743095722));
#97020=CARTESIAN_POINT('Ctrl Pts',(-2.3663380164592,-0.160210338443474,
19.8570936487721));
#97021=CARTESIAN_POINT('Ctrl Pts',(-2.36697882313379,-0.150440561584785,
19.8564335459404));
#97022=CARTESIAN_POINT('Ctrl Pts',(-2.36727850320949,-0.145648896402515,
19.8561106840891));
#97023=CARTESIAN_POINT('Ctrl Pts',(-2.36790409929548,-0.135133651120503,
19.8554040571721));
#97024=CARTESIAN_POINT('Ctrl Pts',(-2.36822381866285,-0.129409711999625,
19.8550206345085));
#97025=CARTESIAN_POINT('Ctrl Pts',(-2.3689612473943,-0.115288173676648,
19.8540775939886));
#97026=CARTESIAN_POINT('Ctrl Pts',(-2.369355066575,-0.106889327244002,19.8535192466475));
#97027=CARTESIAN_POINT('Ctrl Pts',(-2.37105288670264,-0.0660385161150878,
19.8508150476696));
#97028=CARTESIAN_POINT('Ctrl Pts',(-2.37173494361115,-0.033562651862194,
19.848700587004));
#97029=CARTESIAN_POINT('Ctrl Pts',(-2.37174975346702,-0.0010814014724484,
19.8466119453452));
#97030=CARTESIAN_POINT('Ctrl Pts',(-2.37174975209625,-0.00108440369412818,
19.8466121383971));
#97031=CARTESIAN_POINT('Ctrl Pts',(-2.3717763463339,0.0570810902993918,
19.8428719200797));
#97032=CARTESIAN_POINT('Ctrl Pts',(-2.36966322473608,0.115173800467578,
19.8392200188351));
#97033=CARTESIAN_POINT('Ctrl Pts',(-2.3654264700169,0.173077085263747,19.8356128877059));
#97034=CARTESIAN_POINT('',(-2.37174882624039,-0.00199382054561831,19.6502626448933));
#97035=CARTESIAN_POINT('Ctrl Pts',(-2.36542650053005,0.173076668243166,
19.6378399312857));
#97036=CARTESIAN_POINT('Ctrl Pts',(-2.36968866610404,0.114825954841437,
19.6419243157527));
#97037=CARTESIAN_POINT('Ctrl Pts',(-2.37179834147902,0.0564287005146955,
19.646069626348));
#97038=CARTESIAN_POINT('Ctrl Pts',(-2.37174915967572,-0.00199651634874111,
19.6502622558783));
#97039=CARTESIAN_POINT('Ctrl Pts',(-2.3717491619083,-0.00199386240332,19.6502620654296));
#97040=CARTESIAN_POINT('Ctrl Pts',(-2.37157024597321,-0.214818838888831,
19.6655345118503));
#97041=CARTESIAN_POINT('Ctrl Pts',(-2.34274834294621,-0.42664617522283,
19.6814441245475));
#97042=CARTESIAN_POINT('Ctrl Pts',(-2.27897125142913,-0.657415288275099,
19.6982202130785));
#97043=CARTESIAN_POINT('Ctrl Pts',(-2.27145876365937,-0.682920245629553,
19.700064711527));
#97044=CARTESIAN_POINT('Ctrl Pts',(-2.26094848674177,-0.716508247645402,
19.7024761970154));
#97045=CARTESIAN_POINT('Ctrl Pts',(-2.25833362045104,-0.724707798489459,
19.7030634928898));
#97046=CARTESIAN_POINT('Ctrl Pts',(-2.25396140539591,-0.738164457410525,
19.7040248194749));
#97047=CARTESIAN_POINT('Ctrl Pts',(-2.25223018619591,-0.743429871076609,
19.7044003391736));
#97048=CARTESIAN_POINT('Ctrl Pts',(-2.24880291172266,-0.753731894933052,
19.7051337494477));
#97049=CARTESIAN_POINT('Ctrl Pts',(-2.24710836549643,-0.758768937049329,
19.7054917205684));
#97050=CARTESIAN_POINT('Ctrl Pts',(-2.24289145036374,-0.77116569612999,
19.7063712964613));
#97051=CARTESIAN_POINT('Ctrl Pts',(-2.24034974256688,-0.77851886571668,
19.7068917715871));
#97052=CARTESIAN_POINT('Ctrl Pts',(-2.23147938372618,-0.803777628514846,
19.7086757827665));
#97053=CARTESIAN_POINT('Ctrl Pts',(-2.22497168537623,-0.82162021142403,
19.7099292899358));
#97054=CARTESIAN_POINT('Ctrl Pts',(-2.16803549896793,-0.972086260010119,
19.7204586171915));
#97055=CARTESIAN_POINT('Ctrl Pts',(-2.10600646113119,-1.10003544548114,
19.7291482806169));
#97056=CARTESIAN_POINT('Ctrl Pts',(-1.98923896046088,-1.29433813444706,
19.7430412670856));
#97057=CARTESIAN_POINT('Ctrl Pts',(-1.94171517372129,-1.36459677578765,
19.7482265955425));
#97058=CARTESIAN_POINT('Ctrl Pts',(-1.8496851272839,-1.48608187577362,19.7577048312356));
#97059=CARTESIAN_POINT('Ctrl Pts',(-1.80655057654368,-1.53822896025964,
19.7619615526537));
#97060=CARTESIAN_POINT('Ctrl Pts',(-1.74189580169375,-1.60991679148301,
19.7681536546521));
#97061=CARTESIAN_POINT('Ctrl Pts',(-1.72215289817705,-1.63101880514636,
19.7700213476072));
#97062=CARTESIAN_POINT('Ctrl Pts',(-1.68646510480953,-1.66779285865292,
19.7733617853692));
#97063=CARTESIAN_POINT('Ctrl Pts',(-1.67067470383039,-1.68361027173912,
19.7748279824724));
#97064=CARTESIAN_POINT('Ctrl Pts',(-1.64648225985331,-1.70716860182,19.7770582042093));
#97065=CARTESIAN_POINT('Ctrl Pts',(-1.63824365054816,-1.71507615013399,
19.7778149414612));
#97066=CARTESIAN_POINT('Ctrl Pts',(-1.62983804483503,-1.7230281579756,19.7785843577324));
#97067=CARTESIAN_POINT('Ctrl Pts',(-1.6297277015848,-1.72313252660832,19.7785944576605));
#97068=CARTESIAN_POINT('Ctrl Pts',(-1.62950312059339,-1.72334490662582,
19.7786150130485));
#97069=CARTESIAN_POINT('Ctrl Pts',(-1.62938888213956,-1.72345291724976,
19.7786254685406));
#97070=CARTESIAN_POINT('Ctrl Pts',(-1.62915626121533,-1.723672812797,19.7786467577939));
#97071=CARTESIAN_POINT('Ctrl Pts',(-1.62903787795685,-1.72378469688487,
19.7786575915911));
#97072=CARTESIAN_POINT('Ctrl Pts',(-1.62879669677707,-1.72401259032688,
19.7786796621126));
#97073=CARTESIAN_POINT('Ctrl Pts',(-1.62867389798456,-1.72412859875975,
19.7786908988767));
#97074=CARTESIAN_POINT('Ctrl Pts',(-1.62842359172832,-1.72436501331894,
19.778713802114));
#97075=CARTESIAN_POINT('Ctrl Pts',(-1.62829608330105,-1.72448541842551,
19.7787254686311));
#97076=CARTESIAN_POINT('Ctrl Pts',(-1.62209645605825,-1.73033837225139,
19.7792926802221));
#97077=CARTESIAN_POINT('Ctrl Pts',(-1.61599418539465,-1.73603876251197,
19.779849595243));
#97078=CARTESIAN_POINT('Ctrl Pts',(-1.60220846672796,-1.74878092174392,
19.7811047058551));
#97079=CARTESIAN_POINT('Ctrl Pts',(-1.59450849113973,-1.75580447338948,
19.7818036600613));
#97080=CARTESIAN_POINT('Ctrl Pts',(-1.57371699991801,-1.77451992132172,
19.7836855900221));
#97081=CARTESIAN_POINT('Ctrl Pts',(-1.56054178135121,-1.78611742803415,
19.7848724818437));
#97082=CARTESIAN_POINT('Ctrl Pts',(-1.49976134871859,-1.83843361895336,
19.7903234447539));
#97083=CARTESIAN_POINT('Ctrl Pts',(-1.45068720200129,-1.87739916933862,
19.7946579870328));
#97084=CARTESIAN_POINT('Ctrl Pts',(-1.22466864717369,-2.04270431775677,
19.8143484130582));
#97085=CARTESIAN_POINT('Ctrl Pts',(-1.03240154395743,-2.14629325745103,
19.8305104174073));
#97086=CARTESIAN_POINT('Ctrl Pts',(-0.788312453771228,-2.23732580172646,
19.8492283164366));
#97087=CARTESIAN_POINT('Ctrl Pts',(-0.747439717222321,-2.25131019765726,
19.8523016111626));
#97088=CARTESIAN_POINT('Ctrl Pts',(-0.681109336855299,-2.27199894799178,
19.8571688566933));
#97089=CARTESIAN_POINT('Ctrl Pts',(-0.655883468557604,-2.27940917129099,
19.8589924177495));
#97090=CARTESIAN_POINT('Ctrl Pts',(-0.622276294826786,-2.2886772878218,
19.8613809652386));
#97091=CARTESIAN_POINT('Ctrl Pts',(-0.61400182677619,-2.29091101471607,
19.8619657898102));
#97092=CARTESIAN_POINT('Ctrl Pts',(-0.600364010182595,-2.29451340196958,
19.8629241190917));
#97093=CARTESIAN_POINT('Ctrl Pts',(-0.59500774595686,-2.29590820382869,
19.8632990950955));
#97094=CARTESIAN_POINT('Ctrl Pts',(-0.584493682788414,-2.29860686044341,
19.8640323267075));
#97095=CARTESIAN_POINT('Ctrl Pts',(-0.579336312819429,-2.29991212912285,
19.8643906581024));
#97096=CARTESIAN_POINT('Ctrl Pts',(-0.566598663785245,-2.30309031169753,
19.8652724713485));
#97097=CARTESIAN_POINT('Ctrl Pts',(-0.559013355726528,-2.3049431884749,
19.8657948103287));
#97098=CARTESIAN_POINT('Ctrl Pts',(-0.532783196890197,-2.31121337441078,
19.8675919088273));
#97099=CARTESIAN_POINT('Ctrl Pts',(-0.514093456859698,-2.31544232760589,
19.8688564415791));
#97100=CARTESIAN_POINT('Ctrl Pts',(-0.362564046464306,-2.34780381257082,
19.8789954247396));
#97101=CARTESIAN_POINT('Ctrl Pts',(-0.22756450719299,-2.36471144317895,
19.8873347877119));
#97102=CARTESIAN_POINT('Ctrl Pts',(0.0370700351081663,-2.37496686942844,
19.9035705859503));
#97103=CARTESIAN_POINT('Ctrl Pts',(0.166167912273642,-2.36943603931554,
19.9114447013755));
#97104=CARTESIAN_POINT('Ctrl Pts',(0.36117711351004,-2.34506057236381,19.9238642227435));
#97105=CARTESIAN_POINT('Ctrl Pts',(0.427789053874646,-2.33382800857599,
19.9281989334918));
#97106=CARTESIAN_POINT('Ctrl Pts',(0.510717960794892,-2.31617431853829,
19.9337559505278));
#97107=CARTESIAN_POINT('Ctrl Pts',(0.527569133832011,-2.31239423371589,
19.9348934915524));
#97108=CARTESIAN_POINT('Ctrl Pts',(0.55446062538462,-2.3060526464199,19.9367228673396));
#97109=CARTESIAN_POINT('Ctrl Pts',(0.564528263053351,-2.30360874012265,
19.9374109190566));
#97110=CARTESIAN_POINT('Ctrl Pts',(0.583592422531735,-2.29884846080211,
19.9387199882216));
#97111=CARTESIAN_POINT('Ctrl Pts',(0.592592000944862,-2.2965450305942,19.9393405772122));
#97112=CARTESIAN_POINT('Ctrl Pts',(0.613018741624507,-2.29118877059502,
19.9407552317265));
#97113=CARTESIAN_POINT('Ctrl Pts',(0.62443699166633,-2.28810323077901,19.9415503434307));
#97114=CARTESIAN_POINT('Ctrl Pts',(0.653988318800632,-2.27987993963632,
19.9436196637802));
#97115=CARTESIAN_POINT('Ctrl Pts',(0.672083788168037,-2.27461130880577,
19.944898088465));
#97116=CARTESIAN_POINT('Ctrl Pts',(0.839093423625611,-2.22381835273104,
19.9568046770135));
#97117=CARTESIAN_POINT('Ctrl Pts',(0.983219217450222,-2.16395667493931,
19.9679138515918));
#97118=CARTESIAN_POINT('Ctrl Pts',(1.21777542597114,-2.03824011660773,19.9872827240615));
#97119=CARTESIAN_POINT('Ctrl Pts',(1.31137035335171,-1.97932012397947,19.9953994744278));
#97120=CARTESIAN_POINT('Ctrl Pts',(1.4581938113858,-1.87189105104362,20.0085129619603));
#97121=CARTESIAN_POINT('Ctrl Pts',(1.51393849280968,-1.82710092110257,20.013590960981));
#97122=CARTESIAN_POINT('Ctrl Pts',(1.57630593589758,-1.7721717894522,20.0193150920411));
#97123=CARTESIAN_POINT('Ctrl Pts',(1.58497507123793,-1.76442265128377,20.0201117409757));
#97124=CARTESIAN_POINT('Ctrl Pts',(1.59818240755923,-1.75244102637643,20.0213264812243));
#97125=CARTESIAN_POINT('Ctrl Pts',(1.60276141752954,-1.74825410037618,20.0217478309889));
#97126=CARTESIAN_POINT('Ctrl Pts',(1.61113591430251,-1.74053612441792,20.0225187081789));
#97127=CARTESIAN_POINT('Ctrl Pts',(1.61493624558862,-1.7370106097964,20.0228686270573));
#97128=CARTESIAN_POINT('Ctrl Pts',(1.6234606947411,-1.72905043765951,20.0236537635251));
#97129=CARTESIAN_POINT('Ctrl Pts',(1.6281782101814,-1.72460887210978,20.0240884443763));
#97130=CARTESIAN_POINT('Ctrl Pts',(1.6402409499946,-1.7131581264285,20.0252005756559));
#97131=CARTESIAN_POINT('Ctrl Pts',(1.64755956986613,-1.70612092569312,20.02587594176));
#97132=CARTESIAN_POINT('Ctrl Pts',(1.69212893107081,-1.66271112590344,20.029994382324));
#97133=CARTESIAN_POINT('Ctrl Pts',(1.72822208605996,-1.62516398832108,20.0333536445523));
#97134=CARTESIAN_POINT('Ctrl Pts',(1.78255766821713,-1.56478001647894,20.0385080836743));
#97135=CARTESIAN_POINT('Ctrl Pts',(1.8016616277813,-1.54274554940053,20.040340601405));
#97136=CARTESIAN_POINT('Ctrl Pts',(1.94640058823581,-1.36944735245991,20.0544339077607));
#97137=CARTESIAN_POINT('Ctrl Pts',(2.05318893108956,-1.20344539758727,20.0661572551653));
#97138=CARTESIAN_POINT('Ctrl Pts',(2.15743320750219,-0.986226268891222,
20.0813870848865));
#97139=CARTESIAN_POINT('Ctrl Pts',(2.17547525944371,-0.945762828016393,
20.0842161700404));
#97140=CARTESIAN_POINT('Ctrl Pts',(2.20440890858809,-0.875656764595192,
20.0891225334243));
#97141=CARTESIAN_POINT('Ctrl Pts',(2.21586125735014,-0.84625772678302,20.0911813543414));
#97142=CARTESIAN_POINT('Ctrl Pts',(2.23124374411759,-0.804314473095703,
20.0941246538844));
#97143=CARTESIAN_POINT('Ctrl Pts',(2.23566161305553,-0.79195173939036,20.0949929083142));
#97144=CARTESIAN_POINT('Ctrl Pts',(2.24309499112943,-0.770592590154836,
20.0964945255721));
#97145=CARTESIAN_POINT('Ctrl Pts',(2.24615960361072,-0.761613491117937,
20.0971262474087));
#97146=CARTESIAN_POINT('Ctrl Pts',(2.25192125198599,-0.744394986849645,
20.0983386414704));
#97147=CARTESIAN_POINT('Ctrl Pts',(2.25462715309951,-0.736158691209482,
20.0989190093652));
#97148=CARTESIAN_POINT('Ctrl Pts',(2.26086899036562,-0.716802362847696,
20.1002840480392));
#97149=CARTESIAN_POINT('Ctrl Pts',(2.26436811312505,-0.70567078638689,20.1010699138073));
#97150=CARTESIAN_POINT('Ctrl Pts',(2.27614968476158,-0.667200619179409,
20.1037890290716));
#97151=CARTESIAN_POINT('Ctrl Pts',(2.2840200066732,-0.639739430066774,20.1057356087649));
#97152=CARTESIAN_POINT('Ctrl Pts',(2.33724176262188,-0.440518410633928,
20.1199033881569));
#97153=CARTESIAN_POINT('Ctrl Pts',(2.36365571946768,-0.264317348793432,
20.1327433523245));
#97154=CARTESIAN_POINT('Ctrl Pts',(2.37393935773052,0.0162985479320983,
20.1532532163247));
#97155=CARTESIAN_POINT('Ctrl Pts',(2.37098132276801,0.119598232651939,20.1608004580911));
#97156=CARTESIAN_POINT('Ctrl Pts',(2.35840848356111,0.253099708535496,20.170339260319));
#97157=CARTESIAN_POINT('Ctrl Pts',(2.35491622382643,0.283760133985833,20.1725146488013));
#97158=CARTESIAN_POINT('Ctrl Pts',(2.34810159740941,0.33472322850215,20.1760959358623));
#97159=CARTESIAN_POINT('Ctrl Pts',(2.34511173893536,0.355065847022341,20.1775162070948));
#97160=CARTESIAN_POINT('Ctrl Pts',(2.34062296809238,0.383070540873555,20.1794563221296));
#97161=CARTESIAN_POINT('Ctrl Pts',(2.33935031660775,0.390767217915297,20.1799879542716));
#97162=CARTESIAN_POINT('Ctrl Pts',(2.337137206279,0.40375314069712,20.1808821015825));
#97163=CARTESIAN_POINT('Ctrl Pts',(2.33621671836057,0.409045677780673,20.1812457245516));
#97164=CARTESIAN_POINT('Ctrl Pts',(2.33442484523708,0.419145043980085,20.1819380236679));
#97165=CARTESIAN_POINT('Ctrl Pts',(2.33355658329321,0.423952355379567,20.1822668797209));
#97166=CARTESIAN_POINT('Ctrl Pts',(2.33121669153173,0.436682650978163,20.1831360093288));
#97167=CARTESIAN_POINT('Ctrl Pts',(2.32971950818885,0.444600965429108,20.1836748475911));
#97168=CARTESIAN_POINT('Ctrl Pts',(2.32423851386881,0.47280079726762,20.1855880375521));
#97169=CARTESIAN_POINT('Ctrl Pts',(2.32002984352498,0.493038396420186,20.1869503292901));
#97170=CARTESIAN_POINT('Ctrl Pts',(2.25841851529484,0.771018120938335,20.205547222769));
#97171=CARTESIAN_POINT('Ctrl Pts',(2.15862529872752,1.01750198262787,20.2208522071533));
#97172=CARTESIAN_POINT('Ctrl Pts',(1.98527877126335,1.2993539626881,20.2417719577173));
#97173=CARTESIAN_POINT('Ctrl Pts',(1.94793322235289,1.35469826046254,20.2460576299516));
#97174=CARTESIAN_POINT('Ctrl Pts',(1.89808883523727,1.42223517987368,20.251559425109));
#97175=CARTESIAN_POINT('Ctrl Pts',(1.88772103548177,1.43596775714638,20.2526928688641));
#97176=CARTESIAN_POINT('Ctrl Pts',(1.8708814949395,1.45777485837654,20.2545172091411));
#97177=CARTESIAN_POINT('Ctrl Pts',(1.86450460563408,1.46592212467353,20.255204359837));
#97178=CARTESIAN_POINT('Ctrl Pts',(1.85229950074898,1.48130718342552,20.2565127203402));
#97179=CARTESIAN_POINT('Ctrl Pts',(1.84648164104521,1.48855297426195,20.2571335083828));
#97180=CARTESIAN_POINT('Ctrl Pts',(1.83314674959439,1.50496230215366,20.2585500152574));
#97181=CARTESIAN_POINT('Ctrl Pts',(1.82560335630937,1.51410399676119,20.2593467906327));
#97182=CARTESIAN_POINT('Ctrl Pts',(1.80583613011872,1.53769704103044,20.2614233014497));
#97183=CARTESIAN_POINT('Ctrl Pts',(1.79350745971684,1.55205904349492,20.262707301507));
#97184=CARTESIAN_POINT('Ctrl Pts',(1.67840705571719,1.68293979311044,20.2745964962048));
#97185=CARTESIAN_POINT('Ctrl Pts',(1.56461055004067,1.78922140004199,20.2856802486314));
#97186=CARTESIAN_POINT('Ctrl Pts',(1.35229044790468,1.95168138706883,20.3051373627429));
#97187=CARTESIAN_POINT('Ctrl Pts',(1.25860253412578,2.01337279297222,20.3133709755619));
#97188=CARTESIAN_POINT('Ctrl Pts',(1.09971187038921,2.10255942266117,20.3264975827861));
#97189=CARTESIAN_POINT('Ctrl Pts',(1.03701839440196,2.13417836872652,20.3314808547102));
#97190=CARTESIAN_POINT('Ctrl Pts',(0.962448187286882,2.1677236073271,20.3371122926824));
#97191=CARTESIAN_POINT('Ctrl Pts',(0.951852924571789,2.17239687320872,20.3379056388596));
#97192=CARTESIAN_POINT('Ctrl Pts',(0.935537801807546,2.17945072325493,20.339116411483));
#97193=CARTESIAN_POINT('Ctrl Pts',(0.929842320872545,2.18188672809922,20.3395370642063));
#97194=CARTESIAN_POINT('Ctrl Pts',(0.91936265629075,2.18632048116515,20.340307275231));
#97195=CARTESIAN_POINT('Ctrl Pts',(0.914581480845411,2.18832485159819,20.340657220278));
#97196=CARTESIAN_POINT('Ctrl Pts',(0.903799031219766,2.19280357276485,20.3414431725301));
#97197=CARTESIAN_POINT('Ctrl Pts',(0.897794157648528,2.19526896998961,20.3418786377283));
#97198=CARTESIAN_POINT('Ctrl Pts',(0.880100683417117,2.20244856756057,20.3431553793116));
#97199=CARTESIAN_POINT('Ctrl Pts',(0.868384312822484,2.20709438137374,20.343992676773));
#97200=CARTESIAN_POINT('Ctrl Pts',(0.7710684135213,2.2447874859237,20.3508844868521));
#97201=CARTESIAN_POINT('Ctrl Pts',(0.683643107167049,2.27293945758212,20.3566765698928));
#97202=CARTESIAN_POINT('Ctrl Pts',(0.427301384596625,2.33934794636473,20.3731121459505));
#97203=CARTESIAN_POINT('Ctrl Pts',(0.25556560849099,2.3642805980477,20.3834963568574));
#97204=CARTESIAN_POINT('Ctrl Pts',(0.00637389640235237,2.37296892818386,
20.3991811390228));
#97205=CARTESIAN_POINT('Ctrl Pts',(-0.0699722647303788,2.37194522724757,
20.404062511011));
#97206=CARTESIAN_POINT('Ctrl Pts',(-0.16401617465828,2.36613986579056,20.4102335537611));
#97207=CARTESIAN_POINT('Ctrl Pts',(-0.181888095085075,2.36483315725268,
20.4114132549643));
#97208=CARTESIAN_POINT('Ctrl Pts',(-0.210208415970183,2.36243958434211,
20.4132944442971));
#97209=CARTESIAN_POINT('Ctrl Pts',(-0.220667600881361,2.36148558574624,
20.4139917575508));
#97210=CARTESIAN_POINT('Ctrl Pts',(-0.240342362625392,2.35955917054005,
20.4153084425433));
#97211=CARTESIAN_POINT('Ctrl Pts',(-0.24955927623352,2.35860214830596,20.4159273184167));
#97212=CARTESIAN_POINT('Ctrl Pts',(-0.27029748853394,2.35632591307525,20.4173245444541));
#97213=CARTESIAN_POINT('Ctrl Pts',(-0.281815127435365,2.3549761711269,20.4181038424357));
#97214=CARTESIAN_POINT('Ctrl Pts',(-0.311265727558613,2.35130573926824,
20.4201051837135));
#97215=CARTESIAN_POINT('Ctrl Pts',(-0.329182616076211,2.34886436524211,
20.4213309965651));
#97216=CARTESIAN_POINT('Ctrl Pts',(-0.446469897195048,2.33151439157166,
20.4294112379196));
#97217=CARTESIAN_POINT('Ctrl Pts',(-0.544821428572625,2.31051061879522,
20.4364569984638));
#97218=CARTESIAN_POINT('Ctrl Pts',(-0.814036385168842,2.23487113355375,
20.4564871634325));
#97219=CARTESIAN_POINT('Ctrl Pts',(-0.980474737241934,2.16701785997372,
20.4697753173988));
#97220=CARTESIAN_POINT('Ctrl Pts',(-1.19056418310103,2.05216656974204,20.4869449614003));
#97221=CARTESIAN_POINT('Ctrl Pts',(-1.24233316641792,2.02124725077275,20.4912052658111));
#97222=CARTESIAN_POINT('Ctrl Pts',(-1.30223098621361,1.98230096870914,20.4961226529638));
#97223=CARTESIAN_POINT('Ctrl Pts',(-1.31154666811942,1.97614979738926,20.4968870687436));
#97224=CARTESIAN_POINT('Ctrl Pts',(-1.32588983854891,1.96653285618694,20.4980630317081));
#97225=CARTESIAN_POINT('Ctrl Pts',(-1.33094780090554,1.96311316327842,20.4984775292433));
#97226=CARTESIAN_POINT('Ctrl Pts',(-1.34028162276164,1.95674990227554,20.499241989747));
#97227=CARTESIAN_POINT('Ctrl Pts',(-1.34456099803503,1.9538118465842,20.4995922975427));
#97228=CARTESIAN_POINT('Ctrl Pts',(-1.35426213006472,1.9471044518167,20.5003860457769));
#97229=CARTESIAN_POINT('Ctrl Pts',(-1.35967780893578,1.94332650930587,20.5008288948324));
#97230=CARTESIAN_POINT('Ctrl Pts',(-1.37371402847236,1.93344753311428,20.5019761759846));
#97231=CARTESIAN_POINT('Ctrl Pts',(-1.38230983837189,1.92731136984549,20.5026782958483));
#97232=CARTESIAN_POINT('Ctrl Pts',(-1.43943555768982,1.88595308517009,20.5073433275271));
#97233=CARTESIAN_POINT('Ctrl Pts',(-1.48666035210265,1.84895542669313,20.5111946861712));
#97234=CARTESIAN_POINT('Ctrl Pts',(-1.58533791335619,1.76541949579703,20.5193539173349));
#97235=CARTESIAN_POINT('Ctrl Pts',(-1.63625405648837,1.71833523658822,20.5236358174434));
#97236=CARTESIAN_POINT('Ctrl Pts',(-1.77145566899804,1.58184154136373,20.5354399724279));
#97237=CARTESIAN_POINT('Ctrl Pts',(-1.85096499141975,1.48802057772727,20.5429036350827));
#97238=CARTESIAN_POINT('Ctrl Pts',(-1.95735022198074,1.3406904690135,20.5542655098095));
#97239=CARTESIAN_POINT('Ctrl Pts',(-1.99005426526717,1.29164781189407,20.5579930054323));
#97240=CARTESIAN_POINT('Ctrl Pts',(-2.04135038360049,1.2081447202317,20.5642970916508));
#97241=CARTESIAN_POINT('Ctrl Pts',(-2.06097722185571,1.17434988770958,20.5668372652006));
#97242=CARTESIAN_POINT('Ctrl Pts',(-2.08661689510833,1.12757771650778,20.5703458204976));
#97243=CARTESIAN_POINT('Ctrl Pts',(-2.09336122326067,1.11500688237109,20.5712881089498));
#97244=CARTESIAN_POINT('Ctrl Pts',(-2.10450476105194,1.093778797105,20.5728785414911));
#97245=CARTESIAN_POINT('Ctrl Pts',(-2.10896500963325,1.08515387371081,20.5735245135664));
#97246=CARTESIAN_POINT('Ctrl Pts',(-2.11766643368586,1.06807137091467,20.5748036194338));
#97247=CARTESIAN_POINT('Ctrl Pts',(-2.12191021405711,1.05961531544192,20.5754366468689));
#97248=CARTESIAN_POINT('Ctrl Pts',(-2.13114861729148,1.0409290249592,20.5768353093216));
#97249=CARTESIAN_POINT('Ctrl Pts',(-2.13612038152753,1.03068781487539,20.5776017238098));
#97250=CARTESIAN_POINT('Ctrl Pts',(-2.15337433947967,0.994485711985041,
20.5803107456412));
#97251=CARTESIAN_POINT('Ctrl Pts',(-2.16525811169484,0.968338814954784,
20.5822669909664));
#97252=CARTESIAN_POINT('Ctrl Pts',(-2.25034662993263,0.771722757072405,
20.5969811003242));
#97253=CARTESIAN_POINT('Ctrl Pts',(-2.30378432406054,0.593436784887765,
20.6104203007494));
#97254=CARTESIAN_POINT('Ctrl Pts',(-2.34974818616782,0.332069520135731,
20.6298043678859));
#97255=CARTESIAN_POINT('Ctrl Pts',(-2.35959834086284,0.252729769170749,
20.6356362497434));
#97256=CARTESIAN_POINT('Ctrl Pts',(-2.36542650966497,0.173076543396847,
20.6413652673669));
#97257=CARTESIAN_POINT('Origin',(0.,0.,-1.84858989190503));
#97258=CARTESIAN_POINT('',(-2.36542649448459,0.173076750866022,21.8391485779751));
#97259=CARTESIAN_POINT('',(-2.36542651121823,0.173076522168564,21.6404818371561));
#97260=CARTESIAN_POINT('',(-2.36542649454111,0.173076750093529,-1.84858989190503));
#97261=CARTESIAN_POINT('Ctrl Pts',(-2.36542649448459,0.173076750866022,
21.8391485779751));
#97262=CARTESIAN_POINT('Ctrl Pts',(-2.36468712736919,0.183181623734164,
21.8384536730529));
#97263=CARTESIAN_POINT('Ctrl Pts',(-2.36388300950187,0.193281761835121,
21.837756770496));
#97264=CARTESIAN_POINT('Ctrl Pts',(-2.36044576508709,0.233218801663289,
21.8349918553977));
#97265=CARTESIAN_POINT('Ctrl Pts',(-2.35731236789479,0.263008521156516,
21.8329088847253));
#97266=CARTESIAN_POINT('Ctrl Pts',(-2.32574312133706,0.516832612027184,
21.8149835579103));
#97267=CARTESIAN_POINT('Ctrl Pts',(-2.26600391909561,0.735792982116718,
21.7981782907456));
#97268=CARTESIAN_POINT('Ctrl Pts',(-2.15110529057982,1.00097132946833,21.777423661427));
#97269=CARTESIAN_POINT('Ctrl Pts',(-2.1236485197876,1.05797739941211,21.772947313464));
#97270=CARTESIAN_POINT('Ctrl Pts',(-2.08868923669694,1.12369946214713,21.7678233704948));
#97271=CARTESIAN_POINT('Ctrl Pts',(-2.08336570408184,1.13353895576957,21.7670572616316));
#97272=CARTESIAN_POINT('Ctrl Pts',(-2.07505218050508,1.14864842841117,21.7658828249079));
#97273=CARTESIAN_POINT('Ctrl Pts',(-2.0721113740882,1.15394506774771,21.7654715062615));
#97274=CARTESIAN_POINT('Ctrl Pts',(-2.06665135091455,1.16369085067634,21.7647154685142));
#97275=CARTESIAN_POINT('Ctrl Pts',(-2.06413805587836,1.16814309458145,21.7643703948227));
#97276=CARTESIAN_POINT('Ctrl Pts',(-2.05842180800591,1.17819324209875,21.7635921342977));
#97277=CARTESIAN_POINT('Ctrl Pts',(-2.05521041191576,1.18378622252947,21.7631594971263));
#97278=CARTESIAN_POINT('Ctrl Pts',(-2.04562884991697,1.20031699201036,21.7618819662574));
#97279=CARTESIAN_POINT('Ctrl Pts',(-2.03919377030269,1.211217180222,21.7610411204126));
#97280=CARTESIAN_POINT('Ctrl Pts',(-1.97193122046302,1.3230955189846,21.752421134258));
#97281=CARTESIAN_POINT('Ctrl Pts',(-1.90373366457773,1.41947201691655,21.7450792182251));
#97282=CARTESIAN_POINT('Ctrl Pts',(-1.74468269032294,1.61203654189652,21.729705624385));
#97283=CARTESIAN_POINT('Ctrl Pts',(-1.65239815888481,1.70650489198943,21.7217146101116));
#97284=CARTESIAN_POINT('Ctrl Pts',(-1.50769483927149,1.83183131191092,21.7097508455015));
#97285=CARTESIAN_POINT('Ctrl Pts',(-1.46119471909068,1.86913318817856,21.7059825366025));
#97286=CARTESIAN_POINT('Ctrl Pts',(-1.3817869590987,1.9280577899961,21.6996224881377));
#97287=CARTESIAN_POINT('Ctrl Pts',(-1.34965675315427,1.95068408503323,21.6970683611582));
#97288=CARTESIAN_POINT('Ctrl Pts',(-1.30805831461342,1.97845813913366,21.6937781314321));
#97289=CARTESIAN_POINT('Ctrl Pts',(-1.29909562485786,1.98435473488713,21.6930701912888));
#97290=CARTESIAN_POINT('Ctrl Pts',(-1.28280179228545,1.99491682326788,21.6917847443266));
#97291=CARTESIAN_POINT('Ctrl Pts',(-1.27548438889214,1.99960324572541,21.691208026188));
#97292=CARTESIAN_POINT('Ctrl Pts',(-1.26059784638463,2.00902235444399,21.690035793993));
#97293=CARTESIAN_POINT('Ctrl Pts',(-1.25302741631526,2.01375272592525,21.6894402067113));
#97294=CARTESIAN_POINT('Ctrl Pts',(-1.23661769465289,2.02387795468546,21.6881502753306));
#97295=CARTESIAN_POINT('Ctrl Pts',(-1.22776944418407,2.02925786537913,21.6874553971709));
#97296=CARTESIAN_POINT('Ctrl Pts',(-1.20359517971738,2.04374030764256,21.6855585507539));
#97297=CARTESIAN_POINT('Ctrl Pts',(-1.18820158302909,2.05272812848332,21.6843524442027));
#97298=CARTESIAN_POINT('Ctrl Pts',(-1.11046477410924,2.09694873827737,21.6782691685758));
#97299=CARTESIAN_POINT('Ctrl Pts',(-1.04665583652984,2.12951536658619,21.6732981136789));
#97300=CARTESIAN_POINT('Ctrl Pts',(-0.791632461300696,2.24544079790653,
21.6535027198239));
#97301=CARTESIAN_POINT('Ctrl Pts',(-0.591240610592655,2.3063174538201,21.6379999090804));
#97302=CARTESIAN_POINT('Ctrl Pts',(-0.323013246548215,2.35050509894705,
21.6184764021275));
#97303=CARTESIAN_POINT('Ctrl Pts',(-0.260107701516837,2.35829544555292,
21.613991873548));
#97304=CARTESIAN_POINT('Ctrl Pts',(-0.185806635859397,2.36448709258617,
21.6088598331498));
#97305=CARTESIAN_POINT('Ctrl Pts',(-0.174646861916907,2.36533756640409,
21.6080933887107));
#97306=CARTESIAN_POINT('Ctrl Pts',(-0.157436429618534,2.36652668418171,
21.6069185488095));
#97307=CARTESIAN_POINT('Ctrl Pts',(-0.151389983332795,2.36692117556907,
21.6065071593911));
#97308=CARTESIAN_POINT('Ctrl Pts',(-0.140239001274649,2.36760579992453,
21.6057510561521));
#97309=CARTESIAN_POINT('Ctrl Pts',(-0.135135064576743,2.36790259862969,
21.6054059872618));
#97310=CARTESIAN_POINT('Ctrl Pts',(-0.12359180289652,2.3685364056116,21.604627818832));
#97311=CARTESIAN_POINT('Ctrl Pts',(-0.117152047630164,2.36886365979163,
21.6041952683868));
#97312=CARTESIAN_POINT('Ctrl Pts',(-0.0980734690518432,2.3697552007801,
21.6029182324184));
#97313=CARTESIAN_POINT('Ctrl Pts',(-0.0854311269601467,2.37024464076233,
21.6020777901016));
#97314=CARTESIAN_POINT('Ctrl Pts',(0.0396632502390338,2.37408539162219,
21.5938135032376));
#97315=CARTESIAN_POINT('Ctrl Pts',(0.152231820966934,2.36953315482627,21.5867874075629));
#97316=CARTESIAN_POINT('Ctrl Pts',(0.311289197405841,2.35171323335402,21.5769222534212));
#97317=CARTESIAN_POINT('Ctrl Pts',(0.358343429449025,2.34500451835959,21.574012227221));
#97318=CARTESIAN_POINT('Ctrl Pts',(0.57778800212076,2.30695764947052,21.5603663607412));
#97319=CARTESIAN_POINT('Ctrl Pts',(0.746537563479894,2.25799975039015,21.5496052531584));
#97320=CARTESIAN_POINT('Ctrl Pts',(0.928084954148645,2.18273060458787,21.5367789929547));
#97321=CARTESIAN_POINT('Ctrl Pts',(0.947709979687433,2.17428156400196,21.5353760319599));
#97322=CARTESIAN_POINT('Ctrl Pts',(0.977392396780473,2.16102437327209,21.5332276411493));
#97323=CARTESIAN_POINT('Ctrl Pts',(0.98753482649677,2.1564084025092,21.532488786251));
#97324=CARTESIAN_POINT('Ctrl Pts',(1.00591197088979,2.14788785084186,21.5311412002221));
#97325=CARTESIAN_POINT('Ctrl Pts',(1.01415747266829,2.14400693319998,21.5305332956394));
#97326=CARTESIAN_POINT('Ctrl Pts',(1.03190825303541,2.13552684843694,21.5292174341529));
#97327=CARTESIAN_POINT('Ctrl Pts',(1.04140556040252,2.13091154569335,21.5285089260731));
#97328=CARTESIAN_POINT('Ctrl Pts',(1.0671179251063,2.11820344018102,21.5265783866353));
#97329=CARTESIAN_POINT('Ctrl Pts',(1.08327127962135,2.10998810018982,21.525352091696));
#97330=CARTESIAN_POINT('Ctrl Pts',(1.16472122348156,2.06738211916254,21.5190987095369));
#97331=CARTESIAN_POINT('Ctrl Pts',(1.22847483901889,2.03014577377484,21.5139717186042));
#97332=CARTESIAN_POINT('Ctrl Pts',(1.46347324126149,1.87776496753466,21.4941577576237));
#97333=CARTESIAN_POINT('Ctrl Pts',(1.62117283861821,1.74342607558306,21.4788234782505));
#97334=CARTESIAN_POINT('Ctrl Pts',(1.8018167435931,1.54358070660903,21.4594781839303));
#97335=CARTESIAN_POINT('Ctrl Pts',(1.84227489054645,1.4950618167598,21.4550091023024));
#97336=CARTESIAN_POINT('Ctrl Pts',(1.88756475763463,1.43611364358557,21.4498923563373));
#97337=CARTESIAN_POINT('Ctrl Pts',(1.89431505230589,1.42719781621834,21.4491265488468));
#97338=CARTESIAN_POINT('Ctrl Pts',(1.90462424015947,1.41337937452946,21.4479524754598));
#97339=CARTESIAN_POINT('Ctrl Pts',(1.90822771988776,1.4085104627563,21.4475412216012));
#97340=CARTESIAN_POINT('Ctrl Pts',(1.91483834649784,1.39950645215011,21.4467852447925));
#97341=CARTESIAN_POINT('Ctrl Pts',(1.91785076082092,1.39537545592722,21.4464401676852));
#97342=CARTESIAN_POINT('Ctrl Pts',(1.92463361009703,1.38601051123391,21.4456618266865));
#97343=CARTESIAN_POINT('Ctrl Pts',(1.92839606091981,1.38077090970669,21.4452291129645));
#97344=CARTESIAN_POINT('Ctrl Pts',(1.93806118048639,1.36719466830274,21.4441148421737));
#97345=CARTESIAN_POINT('Ctrl Pts',(1.94393152978422,1.35883502206309,21.4434354265726));
#97346=CARTESIAN_POINT('Ctrl Pts',(1.98101635764553,1.30529232875984,21.4391245586984));
#97347=CARTESIAN_POINT('Ctrl Pts',(2.01071044326692,1.25907049023229,21.4355867641089));
#97348=CARTESIAN_POINT('Ctrl Pts',(2.05132915233621,1.19073524402782,21.4305525145929));
#97349=CARTESIAN_POINT('Ctrl Pts',(2.06355434322322,1.16942090406961,21.4290088453607));
#97350=CARTESIAN_POINT('Ctrl Pts',(2.1653413638624,0.985389324429527,21.4158732304707));
#97351=CARTESIAN_POINT('Ctrl Pts',(2.23583413236536,0.812862584864275,21.404780432448));
#97352=CARTESIAN_POINT('Ctrl Pts',(2.30644683703887,0.558263028975817,21.3881775894915));
#97353=CARTESIAN_POINT('Ctrl Pts',(2.32365009509977,0.48166671447982,21.3831626753346));
#97354=CARTESIAN_POINT('Ctrl Pts',(2.34007646536301,0.386730484296695,21.3768526656097));
#97355=CARTESIAN_POINT('Ctrl Pts',(2.34292784425433,0.369062892568961,21.3756745322218));
#97356=CARTESIAN_POINT('Ctrl Pts',(2.34712026530927,0.341075895435963,21.3738014626047));
#97357=CARTESIAN_POINT('Ctrl Pts',(2.34859383879468,0.330776783897866,21.3731107295425));
#97358=CARTESIAN_POINT('Ctrl Pts',(2.35123283219823,0.311425008639067,21.371809990519));
#97359=CARTESIAN_POINT('Ctrl Pts',(2.35241385444851,0.302374636155485,21.3712004903943));
#97360=CARTESIAN_POINT('Ctrl Pts',(2.35494650264956,0.282053006108913,21.36982918303));
#97361=CARTESIAN_POINT('Ctrl Pts',(2.35626949645607,0.270778471935944,21.3690664865753));
#97362=CARTESIAN_POINT('Ctrl Pts',(2.35943297939522,0.242038241441896,21.3671172662907));
#97363=CARTESIAN_POINT('Ctrl Pts',(2.36116047653273,0.224561059887744,21.3659272212151));
#97364=CARTESIAN_POINT('Ctrl Pts',(2.37067359297253,0.116013528040631,21.3585054595592));
#97365=CARTESIAN_POINT('Ctrl Pts',(2.37338241102787,0.0245870486302439,
21.3521162920509));
#97366=CARTESIAN_POINT('Ctrl Pts',(2.36495765184394,-0.274605748820411,
21.3307601788161));
#97367=CARTESIAN_POINT('Ctrl Pts',(2.33180083118807,-0.48075546460797,21.3152503519221));
#97368=CARTESIAN_POINT('Ctrl Pts',(2.26383514195862,-0.707884099840714,
21.29841322483));
#97369=CARTESIAN_POINT('Ctrl Pts',(2.25495470880947,-0.735682594807681,
21.2963590033748));
#97370=CARTESIAN_POINT('Ctrl Pts',(2.23923502575379,-0.78192785902656,21.2929602432573));
#97371=CARTESIAN_POINT('Ctrl Pts',(2.23267542038401,-0.800465619664024,
21.2916029133169));
#97372=CARTESIAN_POINT('Ctrl Pts',(2.22326157143464,-0.826053152008092,
21.2897385322571));
#97373=CARTESIAN_POINT('Ctrl Pts',(2.22060306347414,-0.833173369411592,
21.2892207215183));
#97374=CARTESIAN_POINT('Ctrl Pts',(2.21604044731529,-0.845216335769105,
21.2883467344542));
#97375=CARTESIAN_POINT('Ctrl Pts',(2.21415406458807,-0.85014569263355,21.287989520228));
#97376=CARTESIAN_POINT('Ctrl Pts',(2.21050940150974,-0.859575238204033,
21.2873072445561));
#97377=CARTESIAN_POINT('Ctrl Pts',(2.20875381187642,-0.864076387764508,
21.2869820200075));
#97378=CARTESIAN_POINT('Ctrl Pts',(2.20452764093215,-0.874814808444424,
21.2862071492798));
#97379=CARTESIAN_POINT('Ctrl Pts',(2.20204430847061,-0.881047067414209,
21.285758261366));
#97380=CARTESIAN_POINT('Ctrl Pts',(2.19306432156613,-0.903308406069299,
21.2841575175206));
#97381=CARTESIAN_POINT('Ctrl Pts',(2.18641862734327,-0.919277338028167,
21.2830141954987));
#97382=CARTESIAN_POINT('Ctrl Pts',(2.11213800682284,-1.09240250978723,21.2706580902213));
#97383=CARTESIAN_POINT('Ctrl Pts',(2.02785132646807,-1.24189685649614,21.260316950865));
#97384=CARTESIAN_POINT('Ctrl Pts',(1.83703761445154,-1.50831016763068,21.2402183305204));
#97385=CARTESIAN_POINT('Ctrl Pts',(1.73351629926569,-1.62622819813745,21.2305289606676));
#97386=CARTESIAN_POINT('Ctrl Pts',(1.60336702902551,-1.74782103547055,21.2189073895246));
#97387=CARTESIAN_POINT('Ctrl Pts',(1.5873905488428,-1.76234372258896,21.2174899309549));
#97388=CARTESIAN_POINT('Ctrl Pts',(1.56283648023269,-1.78405868895823,21.2153238683512));
#97389=CARTESIAN_POINT('Ctrl Pts',(1.55440227454752,-1.79141196579194,21.2145820086449));
#97390=CARTESIAN_POINT('Ctrl Pts',(1.53900317157983,-1.80464689012095,21.2132312613664));
#97391=CARTESIAN_POINT('Ctrl Pts',(1.53205575732524,-1.8105486219941,21.2126232198182));
#97392=CARTESIAN_POINT('Ctrl Pts',(1.51701543801442,-1.82317661209782,21.211309688343));
#97393=CARTESIAN_POINT('Ctrl Pts',(1.50891147160832,-1.82988933072939,21.2106036632936));
#97394=CARTESIAN_POINT('Ctrl Pts',(1.48685313168408,-1.8479146416132,21.2086863911297));
#97395=CARTESIAN_POINT('Ctrl Pts',(1.47281470463787,-1.8591227965458,21.2074709778796));
#97396=CARTESIAN_POINT('Ctrl Pts',(1.40222185981162,-1.91418211791575,21.2013815326785));
#97397=CARTESIAN_POINT('Ctrl Pts',(1.34383585122908,-1.9556131121364,21.1964138437282));
#97398=CARTESIAN_POINT('Ctrl Pts',(1.10826754235946,-2.10723851527118,21.1766181611081));
#97399=CARTESIAN_POINT('Ctrl Pts',(0.918740089505553,-2.19649881505852,
21.1611108941741));
#97400=CARTESIAN_POINT('Ctrl Pts',(0.659665629835438,-2.27904667216431,
21.1415826794664));
#97401=CARTESIAN_POINT('Ctrl Pts',(0.598543555017432,-2.29585708124241,
21.1370977485944));
#97402=CARTESIAN_POINT('Ctrl Pts',(0.525914212829848,-2.31273378561264,
21.1319653095695));
#97403=CARTESIAN_POINT('Ctrl Pts',(0.514994632602176,-2.31518981149414,
21.1311988482973));
#97404=CARTESIAN_POINT('Ctrl Pts',(0.498136980785032,-2.31885625370446,
21.1300239879931));
#97405=CARTESIAN_POINT('Ctrl Pts',(0.492211156861529,-2.32012132357915,
21.129612594849));
#97406=CARTESIAN_POINT('Ctrl Pts',(0.481276468004334,-2.32241192785565,
21.1288564879576));
#97407=CARTESIAN_POINT('Ctrl Pts',(0.476269160230746,-2.32344397162374,
21.1285114191165));
#97408=CARTESIAN_POINT('Ctrl Pts',(0.464939079142822,-2.32574101962232,
21.1277332547696));
#97409=CARTESIAN_POINT('Ctrl Pts',(0.458614469081092,-2.32699643508795,
21.1273007083304));
#97410=CARTESIAN_POINT('Ctrl Pts',(0.43986590918429,-2.33063855874844,21.1260236956619));
#97411=CARTESIAN_POINT('Ctrl Pts',(0.427427650561155,-2.33295172060679,
21.1251832724169));
#97412=CARTESIAN_POINT('Ctrl Pts',(0.303710364290955,-2.35493693211906,
21.1168858184041));
#97413=CARTESIAN_POINT('Ctrl Pts',(0.191161880748561,-2.36673455123434,
21.1098301501645));
#97414=CARTESIAN_POINT('Ctrl Pts',(-0.0842443173053113,-2.37581850165966,
21.0928479563442));
#97415=CARTESIAN_POINT('Ctrl Pts',(-0.246787335855732,-2.36446710196096,
21.0830378534763));
#97416=CARTESIAN_POINT('Ctrl Pts',(-0.473100331433842,-2.32505713966609,
21.0685175478187));
#97417=CARTESIAN_POINT('Ctrl Pts',(-0.538783804257595,-2.3107196511006,
21.0642025391191));
#97418=CARTESIAN_POINT('Ctrl Pts',(-0.620289577317182,-2.28926426309865,
21.0586777748752));
#97419=CARTESIAN_POINT('Ctrl Pts',(-0.636765737865761,-2.28473617637862,
21.057552162054));
#97420=CARTESIAN_POINT('Ctrl Pts',(-0.663022232907123,-2.27721412322809,
21.0557436345621));
#97421=CARTESIAN_POINT('Ctrl Pts',(-0.672834830991789,-2.27433417266923,
21.0550644369151));
#97422=CARTESIAN_POINT('Ctrl Pts',(-0.691394652965542,-2.26875633002332,
21.0537733514402));
#97423=CARTESIAN_POINT('Ctrl Pts',(-0.700145505347256,-2.26607107533139,
21.0531618872933));
#97424=CARTESIAN_POINT('Ctrl Pts',(-0.71997939247914,-2.2598590678387,21.0517696929393));
#97425=CARTESIAN_POINT('Ctrl Pts',(-0.731052399843292,-2.25630133456845,
21.0509879566445));
#97426=CARTESIAN_POINT('Ctrl Pts',(-0.759650405468366,-2.24688024200492,
21.0489571090471));
#97427=CARTESIAN_POINT('Ctrl Pts',(-0.777133562078111,-2.24089333823027,
21.0477039537643));
#97428=CARTESIAN_POINT('Ctrl Pts',(-0.90563739323192,-2.19520403470242,
21.0384050868149));
#97429=CARTESIAN_POINT('Ctrl Pts',(-1.01361218477934,-2.14748277048992,
21.0300917884416));
#97430=CARTESIAN_POINT('Ctrl Pts',(-1.29466764483622,-1.99733441905921,
21.0071203372578));
#97431=CARTESIAN_POINT('Ctrl Pts',(-1.45902101127502,-1.88062923851374,
20.9921480015438));
#97432=CARTESIAN_POINT('Ctrl Pts',(-1.62574206293377,-1.72708726458613,
20.9762773333855));
#97433=CARTESIAN_POINT('Ctrl Pts',(-1.64448947476798,-1.70924608585119,
20.9744829018701));
#97434=CARTESIAN_POINT('Ctrl Pts',(-1.66896422388565,-1.6851788678676,20.9721314757504));
#97435=CARTESIAN_POINT('Ctrl Pts',(-1.67495481219333,-1.67922475563294,
20.9715552100378));
#97436=CARTESIAN_POINT('Ctrl Pts',(-1.68476253771582,-1.66937204336446,
20.9706107646022));
#97437=CARTESIAN_POINT('Ctrl Pts',(-1.68859819205367,-1.66549211195983,
20.9702411540135));
#97438=CARTESIAN_POINT('Ctrl Pts',(-1.6960928164822,-1.6578584672812,20.9695185257588));
#97439=CARTESIAN_POINT('Ctrl Pts',(-1.6997527762559,-1.65410581286782,20.9691654335887));
#97440=CARTESIAN_POINT('Ctrl Pts',(-1.7087472918753,-1.64482211915427,20.9682971042078));
#97441=CARTESIAN_POINT('Ctrl Pts',(-1.71406752773735,-1.63927716559819,
20.9677829732597));
#97442=CARTESIAN_POINT('Ctrl Pts',(-1.73231273249455,-1.62007537331697,
20.9660176054774));
#97443=CARTESIAN_POINT('Ctrl Pts',(-1.7451025999597,-1.60629031901468,20.9647762290587));
#97444=CARTESIAN_POINT('Ctrl Pts',(-1.85582319130809,-1.48407086533995,
20.9539798535635));
#97445=CARTESIAN_POINT('Ctrl Pts',(-1.9437178133738,-1.36693803622698,20.9450492864254));
#97446=CARTESIAN_POINT('Ctrl Pts',(-2.08509320472877,-1.13705418035971,
20.9285137168175));
#97447=CARTESIAN_POINT('Ctrl Pts',(-2.141556035136,-1.02676216291712,20.9209404130938));
#97448=CARTESIAN_POINT('Ctrl Pts',(-2.20543298887878,-0.873528956500393,
20.910428351251));
#97449=CARTESIAN_POINT('Ctrl Pts',(-2.22066108025742,-0.834057281210004,
20.9077226876439));
#97450=CARTESIAN_POINT('Ctrl Pts',(-2.24499579089928,-0.76558116238951,
20.9030169534428));
#97451=CARTESIAN_POINT('Ctrl Pts',(-2.25461553340185,-0.73676948642199,
20.9010335023841));
#97452=CARTESIAN_POINT('Ctrl Pts',(-2.26750574033933,-0.695543108657033,
20.8981868038184));
#97453=CARTESIAN_POINT('Ctrl Pts',(-2.27123309547361,-0.683273527652343,
20.8973385213324));
#97454=CARTESIAN_POINT('Ctrl Pts',(-2.27750046492205,-0.662024743991826,
20.8958673381842));
#97455=CARTESIAN_POINT('Ctrl Pts',(-2.28008734843247,-0.653059575094418,
20.8952459815119));
#97456=CARTESIAN_POINT('Ctrl Pts',(-2.28494835572515,-0.635832138523277,
20.8940506494781));
#97457=CARTESIAN_POINT('Ctrl Pts',(-2.28723073930303,-0.627572337309024,
20.8934769540904));
#97458=CARTESIAN_POINT('Ctrl Pts',(-2.29249672779055,-0.608104704444415,
20.8921233391253));
#97459=CARTESIAN_POINT('Ctrl Pts',(-2.29544295997697,-0.596887081154943,
20.8913422211521));
#97460=CARTESIAN_POINT('Ctrl Pts',(-2.30542208102913,-0.557725224820697,
20.8886110197272));
#97461=CARTESIAN_POINT('Ctrl Pts',(-2.31202765169595,-0.529675757463541,
20.8866472759853));
#97462=CARTESIAN_POINT('Ctrl Pts',(-2.35393100300824,-0.335988205452596,
20.8730298617291));
#97463=CARTESIAN_POINT('Ctrl Pts',(-2.37190321514705,-0.167133874586679,
20.8608188306911));
#97464=CARTESIAN_POINT('Ctrl Pts',(-2.37169704770757,0.0592161657391793,
20.8442899294982));
#97465=CARTESIAN_POINT('Ctrl Pts',(-2.369586273947,0.116225454262654,20.8401188173442));
#97466=CARTESIAN_POINT('Ctrl Pts',(-2.3654264754702,0.173077010733998,20.8359749974364));
#97467=CARTESIAN_POINT('Ctrl Pts',(-2.36542650966497,0.173076543396847,
20.6413652673669));
#97468=CARTESIAN_POINT('Ctrl Pts',(-2.3696452004405,0.11541995515753,20.6455121880587));
#97469=CARTESIAN_POINT('Ctrl Pts',(-2.37175659210489,0.0575990783915476,
20.6496045891759));
#97470=CARTESIAN_POINT('Ctrl Pts',(-2.37174851271759,-0.0131612086354773,
20.6544884432378));
#97471=CARTESIAN_POINT('Ctrl Pts',(-2.3716419523089,-0.0260517523897936,
20.6553730834095));
#97472=CARTESIAN_POINT('Ctrl Pts',(-2.37132271330337,-0.045492707167401,
20.6566989915195));
#97473=CARTESIAN_POINT('Ctrl Pts',(-2.37118797917937,-0.0520438954879125,
20.6571443779233));
#97474=CARTESIAN_POINT('Ctrl Pts',(-2.37089793521941,-0.0637805144074743,
20.657939660729));
#97475=CARTESIAN_POINT('Ctrl Pts',(-2.37075276202606,-0.0689660517614046,
20.6582901073936));
#97476=CARTESIAN_POINT('Ctrl Pts',(-2.37039847004216,-0.0802926495732673,
20.6590535383995));
#97477=CARTESIAN_POINT('Ctrl Pts',(-2.37018250124127,-0.0864333809034787,
20.6594661376441));
#97478=CARTESIAN_POINT('Ctrl Pts',(-2.36949986201149,-0.103909434823094,
20.6606368515593));
#97479=CARTESIAN_POINT('Ctrl Pts',(-2.36897571476367,-0.115242537261224,
20.6613918447916));
#97480=CARTESIAN_POINT('Ctrl Pts',(-2.3649381690402,-0.190791822333342,
20.6663993688259));
#97481=CARTESIAN_POINT('Ctrl Pts',(-2.35889506676514,-0.254852587822693,
20.6705229562528));
#97482=CARTESIAN_POINT('Ctrl Pts',(-2.32100559644241,-0.534361006591841,
20.6882847708484));
#97483=CARTESIAN_POINT('Ctrl Pts',(-2.26218565627446,-0.745074381662656,
20.7011681468132));
#97484=CARTESIAN_POINT('Ctrl Pts',(-2.15062384474508,-1.00194545887362,
20.7189065764197));
#97485=CARTESIAN_POINT('Ctrl Pts',(-2.12357249757711,-1.0580720205822,20.7229106064955));
#97486=CARTESIAN_POINT('Ctrl Pts',(-2.08612418841368,-1.12853481350844,
20.7281390534488));
#97487=CARTESIAN_POINT('Ctrl Pts',(-2.07773185831141,-1.14391225728876,
20.7292927252315));
#97488=CARTESIAN_POINT('Ctrl Pts',(-2.06407996086349,-1.16828097766345,
20.7311419260452));
#97489=CARTESIAN_POINT('Ctrl Pts',(-2.05893006619404,-1.17733321716219,
20.7318335240213));
#97490=CARTESIAN_POINT('Ctrl Pts',(-2.04954324217532,-1.19358297260235,
20.733083617031));
#97491=CARTESIAN_POINT('Ctrl Pts',(-2.04532757367536,-1.20079262461028,
20.7336413358725));
#97492=CARTESIAN_POINT('Ctrl Pts',(-2.03532646531623,-1.21769108777459,
20.7349559052645));
#97493=CARTESIAN_POINT('Ctrl Pts',(-2.02950982341799,-1.22736110198178,
20.735713883741));
#97494=CARTESIAN_POINT('Ctrl Pts',(-2.01236812567664,-1.2554036767555,20.7379289626199));
#97495=CARTESIAN_POINT('Ctrl Pts',(-2.00086127924025,-1.27366320207019,
20.7393927066824));
#97496=CARTESIAN_POINT('Ctrl Pts',(-1.90068407350219,-1.42792002352111,
20.7519461498186));
#97497=CARTESIAN_POINT('Ctrl Pts',(-1.79853245359352,-1.55461158586091,
20.7635589884005));
#97498=CARTESIAN_POINT('Ctrl Pts',(-1.56870983101207,-1.78641745387736,
20.7873461045678));
#97499=CARTESIAN_POINT('Ctrl Pts',(-1.44135462155368,-1.89067267068279,
20.7994552010222));
#97500=CARTESIAN_POINT('Ctrl Pts',(-1.28924575722734,-1.99082041667007,
20.8121091302878));
#97501=CARTESIAN_POINT('Ctrl Pts',(-1.27413449596935,-2.00052540323376,
20.8133477085353));
#97502=CARTESIAN_POINT('Ctrl Pts',(-1.25309534420424,-2.0137023753804,20.8150451811488));
#97503=CARTESIAN_POINT('Ctrl Pts',(-1.24726090217526,-2.01732135346785,
20.8155130811788));
#97504=CARTESIAN_POINT('Ctrl Pts',(-1.23722129010457,-2.02348850161555,
20.8163132625005));
#97505=CARTESIAN_POINT('Ctrl Pts',(-1.23302380233644,-2.0260489976463,20.8166463349663));
#97506=CARTESIAN_POINT('Ctrl Pts',(-1.22424844119997,-2.03136465549287,
20.8173395370334));
#97507=CARTESIAN_POINT('Ctrl Pts',(-1.21966918587069,-2.03411742216213,
20.8176994992834));
#97508=CARTESIAN_POINT('Ctrl Pts',(-1.20850857505186,-2.0407752568808,20.8185725957647));
#97509=CARTESIAN_POINT('Ctrl Pts',(-1.20191746855148,-2.04466403791797,
20.8190846792412));
#97510=CARTESIAN_POINT('Ctrl Pts',(-1.17839443154228,-2.05838967932137,
20.8209001228028));
#97511=CARTESIAN_POINT('Ctrl Pts',(-1.16135906852133,-2.06804900427308,
20.8221926059982));
#97512=CARTESIAN_POINT('Ctrl Pts',(-1.11887979282501,-2.09144495780304,
20.8253657839801));
#97513=CARTESIAN_POINT('Ctrl Pts',(-1.09330005787436,-2.10492972531439,
20.8272330944833));
#97514=CARTESIAN_POINT('Ctrl Pts',(-0.88109591951423,-2.21188413214313,
20.8424228264066));
#97515=CARTESIAN_POINT('Ctrl Pts',(-0.683114109363354,-2.28081890118502,
20.8547781147088));
#97516=CARTESIAN_POINT('Ctrl Pts',(-0.390027147579792,-2.34120991195955,
20.873465687652));
#97517=CARTESIAN_POINT('Ctrl Pts',(-0.300444277150448,-2.35438215506194,
20.8792158416831));
#97518=CARTESIAN_POINT('Ctrl Pts',(-0.192728834378511,-2.36397252436587,
20.8862857501647));
#97519=CARTESIAN_POINT('Ctrl Pts',(-0.17510602318451,-2.36534317855025,
20.8874472191432));
#97520=CARTESIAN_POINT('Ctrl Pts',(-0.14602286956667,-2.36727839496821,
20.8893726702298));
#97521=CARTESIAN_POINT('Ctrl Pts',(-0.134570614173728,-2.36795701389958,
20.8901330772944));
#97522=CARTESIAN_POINT('Ctrl Pts',(-0.113870182078115,-2.36903299347542,
20.8915117342182));
#97523=CARTESIAN_POINT('Ctrl Pts',(-0.10462369074526,-2.36945935219341,
20.892129062778));
#97524=CARTESIAN_POINT('Ctrl Pts',(-0.0847955983121818,-2.37025734365144,
20.8934561991348));
#97525=CARTESIAN_POINT('Ctrl Pts',(-0.0742135639136895,-2.37061226463634,
20.894166516994));
#97526=CARTESIAN_POINT('Ctrl Pts',(-0.0453261631996215,-2.37138753908803,
20.8961113290445));
#97527=CARTESIAN_POINT('Ctrl Pts',(-0.0270180601373795,-2.37166677954516,
20.8973502045664));
#97528=CARTESIAN_POINT('Ctrl Pts',(0.0736176830453946,-2.37203631360565,
20.9041961852921));
#97529=CARTESIAN_POINT('Ctrl Pts',(0.155894547547436,-2.36805191886237,
20.9099291446253));
#97530=CARTESIAN_POINT('Ctrl Pts',(0.448260354323311,-2.33859110567113,
20.9307947711502));
#97531=CARTESIAN_POINT('Ctrl Pts',(0.654914652286427,-2.28932643646113,
20.9465618831532));
#97532=CARTESIAN_POINT('Ctrl Pts',(0.898435089325787,-2.19555419551166,
20.965171444833));
#97533=CARTESIAN_POINT('Ctrl Pts',(0.94402342773639,-2.17634198733309,20.968650677293));
#97534=CARTESIAN_POINT('Ctrl Pts',(0.998946105131645,-2.15114502962015,
20.9728091823508));
#97535=CARTESIAN_POINT('Ctrl Pts',(1.00887935094984,-2.14650430383177,20.9735599249432));
#97536=CARTESIAN_POINT('Ctrl Pts',(1.02431521825704,-2.13916197680044,20.9747240191271));
#97537=CARTESIAN_POINT('Ctrl Pts',(1.0298399911156,-2.13650771686113,20.9751401604018));
#97538=CARTESIAN_POINT('Ctrl Pts',(1.0400228023075,-2.13156692529489,20.9759061322126));
#97539=CARTESIAN_POINT('Ctrl Pts',(1.04468360199809,-2.12928653755461,20.9762563188353));
#97540=CARTESIAN_POINT('Ctrl Pts',(1.0552307346398,-2.12408317850289,20.9770478757895));
#97541=CARTESIAN_POINT('Ctrl Pts',(1.06111241955384,-2.12115102909511,20.9774886684539));
#97542=CARTESIAN_POINT('Ctrl Pts',(1.07896600048825,-2.1121577808734,20.9788250014417));
#97543=CARTESIAN_POINT('Ctrl Pts',(1.09089897173506,-2.10601936738839,20.9797158822237));
#97544=CARTESIAN_POINT('Ctrl Pts',(1.11844141151013,-2.09155440360074,20.9817682760086));
#97545=CARTESIAN_POINT('Ctrl Pts',(1.13401129003754,-2.08315372704289,20.9829256104635));
#97546=CARTESIAN_POINT('Ctrl Pts',(1.18727400993353,-2.05364183420262,20.986879794979));
#97547=CARTESIAN_POINT('Ctrl Pts',(1.22448509815896,-2.03167444999079,20.9896337950729));
#97548=CARTESIAN_POINT('Ctrl Pts',(1.44534283158833,-1.89301834351864,21.0060551261749));
#97549=CARTESIAN_POINT('Ctrl Pts',(1.61281711628574,-1.75253142672316,21.0189288848144));
#97550=CARTESIAN_POINT('Ctrl Pts',(1.80069029088014,-1.54486623879113,21.0366648561276));
#97551=CARTESIAN_POINT('Ctrl Pts',(1.84073424094568,-1.4969280527704,21.0406787183646));
#97552=CARTESIAN_POINT('Ctrl Pts',(1.88953829609246,-1.43357961271023,21.0459183491342));
#97553=CARTESIAN_POINT('Ctrl Pts',(1.90008418972768,-1.41957230280426,21.0470729903874));
#97554=CARTESIAN_POINT('Ctrl Pts',(1.91664703559409,-1.39705788601958,21.0489233826871));
#97555=CARTESIAN_POINT('Ctrl Pts',(1.92276504495133,-1.38862564139934,21.0496151937078));
#97556=CARTESIAN_POINT('Ctrl Pts',(1.93368691997316,-1.37336182459283,21.050865464682));
#97557=CARTESIAN_POINT('Ctrl Pts',(1.93851066049169,-1.36654462854578,21.0514231469281));
#97558=CARTESIAN_POINT('Ctrl Pts',(1.94976489629137,-1.35045997626401,21.0527373563463));
#97559=CARTESIAN_POINT('Ctrl Pts',(1.95616543479715,-1.34117190634214,21.0534950094901));
#97560=CARTESIAN_POINT('Ctrl Pts',(1.97460591897388,-1.31399936692707,21.0557081961122));
#97561=CARTESIAN_POINT('Ctrl Pts',(1.98646829077914,-1.2959963532558,21.0571703558814));
#97562=CARTESIAN_POINT('Ctrl Pts',(2.09089826377963,-1.13270466061889,21.0703990697946));
#97563=CARTESIAN_POINT('Ctrl Pts',(2.167606231319,-0.977924221130729,21.0827603247273));
#97564=CARTESIAN_POINT('Ctrl Pts',(2.27969697486948,-0.672117107464571,
21.1065238119082));
#97565=CARTESIAN_POINT('Ctrl Pts',(2.31841202263608,-0.523195624988745,
21.1178138206501));
#97566=CARTESIAN_POINT('Ctrl Pts',(2.34536531780108,-0.353274135405132,
21.1297753641064));
#97567=CARTESIAN_POINT('Ctrl Pts',(2.34805262375522,-0.334947784231481,
21.1310533285733));
#97568=CARTESIAN_POINT('Ctrl Pts',(2.35145144164751,-0.309713323131881,
21.1327947063899));
#97569=CARTESIAN_POINT('Ctrl Pts',(2.35234763376866,-0.302831368788849,
21.1332677481744));
#97570=CARTESIAN_POINT('Ctrl Pts',(2.35382959894123,-0.291047506660982,
21.1340744226826));
#97571=CARTESIAN_POINT('Ctrl Pts',(2.35443029190172,-0.28614757330336,21.1344088745463));
#97572=CARTESIAN_POINT('Ctrl Pts',(2.35564736421591,-0.275956398973795,
21.135102406473));
#97573=CARTESIAN_POINT('Ctrl Pts',(2.35626122041093,-0.270664922967461,
21.1354613312695));
#97574=CARTESIAN_POINT('Ctrl Pts',(2.35770402871674,-0.257850831249838,
21.1363277759289));
#97575=CARTESIAN_POINT('Ctrl Pts',(2.35851482188043,-0.250326141538377,
21.136834283689));
#97576=CARTESIAN_POINT('Ctrl Pts',(2.3612388165966,-0.223856797556103,21.1386083852662));
#97577=CARTESIAN_POINT('Ctrl Pts',(2.36295995288263,-0.204892491303803,
21.1398657465504));
#97578=CARTESIAN_POINT('Ctrl Pts',(2.3666362029517,-0.158136661947514,21.1429365403592));
#97579=CARTESIAN_POINT('Ctrl Pts',(2.36833045979948,-0.130326901984869,
21.1447376784462));
#97580=CARTESIAN_POINT('Ctrl Pts',(2.37760100822646,0.0839999240548525,
21.1584683102904));
#97581=CARTESIAN_POINT('Ctrl Pts',(2.36362421554544,0.270809630366736,21.1696041734351));
#97582=CARTESIAN_POINT('Ctrl Pts',(2.30630342376191,0.564680969256217,21.1881462629775));
#97583=CARTESIAN_POINT('Ctrl Pts',(2.27687258857723,0.673606879778546,21.1952469049075));
#97584=CARTESIAN_POINT('Ctrl Pts',(2.23373210864795,0.797484129998888,21.203814806863));
#97585=CARTESIAN_POINT('Ctrl Pts',(2.22744607681222,0.81487668628204,21.2050291609565));
#97586=CARTESIAN_POINT('Ctrl Pts',(2.216844708056,0.843169609951421,21.2070241726166));
#97587=CARTESIAN_POINT('Ctrl Pts',(2.21265073162711,0.854114853081182,21.2078007880634));
#97588=CARTESIAN_POINT('Ctrl Pts',(2.20499183407692,0.873667649917114,21.2091970483341));
#97589=CARTESIAN_POINT('Ctrl Pts',(2.2015571838178,0.882286865498201,21.2098156657354));
#97590=CARTESIAN_POINT('Ctrl Pts',(2.19415687556208,0.900545563355231,21.2111328798036));
#97591=CARTESIAN_POINT('Ctrl Pts',(2.19017808066226,0.910179474181156,21.2118319100923));
#97592=CARTESIAN_POINT('Ctrl Pts',(2.17932704549678,0.935970060086562,21.2137142600443));
#97593=CARTESIAN_POINT('Ctrl Pts',(2.17233879851819,0.952076908717332,21.2149014988092));
#97594=CARTESIAN_POINT('Ctrl Pts',(2.13608856483242,1.03315082705193,21.2209380053448));
#97595=CARTESIAN_POINT('Ctrl Pts',(2.10409118424908,1.09684703299919,21.2258803285694));
#97596=CARTESIAN_POINT('Ctrl Pts',(1.99609897720886,1.28965611120571,21.2414843083434));
#97597=CARTESIAN_POINT('Ctrl Pts',(1.91071657903993,1.41307334109011,21.252436384304));
#97598=CARTESIAN_POINT('Ctrl Pts',(1.80496131492765,1.53867548534734,21.264418347522));
#97599=CARTESIAN_POINT('Ctrl Pts',(1.79553678556956,1.54966294839946,21.2654738977897));
#97600=CARTESIAN_POINT('Ctrl Pts',(1.71627096695985,1.64038000044255,21.2742474841337));
#97601=CARTESIAN_POINT('Ctrl Pts',(1.64124847199267,1.71544210806391,21.2818925338484));
#97602=CARTESIAN_POINT('Ctrl Pts',(1.55183822849854,1.79364408996817,21.2900895254204));
#97603=CARTESIAN_POINT('Ctrl Pts',(1.54216188838417,1.80197051506445,21.2909654446803));
#97604=CARTESIAN_POINT('Ctrl Pts',(1.52743779261396,1.81443501888759,21.2922808821841));
#97605=CARTESIAN_POINT('Ctrl Pts',(1.52243960168572,1.81863088885225,21.2927244254997));
#97606=CARTESIAN_POINT('Ctrl Pts',(1.5134383539737,1.82612412125847,21.2935177553389));
#97607=CARTESIAN_POINT('Ctrl Pts',(1.50944176038794,1.82942901780323,21.2938680801313));
#97608=CARTESIAN_POINT('Ctrl Pts',(1.50066973026009,1.83663454186072,21.2946328093154));
#97609=CARTESIAN_POINT('Ctrl Pts',(1.49588991818402,1.84052966141355,21.2950468186593));
#97610=CARTESIAN_POINT('Ctrl Pts',(1.48219464625476,1.85160149075079,21.2962255844801));
#97611=CARTESIAN_POINT('Ctrl Pts',(1.47324220181304,1.85873249228641,21.2969871515889));
#97612=CARTESIAN_POINT('Ctrl Pts',(1.41175610405579,1.90698544825356,21.3021594392204));
#97613=CARTESIAN_POINT('Ctrl Pts',(1.35755378371209,1.94594409293718,21.3064312754567));
#97614=CARTESIAN_POINT('Ctrl Pts',(1.089027520532,2.12226120962693,21.3266302084878));
#97615=CARTESIAN_POINT('Ctrl Pts',(0.855190424216477,2.22679966279556,21.3415830952711));
#97616=CARTESIAN_POINT('Ctrl Pts',(0.578722595261967,2.30027655249391,21.3600797859028));
#97617=CARTESIAN_POINT('Ctrl Pts',(0.548095414337796,2.30776587287932,21.3621361185582));
#97618=CARTESIAN_POINT('Ctrl Pts',(0.505460803794458,2.31729483088571,21.3650127179139));
#97619=CARTESIAN_POINT('Ctrl Pts',(0.493572383321684,2.31985608402364,21.3658163383191));
#97620=CARTESIAN_POINT('Ctrl Pts',(0.473054137302115,2.3241116973564,21.367206120419));
#97621=CARTESIAN_POINT('Ctrl Pts',(0.464433534357405,2.32584971294576,21.3677908797526));
#97622=CARTESIAN_POINT('Ctrl Pts',(0.446581686602045,2.32934565147967,21.369003675859));
#97623=CARTESIAN_POINT('Ctrl Pts',(0.437349275352296,2.33109673197665,21.3696319190955));
#97624=CARTESIAN_POINT('Ctrl Pts',(0.415712591092952,2.3350674282499,21.3711067547596));
#97625=CARTESIAN_POINT('Ctrl Pts',(0.403300649788364,2.3372431255799,21.3719547262087));
#97626=CARTESIAN_POINT('Ctrl Pts',(0.362805276837944,2.34400941477819,21.3747279435138));
#97627=CARTESIAN_POINT('Ctrl Pts',(0.33465738406256,2.34819337315646,21.3766659500521));
#97628=CARTESIAN_POINT('Ctrl Pts',(0.184345764931605,2.36777855768801,21.3870745291786));
#97629=CARTESIAN_POINT('Ctrl Pts',(0.0612154670472332,2.37415305845575,
21.3958240202191));
#97630=CARTESIAN_POINT('Ctrl Pts',(-0.111553816657242,2.3696470897217,21.4083459363374));
#97631=CARTESIAN_POINT('Ctrl Pts',(-0.16121722612389,2.36678693061316,21.4119718441474));
#97632=CARTESIAN_POINT('Ctrl Pts',(-0.35160722406399,2.34980175411044,21.4259301487461));
#97633=CARTESIAN_POINT('Ctrl Pts',(-0.491069034400797,2.32466230383876,
21.4362940625826));
#97634=CARTESIAN_POINT('Ctrl Pts',(-0.645797912876436,2.28221477861414,
21.4474551150239));
#97635=CARTESIAN_POINT('Ctrl Pts',(-0.664065076890717,2.27696659421323,
21.4487669659708));
#97636=CARTESIAN_POINT('Ctrl Pts',(-0.689721124159214,2.26926053938407,
21.4505993489995));
#97637=CARTESIAN_POINT('Ctrl Pts',(-0.697163425399591,2.26698517580838,
21.4511296803836));
#97638=CARTESIAN_POINT('Ctrl Pts',(-0.70966936518123,2.26309427589203,21.4520186523635));
#97639=CARTESIAN_POINT('Ctrl Pts',(-0.714738969277246,2.26149829034101,
21.4523784119759));
#97640=CARTESIAN_POINT('Ctrl Pts',(-0.725083850661469,2.25820330918063,
21.453111224038));
#97641=CARTESIAN_POINT('Ctrl Pts',(-0.730358602131399,2.25650284511101,
21.4534841881488));
#97642=CARTESIAN_POINT('Ctrl Pts',(-0.743806376482816,2.25211548385002,
21.4544334006122));
#97643=CARTESIAN_POINT('Ctrl Pts',(-0.751970918170312,2.24940254784854,
21.455008140662));
#97644=CARTESIAN_POINT('Ctrl Pts',(-0.784589988457899,2.23836634604835,
21.4572987982288));
#97645=CARTESIAN_POINT('Ctrl Pts',(-0.808923671612739,2.2296878658109,21.4589950968454));
#97646=CARTESIAN_POINT('Ctrl Pts',(-1.02135635090556,2.1499890663138,21.4737337164913));
#97647=CARTESIAN_POINT('Ctrl Pts',(-1.19988225430784,2.05570618049798,21.4856895851367));
#97648=CARTESIAN_POINT('Ctrl Pts',(-1.46000987859554,1.87276143993761,21.5053579807119));
#97649=CARTESIAN_POINT('Ctrl Pts',(-1.55051696540666,1.79854270958477,21.5127110460673));
#97650=CARTESIAN_POINT('Ctrl Pts',(-1.64866421063376,1.70512494015636,21.5215601578593));
#97651=CARTESIAN_POINT('Ctrl Pts',(-1.66199902562371,1.692130003073,21.5227826478116));
#97652=CARTESIAN_POINT('Ctrl Pts',(-1.6835036541298,1.67067405267722,21.5247883460952));
#97653=CARTESIAN_POINT('Ctrl Pts',(-1.69176613996554,1.66230672951337,21.5255674381987));
#97654=CARTESIAN_POINT('Ctrl Pts',(-1.70643871200612,1.64722528691826,21.52696642653));
#97655=CARTESIAN_POINT('Ctrl Pts',(-1.71287229353528,1.64053428050837,21.5275852791132));
#97656=CARTESIAN_POINT('Ctrl Pts',(-1.72643065326025,1.62626671440785,21.5289011618166));
#97657=CARTESIAN_POINT('Ctrl Pts',(-1.73354518531059,1.61868073177298,21.5295986146523));
#97658=CARTESIAN_POINT('Ctrl Pts',(-1.75167199125929,1.59909616036568,21.5313937829524));
#97659=CARTESIAN_POINT('Ctrl Pts',(-1.76261083762612,1.58703065724405,21.5324945796743));
#97660=CARTESIAN_POINT('Ctrl Pts',(-1.81438669085634,1.52872647525026,21.5377904706223));
#97661=CARTESIAN_POINT('Ctrl Pts',(-1.85353017782231,1.48102274075293,21.5420546422733));
#97662=CARTESIAN_POINT('Ctrl Pts',(-1.96079502784208,1.33937895031534,21.5545343906508));
#97663=CARTESIAN_POINT('Ctrl Pts',(-2.0239369689956,1.241904399001,21.5629146522692));
#97664=CARTESIAN_POINT('Ctrl Pts',(-2.15499440917576,1.00286257298039,21.5827983924731));
#97665=CARTESIAN_POINT('Ctrl Pts',(-2.21651301019787,0.858377939139675,
21.5943298494037));
#97666=CARTESIAN_POINT('Ctrl Pts',(-2.26881328028884,0.691389883826201,
21.6064931701347));
#97667=CARTESIAN_POINT('Ctrl Pts',(-2.2740861633845,0.673844081010464,21.6077570459858));
#97668=CARTESIAN_POINT('Ctrl Pts',(-2.28106826297322,0.64959482498718,21.6094827235657));
#97669=CARTESIAN_POINT('Ctrl Pts',(-2.28295208999073,0.642942932797866,
21.6099539288732));
#97670=CARTESIAN_POINT('Ctrl Pts',(-2.28612928575771,0.631534045628689,
21.6107582828366));
#97671=CARTESIAN_POINT('Ctrl Pts',(-2.28743694512057,0.626781130241172,
21.6110922406155));
#97672=CARTESIAN_POINT('Ctrl Pts',(-2.2901283108459,0.616878284436149,21.611785643129));
#97673=CARTESIAN_POINT('Ctrl Pts',(-2.291509477117,0.611727729402215,21.6121449283164));
#97674=CARTESIAN_POINT('Ctrl Pts',(-2.29481638174934,0.599227470959713,
21.6130137024167));
#97675=CARTESIAN_POINT('Ctrl Pts',(-2.29672421985806,0.59187300143213,21.613522165707));
#97676=CARTESIAN_POINT('Ctrl Pts',(-2.3007227584584,0.576148655046813,21.6146038382331));
#97677=CARTESIAN_POINT('Ctrl Pts',(-2.30280320806519,0.567776253862717,
21.6151764832947));
#97678=CARTESIAN_POINT('Ctrl Pts',(-2.31151018542596,0.531901316625478,
21.6176168919629));
#97679=CARTESIAN_POINT('Ctrl Pts',(-2.31769036539249,0.504291469635803,
21.6194616419155));
#97680=CARTESIAN_POINT('Ctrl Pts',(-2.34393021934912,0.376368534512657,
21.6278830901827));
#97681=CARTESIAN_POINT('Ctrl Pts',(-2.35796962568734,0.274989332207001,
21.6342053888481));
#97682=CARTESIAN_POINT('Ctrl Pts',(-2.36542651121823,0.173076522168559,
21.6404818371561));
#97683=CARTESIAN_POINT('Origin',(0.,0.,-1.84858989190503));
#97684=CARTESIAN_POINT('',(-2.36542647205564,0.173077057400502,22.8373161962119));
#97685=CARTESIAN_POINT('',(-2.36542649454112,0.173076750093424,22.6375488994376));
#97686=CARTESIAN_POINT('',(-2.36542649454111,0.173076750093529,-1.84858989190503));
#97687=CARTESIAN_POINT('',(-2.37174999975095,-3.43714120204603E-5,21.8508342761113));
#97688=CARTESIAN_POINT('Ctrl Pts',(-2.36542647205563,0.173077057400639,
22.8373161962119));
#97689=CARTESIAN_POINT('Ctrl Pts',(-2.35558699271399,0.307552216936542,
22.8290336145396));
#97690=CARTESIAN_POINT('Ctrl Pts',(-2.33429152119662,0.441040438584974,
22.8206514246345));
#97691=CARTESIAN_POINT('Ctrl Pts',(-2.29496692921169,0.599256497923799,
22.8100741087363));
#97692=CARTESIAN_POINT('Ctrl Pts',(-2.28773509460163,0.626298319391269,
22.8082437799283));
#97693=CARTESIAN_POINT('Ctrl Pts',(-2.27694933891818,0.663946245068075,
22.8056612080991));
#97694=CARTESIAN_POINT('Ctrl Pts',(-2.27379623434611,0.674665536243362,
22.8049219575777));
#97695=CARTESIAN_POINT('Ctrl Pts',(-2.26787604431434,0.694278808476925,
22.8035619283539));
#97696=CARTESIAN_POINT('Ctrl Pts',(-2.26513206928857,0.70317957927455,22.8029419144976));
#97697=CARTESIAN_POINT('Ctrl Pts',(-2.25945757425223,0.721208318025415,
22.8016802306059));
#97698=CARTESIAN_POINT('Ctrl Pts',(-2.25652399827277,0.730335134288215,
22.8010384700706));
#97699=CARTESIAN_POINT('Ctrl Pts',(-2.24912857528644,0.752873488223653,
22.7994459761405));
#97700=CARTESIAN_POINT('Ctrl Pts',(-2.24460206797607,0.766263256834902,
22.7984931247612));
#97701=CARTESIAN_POINT('Ctrl Pts',(-2.22713477775099,0.81644974683606,22.7948956662897));
#97702=CARTESIAN_POINT('Ctrl Pts',(-2.21340722534166,0.852964036057281,
22.7922251760598));
#97703=CARTESIAN_POINT('Ctrl Pts',(-2.17666804699988,0.943819568435279,
22.7854416365893));
#97704=CARTESIAN_POINT('Ctrl Pts',(-2.15251820409061,0.997669059529739,
22.7812929824227));
#97705=CARTESIAN_POINT('Ctrl Pts',(-2.07201206217199,1.1606178629502,22.7683453512165));
#97706=CARTESIAN_POINT('Ctrl Pts',(-2.00917770111188,1.26628117659205,22.7593750808445));
#97707=CARTESIAN_POINT('Ctrl Pts',(-1.89825471466519,1.42362031733921,22.7453172574431));
#97708=CARTESIAN_POINT('Ctrl Pts',(-1.85555564309847,1.47884409746286,22.7402344746356));
#97709=CARTESIAN_POINT('Ctrl Pts',(-1.77168369245427,1.57795511168974,22.7309207641472));
#97710=CARTESIAN_POINT('Ctrl Pts',(-1.73115354122448,1.62231756327132,22.7266732180056));
#97711=CARTESIAN_POINT('Ctrl Pts',(-1.68162793909208,1.67255348792312,22.7218143507961));
#97712=CARTESIAN_POINT('Ctrl Pts',(-1.67422755887628,1.67996124560529,22.7210965650793));
#97713=CARTESIAN_POINT('Ctrl Pts',(-1.66213391704839,1.69190765733032,22.7199372403654));
#97714=CARTESIAN_POINT('Ctrl Pts',(-1.65747064748957,1.6964762699333,22.7194934610599));
#97715=CARTESIAN_POINT('Ctrl Pts',(-1.64911763937748,1.70459240613741,22.718704426452));
#97716=CARTESIAN_POINT('Ctrl Pts',(-1.64543523197978,1.70814728834145,22.7183586049754));
#97717=CARTESIAN_POINT('Ctrl Pts',(-1.63741204944231,1.71584259941598,22.7176095261008));
#97718=CARTESIAN_POINT('Ctrl Pts',(-1.63306707023926,1.71997848584083,22.7172066166591));
#97719=CARTESIAN_POINT('Ctrl Pts',(-1.62077612658569,1.73158939169322,22.7160744572582));
#97720=CARTESIAN_POINT('Ctrl Pts',(-1.61279408389704,1.73902625866763,22.7153480652338));
#97721=CARTESIAN_POINT('Ctrl Pts',(-1.56258377561651,1.78516412404157,22.7108316097686));
#97722=CARTESIAN_POINT('Ctrl Pts',(-1.51901245084755,1.82238344986652,22.7071438034318));
#97723=CARTESIAN_POINT('Ctrl Pts',(-1.4094963585779,1.90927359956167,22.6982998598725));
#97724=CARTESIAN_POINT('Ctrl Pts',(-1.34222459859286,1.95715111485792,22.6932171694765));
#97725=CARTESIAN_POINT('Ctrl Pts',(-1.11425013608458,2.10210672777954,22.6766430167731));
#97726=CARTESIAN_POINT('Ctrl Pts',(-0.944543093247345,2.18362885398592,
22.6652379419402));
#97727=CARTESIAN_POINT('Ctrl Pts',(-0.740621758548927,2.25332093868393,
22.6512619433395));
#97728=CARTESIAN_POINT('Ctrl Pts',(-0.714075617626403,2.26187350378313,
22.6494391119012));
#97729=CARTESIAN_POINT('Ctrl Pts',(-0.676420285763294,2.27327625387389,
22.6468458191595));
#97730=CARTESIAN_POINT('Ctrl Pts',(-0.665431093368501,2.27651724825956,
22.6460880995843));
#97731=CARTESIAN_POINT('Ctrl Pts',(-0.646215722718315,2.28203333490999,
22.6447614043192));
#97732=CARTESIAN_POINT('Ctrl Pts',(-0.637999877120554,2.28434390043603,
22.6441935927472));
#97733=CARTESIAN_POINT('Ctrl Pts',(-0.620746864045961,2.28909567769971,
22.6429999432978));
#97734=CARTESIAN_POINT('Ctrl Pts',(-0.611707374740382,2.2915278253219,22.6423738225227));
#97735=CARTESIAN_POINT('Ctrl Pts',(-0.590090430321594,2.29720701722337,
22.6408746796482));
#97736=CARTESIAN_POINT('Ctrl Pts',(-0.57750034500473,2.30040434179363,22.6400000669896));
#97737=CARTESIAN_POINT('Ctrl Pts',(-0.534407804666629,2.31097188849553,
22.6370010486823));
#97738=CARTESIAN_POINT('Ctrl Pts',(-0.503786787611022,2.31783983026575,
22.6348606371386));
#97739=CARTESIAN_POINT('Ctrl Pts',(-0.429785016831794,2.33290192351682,
22.6296630101178));
#97740=CARTESIAN_POINT('Ctrl Pts',(-0.386295519493603,2.34049607573808,
22.6265879437685));
#97741=CARTESIAN_POINT('Ctrl Pts',(-0.0971590420607199,2.38270735080721,
22.6060066556091));
#97742=CARTESIAN_POINT('Ctrl Pts',(0.152350240948549,2.37980882727667,22.5873753595239));
#97743=CARTESIAN_POINT('Ctrl Pts',(0.4300275982135,2.3326822994552,22.5675108026101));
#97744=CARTESIAN_POINT('Ctrl Pts',(0.463082687731045,2.326345881876,22.5651643152334));
#97745=CARTESIAN_POINT('Ctrl Pts',(0.505442078512209,2.31728714684873,22.562190204124));
#97746=CARTESIAN_POINT('Ctrl Pts',(0.51487815816828,2.31520882558411,22.5615298004521));
#97747=CARTESIAN_POINT('Ctrl Pts',(0.529884866660682,2.31180727278781,22.5604831830983));
#97748=CARTESIAN_POINT('Ctrl Pts',(0.535463731421846,2.31052146333716,22.5600949022876));
#97749=CARTESIAN_POINT('Ctrl Pts',(0.546072755444561,2.30803582054928,22.559358139311));
#97750=CARTESIAN_POINT('Ctrl Pts',(0.551103589105282,2.30683975120977,22.5590094634566));
#97751=CARTESIAN_POINT('Ctrl Pts',(0.562923237103904,2.30398878379735,22.5581918517174));
#97752=CARTESIAN_POINT('Ctrl Pts',(0.569708702060304,2.30232032625334,22.5577236981664));
#97753=CARTESIAN_POINT('Ctrl Pts',(0.591947468725474,2.2967477653618,22.5561930852083));
#97754=CARTESIAN_POINT('Ctrl Pts',(0.607369211444168,2.29271777127163,22.5551375672198));
#97755=CARTESIAN_POINT('Ctrl Pts',(0.644121114734362,2.28271693628169,22.5526336856405));
#97756=CARTESIAN_POINT('Ctrl Pts',(0.66541091189813,2.27660207741005,22.5511925801612));
#97757=CARTESIAN_POINT('Ctrl Pts',(0.744663886734401,2.25263222773845,22.5458522046485));
#97758=CARTESIAN_POINT('Ctrl Pts',(0.802024664869938,2.23285328398392,22.5420355862054));
#97759=CARTESIAN_POINT('Ctrl Pts',(1.05832617816016,2.13332245266067,22.5249436467309));
#97760=CARTESIAN_POINT('Ctrl Pts',(1.24664005681874,2.02904140806073,22.5121792189246));
#97761=CARTESIAN_POINT('Ctrl Pts',(1.45399992596791,1.87431487606233,22.4956071657126));
#97762=CARTESIAN_POINT('Ctrl Pts',(1.48885312322667,1.84675066100328,22.4927280640453));
#97763=CARTESIAN_POINT('Ctrl Pts',(1.53468669184813,1.80836136024325,22.4888011560118));
#97764=CARTESIAN_POINT('Ctrl Pts',(1.54636706648699,1.7983834208659,22.4877876376396));
#97765=CARTESIAN_POINT('Ctrl Pts',(1.56537471926271,1.78182407411574,22.4861167247011));
#97766=CARTESIAN_POINT('Ctrl Pts',(1.5727595178514,1.77530913837813,22.4854620923861));
#97767=CARTESIAN_POINT('Ctrl Pts',(1.58701347531288,1.76257543013912,22.4841877667408));
#97768=CARTESIAN_POINT('Ctrl Pts',(1.59388719573426,1.75636201302964,22.4835683055141));
#97769=CARTESIAN_POINT('Ctrl Pts',(1.60990487013122,1.74171156191803,22.4821130413663));
#97770=CARTESIAN_POINT('Ctrl Pts',(1.61901912209831,1.73324260499905,22.4812758878397));
#97771=CARTESIAN_POINT('Ctrl Pts',(1.64853913227364,1.70537662186464,22.4785342396491));
#97772=CARTESIAN_POINT('Ctrl Pts',(1.66866555270957,1.6856885379369,22.476617224451));
#97773=CARTESIAN_POINT('Ctrl Pts',(1.77399912010252,1.57891385698854,22.4663210974556));
#97774=CARTESIAN_POINT('Ctrl Pts',(1.85273845465151,1.48573002426072,22.4576685100779));
#97775=CARTESIAN_POINT('Ctrl Pts',(2.00770207900375,1.27076213515345,22.4384757527063));
#97776=CARTESIAN_POINT('Ctrl Pts',(2.08074637188678,1.14725680127547,22.427904910793));
#97777=CARTESIAN_POINT('Ctrl Pts',(2.16855310511449,0.962467910526155,22.4132183864481));
#97778=CARTESIAN_POINT('Ctrl Pts',(2.19274144681989,0.906009656431272,22.4088737109581));
#97779=CARTESIAN_POINT('Ctrl Pts',(2.21849728124602,0.838796577063157,22.4039151222576));
#97780=CARTESIAN_POINT('Ctrl Pts',(2.22221514221361,0.828896710543056,22.4031901058899));
#97781=CARTESIAN_POINT('Ctrl Pts',(2.22813159768663,0.812816502391584,22.4020214760737));
#97782=CARTESIAN_POINT('Ctrl Pts',(2.23037093462263,0.806651461163442,22.4015755638971));
#97783=CARTESIAN_POINT('Ctrl Pts',(2.23431286400689,0.795657154061061,22.4007842464348));
#97784=CARTESIAN_POINT('Ctrl Pts',(2.23602541830358,0.790831594938553,22.4004382612361));
#97785=CARTESIAN_POINT('Ctrl Pts',(2.23970269751516,0.780362477826645,22.3996905463802));
#97786=CARTESIAN_POINT('Ctrl Pts',(2.24166172466497,0.774717034943749,22.3992891540903));
#97787=CARTESIAN_POINT('Ctrl Pts',(2.24710241347357,0.758844853203738,22.3981655556702));
#97788=CARTESIAN_POINT('Ctrl Pts',(2.25053562617268,0.748601478982124,22.3974461389909));
#97789=CARTESIAN_POINT('Ctrl Pts',(2.27108654838645,0.685866116138081,22.3930728651433));
#97790=CARTESIAN_POINT('Ctrl Pts',(2.28643854959801,0.63280829443864,22.3895139067073));
#97791=CARTESIAN_POINT('Ctrl Pts',(2.33567686229873,0.437309186656213,22.3767417755981));
#97792=CARTESIAN_POINT('Ctrl Pts',(2.35821259573262,0.292345100244275,22.3679059322618));
#97793=CARTESIAN_POINT('Ctrl Pts',(2.37573060778353,0.0087345427848194,
22.3504251767472));
#97794=CARTESIAN_POINT('Ctrl Pts',(2.37222878365669,-0.129208747688607,
22.3418307580727));
#97795=CARTESIAN_POINT('Ctrl Pts',(2.35467101395557,-0.284738299946942,
22.3316111759174));
#97796=CARTESIAN_POINT('Ctrl Pts',(2.35234014830279,-0.303392940979651,
22.3303770596217));
#97797=CARTESIAN_POINT('Ctrl Pts',(2.34819565296708,-0.333635662487942,
22.3283618240845));
#97798=CARTESIAN_POINT('Ctrl Pts',(2.34651736325497,-0.345241705859396,
22.3275849727099));
#97799=CARTESIAN_POINT('Ctrl Pts',(2.34337426835055,-0.365894917318421,
22.3261961356001));
#97800=CARTESIAN_POINT('Ctrl Pts',(2.34194295242273,-0.374947003757861,
22.3255852220063));
#97801=CARTESIAN_POINT('Ctrl Pts',(2.33881233944465,-0.394028394591959,
22.3242926905392));
#97802=CARTESIAN_POINT('Ctrl Pts',(2.33710091524349,-0.404055492786182,
22.3236106987906));
#97803=CARTESIAN_POINT('Ctrl Pts',(2.33238516107864,-0.430651934568372,
22.3217942003855));
#97804=CARTESIAN_POINT('Ctrl Pts',(2.3292688244095,-0.447200566225111,22.3206561536112));
#97805=CARTESIAN_POINT('Ctrl Pts',(2.31343137277644,-0.526640743817441,
22.3151544099515));
#97806=CARTESIAN_POINT('Ctrl Pts',(2.29833889832132,-0.589026421161469,
22.3107158148247));
#97807=CARTESIAN_POINT('Ctrl Pts',(2.24667769393948,-0.770096421624441,
22.2974731939092));
#97808=CARTESIAN_POINT('Ctrl Pts',(2.20330182225574,-0.886602234784846,
22.2884769534929));
#97809=CARTESIAN_POINT('Ctrl Pts',(2.08969720088046,-1.13117159459081,22.2687865486903));
#97810=CARTESIAN_POINT('Ctrl Pts',(2.01635211822775,-1.25726515815862,22.2581052159777));
#97811=CARTESIAN_POINT('Ctrl Pts',(1.92099084130839,-1.39116713934443,22.2466725232534));
#97812=CARTESIAN_POINT('Ctrl Pts',(1.90989778446525,-1.40635782459123,22.2453744506698));
#97813=CARTESIAN_POINT('Ctrl Pts',(1.89401888562998,-1.42756771711007,22.2435623154559));
#97814=CARTESIAN_POINT('Ctrl Pts',(1.88938305526383,-1.43369759737538,22.2430386246045));
#97815=CARTESIAN_POINT('Ctrl Pts',(1.88153516020645,-1.44397056154901,22.2421611902558));
#97816=CARTESIAN_POINT('Ctrl Pts',(1.87833903752116,-1.44812568643083,22.2418063514578));
#97817=CARTESIAN_POINT('Ctrl Pts',(1.87178857893538,-1.45658344802342,22.2410842537291));
#97818=CARTESIAN_POINT('Ctrl Pts',(1.86843313390856,-1.4608851600815,22.2407170768141));
#97819=CARTESIAN_POINT('Ctrl Pts',(1.85984586255607,-1.47181613912727,22.2397841711837));
#97820=CARTESIAN_POINT('Ctrl Pts',(1.85459336189353,-1.47842918238691,22.2392198924448));
#97821=CARTESIAN_POINT('Ctrl Pts',(1.83310875999604,-1.50518420920423,22.2369367355733));
#97822=CARTESIAN_POINT('Ctrl Pts',(1.81658223073776,-1.52508896983998,22.2352376846321));
#97823=CARTESIAN_POINT('Ctrl Pts',(1.66898045397467,-1.69705777631759,22.2205137942694));
#97824=CARTESIAN_POINT('Ctrl Pts',(1.51939838463671,-1.83219894696173,22.2085757046488));
#97825=CARTESIAN_POINT('Ctrl Pts',(1.25777705256605,-2.0142232443051,22.1888706192198));
#97826=CARTESIAN_POINT('Ctrl Pts',(1.15612409711372,-2.07423957517887,22.1814570447898));
#97827=CARTESIAN_POINT('Ctrl Pts',(1.03387126812045,-2.13463106299017,22.172550809892));
#97828=CARTESIAN_POINT('Ctrl Pts',(1.01720788026547,-2.14262168163942,22.1713373490584));
#97829=CARTESIAN_POINT('Ctrl Pts',(0.989907924936696,-2.15532262892487,
22.1693492213105));
#97830=CARTESIAN_POINT('Ctrl Pts',(0.979326869954151,-2.16015096884906,
22.1685786324842));
#97831=CARTESIAN_POINT('Ctrl Pts',(0.960355589066737,-2.16863989490611,
22.1671967653391));
#97832=CARTESIAN_POINT('Ctrl Pts',(0.951978819150639,-2.17233012571177,
22.1665865186913));
#97833=CARTESIAN_POINT('Ctrl Pts',(0.93419870359439,-2.18004023469208,22.165290958559));
#97834=CARTESIAN_POINT('Ctrl Pts',(0.924790324524047,-2.18404796024462,
22.1646052453137));
#97835=CARTESIAN_POINT('Ctrl Pts',(0.899593656440859,-2.19458908861085,
22.1627682266017));
#97836=CARTESIAN_POINT('Ctrl Pts',(0.883760436108778,-2.20101283036097,
22.1616132377799));
#97837=CARTESIAN_POINT('Ctrl Pts',(0.80531821378666,-2.23185499830731,22.1558868524616));
#97838=CARTESIAN_POINT('Ctrl Pts',(0.741766087422282,-2.2537736483378,22.151232922541));
#97839=CARTESIAN_POINT('Ctrl Pts',(0.520727822627718,-2.31964610485719,
22.1349843343499));
#97840=CARTESIAN_POINT('Ctrl Pts',(0.359690986436795,-2.35000530284568,
22.1230036226616));
#97841=CARTESIAN_POINT('Ctrl Pts',(0.0851343241601928,-2.37287059348336,
22.1029173686899));
#97842=CARTESIAN_POINT('Ctrl Pts',(-0.0271048666478931,-2.37424395256842,
22.0948135971194));
#97843=CARTESIAN_POINT('Ctrl Pts',(-0.15166199778756,-2.36692981711399,
22.0862046294874));
#97844=CARTESIAN_POINT('Ctrl Pts',(-0.164285871328655,-2.36608712666981,
22.0853365979133));
#97845=CARTESIAN_POINT('Ctrl Pts',(-0.183332743319528,-2.3646625010613,
22.0840342921502));
#97846=CARTESIAN_POINT('Ctrl Pts',(-0.18976085257933,-2.36415533754365,
22.0835960485616));
#97847=CARTESIAN_POINT('Ctrl Pts',(-0.201281946383875,-2.36319905611051,
22.0828129587086));
#97848=CARTESIAN_POINT('Ctrl Pts',(-0.206375599236724,-2.3627596818984,
22.0824675815885));
#97849=CARTESIAN_POINT('Ctrl Pts',(-0.217502963796395,-2.36176358606488,
22.081714926538));
#97850=CARTESIAN_POINT('Ctrl Pts',(-0.223535968465657,-2.36120021357984,
22.0813080247748));
#97851=CARTESIAN_POINT('Ctrl Pts',(-0.240705807942999,-2.35953046742589,
22.0801531528503));
#97852=CARTESIAN_POINT('Ctrl Pts',(-0.251837250040576,-2.35836836065011,
22.0794082264967));
#97853=CARTESIAN_POINT('Ctrl Pts',(-0.325919585033467,-2.35010376110711,
22.0744733418479));
#97854=CARTESIAN_POINT('Ctrl Pts',(-0.388578810020382,-2.34055963903911,
22.07040882942));
#97855=CARTESIAN_POINT('Ctrl Pts',(-0.655453211487854,-2.2888943756156,
22.0532807400586));
#97856=CARTESIAN_POINT('Ctrl Pts',(-0.854007189412205,-2.22246232191954,
22.0409229353592));
#97857=CARTESIAN_POINT('Ctrl Pts',(-1.1056949917092,-2.09946873554599,22.0232697713006));
#97858=CARTESIAN_POINT('Ctrl Pts',(-1.16859702136822,-2.06511738399075,
22.0186819910675));
#97859=CARTESIAN_POINT('Ctrl Pts',(-1.24509278078565,-2.01872734046536,
22.0128247049149));
#97860=CARTESIAN_POINT('Ctrl Pts',(-1.26023652631886,-2.00930833293617,
22.0116510711955));
#97861=CARTESIAN_POINT('Ctrl Pts',(-1.28400505475438,-1.99415053552777,
22.0097858828075));
#97862=CARTESIAN_POINT('Ctrl Pts',(-1.29270113915319,-1.98852435187852,
22.0090985033454));
#97863=CARTESIAN_POINT('Ctrl Pts',(-1.30825575156846,-1.97831569404206,
22.0078598845519));
#97864=CARTESIAN_POINT('Ctrl Pts',(-1.31512779394561,-1.97375403215099,
22.0073094319387));
#97865=CARTESIAN_POINT('Ctrl Pts',(-1.32220960092254,-1.96899972397383,
22.0067387890254));
#97866=CARTESIAN_POINT('Ctrl Pts',(-1.32244334638204,-1.968842740645,22.0067199502854));
#97867=CARTESIAN_POINT('Ctrl Pts',(-1.32286524144993,-1.96855928710787,
22.0066859406889));
#97868=CARTESIAN_POINT('Ctrl Pts',(-1.32305340092178,-1.9684328315196,22.0066707703857));
#97869=CARTESIAN_POINT('Ctrl Pts',(-1.32339807141807,-1.96820111844338,
22.006642976872));
#97870=CARTESIAN_POINT('Ctrl Pts',(-1.32355458804031,-1.96809586924831,
22.0066303539755));
#97871=CARTESIAN_POINT('Ctrl Pts',(-1.32384448485905,-1.96790087866541,
22.0066069709215));
#97872=CARTESIAN_POINT('Ctrl Pts',(-1.32397786850046,-1.96781114237743,
22.0065962109571));
#97873=CARTESIAN_POINT('Ctrl Pts',(-1.32444671828358,-1.96749564584857,
22.0065583847778));
#97874=CARTESIAN_POINT('Ctrl Pts',(-1.32478213565962,-1.96726981348315,
22.0065313158332));
#97875=CARTESIAN_POINT('Ctrl Pts',(-1.32544671157619,-1.9668221157089,22.0064776673505));
#97876=CARTESIAN_POINT('Ctrl Pts',(-1.32577587221057,-1.96660025341546,
22.0064510879309));
#97877=CARTESIAN_POINT('Ctrl Pts',(-1.32643079394499,-1.9661585810436,22.0063981883991));
#97878=CARTESIAN_POINT('Ctrl Pts',(-1.32675655614569,-1.96593877261247,
22.0063718683498));
#97879=CARTESIAN_POINT('Ctrl Pts',(-1.32740710142896,-1.9654995810707,22.0063192923926));
#97880=CARTESIAN_POINT('Ctrl Pts',(-1.32773188479249,-1.96528019839874,
22.006293036502));
#97881=CARTESIAN_POINT('Ctrl Pts',(-1.3283825898726,-1.96484042919996,22.0062404177473));
#97882=CARTESIAN_POINT('Ctrl Pts',(-1.32870851115816,-1.96462004206179,
22.0062140548607));
#97883=CARTESIAN_POINT('Ctrl Pts',(-1.32936340082975,-1.96417696983835,
22.0061610674971));
#97884=CARTESIAN_POINT('Ctrl Pts',(-1.32969236813491,-1.96395428318289,
22.0061344429611));
#97885=CARTESIAN_POINT('Ctrl Pts',(-1.3303551175035,-1.96350540778583,22.0060807887469));
#97886=CARTESIAN_POINT('Ctrl Pts',(-1.33068889786266,-1.96327921656006,
22.0060537589749));
#97887=CARTESIAN_POINT('Ctrl Pts',(-1.33136295002236,-1.96282218422363,
22.0059991577652));
#97888=CARTESIAN_POINT('Ctrl Pts',(-1.33170321949915,-1.96259133972101,
22.0059715861992));
#97889=CARTESIAN_POINT('Ctrl Pts',(-1.33239187388041,-1.96212388351877,
22.005915768812));
#97890=CARTESIAN_POINT('Ctrl Pts',(-1.3327402558166,-1.96188726750107,22.0058875228276));
#97891=CARTESIAN_POINT('Ctrl Pts',(-1.33344673639335,-1.96140716100058,
22.005830225511));
#97892=CARTESIAN_POINT('Ctrl Pts',(-1.33380483139542,-1.96116366521722,
22.0058011739782));
#97893=CARTESIAN_POINT('Ctrl Pts',(-1.34477760200122,-1.95369805597566,
22.0049106945234));
#97894=CARTESIAN_POINT('Ctrl Pts',(-1.35533334239517,-1.94639009770567,
22.0040460111039));
#97895=CARTESIAN_POINT('Ctrl Pts',(-1.39232117469314,-1.92033587589226,
22.0009872205718));
#97896=CARTESIAN_POINT('Ctrl Pts',(-1.4184268609842,-1.9011347106955,21.9987757498885));
#97897=CARTESIAN_POINT('Ctrl Pts',(-1.57354345669432,-1.78207026290825,
21.9853066189334));
#97898=CARTESIAN_POINT('Ctrl Pts',(-1.69233947505689,-1.66966532434441,
21.9735434158214));
#97899=CARTESIAN_POINT('Ctrl Pts',(-1.89397986574322,-1.4350712283036,21.9509569684146));
#97900=CARTESIAN_POINT('Ctrl Pts',(-1.97885994181885,-1.31556470744714,
21.9402215775618));
#97901=CARTESIAN_POINT('Ctrl Pts',(-2.06161886714287,-1.17272296189314,
21.9287405900638));
#97902=CARTESIAN_POINT('Ctrl Pts',(-2.07085013913471,-1.15634391761101,
21.9274431193352));
#97903=CARTESIAN_POINT('Ctrl Pts',(-2.08357882973607,-1.13311798289429,
21.925631680632));
#97904=CARTESIAN_POINT('Ctrl Pts',(-2.08723892837341,-1.12636173716228,
21.9251080938001));
#97905=CARTESIAN_POINT('Ctrl Pts',(-2.09334054744121,-1.11496676651852,
21.9242307873889));
#97906=CARTESIAN_POINT('Ctrl Pts',(-2.09579961746597,-1.11033756276992,
21.9238759731474));
#97907=CARTESIAN_POINT('Ctrl Pts',(-2.10078687889581,-1.10087343447876,
21.9231538757216));
#97908=CARTESIAN_POINT('Ctrl Pts',(-2.10331376505755,-1.09603788098158,
21.9227866748165));
#97909=CARTESIAN_POINT('Ctrl Pts',(-2.10971011012355,-1.08369398807491,
21.9218536324405));
#97910=CARTESIAN_POINT('Ctrl Pts',(-2.11355622821125,-1.0761735381388,21.9212892417931));
#97911=CARTESIAN_POINT('Ctrl Pts',(-2.12902388036512,-1.04552631413782,
21.9190050451138));
#97912=CARTESIAN_POINT('Ctrl Pts',(-2.14030719151979,-1.02222953401307,
21.9173050890662));
#97913=CARTESIAN_POINT('Ctrl Pts',(-2.23573894869351,-0.81667940615521,
21.9025816310169));
#97914=CARTESIAN_POINT('Ctrl Pts',(-2.29682560593683,-0.624587548032487,
21.8906445207192));
#97915=CARTESIAN_POINT('Ctrl Pts',(-2.35337179105881,-0.315691106495283,
21.8712290678143));
#97916=CARTESIAN_POINT('Ctrl Pts',(-2.36575636723831,-0.203006181453386,
21.8641141618005));
#97917=CARTESIAN_POINT('Ctrl Pts',(-2.37078592792978,-0.0703770985275363,
21.8554684593717));
#97918=CARTESIAN_POINT('Ctrl Pts',(-2.37128469816994,-0.0508693935166852,
21.8541902450946));
#97919=CARTESIAN_POINT('Ctrl Pts',(-2.37168074547895,-0.0209173389730879,
21.8522166034159));
#97920=CARTESIAN_POINT('Ctrl Pts',(-2.37174984843327,-0.010475830427131,
21.8515265134037));
#97921=CARTESIAN_POINT('Ctrl Pts',(-2.37174999975095,-3.43714120204603E-5,
21.8508342761113));
#97922=CARTESIAN_POINT('Ctrl Pts',(-2.37174999975776,-3.38978675131843E-5,
21.8508342447167));
#97923=CARTESIAN_POINT('Ctrl Pts',(-2.37175006607408,0.00460609143751829,
21.8505266273684));
#97924=CARTESIAN_POINT('Ctrl Pts',(-2.37173651617879,0.0092460494356073,
21.8502185875369));
#97925=CARTESIAN_POINT('Ctrl Pts',(-2.37166471319693,0.021509971748285,
21.8494032634202));
#97926=CARTESIAN_POINT('Ctrl Pts',(-2.3715833142655,0.0291336896286714,
21.8488952616669));
#97927=CARTESIAN_POINT('Ctrl Pts',(-2.37133201731076,0.0453467948163564,
21.8478123708432));
#97928=CARTESIAN_POINT('Ctrl Pts',(-2.37115220595646,0.0539358966119043,
21.8472371785136));
#97929=CARTESIAN_POINT('Ctrl Pts',(-2.37057114567083,0.0759699415556194,
21.8457576209211));
#97930=CARTESIAN_POINT('Ctrl Pts',(-2.37010218248026,0.0894126405761821,
21.8448511483548));
#97931=CARTESIAN_POINT('Ctrl Pts',(-2.36850195743618,0.126279430017873,
21.8423543364406));
#97932=CARTESIAN_POINT('Ctrl Pts',(-2.36713763174833,0.149690770951987,
21.8407568151855));
#97933=CARTESIAN_POINT('Ctrl Pts',(-2.36542649448459,0.173076750866022,
21.8391485779751));
#97934=CARTESIAN_POINT('',(-2.37174904524198,0.00212811977154857,21.6509744404708));
#97935=CARTESIAN_POINT('Ctrl Pts',(-2.36542651121823,0.173076522168564,
21.6404818371561));
#97936=CARTESIAN_POINT('Ctrl Pts',(-2.36958643853432,0.116223043516792,
21.643983241148));
#97937=CARTESIAN_POINT('Ctrl Pts',(-2.37169783275593,0.0592034623896574,
21.647469736661));
#97938=CARTESIAN_POINT('Ctrl Pts',(-2.37174904524198,0.00212811976785121,
21.650974440471));
#97939=CARTESIAN_POINT('Ctrl Pts',(-2.37174904629756,0.0021269430199922,
21.650974512729));
#97940=CARTESIAN_POINT('Ctrl Pts',(-2.37188012947853,-0.14404359682661,
21.6599500957589));
#97941=CARTESIAN_POINT('Ctrl Pts',(-2.35849905695474,-0.289898015962181,
21.669026738009));
#97942=CARTESIAN_POINT('Ctrl Pts',(-2.32884688216636,-0.449363718668568,
21.6795982553866));
#97943=CARTESIAN_POINT('Ctrl Pts',(-2.32575340206418,-0.465109282263969,
21.6806488982764));
#97944=CARTESIAN_POINT('Ctrl Pts',(-2.32032181906543,-0.491345302365815,
21.6824115454637));
#97945=CARTESIAN_POINT('Ctrl Pts',(-2.31807172338858,-0.501853593239797,
21.6831207704345));
#97946=CARTESIAN_POINT('Ctrl Pts',(-2.31350809805088,-0.522480698865444,
21.6845194900442));
#97947=CARTESIAN_POINT('Ctrl Pts',(-2.3111994006053,-0.532600342880585,
21.6852088169083));
#97948=CARTESIAN_POINT('Ctrl Pts',(-2.3066995574121,-0.551744002370816,
21.6865188991827));
#97949=CARTESIAN_POINT('Ctrl Pts',(-2.30452168872987,-0.560770964172024,
21.687139216707));
#97950=CARTESIAN_POINT('Ctrl Pts',(-2.2994575308212,-0.581233364623295,
21.6885512996239));
#97951=CARTESIAN_POINT('Ctrl Pts',(-2.29653885948676,-0.592660457870983,
21.6893440967877));
#97952=CARTESIAN_POINT('Ctrl Pts',(-2.28876367355726,-0.62218154948984,
21.6914034265844));
#97953=CARTESIAN_POINT('Ctrl Pts',(-2.28377786121515,-0.640240329378653,
21.6926741081978));
#97954=CARTESIAN_POINT('Ctrl Pts',(-2.24499355612233,-0.774497441852405,
21.7022048171245));
#97955=CARTESIAN_POINT('Ctrl Pts',(-2.20256557026734,-0.887997041866107,
21.7107468357777));
#97956=CARTESIAN_POINT('Ctrl Pts',(-2.11208029886235,-1.08313079961061,
21.7262690843966));
#97957=CARTESIAN_POINT('Ctrl Pts',(-2.06744264598954,-1.16607681094537,
21.7331578184411));
#97958=CARTESIAN_POINT('Ctrl Pts',(-1.96579793672407,-1.33067911144673,
21.7472751976184));
#97959=CARTESIAN_POINT('Ctrl Pts',(-1.90833360287904,-1.41185510616907,
21.7544878512084));
#97960=CARTESIAN_POINT('Ctrl Pts',(-1.82814147477453,-1.511257924464,21.7634521995085));
#97961=CARTESIAN_POINT('Ctrl Pts',(-1.80994585977779,-1.53300291306676,
21.7654216626015));
#97962=CARTESIAN_POINT('Ctrl Pts',(-1.78702116032091,-1.55942211674064,
21.7678196812142));
#97963=CARTESIAN_POINT('Ctrl Pts',(-1.7826575762754,-1.56440849332449,21.7682725178389));
#97964=CARTESIAN_POINT('Ctrl Pts',(-1.77417618846818,-1.57401882125165,
21.7691456193532));
#97965=CARTESIAN_POINT('Ctrl Pts',(-1.77006106671405,-1.57864505817989,
21.7695660693773));
#97966=CARTESIAN_POINT('Ctrl Pts',(-1.7624668964809,-1.58711542764778,21.7703360877015));
#97967=CARTESIAN_POINT('Ctrl Pts',(-1.75899337097757,-1.59096425597922,
21.7706860413732));
#97968=CARTESIAN_POINT('Ctrl Pts',(-1.75114003275701,-1.59960896119347,
21.7714722348941));
#97969=CARTESIAN_POINT('Ctrl Pts',(-1.7467531316196,-1.60439824943147,21.7719079311884));
#97970=CARTESIAN_POINT('Ctrl Pts',(-1.73378448791691,-1.61844019539197,
21.7731859827644));
#97971=CARTESIAN_POINT('Ctrl Pts',(-1.72514834036726,-1.627642632073,21.774024346926));
#97972=CARTESIAN_POINT('Ctrl Pts',(-1.65236556098458,-1.70396779751785,
21.7809889065736));
#97973=CARTESIAN_POINT('Ctrl Pts',(-1.58439336221097,-1.76734838936921,
21.7868463307339));
#97974=CARTESIAN_POINT('Ctrl Pts',(-1.36661359983591,-1.94772457219401,
21.8043899183517));
#97975=CARTESIAN_POINT('Ctrl Pts',(-1.20634289595142,-2.05085375841614,
21.815760416059));
#97976=CARTESIAN_POINT('Ctrl Pts',(-0.981023734734813,-2.16019799228492,
21.8316485274383));
#97977=CARTESIAN_POINT('Ctrl Pts',(-0.925572170371445,-2.18453155107848,
21.8355455080405));
#97978=CARTESIAN_POINT('Ctrl Pts',(-0.854011731363886,-2.21272013681538,
21.8405892147893));
#97979=CARTESIAN_POINT('Ctrl Pts',(-0.838707924389162,-2.21856607661768,
21.8416686272028));
#97980=CARTESIAN_POINT('Ctrl Pts',(-0.813644479467798,-2.22784373772877,
21.8434382416649));
#97981=CARTESIAN_POINT('Ctrl Pts',(-0.803920606814808,-2.23137103836728,
21.8441252445542));
#97982=CARTESIAN_POINT('Ctrl Pts',(-0.785417633066153,-2.23794628234331,
21.8454334906877));
#97983=CARTESIAN_POINT('Ctrl Pts',(-0.77664306145962,-2.24100646403119,
21.8460543132755));
#97984=CARTESIAN_POINT('Ctrl Pts',(-0.756633130805078,-2.24785340680719,
21.8474711316777));
#97985=CARTESIAN_POINT('Ctrl Pts',(-0.745386979465549,-2.25160762014272,
21.8482681857652));
#97986=CARTESIAN_POINT('Ctrl Pts',(-0.716102296300976,-2.26114005158752,
21.8503458996879));
#97987=CARTESIAN_POINT('Ctrl Pts',(-0.698022151720042,-2.26678668405509,
21.8516308322753));
#97988=CARTESIAN_POINT('Ctrl Pts',(-0.551807373138127,-2.31053605892426,
21.8620417890489));
#97989=CARTESIAN_POINT('Ctrl Pts',(-0.420750495740637,-2.33795337832828,
21.8715154523044));
#97990=CARTESIAN_POINT('Ctrl Pts',(-0.141558102718332,-2.37212064573167,
21.891889276526));
#97991=CARTESIAN_POINT('Ctrl Pts',(0.00633822451968406,-2.37633222090603,
21.9027934306858));
#97992=CARTESIAN_POINT('Ctrl Pts',(0.210758979647264,-2.36305989733668,
21.9174598193607));
#97993=CARTESIAN_POINT('Ctrl Pts',(0.26770496432654,-2.3572880040321,21.9214979645194));
#97994=CARTESIAN_POINT('Ctrl Pts',(0.335300960880602,-2.34795498544842,
21.9261933774168));
#97995=CARTESIAN_POINT('Ctrl Pts',(0.346200083593711,-2.34637270314822,
21.9269473929202));
#97996=CARTESIAN_POINT('Ctrl Pts',(0.363091922640616,-2.34380016228095,
21.9281108187206));
#97997=CARTESIAN_POINT('Ctrl Pts',(0.369092343728505,-2.34286273368837,
21.9285230827554));
#97998=CARTESIAN_POINT('Ctrl Pts',(0.380218101115711,-2.34108078431641,
21.9292855202694));
#97999=CARTESIAN_POINT('Ctrl Pts',(0.385344227360794,-2.34024248111527,
21.9296360231955));
#98000=CARTESIAN_POINT('Ctrl Pts',(0.397024076402254,-2.33829299460417,
21.9304328868139));
#98001=CARTESIAN_POINT('Ctrl Pts',(0.403575904828265,-2.33717109720774,
21.930878636808));
#98002=CARTESIAN_POINT('Ctrl Pts',(0.420668806571474,-2.33417018638141,
21.9320384780676));
#98003=CARTESIAN_POINT('Ctrl Pts',(0.431202169631757,-2.33224728607302,
21.932750173015));
#98004=CARTESIAN_POINT('Ctrl Pts',(0.503407777303255,-2.31856000283583,
21.9376101181506));
#98005=CARTESIAN_POINT('Ctrl Pts',(0.564610929381537,-2.30442096159721,
21.9416360058439));
#98006=CARTESIAN_POINT('Ctrl Pts',(0.689962150613862,-2.27016728151205,
21.9498218072764));
#98007=CARTESIAN_POINT('Ctrl Pts',(0.753960159498969,-2.24972270179852,
21.9539681057298));
#98008=CARTESIAN_POINT('Ctrl Pts',(0.931216382963815,-2.18468168759888,
21.965567187769));
#98009=CARTESIAN_POINT('Ctrl Pts',(1.04202787766788,-2.13405124425065,21.9729632454886));
#98010=CARTESIAN_POINT('Ctrl Pts',(1.2001391844809,-2.04654639097371,21.9842607170541));
#98011=CARTESIAN_POINT('Ctrl Pts',(1.25072412760167,-2.01602940660697,21.9879961495904));
#98012=CARTESIAN_POINT('Ctrl Pts',(1.33285041215006,-1.96220278919546,21.9943123989141));
#98013=CARTESIAN_POINT('Ctrl Pts',(1.36504817828165,-1.93994154315187,21.9968566097392));
#98014=CARTESIAN_POINT('Ctrl Pts',(1.40821591042066,-1.90848887172132,22.0003698654468));
#98015=CARTESIAN_POINT('Ctrl Pts',(1.4196765008619,-1.8999790635134,22.0013127240924));
#98016=CARTESIAN_POINT('Ctrl Pts',(1.43880408341467,-1.8855066137805,22.0029038462866));
#98017=CARTESIAN_POINT('Ctrl Pts',(1.44651263137386,-1.8795993146238,22.0035499335655));
#98018=CARTESIAN_POINT('Ctrl Pts',(1.46165766848853,-1.8678448571244,22.00482905456));
#98019=CARTESIAN_POINT('Ctrl Pts',(1.46909589040661,-1.86200021762661,22.0054619806849));
#98020=CARTESIAN_POINT('Ctrl Pts',(1.48540368264511,-1.84902770004391,22.0068601590178));
#98021=CARTESIAN_POINT('Ctrl Pts',(1.4942572795649,-1.84188021069459,22.0076261887216));
#98022=CARTESIAN_POINT('Ctrl Pts',(1.52524760055357,-1.8164912877595,22.0103324090326));
#98023=CARTESIAN_POINT('Ctrl Pts',(1.54710374133569,-1.79791288138436,22.0122862003529));
#98024=CARTESIAN_POINT('Ctrl Pts',(1.70815172666794,-1.65590579126623,22.0270326294601));
#98025=CARTESIAN_POINT('Ctrl Pts',(1.8326998453104,-1.51690172445385,22.0405108620913));
#98026=CARTESIAN_POINT('Ctrl Pts',(1.95804916479291,-1.33875208261829,22.0564217552804));
#98027=CARTESIAN_POINT('Ctrl Pts',(1.97586081226877,-1.31232151241464,22.0587488866696));
#98028=CARTESIAN_POINT('Ctrl Pts',(2.04567817146216,-1.20407485659599,22.0681292942927));
#98029=CARTESIAN_POINT('Ctrl Pts',(2.09318381532347,-1.11945569501166,22.0751259025091));
#98030=CARTESIAN_POINT('Ctrl Pts',(2.14356201109512,-1.01523072815927,22.0831734269785));
#98031=CARTESIAN_POINT('Ctrl Pts',(2.15154260214543,-0.998206398457185,
22.0844703903553));
#98032=CARTESIAN_POINT('Ctrl Pts',(2.16243502308225,-0.974232792292616,
22.0862705391073));
#98033=CARTESIAN_POINT('Ctrl Pts',(2.16551721945634,-0.967362361685569,
22.0867834433047));
#98034=CARTESIAN_POINT('Ctrl Pts',(2.17072101933894,-0.955613216022753,
22.0876553298763));
#98035=CARTESIAN_POINT('Ctrl Pts',(2.17285900938145,-0.950741862988018,
22.0880152975193));
#98036=CARTESIAN_POINT('Ctrl Pts',(2.17722749210149,-0.940696684311967,
22.0887543870363));
#98037=CARTESIAN_POINT('Ctrl Pts',(2.17945595923357,-0.935522061575013,
22.089133387077));
#98038=CARTESIAN_POINT('Ctrl Pts',(2.185204353286,-0.922041954443394,22.0901163275754));
#98039=CARTESIAN_POINT('Ctrl Pts',(2.18869541662435,-0.913724143938163,
22.0907185441087));
#98040=CARTESIAN_POINT('Ctrl Pts',(2.20260671050952,-0.880041852812717,
22.0931406350282));
#98041=CARTESIAN_POINT('Ctrl Pts',(2.21263465175103,-0.854516262387042,
22.0949384497254));
#98042=CARTESIAN_POINT('Ctrl Pts',(2.31160534342605,-0.589158087416821,
22.1132981743857));
#98043=CARTESIAN_POINT('Ctrl Pts',(2.36164696135619,-0.336587324802956,
22.1281801197011));
#98044=CARTESIAN_POINT('Ctrl Pts',(2.37263024203067,-0.014643083981033,
22.1485513928182));
#98045=CARTESIAN_POINT('Ctrl Pts',(2.37211312761258,0.0516402607674147,
22.1528070897304));
#98046=CARTESIAN_POINT('Ctrl Pts',(2.36796946157724,0.134957109608505,22.1582751161096));
#98047=CARTESIAN_POINT('Ctrl Pts',(2.36693057451503,0.152093464806864,22.1594060273946));
#98048=CARTESIAN_POINT('Ctrl Pts',(2.36496821508573,0.179527908339262,22.1612272548627));
#98049=CARTESIAN_POINT('Ctrl Pts',(2.36416326534706,0.189834078216609,22.1619138481391));
#98050=CARTESIAN_POINT('Ctrl Pts',(2.36250670901786,0.209395544393419,22.1632217724663));
#98051=CARTESIAN_POINT('Ctrl Pts',(2.36166802196505,0.218651764112619,22.1638426859007));
#98052=CARTESIAN_POINT('Ctrl Pts',(2.35963461996036,0.239715158632776,22.1652603506821));
#98053=CARTESIAN_POINT('Ctrl Pts',(2.35840565476579,0.251518698414878,22.1660581650507));
#98054=CARTESIAN_POINT('Ctrl Pts',(2.35498120107995,0.282173317508111,22.1681391718902));
#98055=CARTESIAN_POINT('Ctrl Pts',(2.35264797285727,0.3010078367596,22.1694266594914));
#98056=CARTESIAN_POINT('Ctrl Pts',(2.3312838109564,0.457999145687072,22.180234965604));
#98057=CARTESIAN_POINT('Ctrl Pts',(2.3003307894739,0.594233102229342,22.1901359903791));
#98058=CARTESIAN_POINT('Ctrl Pts',(2.22795590310611,0.819002502240006,22.2072651171016));
#98059=CARTESIAN_POINT('Ctrl Pts',(2.19270809477539,0.909166234695663,22.2143609871841));
#98060=CARTESIAN_POINT('Ctrl Pts',(2.1137449647882,1.07962368753853,22.2280239530832));
#98061=CARTESIAN_POINT('Ctrl Pts',(2.07069502286623,1.16005638319759,22.2345860480154));
#98062=CARTESIAN_POINT('Ctrl Pts',(2.01359560193973,1.25338089059117,22.2421869587339));
#98063=CARTESIAN_POINT('Ctrl Pts',(2.00389443805835,1.26883333715996,22.243444943498));
#98064=CARTESIAN_POINT('Ctrl Pts',(1.98998708262334,1.29042815785981,22.2452005312094));
#98065=CARTESIAN_POINT('Ctrl Pts',(1.98592912047796,1.29666454869589,22.2457072374982));
#98066=CARTESIAN_POINT('Ctrl Pts',(1.97892840409493,1.30731349008542,22.2465718223577));
#98067=CARTESIAN_POINT('Ctrl Pts',(1.97600009318352,1.31173542450993,22.2469306459759));
#98068=CARTESIAN_POINT('Ctrl Pts',(1.96991286461586,1.32086088151078,22.2476706926283));
#98069=CARTESIAN_POINT('Ctrl Pts',(1.96675190355217,1.32556294233046,22.2480517751314));
#98070=CARTESIAN_POINT('Ctrl Pts',(1.95843474268517,1.33783981972731,22.2490462625423));
#98071=CARTESIAN_POINT('Ctrl Pts',(1.95325137908773,1.34539625449051,22.2496578675058));
#98072=CARTESIAN_POINT('Ctrl Pts',(1.93173469802664,1.37637734385366,22.2521641944863));
#98073=CARTESIAN_POINT('Ctrl Pts',(1.91502196940298,1.3995372711884,22.2540348914062));
#98074=CARTESIAN_POINT('Ctrl Pts',(1.74529017117802,1.62601015470865,22.272360390465));
#98075=CARTESIAN_POINT('Ctrl Pts',(1.56089894808136,1.80376848451313,22.2871738322896));
#98076=CARTESIAN_POINT('Ctrl Pts',(1.29737515059554,1.98655353019216,22.3074562274472));
#98077=CARTESIAN_POINT('Ctrl Pts',(1.24144972943193,2.02197391305081,22.3117065141737));
#98078=CARTESIAN_POINT('Ctrl Pts',(1.16925153232451,2.06357539426526,22.3171684512662));
#98079=CARTESIAN_POINT('Ctrl Pts',(1.15429035615847,2.07198125029782,22.3182989114494));
#98080=CARTESIAN_POINT('Ctrl Pts',(1.13017394057919,2.08518866347215,22.3201195897213));
#98081=CARTESIAN_POINT('Ctrl Pts',(1.12107604676841,2.09009411028116,22.320806089069));
#98082=CARTESIAN_POINT('Ctrl Pts',(1.10373667803629,2.09929745338874,22.32211394973));
#98083=CARTESIAN_POINT('Ctrl Pts',(1.09550141403624,2.10360668848688,22.3227348941856));
#98084=CARTESIAN_POINT('Ctrl Pts',(1.07669150728283,2.11330886652205,22.324152790807));
#98085=CARTESIAN_POINT('Ctrl Pts',(1.06610134918203,2.11867101540827,22.3249508072048));
#98086=CARTESIAN_POINT('Ctrl Pts',(1.03846746618552,2.1324033213596,22.3270326718392));
#98087=CARTESIAN_POINT('Ctrl Pts',(1.02136296788795,2.14064855930857,22.3283208209198));
#98088=CARTESIAN_POINT('Ctrl Pts',(0.876800030451471,2.20820821235097,22.339206474802));
#98089=CARTESIAN_POINT('Ctrl Pts',(0.744422202246773,2.25627666622694,22.3491906896422));
#98090=CARTESIAN_POINT('Ctrl Pts',(0.470109495060137,2.32910363622487,22.3697841554716));
#98091=CARTESIAN_POINT('Ctrl Pts',(0.328582878283811,2.3532447326379,22.3803581365282));
#98092=CARTESIAN_POINT('Ctrl Pts',(0.13110300111649,2.36875788384632,22.3945217323217));
#98093=CARTESIAN_POINT('Ctrl Pts',(0.0763263095821373,2.371155271999,22.398385473687));
#98094=CARTESIAN_POINT('Ctrl Pts',(0.0106244495738307,2.37175119057223,
22.4029057009315));
#98095=CARTESIAN_POINT('Ctrl Pts',(-0.000262903066657681,2.37177497484476,
22.4036509760575));
#98096=CARTESIAN_POINT('Ctrl Pts',(-0.0171960727512356,2.37169536615083,
22.4048038573033));
#98097=CARTESIAN_POINT('Ctrl Pts',(-0.0232418063662103,2.37164382554773,
22.4052142370099));
#98098=CARTESIAN_POINT('Ctrl Pts',(-0.0344844800221831,2.37150498571862,
22.4059749945917));
#98099=CARTESIAN_POINT('Ctrl Pts',(-0.039681288991119,2.3714237227401,22.4063256888757));
#98100=CARTESIAN_POINT('Ctrl Pts',(-0.0515623861758423,2.37119886987704,
22.4071253055671));
#98101=CARTESIAN_POINT('Ctrl Pts',(-0.0582463598604284,2.37104410007626,
22.4075736003437));
#98102=CARTESIAN_POINT('Ctrl Pts',(-0.0757616024085256,2.37056441809999,
22.4087445041672));
#98103=CARTESIAN_POINT('Ctrl Pts',(-0.0865916066402694,2.37019353333702,
22.4094646415977));
#98104=CARTESIAN_POINT('Ctrl Pts',(-0.163202786603556,2.36704409349722,
22.4145340127815));
#98105=CARTESIAN_POINT('Ctrl Pts',(-0.228852550289266,2.36160140775172,
22.4187485629111));
#98106=CARTESIAN_POINT('Ctrl Pts',(-0.429622478481986,2.33650363113286,
22.4314701649112));
#98107=CARTESIAN_POINT('Ctrl Pts',(-0.563340803168248,2.3079159633336,22.4397203620771));
#98108=CARTESIAN_POINT('Ctrl Pts',(-0.811402457582291,2.23202430107256,
22.4556909955144));
#98109=CARTESIAN_POINT('Ctrl Pts',(-0.925953221603575,2.18698684515527,
22.4633581653699));
#98110=CARTESIAN_POINT('Ctrl Pts',(-1.06206334168855,2.12085546286663,22.473172376375));
#98111=CARTESIAN_POINT('Ctrl Pts',(-1.08741010812859,2.10797191143811,22.4750310229163));
#98112=CARTESIAN_POINT('Ctrl Pts',(-1.12364331012592,2.08872747242237,22.4777361196238));
#98113=CARTESIAN_POINT('Ctrl Pts',(-1.13472089207309,2.08273023437895,22.4785697568969));
#98114=CARTESIAN_POINT('Ctrl Pts',(-1.15397707441661,2.07210599699617,22.480030715553));
#98115=CARTESIAN_POINT('Ctrl Pts',(-1.16217700219262,2.06751806818695,22.4806566320012));
#98116=CARTESIAN_POINT('Ctrl Pts',(-1.17799904624854,2.05854163489464,22.4818718292058));
#98117=CARTESIAN_POINT('Ctrl Pts',(-1.18562445104928,2.05415921316244,22.4824608831453));
#98118=CARTESIAN_POINT('Ctrl Pts',(-1.20373883479151,2.04361416982451,22.4838684029715));
#98119=CARTESIAN_POINT('Ctrl Pts',(-1.21420503378303,2.03741311073883,22.4846882537639));
#98120=CARTESIAN_POINT('Ctrl Pts',(-1.25164647371089,2.0148386809647,22.4876453432213));
#98121=CARTESIAN_POINT('Ctrl Pts',(-1.27834099522613,1.99800849295929,22.4897991913964));
#98122=CARTESIAN_POINT('Ctrl Pts',(-1.5172480024249,1.84063615071706,22.5095026416014));
#98123=CARTESIAN_POINT('Ctrl Pts',(-1.70585503767571,1.66732762664449,22.5284260927669));
#98124=CARTESIAN_POINT('Ctrl Pts',(-1.90454155807901,1.41505123651421,22.5515249591234));
#98125=CARTESIAN_POINT('Ctrl Pts',(-1.94359283469667,1.3609178219825,22.5562548987976));
#98126=CARTESIAN_POINT('Ctrl Pts',(-1.98661120255633,1.29564847633764,22.5616374814979));
#98127=CARTESIAN_POINT('Ctrl Pts',(-1.99284029585741,1.28604689372995,22.5624214610316));
#98128=CARTESIAN_POINT('Ctrl Pts',(-2.00231797058502,1.27120369051112,22.5636209692646));
#98129=CARTESIAN_POINT('Ctrl Pts',(-2.00561591425012,1.26599403032063,22.5640396338283));
#98130=CARTESIAN_POINT('Ctrl Pts',(-2.01165030430024,1.25637892772263,22.5648079532478));
#98131=CARTESIAN_POINT('Ctrl Pts',(-2.01439260692912,1.25197738917158,22.5651579814293));
#98132=CARTESIAN_POINT('Ctrl Pts',(-2.02055308143064,1.2420168642996,22.565946305158));
#98133=CARTESIAN_POINT('Ctrl Pts',(-2.02396275696216,1.23645275166331,22.5663840434118));
#98134=CARTESIAN_POINT('Ctrl Pts',(-2.03397400628247,1.21996341811316,22.5676737460992));
#98135=CARTESIAN_POINT('Ctrl Pts',(-2.04051052669679,1.20899867998439,22.5685216097931));
#98136=CARTESIAN_POINT('Ctrl Pts',(-2.10045129965389,1.10657950429431,22.5763564263201));
#98137=CARTESIAN_POINT('Ctrl Pts',(-2.14776992026356,1.01168397188873,22.5829925433187));
#98138=CARTESIAN_POINT('Ctrl Pts',(-2.22777191451311,0.820103133794522,
22.595814061272));
#98139=CARTESIAN_POINT('Ctrl Pts',(-2.26087917626553,0.723852633869651,
22.6019948224209));
#98140=CARTESIAN_POINT('Ctrl Pts',(-2.31046247031473,0.542585729870637,
22.613582236249));
#98141=CARTESIAN_POINT('Ctrl Pts',(-2.32866145897594,0.45822487196253,22.6189544039954));
#98142=CARTESIAN_POINT('Ctrl Pts',(-2.35026819610624,0.322570682446353,
22.6277192803704));
#98143=CARTESIAN_POINT('Ctrl Pts',(-2.35667537937432,0.271832627306682,
22.6310244615013));
#98144=CARTESIAN_POINT('Ctrl Pts',(-2.36290425392802,0.205254525262823,
22.6354148335364));
#98145=CARTESIAN_POINT('Ctrl Pts',(-2.36421465984301,0.189565175022731,
22.6364532564907));
#98146=CARTESIAN_POINT('Ctrl Pts',(-2.36538803639278,0.173601754216798,
22.6375140099822));
#98147=CARTESIAN_POINT('Ctrl Pts',(-2.36540728732125,0.173339253674963,
22.6375314540332));
#98148=CARTESIAN_POINT('Ctrl Pts',(-2.36542649454112,0.173076750093424,
22.6375488994376));
#98149=CARTESIAN_POINT('Origin',(0.,0.,-1.84858989190503));
#98150=CARTESIAN_POINT('',(-2.36542649454004,0.173076750108263,23.8347324553251));
#98151=CARTESIAN_POINT('',(-2.36542649498006,0.173076744094521,23.6397760267629));
#98152=CARTESIAN_POINT('',(-2.36542649454111,0.173076750093529,-1.84858989190503));
#98153=CARTESIAN_POINT('Ctrl Pts',(-2.36542649454004,0.173076750108263,
23.8347324553251));
#98154=CARTESIAN_POINT('Ctrl Pts',(-2.36521313794873,0.175992678062693,
23.8345313836012));
#98155=CARTESIAN_POINT('Ctrl Pts',(-2.36499438735582,0.178908241316125,
23.834330581952));
#98156=CARTESIAN_POINT('Ctrl Pts',(-2.36425986193181,0.188461377098688,
23.8336734540962));
#98157=CARTESIAN_POINT('Ctrl Pts',(-2.36372152556061,0.195097251863204,
23.833218290546));
#98158=CARTESIAN_POINT('Ctrl Pts',(-2.36272707028727,0.206746694398436,
23.8324216189125));
#98159=CARTESIAN_POINT('Ctrl Pts',(-2.3622829210848,0.211761201046456,23.8320794661881));
#98160=CARTESIAN_POINT('Ctrl Pts',(-2.3613697446941,0.221710538565071,23.8314021861645));
#98161=CARTESIAN_POINT('Ctrl Pts',(-2.36090121088067,0.226645335461349,
23.8310670422598));
#98162=CARTESIAN_POINT('Ctrl Pts',(-2.35985728557643,0.237285771784479,
23.8303460997473));
#98163=CARTESIAN_POINT('Ctrl Pts',(-2.35927667342204,0.242990793664687,
23.8299605980873));
#98164=CARTESIAN_POINT('Ctrl Pts',(-2.35765841762324,0.258338748278819,
23.8289261700615));
#98165=CARTESIAN_POINT('Ctrl Pts',(-2.3565822948449,0.267977646112384,23.8282793613162));
#98166=CARTESIAN_POINT('Ctrl Pts',(-2.35146978022023,0.311355992487421,
23.8253801864661));
#98167=CARTESIAN_POINT('Ctrl Pts',(-2.34676749748528,0.345014911616439,
23.8231624700867));
#98168=CARTESIAN_POINT('Ctrl Pts',(-2.33491738404618,0.418305656405469,
23.8183803982314));
#98169=CARTESIAN_POINT('Ctrl Pts',(-2.32748037347506,0.457880193432647,
23.8158284349045));
#98170=CARTESIAN_POINT('Ctrl Pts',(-2.27523796823757,0.701525462369068,
23.8001994040348));
#98171=CARTESIAN_POINT('Ctrl Pts',(-2.20463981528273,0.899120122662086,
23.7877997598158));
#98172=CARTESIAN_POINT('Ctrl Pts',(-2.07902091174658,1.14332131371335,23.7704256929237));
#98173=CARTESIAN_POINT('Ctrl Pts',(-2.04656744409077,1.20044659412911,23.7662058700489));
#98174=CARTESIAN_POINT('Ctrl Pts',(-2.0027876216054,1.27056230931542,23.7607864832281));
#98175=CARTESIAN_POINT('Ctrl Pts',(-1.99363295087202,1.28487916603263,23.7596668854329));
#98176=CARTESIAN_POINT('Ctrl Pts',(-1.97872578581389,1.30764935705449,23.757864606012));
#98177=CARTESIAN_POINT('Ctrl Pts',(-1.9730709862839,1.31616619541743,23.757185572392));
#98178=CARTESIAN_POINT('Ctrl Pts',(-1.96223187422345,1.33226442004618,23.7558925695491));
#98179=CARTESIAN_POINT('Ctrl Pts',(-1.95705822815673,1.33985279066526,23.7552790106854));
#98180=CARTESIAN_POINT('Ctrl Pts',(-1.94518470362675,1.35705261415231,23.7538789233561));
#98181=CARTESIAN_POINT('Ctrl Pts',(-1.93845746113787,1.36664479349996,23.7530913632644));
#98182=CARTESIAN_POINT('Ctrl Pts',(-1.92080248554561,1.39142588213364,23.7510388989541));
#98183=CARTESIAN_POINT('Ctrl Pts',(-1.90976576391999,1.40653576773763,23.7497698333138));
#98184=CARTESIAN_POINT('Ctrl Pts',(-1.80584043185118,1.54533688914444,23.737945009887));
#98185=CARTESIAN_POINT('Ctrl Pts',(-1.70125634563476,1.65976976458415,23.7269158091475));
#98186=CARTESIAN_POINT('Ctrl Pts',(-1.48959879474454,1.85019298693801,23.7062066580574));
#98187=CARTESIAN_POINT('Ctrl Pts',(-1.38590113822146,1.92909264605851,23.6966348156477));
#98188=CARTESIAN_POINT('Ctrl Pts',(-1.24611658568828,2.01833347925838,23.6847896863805));
#98189=CARTESIAN_POINT('Ctrl Pts',(-1.21554538902937,2.03689132620092,23.6822594883462));
#98190=CARTESIAN_POINT('Ctrl Pts',(-1.1711530099552,2.06248353705227,23.6786825573337));
#98191=CARTESIAN_POINT('Ctrl Pts',(-1.15766563500709,2.07008406118458,23.677608356588));
#98192=CARTESIAN_POINT('Ctrl Pts',(-1.13363324103126,2.08331865887766,23.6757176755115));
#98193=CARTESIAN_POINT('Ctrl Pts',(-1.12311835901335,2.08900601393742,23.6748982689628));
#98194=CARTESIAN_POINT('Ctrl Pts',(-1.1071052755875,2.09751141325316,23.6736627212651));
#98195=CARTESIAN_POINT('Ctrl Pts',(-1.10163852005926,2.10038777212284,23.6732430746725));
#98196=CARTESIAN_POINT('Ctrl Pts',(-1.09614594010506,2.10325037519577,23.6728236548216));
#98197=CARTESIAN_POINT('Ctrl Pts',(-1.09613136919284,2.10325796901888,23.6728225421852));
#98198=CARTESIAN_POINT('Ctrl Pts',(-1.09610218260238,2.1032731796098,23.6728203135252));
#98199=CARTESIAN_POINT('Ctrl Pts',(-1.09608756691289,2.10328079638231,23.6728191975009));
#98200=CARTESIAN_POINT('Ctrl Pts',(-1.09605829047896,2.10329605301908,23.6728169620432));
#98201=CARTESIAN_POINT('Ctrl Pts',(-1.09604362975711,2.10330369287038,23.6728158426118));
#98202=CARTESIAN_POINT('Ctrl Pts',(-1.0960142629681,2.10331899581245,23.672813600318));
#98203=CARTESIAN_POINT('Ctrl Pts',(-1.0959995569568,2.10332665887291,23.6728124774601));
#98204=CARTESIAN_POINT('Ctrl Pts',(-1.0959700994035,2.10334200832631,23.6728102282995));
#98205=CARTESIAN_POINT('Ctrl Pts',(-1.09595534779118,2.10334969475468,23.6728091019916));
#98206=CARTESIAN_POINT('Ctrl Pts',(-1.09592579876749,2.10336509108006,23.6728068459109));
#98207=CARTESIAN_POINT('Ctrl Pts',(-1.09591100136163,2.10337280097299,23.6728057161386));
#98208=CARTESIAN_POINT('Ctrl Pts',(-1.09588136045039,2.10338824438037,23.6728034531066));
#98209=CARTESIAN_POINT('Ctrl Pts',(-1.09586651697123,2.10339597787993,23.6728023198489));
#98210=CARTESIAN_POINT('Ctrl Pts',(-1.09583678367889,2.10341146861906,23.6728000498284));
#98211=CARTESIAN_POINT('Ctrl Pts',(-1.09582189383909,2.10341922587125,23.6727989130636));
#98212=CARTESIAN_POINT('Ctrl Pts',(-1.09579206756248,2.10343476424889,23.6727966360093));
#98213=CARTESIAN_POINT('Ctrl Pts',(-1.09577713112336,2.1034425453743,23.6727954957195));
#98214=CARTESIAN_POINT('Ctrl Pts',(-1.09574721135856,2.10345813164545,23.6727932115934));
#98215=CARTESIAN_POINT('Ctrl Pts',(-1.09573222805405,2.1034659367789,23.6727920677587));
#98216=CARTESIAN_POINT('Ctrl Pts',(-1.09570221429531,2.10348157119942,23.6727897765228));
#98217=CARTESIAN_POINT('Ctrl Pts',(-1.09568718384419,2.10348940048359,23.6727886291219));
#98218=CARTESIAN_POINT('Ctrl Pts',(-1.0956570755362,2.10350508333507,23.6727863307345));
#98219=CARTESIAN_POINT('Ctrl Pts',(-1.09564199767223,2.10351293690479,23.6727851797475));
#98220=CARTESIAN_POINT('Ctrl Pts',(-1.09561179429435,2.1035286684507,23.6727828741695));
#98221=CARTESIAN_POINT('Ctrl Pts',(-1.09559666873913,2.1035365464471,23.6727817195754));
#98222=CARTESIAN_POINT('Ctrl Pts',(-1.09556636967161,2.10355232700241,23.6727794067601));
#98223=CARTESIAN_POINT('Ctrl Pts',(-1.09555119618796,2.10356022954509,23.6727782485411));
#98224=CARTESIAN_POINT('Ctrl Pts',(-1.09552105426528,2.10357592742604,23.6727759477882));
#98225=CARTESIAN_POINT('Ctrl Pts',(-1.09550608588474,2.10358372273944,23.6727748052582));
#98226=CARTESIAN_POINT('Ctrl Pts',(-1.09547592681293,2.10359942873321,23.6727725032624));
#98227=CARTESIAN_POINT('Ctrl Pts',(-1.0954607360854,2.10360733942639,23.6727713437943));
#98228=CARTESIAN_POINT('Ctrl Pts',(-1.09543012873505,2.10362327802809,23.6727690076503));
#98229=CARTESIAN_POINT('Ctrl Pts',(-1.09541471208834,2.10363130594279,23.672767830973));
#98230=CARTESIAN_POINT('Ctrl Pts',(-1.09538364918485,2.10364748090303,23.6727654601285));
#98231=CARTESIAN_POINT('Ctrl Pts',(-1.09536800296256,2.10365562792416,23.6727642659645));
#98232=CARTESIAN_POINT('Ctrl Pts',(-1.09533647720975,2.10367204300343,23.6727618598658));
#98233=CARTESIAN_POINT('Ctrl Pts',(-1.09532059762454,2.1036803110834,23.6727606479275));
#98234=CARTESIAN_POINT('Ctrl Pts',(-1.09528860131534,2.10369697025471,23.6727582059896));
#98235=CARTESIAN_POINT('Ctrl Pts',(-1.09527248461808,2.10370536132527,23.6727569759927));
#98236=CARTESIAN_POINT('Ctrl Pts',(-1.09524001018804,2.10372226848588,23.6727544976417));
#98237=CARTESIAN_POINT('Ctrl Pts',(-1.09522365247353,2.10373078455934,23.6727532492896));
#98238=CARTESIAN_POINT('Ctrl Pts',(-1.09519069208353,2.103747943748,23.6727507339307));
#98239=CARTESIAN_POINT('Ctrl Pts',(-1.09517408940007,2.10375658686006,23.6727494669237));
#98240=CARTESIAN_POINT('Ctrl Pts',(-1.09514063507814,2.10377400218312,23.672746913952));
#98241=CARTESIAN_POINT('Ctrl Pts',(-1.09512378340937,2.10378277440236,23.6727456279855));
#98242=CARTESIAN_POINT('Ctrl Pts',(-1.09508982699332,2.10380045006355,23.6727430367818));
#98243=CARTESIAN_POINT('Ctrl Pts',(-1.09507272227568,2.10380935348229,23.6727417315475));
#98244=CARTESIAN_POINT('Ctrl Pts',(-1.09503825561346,2.10382729367839,23.6727391014935));
#98245=CARTESIAN_POINT('Ctrl Pts',(-1.09502089364249,2.10383633046145,23.6727377766724));
#98246=CARTESIAN_POINT('Ctrl Pts',(-1.09498590822939,2.10385453957107,23.6727351071231));
#98247=CARTESIAN_POINT('Ctrl Pts',(-1.09496828479217,2.10386371188678,23.6727337623958));
#98248=CARTESIAN_POINT('Ctrl Pts',(-1.09493277214936,2.10388219427325,23.6727310527081));
#98249=CARTESIAN_POINT('Ctrl Pts',(-1.09491488289931,2.1038915043586,23.672729687745));
#98250=CARTESIAN_POINT('Ctrl Pts',(-1.09487883419898,2.10391026456504,23.6727269372497));
#98251=CARTESIAN_POINT('Ctrl Pts',(-1.09486067477835,2.10391971466189,23.6727255517204));
#98252=CARTESIAN_POINT('Ctrl Pts',(-1.09482408128368,2.10393875718215,23.6727227597549));
#98253=CARTESIAN_POINT('Ctrl Pts',(-1.09480564716241,2.10394834962105,23.6727213533159));
#98254=CARTESIAN_POINT('Ctrl Pts',(-1.0947684996824,2.10396767918335,23.6727185191836));
#98255=CARTESIAN_POINT('Ctrl Pts',(-1.09474978634802,2.10397741628468,23.672717091493));
#98256=CARTESIAN_POINT('Ctrl Pts',(-1.09471207578653,2.10399703756582,23.6727142145044));
#98257=CARTESIAN_POINT('Ctrl Pts',(-1.09469307856191,2.10400692173463,23.6727127652075));
#98258=CARTESIAN_POINT('Ctrl Pts',(-1.09465479551704,2.10402683956839,23.67270984465));
#98259=CARTESIAN_POINT('Ctrl Pts',(-1.0946355096674,2.10403687323863,23.6727083733881));
#98260=CARTESIAN_POINT('Ctrl Pts',(-1.09459664450278,2.10405709257861,23.6727054085315));
#98261=CARTESIAN_POINT('Ctrl Pts',(-1.09457706525111,2.10406727820509,23.6727039149426));
#98262=CARTESIAN_POINT('Ctrl Pts',(-1.09453760839208,2.10408780397049,23.6727009050615));
#98263=CARTESIAN_POINT('Ctrl Pts',(-1.09451773077602,2.1040981441033,23.6726993887696));
#98264=CARTESIAN_POINT('Ctrl Pts',(-1.09447767224156,2.10411898142243,23.6726963331078));
#98265=CARTESIAN_POINT('Ctrl Pts',(-1.09445749127362,2.10412947862353,23.672694793735));
#98266=CARTESIAN_POINT('Ctrl Pts',(-1.09441682092992,2.10415063270171,23.6726916915249));
#98267=CARTESIAN_POINT('Ctrl Pts',(-1.09439633154815,2.10416128957058,23.6726901286879));
#98268=CARTESIAN_POINT('Ctrl Pts',(-1.09435503917578,2.10418276565521,23.6726869791554));
#98269=CARTESIAN_POINT('Ctrl Pts',(-1.09433423618284,2.10419358486046,23.6726853924606));
#98270=CARTESIAN_POINT('Ctrl Pts',(-1.09429231130924,2.10421538832798,23.6726821948127));
#98271=CARTESIAN_POINT('Ctrl Pts',(-1.09427118942314,2.10422637258097,23.6726805838601));
#98272=CARTESIAN_POINT('Ctrl Pts',(-1.09422862138021,2.10424850890684,23.6726773372889));
#98273=CARTESIAN_POINT('Ctrl Pts',(-1.09420717522818,2.10425966096475,23.6726757016717));
#98274=CARTESIAN_POINT('Ctrl Pts',(-1.09416395319099,2.10428213570325,23.6726724053579));
#98275=CARTESIAN_POINT('Ctrl Pts',(-1.09414217728436,2.10429345838213,23.6726707446606));
#98276=CARTESIAN_POINT('Ctrl Pts',(-1.09409829015848,2.10431627722483,23.6726673977641));
#98277=CARTESIAN_POINT('Ctrl Pts',(-1.09407617893379,2.10432777337816,23.6726657115656));
#98278=CARTESIAN_POINT('Ctrl Pts',(-1.09403161549073,2.10435094208335,23.6726623132368));
#98279=CARTESIAN_POINT('Ctrl Pts',(-1.09400916325981,2.10436261462798,23.6726606011067));
#98280=CARTESIAN_POINT('Ctrl Pts',(-1.09396391200434,2.1043861390896,23.6726571504755));
#98281=CARTESIAN_POINT('Ctrl Pts',(-1.0939411129928,2.10439799098563,23.6726554119768));
#98282=CARTESIAN_POINT('Ctrl Pts',(-1.08964141779047,2.10663306669688,23.6723275534236));
#98283=CARTESIAN_POINT('Ctrl Pts',(-1.08535780243853,2.10884322286384,23.6720022701121));
#98284=CARTESIAN_POINT('Ctrl Pts',(-1.07533399526423,2.11397643150274,23.6712442230504));
#98285=CARTESIAN_POINT('Ctrl Pts',(-1.06958861676846,2.11688916754811,23.6708121069931));
#98286=CARTESIAN_POINT('Ctrl Pts',(-1.05257448115073,2.12542787616847,23.6695392520864));
#98287=CARTESIAN_POINT('Ctrl Pts',(-1.04127247586534,2.1309876450776,23.6687025047322));
#98288=CARTESIAN_POINT('Ctrl Pts',(-0.940926625929911,2.17936157822732,
23.661345926429));
#98289=CARTESIAN_POINT('Ctrl Pts',(-0.849320358175713,2.21666866288519,
23.6551312243294));
#98290=CARTESIAN_POINT('Ctrl Pts',(-0.588121170694252,2.30446205477606,
23.6380722041268));
#98291=CARTESIAN_POINT('Ctrl Pts',(-0.414838402408274,2.34186692684986,
23.6274560766513));
#98292=CARTESIAN_POINT('Ctrl Pts',(-0.172259230618248,2.3664373891252,23.6120422467127));
#98293=CARTESIAN_POINT('Ctrl Pts',(-0.105259339219353,2.37036248404714,
23.6077341991622));
#98294=CARTESIAN_POINT('Ctrl Pts',(-0.0211068496666656,2.37171760426656,
23.6022169764951));
#98295=CARTESIAN_POINT('Ctrl Pts',(-0.00402391345202829,2.37180810273268,
23.6010915718038));
#98296=CARTESIAN_POINT('Ctrl Pts',(0.0232869442456301,2.37165773505211,
23.5992830722208));
#98297=CARTESIAN_POINT('Ctrl Pts',(0.0335151327760142,2.37153524626704,
23.5986036885838));
#98298=CARTESIAN_POINT('Ctrl Pts',(0.0528993367509235,2.37117768348711,
23.5973120486883));
#98299=CARTESIAN_POINT('Ctrl Pts',(0.0620554315771254,2.37095572836017,
23.5967002150144));
#98300=CARTESIAN_POINT('Ctrl Pts',(0.0828459897703354,2.37033122689557,
23.5953068991122));
#98301=CARTESIAN_POINT('Ctrl Pts',(0.0944791624916371,2.36989604469401,
23.5945244081852));
#98302=CARTESIAN_POINT('Ctrl Pts',(0.124595059399102,2.36854735494653,23.5924910365971));
#98303=CARTESIAN_POINT('Ctrl Pts',(0.143070840973736,2.36750315775391,23.5912360998484));
#98304=CARTESIAN_POINT('Ctrl Pts',(0.279728087573277,2.35817422236538,23.5818964810739));
#98305=CARTESIAN_POINT('Ctrl Pts',(0.397134108619264,2.34126246367862,23.573541592238));
#98306=CARTESIAN_POINT('Ctrl Pts',(0.708752002267166,2.27225898370835,23.5505270915312));
#98307=CARTESIAN_POINT('Ctrl Pts',(0.898424657274827,2.20416041600553,23.535556948897));
#98308=CARTESIAN_POINT('Ctrl Pts',(1.10018794678767,2.10129656434137,23.5197002410519));
#98309=CARTESIAN_POINT('Ctrl Pts',(1.12293176815558,2.08923075595065,23.5179151878064));
#98310=CARTESIAN_POINT('Ctrl Pts',(1.1528563298866,2.07272559431387,23.5155741165569));
#98311=CARTESIAN_POINT('Ctrl Pts',(1.16021527926622,2.06861538665671,23.5149990253939));
#98312=CARTESIAN_POINT('Ctrl Pts',(1.17229729156827,2.06178244217671,23.5140560481075));
#98313=CARTESIAN_POINT('Ctrl Pts',(1.17703307824363,2.05908254155913,23.5136867386581));
#98314=CARTESIAN_POINT('Ctrl Pts',(1.18630237719542,2.0537556293337,23.5129645648943));
#98315=CARTESIAN_POINT('Ctrl Pts',(1.19083654679544,2.05112989223599,23.5126116275206));
#98316=CARTESIAN_POINT('Ctrl Pts',(1.20200262901963,2.0446141092736,23.5117431665545));
#98317=CARTESIAN_POINT('Ctrl Pts',(1.20862447628754,2.04070675391773,23.5112287533436));
#98318=CARTESIAN_POINT('Ctrl Pts',(1.23141771033269,2.02710728079874,23.5094597755772));
#98319=CARTESIAN_POINT('Ctrl Pts',(1.24749297544227,2.01725428165373,23.5082151424283));
#98320=CARTESIAN_POINT('Ctrl Pts',(1.38513924237059,1.93061207355577,23.4975680576467));
#98321=CARTESIAN_POINT('Ctrl Pts',(1.49962944556639,1.84309447536245,23.4887704813196));
#98322=CARTESIAN_POINT('Ctrl Pts',(1.69781700365633,1.66082722078565,23.4722735560336));
#98323=CARTESIAN_POINT('Ctrl Pts',(1.78324977539863,1.56874050544723,23.464602431382));
#98324=CARTESIAN_POINT('Ctrl Pts',(1.90100717021844,1.41969535016007,23.4525787980039));
#98325=CARTESIAN_POINT('Ctrl Pts',(1.93892950751035,1.36744810547589,23.448430710302));
#98326=CARTESIAN_POINT('Ctrl Pts',(1.98401058369055,1.29968623565738,23.443094549426));
#98327=CARTESIAN_POINT('Ctrl Pts',(1.99319902750171,1.28555043449443,23.4419837426714));
#98328=CARTESIAN_POINT('Ctrl Pts',(2.00768713422237,1.26273269583808,23.4401938535362));
#98329=CARTESIAN_POINT('Ctrl Pts',(2.01308312556053,1.25411236104989,23.4395183618577));
#98330=CARTESIAN_POINT('Ctrl Pts',(2.0232300493525,1.23766797376387,23.4382309835327));
#98331=CARTESIAN_POINT('Ctrl Pts',(2.02799146682588,1.22985058129126,23.4376194981242));
#98332=CARTESIAN_POINT('Ctrl Pts',(2.03873539359529,1.2119789329157,23.4362226135859));
#98333=CARTESIAN_POINT('Ctrl Pts',(2.04468896029643,1.20190764454556,23.4354361755094));
#98334=CARTESIAN_POINT('Ctrl Pts',(2.05997884896358,1.17560026165529,23.4333836363636));
#98335=CARTESIAN_POINT('Ctrl Pts',(2.06919764401533,1.15929716128147,23.432113336878));
#98336=CARTESIAN_POINT('Ctrl Pts',(2.15372560965346,1.00559177039827,23.4201501425658));
#98337=CARTESIAN_POINT('Ctrl Pts',(2.21542327885618,0.861179899036344,23.4089685305938));
#98338=CARTESIAN_POINT('Ctrl Pts',(2.29598560400879,0.605104599155677,23.3894240088308));
#98339=CARTESIAN_POINT('Ctrl Pts',(2.32195778633276,0.496199761280336,23.3812046810344));
#98340=CARTESIAN_POINT('Ctrl Pts',(2.3515417781784,0.316783438908808,23.3681045635035));
#98341=CARTESIAN_POINT('Ctrl Pts',(2.35986961506396,0.247220582269833,23.3631327452343));
#98342=CARTESIAN_POINT('Ctrl Pts',(2.36596368937732,0.165966785138111,23.3575218083263));
#98343=CARTESIAN_POINT('Ctrl Pts',(2.36673733666838,0.154543022470951,23.3567374642195));
#98344=CARTESIAN_POINT('Ctrl Pts',(2.36779692816067,0.137014967764215,23.355541383649));
#98345=CARTESIAN_POINT('Ctrl Pts',(2.36814204742628,0.130914627751493,23.3551264775818));
#98346=CARTESIAN_POINT('Ctrl Pts',(2.36873234556284,0.119713067216328,23.3543672159242));
#98347=CARTESIAN_POINT('Ctrl Pts',(2.36898462212039,0.114612409981005,23.3540224809888));
#98348=CARTESIAN_POINT('Ctrl Pts',(2.36951494687385,0.10313905708221,23.3532492543183));
#98349=CARTESIAN_POINT('Ctrl Pts',(2.36978376318234,0.096766041198624,23.3528212824365));
#98350=CARTESIAN_POINT('Ctrl Pts',(2.37049660678263,0.0780756713808241,
23.3515704250662));
#98351=CARTESIAN_POINT('Ctrl Pts',(2.37087034413836,0.0657556141695112,
23.350751339451));
#98352=CARTESIAN_POINT('Ctrl Pts',(2.37299230253983,-0.0284088394800388,
23.3445286151073));
#98353=CARTESIAN_POINT('Ctrl Pts',(2.37059831258936,-0.110301374516682,
23.3393337331117));
#98354=CARTESIAN_POINT('Ctrl Pts',(2.35256814407307,-0.332393527750058,
23.325444112802));
#98355=CARTESIAN_POINT('Ctrl Pts',(2.32866451942597,-0.471578742878834,
23.3169423946824));
#98356=CARTESIAN_POINT('Ctrl Pts',(2.26553857495637,-0.709673163410089,
23.3016969477584));
#98357=CARTESIAN_POINT('Ctrl Pts',(2.23178048833928,-0.809600419849382,
23.2950720155049));
#98358=CARTESIAN_POINT('Ctrl Pts',(2.18148942406516,-0.931121121142471,
23.2865260292116));
#98359=CARTESIAN_POINT('Ctrl Pts',(2.17108517973295,-0.955129155046752,
23.2848132653419));
#98360=CARTESIAN_POINT('Ctrl Pts',(2.15529782836025,-0.989967369701426,
23.2822896370721));
#98361=CARTESIAN_POINT('Ctrl Pts',(2.15022544942074,-1.00093687589132,23.2814894065501));
#98362=CARTESIAN_POINT('Ctrl Pts',(2.14113822885043,-1.02020098928727,23.2800739192183));
#98363=CARTESIAN_POINT('Ctrl Pts',(2.13715843700206,-1.02851192730985,23.2794598849882));
#98364=CARTESIAN_POINT('Ctrl Pts',(2.12929527522493,-1.04468974313156,23.278257941064));
#98365=CARTESIAN_POINT('Ctrl Pts',(2.12541648335709,-1.05255869061325,23.277670198773));
#98366=CARTESIAN_POINT('Ctrl Pts',(2.11483981806569,-1.07371882831812,23.2760811983146));
#98367=CARTESIAN_POINT('Ctrl Pts',(2.10806043784326,-1.08696860632082,23.2750770959752));
#98368=CARTESIAN_POINT('Ctrl Pts',(2.0821658779951,-1.13642401131925,23.2712942557773));
#98369=CARTESIAN_POINT('Ctrl Pts',(2.06223995106247,-1.17219465000897,23.2684870737217));
#98370=CARTESIAN_POINT('Ctrl Pts',(1.91775471701896,-1.41647555800478,23.2488044441098));
#98371=CARTESIAN_POINT('Ctrl Pts',(1.76274018414759,-1.60526804795243,23.2307402339452));
#98372=CARTESIAN_POINT('Ctrl Pts',(1.53271798853135,-1.8111657393774,23.2085429045993));
#98373=CARTESIAN_POINT('Ctrl Pts',(1.48177034157325,-1.85307966581385,23.2038700181985));
#98374=CARTESIAN_POINT('Ctrl Pts',(1.42011460329042,-1.89963164421286,23.198551462756));
#98375=CARTESIAN_POINT('Ctrl Pts',(1.4110434529972,-1.90637935804305,23.1977771545701));
#98376=CARTESIAN_POINT('Ctrl Pts',(1.3970152310102,-1.91665947563325,23.1965926807939));
#98377=CARTESIAN_POINT('Ctrl Pts',(1.39209238828904,-1.92023797634512,23.1961794501014));
#98378=CARTESIAN_POINT('Ctrl Pts',(1.38300828209876,-1.92678807838513,23.1954214582325));
#98379=CARTESIAN_POINT('Ctrl Pts',(1.37885119885717,-1.92976516182755,23.1950763305369));
#98380=CARTESIAN_POINT('Ctrl Pts',(1.36945139673063,-1.9364509217487,23.1942998497357));
#98381=CARTESIAN_POINT('Ctrl Pts',(1.36420323213931,-1.94015175804224,23.193869033298));
#98382=CARTESIAN_POINT('Ctrl Pts',(1.34867488510603,-1.9510076859209,23.1926021017682));
#98383=CARTESIAN_POINT('Ctrl Pts',(1.33835278269682,-1.95810285285008,23.1917699339177));
#98384=CARTESIAN_POINT('Ctrl Pts',(1.24980928761275,-2.01793825847819,23.184711871424));
#98385=CARTESIAN_POINT('Ctrl Pts',(1.16855119832032,-2.06605682919888,23.1787643262675));
#98386=CARTESIAN_POINT('Ctrl Pts',(0.915231919940702,-2.19632273165112,
23.1611027647524));
#98387=CARTESIAN_POINT('Ctrl Pts',(0.735962221065859,-2.26270697676572,
23.149696813605));
#98388=CARTESIAN_POINT('Ctrl Pts',(0.512459153630386,-2.31605868697322,
23.1351080087506));
#98389=CARTESIAN_POINT('Ctrl Pts',(0.474018113536081,-2.3242307950135,23.132589053918));
#98390=CARTESIAN_POINT('Ctrl Pts',(0.407184520227784,-2.33671186090213,
23.1281805119068));
#98391=CARTESIAN_POINT('Ctrl Pts',(0.37888341834952,-2.3414672308131,23.1263048000837));
#98392=CARTESIAN_POINT('Ctrl Pts',(0.33810451132477,-2.3475605596802,23.1235862868678));
#98393=CARTESIAN_POINT('Ctrl Pts',(0.325690758578103,-2.34931495579413,
23.1227566400809));
#98394=CARTESIAN_POINT('Ctrl Pts',(0.304063322917073,-2.35219678414945,
23.1213073311147));
#98395=CARTESIAN_POINT('Ctrl Pts',(0.294855764197943,-2.35336871097951,
23.120689087377));
#98396=CARTESIAN_POINT('Ctrl Pts',(0.277067360006177,-2.35552676517372,
23.1194922214471));
#98397=CARTESIAN_POINT('Ctrl Pts',(0.268487526841918,-2.35652012678393,
23.1189138380588));
#98398=CARTESIAN_POINT('Ctrl Pts',(0.24810858295146,-2.35876683502552,23.1175373485811));
#98399=CARTESIAN_POINT('Ctrl Pts',(0.236305209257145,-2.35997853593964,
23.1167379434654));
#98400=CARTESIAN_POINT('Ctrl Pts',(0.19433111571026,-2.36396943070917,23.1138872365677));
#98401=CARTESIAN_POINT('Ctrl Pts',(0.164117909635038,-2.36625890702768,
23.1118206834036));
#98402=CARTESIAN_POINT('Ctrl Pts',(-0.0980878242950857,-2.38108239777978,
23.0937516124217));
#98403=CARTESIAN_POINT('Ctrl Pts',(-0.330679545441945,-2.36003766890093,
23.0766282408757));
#98404=CARTESIAN_POINT('Ctrl Pts',(-0.63622140906218,-2.28629808097498,
23.0538243573354));
#98405=CARTESIAN_POINT('Ctrl Pts',(-0.714974303038032,-2.262907691939,23.0479377427313));
#98406=CARTESIAN_POINT('Ctrl Pts',(-0.808600170055024,-2.22972209040883,
23.0410447956196));
#98407=CARTESIAN_POINT('Ctrl Pts',(-0.824774876025817,-2.2237898468432,
23.0398579553041));
#98408=CARTESIAN_POINT('Ctrl Pts',(-0.847625396393234,-2.21512555599948,
23.0381883455427));
#98409=CARTESIAN_POINT('Ctrl Pts',(-0.854355125574872,-2.21253866956675,
23.0376975047563));
#98410=CARTESIAN_POINT('Ctrl Pts',(-0.865923846672474,-2.20803103616243,
23.0368553682762));
#98411=CARTESIAN_POINT('Ctrl Pts',(-0.870768469027594,-2.20612498296049,
23.0365032074034));
#98412=CARTESIAN_POINT('Ctrl Pts',(-0.880187721617931,-2.20238323924681,
23.0358195294535));
#98413=CARTESIAN_POINT('Ctrl Pts',(-0.884762917691652,-2.20054923562659,
23.03548790981));
#98414=CARTESIAN_POINT('Ctrl Pts',(-0.89723891413959,-2.19550293407542,
23.0345847989968));
#98415=CARTESIAN_POINT('Ctrl Pts',(-0.905128256577518,-2.19226222139023,
23.0340149964834));
#98416=CARTESIAN_POINT('Ctrl Pts',(-0.935425379984224,-2.17962560992005,
23.0318311420567));
#98417=CARTESIAN_POINT('Ctrl Pts',(-0.957706697006248,-2.16992774945174,
23.0302342369377));
#98418=CARTESIAN_POINT('Ctrl Pts',(-1.10952596273061,-2.10105475766969,
23.0193901951613));
#98419=CARTESIAN_POINT('Ctrl Pts',(-1.23367115596603,-2.03065141905409,
23.0106972654708));
#98420=CARTESIAN_POINT('Ctrl Pts',(-1.45025201314077,-1.88058969465217,
22.9945538038634));
#98421=CARTESIAN_POINT('Ctrl Pts',(-1.54431306600674,-1.80414594425563,
22.9871363762879));
#98422=CARTESIAN_POINT('Ctrl Pts',(-1.66243185636055,-1.69211791473719,
22.9768234468295));
#98423=CARTESIAN_POINT('Ctrl Pts',(-1.69197198302066,-1.66258028663596,
22.9741508527357));
#98424=CARTESIAN_POINT('Ctrl Pts',(-1.74141615722146,-1.61045724869729,
22.9694976456557));
#98425=CARTESIAN_POINT('Ctrl Pts',(-1.76169893987479,-1.58824415435028,
22.9675331496302));
#98426=CARTESIAN_POINT('Ctrl Pts',(-1.78998464783484,-1.55605789220829,
22.9647090306807));
#98427=CARTESIAN_POINT('Ctrl Pts',(-1.79833842227419,-1.54639584569376,
22.9638640485207));
#98428=CARTESIAN_POINT('Ctrl Pts',(-1.81265275057972,-1.52956691584467,
22.9623968248351));
#98429=CARTESIAN_POINT('Ctrl Pts',(-1.81864990748264,-1.52243142833548,
22.9617761055263));
#98430=CARTESIAN_POINT('Ctrl Pts',(-1.83008569475433,-1.50866099937072,
22.9605807535569));
#98431=CARTESIAN_POINT('Ctrl Pts',(-1.83553070207065,-1.50203152415951,
22.9600063939815));
#98432=CARTESIAN_POINT('Ctrl Pts',(-1.84827828351086,-1.48633809433353,
22.9586492901414));
#98433=CARTESIAN_POINT('Ctrl Pts',(-1.85555028249908,-1.47724970287719,
22.957865331527));
#98434=CARTESIAN_POINT('Ctrl Pts',(-1.88068091814271,-1.44536362410089,
22.9551214029163));
#98435=CARTESIAN_POINT('Ctrl Pts',(-1.89818804956177,-1.42229347198847,
22.9531476272808));
#98436=CARTESIAN_POINT('Ctrl Pts',(-2.00948440161574,-1.26991597792227,
22.9401792960293));
#98437=CARTESIAN_POINT('Ctrl Pts',(-2.09041149552327,-1.13175808072487,
22.928694572674));
#98438=CARTESIAN_POINT('Ctrl Pts',(-2.20565602922112,-0.879804962810913,
22.9084781713023));
#98439=CARTESIAN_POINT('Ctrl Pts',(-2.24649047860357,-0.769583192365358,
22.899862388963));
#98440=CARTESIAN_POINT('Ctrl Pts',(-2.28814372154299,-0.625049815125328,
22.8891408409844));
#98441=CARTESIAN_POINT('Ctrl Pts',(-2.29662663232989,-0.593123351541301,
22.8868080348292));
#98442=CARTESIAN_POINT('Ctrl Pts',(-2.30954187336032,-0.540073632223861,
22.8830010662205));
#98443=CARTESIAN_POINT('Ctrl Pts',(-2.31435761125718,-0.519049249499883,
22.8815100922245));
#98444=CARTESIAN_POINT('Ctrl Pts',(-2.32054047728001,-0.490257121677173,
22.8794951139561));
#98445=CARTESIAN_POINT('Ctrl Pts',(-2.32215648631423,-0.48254472291694,
22.8789579901675));
#98446=CARTESIAN_POINT('Ctrl Pts',(-2.32480186974153,-0.469598528107036,
22.8780609110371));
#98447=CARTESIAN_POINT('Ctrl Pts',(-2.32585206740307,-0.464369113407465,
22.8776997913014));
#98448=CARTESIAN_POINT('Ctrl Pts',(-2.32780948477424,-0.45444899555954,
22.8770171616387));
#98449=CARTESIAN_POINT('Ctrl Pts',(-2.32872018446531,-0.4497590360126,22.8766954497944));
#98450=CARTESIAN_POINT('Ctrl Pts',(-2.33106879238806,-0.437465685025876,
22.8758547620553));
#98451=CARTESIAN_POINT('Ctrl Pts',(-2.33248368798569,-0.429857871779538,
22.8753370848505));
#98452=CARTESIAN_POINT('Ctrl Pts',(-2.33726614076484,-0.403423856062453,
22.8735469120357));
#98453=CARTESIAN_POINT('Ctrl Pts',(-2.34044331634184,-0.384563338206025,
22.8722846497996));
#98454=CARTESIAN_POINT('Ctrl Pts',(-2.36215703217978,-0.245409601646564,
22.863068147003));
#98455=CARTESIAN_POINT('Ctrl Pts',(-2.37163990223934,-0.123870369466769,
22.8555429262571));
#98456=CARTESIAN_POINT('Ctrl Pts',(-2.37180149900125,0.0563807931440272,
22.8444766113764));
#98457=CARTESIAN_POINT('Ctrl Pts',(-2.36968900558597,0.114821446852761,
22.8409042704249));
#98458=CARTESIAN_POINT('Ctrl Pts',(-2.36542647205563,0.173077057400636,
22.8373161962119));
#98459=CARTESIAN_POINT('Ctrl Pts',(-2.36542649454112,0.173076750093424,
22.6375488994376));
#98460=CARTESIAN_POINT('Ctrl Pts',(-2.3661388636995,0.163340856160745,22.6381959253031));
#98461=CARTESIAN_POINT('Ctrl Pts',(-2.36679110884809,0.153600780959581,
22.6388448135099));
#98462=CARTESIAN_POINT('Ctrl Pts',(-2.3679525343904,0.134487787915918,22.640121361727));
#98463=CARTESIAN_POINT('Ctrl Pts',(-2.36846623843217,0.125115319822445,
22.6407488675116));
#98464=CARTESIAN_POINT('Ctrl Pts',(-2.36952546227323,0.103435541717451,
22.6422040098318));
#98465=CARTESIAN_POINT('Ctrl Pts',(-2.37003074984772,0.0911266286698586,
22.6430328907792));
#98466=CARTESIAN_POINT('Ctrl Pts',(-2.37132321985088,0.0522540697189382,
22.6456594248895));
#98467=CARTESIAN_POINT('Ctrl Pts',(-2.37175982230706,0.0256816243651149,
22.6474679495416));
#98468=CARTESIAN_POINT('Ctrl Pts',(-2.37170837929134,-0.111157339372951,
22.656852124219));
#98469=CARTESIAN_POINT('Ctrl Pts',(-2.36397757858074,-0.221269658741762,
22.6646497781992));
#98470=CARTESIAN_POINT('Ctrl Pts',(-2.32873649624718,-0.471753883068607,
22.6828981369618));
#98471=CARTESIAN_POINT('Ctrl Pts',(-2.29614003560575,-0.610986100626804,
22.6934256964943));
#98472=CARTESIAN_POINT('Ctrl Pts',(-2.24597325550628,-0.762286630255959,
22.7049314770699));
#98473=CARTESIAN_POINT('Ctrl Pts',(-2.24055185727853,-0.778077223748826,
22.70613279557));
#98474=CARTESIAN_POINT('Ctrl Pts',(-2.21540362821652,-0.848881851785801,
22.7115183105915));
#98475=CARTESIAN_POINT('Ctrl Pts',(-2.19381229719774,-0.903217889182414,
22.7156483952386));
#98476=CARTESIAN_POINT('Ctrl Pts',(-2.1660027905404,-0.966302214104502,
22.7203969108266));
#98477=CARTESIAN_POINT('Ctrl Pts',(-2.16170854119895,-0.975871021548873,
22.7211158765168));
#98478=CARTESIAN_POINT('Ctrl Pts',(-2.15461655288039,-0.991397439723287,
22.7222799812653));
#98479=CARTESIAN_POINT('Ctrl Pts',(-2.1518572991874,-0.997372317658715,
22.7227273468716));
#98480=CARTESIAN_POINT('Ctrl Pts',(-2.14687775890053,-1.00803813585572,
22.7235247580776));
#98481=CARTESIAN_POINT('Ctrl Pts',(-2.14466691964414,-1.01273333139938,
22.7238753666159));
#98482=CARTESIAN_POINT('Ctrl Pts',(-2.13981405161934,-1.02295228467462,
22.724637530639));
#98483=CARTESIAN_POINT('Ctrl Pts',(-2.13716604138198,-1.0284730749715,22.7250487112479));
#98484=CARTESIAN_POINT('Ctrl Pts',(-2.12959539288709,-1.04410148858156,
22.7262112241099));
#98485=CARTESIAN_POINT('Ctrl Pts',(-2.12462214292929,-1.05418462240831,
22.7269595041109));
#98486=CARTESIAN_POINT('Ctrl Pts',(-2.09176834746567,-1.1196178557757,22.7318064247401));
#98487=CARTESIAN_POINT('Ctrl Pts',(-2.06179635300671,-1.17389791441905,
22.7357854558786));
#98488=CARTESIAN_POINT('Ctrl Pts',(-1.92962405058496,-1.39254965414665,
22.7518980470798));
#98489=CARTESIAN_POINT('Ctrl Pts',(-1.80962582330238,-1.54528556569233,
22.7634144567564));
#98490=CARTESIAN_POINT('Ctrl Pts',(-1.61169767098765,-1.74211262704637,
22.7808843284437));
#98491=CARTESIAN_POINT('Ctrl Pts',(-1.54778221169918,-1.79913686973881,
22.7863349930808));
#98492=CARTESIAN_POINT('Ctrl Pts',(-1.46733189643567,-1.8634479410569,22.7930705632821));
#98493=CARTESIAN_POINT('Ctrl Pts',(-1.453615018906,-1.87416767485568,22.7942147383574));
#98494=CARTESIAN_POINT('Ctrl Pts',(-1.43072987914596,-1.89165002713215,
22.7961174369228));
#98495=CARTESIAN_POINT('Ctrl Pts',(-1.42162852477293,-1.89849944485158,
22.7968725331211));
#98496=CARTESIAN_POINT('Ctrl Pts',(-1.40504654413444,-1.91079246845791,
22.7982455690657));
#98497=CARTESIAN_POINT('Ctrl Pts',(-1.39758269100841,-1.9162584028048,22.7988626226279));
#98498=CARTESIAN_POINT('Ctrl Pts',(-1.38145863066075,-1.92792207393038,
22.8001936561382));
#98499=CARTESIAN_POINT('Ctrl Pts',(-1.37278830550615,-1.93410540902406,
22.8009081736812));
#98500=CARTESIAN_POINT('Ctrl Pts',(-1.34886939536106,-1.9509215742933,22.8028761909784));
#98501=CARTESIAN_POINT('Ctrl Pts',(-1.33353725531349,-1.9614336565659,22.8041342486639));
#98502=CARTESIAN_POINT('Ctrl Pts',(-1.24573399648598,-2.02012831633968,
22.8113210077753));
#98503=CARTESIAN_POINT('Ctrl Pts',(-1.17078646355645,-2.06446780823758,
22.8173910038987));
#98504=CARTESIAN_POINT('Ctrl Pts',(-0.88345515166124,-2.21377030927592,
22.8404355763361));
#98505=CARTESIAN_POINT('Ctrl Pts',(-0.658195280883046,-2.29085875111872,
22.8582198615693));
#98506=CARTESIAN_POINT('Ctrl Pts',(-0.401758654445174,-2.33759687660502,
22.8764464485488));
#98507=CARTESIAN_POINT('Ctrl Pts',(-0.37818344102016,-2.3415265468616,22.8781023300548));
#98508=CARTESIAN_POINT('Ctrl Pts',(-0.346080665181735,-2.34638011309947,
22.8803268281599));
#98509=CARTESIAN_POINT('Ctrl Pts',(-0.3376025417441,-2.34761495810114,22.8809114384758));
#98510=CARTESIAN_POINT('Ctrl Pts',(-0.3241821182491,-2.34949544699558,22.8818321221227));
#98511=CARTESIAN_POINT('Ctrl Pts',(-0.319244261086383,-2.35017148399574,
22.8821698649993));
#98512=CARTESIAN_POINT('Ctrl Pts',(-0.309057419870157,-2.35153345607968,
22.8828644990753));
#98513=CARTESIAN_POINT('Ctrl Pts',(-0.303808249316206,-2.35221738622069,
22.883221262447));
#98514=CARTESIAN_POINT('Ctrl Pts',(-0.29123005893677,-2.35381342942204,
22.8840734188807));
#98515=CARTESIAN_POINT('Ctrl Pts',(-0.283898904720153,-2.35470890416378,
22.8845678819676));
#98516=CARTESIAN_POINT('Ctrl Pts',(-0.258771760707469,-2.35765904026258,
22.8862554209968));
#98517=CARTESIAN_POINT('Ctrl Pts',(-0.240956196738947,-2.35954638298514,
22.8874395440333));
#98518=CARTESIAN_POINT('Ctrl Pts',(-0.135679794203057,-2.36949428514516,
22.8943729847273));
#98519=CARTESIAN_POINT('Ctrl Pts',(-0.0478372558555888,-2.37289429656389,
22.8998997604611));
#98520=CARTESIAN_POINT('Ctrl Pts',(0.051644136535442,-2.3712162609732,22.9060661745913));
#98521=CARTESIAN_POINT('Ctrl Pts',(0.0632861612777919,-2.37093410683426,
22.9067863514726));
#98522=CARTESIAN_POINT('Ctrl Pts',(0.2351799419568,-2.36550111571691,22.9174038103189));
#98523=CARTESIAN_POINT('Ctrl Pts',(0.394501062185377,-2.34419987827504,
22.9270726642322));
#98524=CARTESIAN_POINT('Ctrl Pts',(0.621114370105323,-2.29012927205432,
22.9417458010868));
#98525=CARTESIAN_POINT('Ctrl Pts',(0.690956141472397,-2.27003372628854,
22.9463955245219));
#98526=CARTESIAN_POINT('Ctrl Pts',(0.777004461513788,-2.24093584681048,
22.9523414489791));
#98527=CARTESIAN_POINT('Ctrl Pts',(0.794179880476881,-2.23490664001054,
22.9535392392594));
#98528=CARTESIAN_POINT('Ctrl Pts',(0.821309441411762,-2.22503094276704,
22.9554494729037));
#98529=CARTESIAN_POINT('Ctrl Pts',(0.831310189740711,-2.22131385826566,
22.956157610009));
#98530=CARTESIAN_POINT('Ctrl Pts',(0.849931612688952,-2.21424927081853,
22.957483751261));
#98531=CARTESIAN_POINT('Ctrl Pts',(0.858558479078264,-2.21091856778902,
22.9581011827082));
#98532=CARTESIAN_POINT('Ctrl Pts',(0.877738458997944,-2.20338428246305,
22.9594808563651));
#98533=CARTESIAN_POINT('Ctrl Pts',(0.888281238304005,-2.19915518608325,
22.9602439461024));
#98534=CARTESIAN_POINT('Ctrl Pts',(0.919106150079819,-2.18653235998805,
22.9624891652622));
#98535=CARTESIAN_POINT('Ctrl Pts',(0.939302151461556,-2.17793280154996,
22.9639782200499));
#98536=CARTESIAN_POINT('Ctrl Pts',(0.984824070776736,-2.15779840335284,
22.967376651177));
#98537=CARTESIAN_POINT('Ctrl Pts',(1.01007178846239,-2.14609581997832,22.9692915460008));
#98538=CARTESIAN_POINT('Ctrl Pts',(1.09270560182075,-2.10601299635434,22.9756602539608));
#98539=CARTESIAN_POINT('Ctrl Pts',(1.14914475580988,-2.07575561197449,22.9801750172605));
#98540=CARTESIAN_POINT('Ctrl Pts',(1.301593861362,-1.98590266102623,22.9928236833596));
#98541=CARTESIAN_POINT('Ctrl Pts',(1.39467316866816,-1.92167616410992,23.0010763570968));
#98542=CARTESIAN_POINT('Ctrl Pts',(1.53236254739288,-1.81137883728895,23.0139589192861));
#98543=CARTESIAN_POINT('Ctrl Pts',(1.58029781293401,-1.76971400626846,23.0185856431617));
#98544=CARTESIAN_POINT('Ctrl Pts',(1.67513625438375,-1.68035155469987,23.0279634723725));
#98545=CARTESIAN_POINT('Ctrl Pts',(1.7218145569077,-1.63248868752505,23.0327043849828));
#98546=CARTESIAN_POINT('Ctrl Pts',(1.77366953336858,-1.57461509120875,23.0380600509995));
#98547=CARTESIAN_POINT('Ctrl Pts',(1.78087013053637,-1.5664666892523,23.0388058424641));
#98548=CARTESIAN_POINT('Ctrl Pts',(1.79241427416385,-1.55322051723364,23.0400045267799));
#98549=CARTESIAN_POINT('Ctrl Pts',(1.79679261426107,-1.54815348383766,23.0404598644193));
#98550=CARTESIAN_POINT('Ctrl Pts',(1.80453127423543,-1.53912051542346,23.041265835484));
#98551=CARTESIAN_POINT('Ctrl Pts',(1.80790007389399,-1.53516201275571,23.0416170838312));
#98552=CARTESIAN_POINT('Ctrl Pts',(1.81515351357574,-1.52658187862291,23.0423741988551));
#98553=CARTESIAN_POINT('Ctrl Pts',(1.81903352728858,-1.52195648382285,23.0427797308518));
#98554=CARTESIAN_POINT('Ctrl Pts',(1.82983620864999,-1.50897819840385,23.0439104778261));
#98555=CARTESIAN_POINT('Ctrl Pts',(1.83671940122731,-1.50059241840012,23.0446328980133));
#98556=CARTESIAN_POINT('Ctrl Pts',(1.87758904784791,-1.45009846553379,23.0489360909865));
#98557=CARTESIAN_POINT('Ctrl Pts',(1.91018688171083,-1.4068807144998,23.0524260414535));
#98558=CARTESIAN_POINT('Ctrl Pts',(2.0167664384339,-1.25503602338574,23.0641874890026));
#98559=CARTESIAN_POINT('Ctrl Pts',(2.08319082677375,-1.14139544836367,23.072160228334));
#98560=CARTESIAN_POINT('Ctrl Pts',(2.20600687577525,-0.88445192073966,23.0896372626051));
#98561=CARTESIAN_POINT('Ctrl Pts',(2.25856243028706,-0.740005184954343,
23.099147283715));
#98562=CARTESIAN_POINT('Ctrl Pts',(2.30152987427224,-0.573164136774601,
23.1103949485897));
#98563=CARTESIAN_POINT('Ctrl Pts',(2.30603409105361,-0.554764478467687,
23.1116383491805));
#98564=CARTESIAN_POINT('Ctrl Pts',(2.31299847165395,-0.524763488289189,
23.1136715097836));
#98565=CARTESIAN_POINT('Ctrl Pts',(2.31559292944544,-0.513193944791641,
23.1144569604307));
#98566=CARTESIAN_POINT('Ctrl Pts',(2.32006592893637,-0.49252260039326,23.1158630122859));
#98567=CARTESIAN_POINT('Ctrl Pts',(2.32197794298424,-0.483428231052103,
23.1164825282888));
#98568=CARTESIAN_POINT('Ctrl Pts',(2.32590512007363,-0.464187928985814,
23.1177952509953));
#98569=CARTESIAN_POINT('Ctrl Pts',(2.32790744914565,-0.454039605463795,
23.1184888533661));
#98570=CARTESIAN_POINT('Ctrl Pts',(2.33306157058002,-0.426986501193547,
23.120341210399));
#98571=CARTESIAN_POINT('Ctrl Pts',(2.33609595765507,-0.410060256241769,
23.121503669563));
#98572=CARTESIAN_POINT('Ctrl Pts',(2.34998556372365,-0.327417674790233,
23.1271975520379));
#98573=CARTESIAN_POINT('Ctrl Pts',(2.35825226964407,-0.261302864185152,
23.1318097583441));
#98574=CARTESIAN_POINT('Ctrl Pts',(2.38523700274425,0.0659092742757167,
23.154933606839));
#98575=CARTESIAN_POINT('Ctrl Pts',(2.36342562879834,0.328453439871522,23.1746740265317));
#98576=CARTESIAN_POINT('Ctrl Pts',(2.29367009815016,0.603973795083269,23.1945198682148));
#98577=CARTESIAN_POINT('Ctrl Pts',(2.28782201771796,0.625761434976696,23.196081203516));
#98578=CARTESIAN_POINT('Ctrl Pts',(2.2793846736041,0.655494675196571,23.1981978466196));
#98579=CARTESIAN_POINT('Ctrl Pts',(2.27706319402351,0.663514110784612,23.198767317868));
#98580=CARTESIAN_POINT('Ctrl Pts',(2.27330028395333,0.676260526317819,23.1996700203236));
#98581=CARTESIAN_POINT('Ctrl Pts',(2.27188636956548,0.680995451827686,23.200004810821));
#98582=CARTESIAN_POINT('Ctrl Pts',(2.26891739398172,0.690825811960946,23.2006987143842));
#98583=CARTESIAN_POINT('Ctrl Pts',(2.26735995308383,0.695920460263877,23.2010576740294));
#98584=CARTESIAN_POINT('Ctrl Pts',(2.26355158155666,0.708229777020815,23.2019234582874));
#98585=CARTESIAN_POINT('Ctrl Pts',(2.2612832806096,0.715439101676275,23.2024292770499));
#98586=CARTESIAN_POINT('Ctrl Pts',(2.2532052127656,0.740691314226301,23.2041970169068));
#98587=CARTESIAN_POINT('Ctrl Pts',(2.24721345989887,0.758675870039446,23.2054488149318));
#98588=CARTESIAN_POINT('Ctrl Pts',(2.20873854471694,0.869703347499156,23.213143410879));
#98589=CARTESIAN_POINT('Ctrl Pts',(2.17069420490474,0.960729549417549,23.2193077067805));
#98590=CARTESIAN_POINT('Ctrl Pts',(2.05589304541637,1.19348587954897,23.2353293162124));
#98591=CARTESIAN_POINT('Ctrl Pts',(1.97018928140877,1.3302097032042,23.2450375354138));
#98592=CARTESIAN_POINT('Ctrl Pts',(1.82738695775039,1.51359291011812,23.2596859954296));
#98593=CARTESIAN_POINT('Ctrl Pts',(1.78095066126048,1.56796676292969,23.2642632475828));
#98594=CARTESIAN_POINT('Ctrl Pts',(1.71976458106991,1.63338168327896,23.2701271256744));
#98595=CARTESIAN_POINT('Ctrl Pts',(1.7072446132067,1.64646340321458,23.2713187500619));
#98596=CARTESIAN_POINT('Ctrl Pts',(1.68712430833667,1.66701022085875,23.2732215902467));
#98597=CARTESIAN_POINT('Ctrl Pts',(1.67962117627239,1.67456985705221,23.2739285632099));
#98598=CARTESIAN_POINT('Ctrl Pts',(1.66550375916694,1.68860325249131,23.2752540524203));
#98599=CARTESIAN_POINT('Ctrl Pts',(1.6589019836655,1.69508935473305,23.2758720066497));
#98600=CARTESIAN_POINT('Ctrl Pts',(1.64408532657908,1.70947694250957,23.2772548295635));
#98601=CARTESIAN_POINT('Ctrl Pts',(1.63585115201714,1.71735813929517,23.2780205598831));
#98602=CARTESIAN_POINT('Ctrl Pts',(1.6114709149086,1.74035882546914,23.2802799689226));
#98603=CARTESIAN_POINT('Ctrl Pts',(1.59517014812144,1.75531179328788,23.281780698244));
#98604=CARTESIAN_POINT('Ctrl Pts',(1.46829185996675,1.86847236195672,23.2933898910201));
#98605=CARTESIAN_POINT('Ctrl Pts',(1.34897650987916,1.95635309903308,23.3039255317526));
#98606=CARTESIAN_POINT('Ctrl Pts',(1.08402641862237,2.11568212167048,23.3264022948006));
#98607=CARTESIAN_POINT('Ctrl Pts',(0.937647520516158,2.18450126199222,23.3383270637343));
#98608=CARTESIAN_POINT('Ctrl Pts',(0.756555337324953,2.24805633352086,23.3518289938383));
#98609=CARTESIAN_POINT('Ctrl Pts',(0.727504923768372,2.25762487272788,23.3539574342134));
#98610=CARTESIAN_POINT('Ctrl Pts',(0.689286805912397,2.26939865034461,23.3567017039674));
#98611=CARTESIAN_POINT('Ctrl Pts',(0.680281129544448,2.27211446175078,23.3573443424587));
#98612=CARTESIAN_POINT('Ctrl Pts',(0.665773173933974,2.27639558563376,23.3583729052043));
#98613=CARTESIAN_POINT('Ctrl Pts',(0.660281089432748,2.27799465893488,23.3587607332911));
#98614=CARTESIAN_POINT('Ctrl Pts',(0.649713515610885,2.28103008142851,23.3595039401175));
#98615=CARTESIAN_POINT('Ctrl Pts',(0.644638992526011,2.28246937648357,23.3598594777554));
#98616=CARTESIAN_POINT('Ctrl Pts',(0.632538188190395,2.28585797241889,23.3607041655991));
#98617=CARTESIAN_POINT('Ctrl Pts',(0.625507570527957,2.28779184200947,23.3611924258191));
#98618=CARTESIAN_POINT('Ctrl Pts',(0.601692673283296,2.29422447323487,23.3628381973648));
#98619=CARTESIAN_POINT('Ctrl Pts',(0.584867416428193,2.29857132928951,23.3639873272444));
#98620=CARTESIAN_POINT('Ctrl Pts',(0.487748591326862,2.32252679233712,23.370550327774));
#98621=CARTESIAN_POINT('Ctrl Pts',(0.406512658223501,2.33811460863067,23.3757664584904));
#98622=CARTESIAN_POINT('Ctrl Pts',(0.157871084295467,2.37246936447168,23.3913570572604));
#98623=CARTESIAN_POINT('Ctrl Pts',(-0.0108546185834055,2.3776917500096,
23.4014623286112));
#98624=CARTESIAN_POINT('Ctrl Pts',(-0.2597617503961,2.35888280122194,23.4171148508039));
#98625=CARTESIAN_POINT('Ctrl Pts',(-0.340432658189673,2.34859694853301,
23.4222988470915));
#98626=CARTESIAN_POINT('Ctrl Pts',(-0.43892269547475,2.33085794224683,23.4288450967247));
#98627=CARTESIAN_POINT('Ctrl Pts',(-0.457394077275822,2.32730369824493,
23.4300822092254));
#98628=CARTESIAN_POINT('Ctrl Pts',(-0.486403256315172,2.32136309515186,
23.4320407686154));
#98629=CARTESIAN_POINT('Ctrl Pts',(-0.496970633158464,2.31912374195317,
23.4327575184811));
#98630=CARTESIAN_POINT('Ctrl Pts',(-0.516452998849367,2.31485592405895,
23.4340851936952));
#98631=CARTESIAN_POINT('Ctrl Pts',(-0.525372304277465,2.31284793858812,
23.4346954513427));
#98632=CARTESIAN_POINT('Ctrl Pts',(-0.54512965951049,2.30827982106654,23.4360527481966));
#98633=CARTESIAN_POINT('Ctrl Pts',(-0.555961681239863,2.30569483662775,
23.4368005750237));
#98634=CARTESIAN_POINT('Ctrl Pts',(-0.587071131271974,2.29803882334521,
23.4389591637181));
#98635=CARTESIAN_POINT('Ctrl Pts',(-0.607299819618479,2.29277600889447,
23.4403760740188));
#98636=CARTESIAN_POINT('Ctrl Pts',(-0.786544220108168,2.24360425477636,
23.4530532963383));
#98637=CARTESIAN_POINT('Ctrl Pts',(-0.940613108902813,2.18349226559486,
23.4648569039047));
#98638=CARTESIAN_POINT('Ctrl Pts',(-1.23183282770601,2.033292702644,23.4887415972583));
#98639=CARTESIAN_POINT('Ctrl Pts',(-1.36843905867133,1.94398414650229,23.500745819513));
#98640=CARTESIAN_POINT('Ctrl Pts',(-1.50871661848653,1.83010715544336,23.5132995216918));
#98641=CARTESIAN_POINT('Ctrl Pts',(-1.52247689346887,1.81867594488152,23.5145332291178));
#98642=CARTESIAN_POINT('Ctrl Pts',(-1.54132792955243,1.80265172169718,23.5162249969383));
#98643=CARTESIAN_POINT('Ctrl Pts',(-1.54652965642546,1.79819104683339,23.5166919958253));
#98644=CARTESIAN_POINT('Ctrl Pts',(-1.55542566550005,1.79049523127157,23.5174908509254));
#98645=CARTESIAN_POINT('Ctrl Pts',(-1.55912932943563,1.7872710788591,23.5178234949254));
#98646=CARTESIAN_POINT('Ctrl Pts',(-1.56651620959089,1.78080013881076,23.5184870148891));
#98647=CARTESIAN_POINT('Ctrl Pts',(-1.57019938452929,1.77755339236576,23.5188178825288));
#98648=CARTESIAN_POINT('Ctrl Pts',(-1.57925866939608,1.76951743585439,23.5196318455953));
#98649=CARTESIAN_POINT('Ctrl Pts',(-1.58462316563945,1.76471508380249,23.5201139677787));
#98650=CARTESIAN_POINT('Ctrl Pts',(-1.60225894344346,1.748782093305,23.5216997067464));
#98651=CARTESIAN_POINT('Ctrl Pts',(-1.61443581111957,1.7375470012838,23.5227958305708));
#98652=CARTESIAN_POINT('Ctrl Pts',(-1.64368904090397,1.70998320147671,23.5254350843012));
#98653=CARTESIAN_POINT('Ctrl Pts',(-1.66064140238457,1.69352485640265,23.5269695964148));
#98654=CARTESIAN_POINT('Ctrl Pts',(-1.72445087527935,1.62969519827923,23.5327785894735));
#98655=CARTESIAN_POINT('Ctrl Pts',(-1.76955331795264,1.58060737595379,23.5369547406256));
#98656=CARTESIAN_POINT('Ctrl Pts',(-1.84856984134563,1.48698008886257,23.5445453325266));
#98657=CARTESIAN_POINT('Ctrl Pts',(-1.8830884051977,1.44301717751472,23.5479713848785));
#98658=CARTESIAN_POINT('Ctrl Pts',(-2.01661899165418,1.25999110305726,23.5618550429729));
#98659=CARTESIAN_POINT('Ctrl Pts',(-2.10202537335978,1.11166987272222,23.5722988597832));
#98660=CARTESIAN_POINT('Ctrl Pts',(-2.18240899964653,0.929044186277643,
23.5852288000051));
#98661=CARTESIAN_POINT('Ctrl Pts',(-2.19355948442685,0.902401690823416,
23.5871153699846));
#98662=CARTESIAN_POINT('Ctrl Pts',(-2.20854914650283,0.864665386103283,
23.5897909809212));
#98663=CARTESIAN_POINT('Ctrl Pts',(-2.21279702455577,0.853735838678894,
23.5905663159395));
#98664=CARTESIAN_POINT('Ctrl Pts',(-2.22005027253388,0.834655800507353,
23.591920746519));
#98665=CARTESIAN_POINT('Ctrl Pts',(-2.22309226170503,0.826519395060308,
23.5924986079923));
#98666=CARTESIAN_POINT('Ctrl Pts',(-2.22936101663033,0.809467367280539,
23.5937103580647));
#98667=CARTESIAN_POINT('Ctrl Pts',(-2.2325791465368,0.80054875622889,23.5943445217906));
#98668=CARTESIAN_POINT('Ctrl Pts',(-2.24010736825965,0.779286836110114,
23.5958574127246));
#98669=CARTESIAN_POINT('Ctrl Pts',(-2.24436900536133,0.766926821878375,
23.5967377258283));
#98670=CARTESIAN_POINT('Ctrl Pts',(-2.25845288549978,0.724956456675117,
23.5997301811685));
#98671=CARTESIAN_POINT('Ctrl Pts',(-2.26779266929493,0.695188857372109,
23.6018580307696));
#98672=CARTESIAN_POINT('Ctrl Pts',(-2.32348697165967,0.504597316193869,
23.61552282045));
#98673=CARTESIAN_POINT('Ctrl Pts',(-2.35324136537112,0.339609969413825,
23.6275853298065));
#98674=CARTESIAN_POINT('Ctrl Pts',(-2.36542649498009,0.173076744094113,
23.6397760267629));
#98675=CARTESIAN_POINT('Origin',(0.,0.,0.));
#98676=CARTESIAN_POINT('',(-2.94561598299575,0.00187102060485729,0.322176117089595));
#98677=CARTESIAN_POINT('',(1.2910272435207,2.64899789736804,5.96387826521875E-5));
#98678=CARTESIAN_POINT('Ctrl Pts',(-2.94561598299575,0.00187102060485729,
0.322176117089595));
#98679=CARTESIAN_POINT('Ctrl Pts',(-2.94627700058788,0.099138654117573,
0.316895328369764));
#98680=CARTESIAN_POINT('Ctrl Pts',(-2.8977661387304,1.17124645315207,0.258650561155306));
#98681=CARTESIAN_POINT('Ctrl Pts',(-1.62977873101038,3.0288441099736,0.151278401719662));
#98682=CARTESIAN_POINT('Ctrl Pts',(0.47570852676496,3.04092581158969,0.0491870310038447));
#98683=CARTESIAN_POINT('Ctrl Pts',(1.29102724352071,2.64899789736804,5.96387826521875E-5));
#98684=CARTESIAN_POINT('',(-1.28892185405319,2.64462557919719,0.));
#98685=CARTESIAN_POINT('Origin',(0.,0.,0.));
#98686=CARTESIAN_POINT('',(-2.94199832420209,0.00314012613217853,0.177823882943095));
#98687=CARTESIAN_POINT('Ctrl Pts',(-1.28892185405319,2.64462557919719,-1.94289029309402E-15));
#98688=CARTESIAN_POINT('Ctrl Pts',(-1.37483881637629,2.60275188212522,0.00517052748665724));
#98689=CARTESIAN_POINT('Ctrl Pts',(-1.45877171164705,2.55665900158965,0.0103410549733164));
#98690=CARTESIAN_POINT('Ctrl Pts',(-1.54029698572466,2.50656122920776,0.0155115824599756));
#98691=CARTESIAN_POINT('Ctrl Pts',(-1.6217746032091,2.45649274208967,0.0206790874517372));
#98692=CARTESIAN_POINT('Ctrl Pts',(-1.70084704886668,2.40242423989201,0.0258465924434988));
#98693=CARTESIAN_POINT('Ctrl Pts',(-1.77711654308791,2.3446152759639,0.0310140974352603));
#98694=CARTESIAN_POINT('Ctrl Pts',(-1.85580329515119,2.28497413558277,0.0363453794664889));
#98695=CARTESIAN_POINT('Ctrl Pts',(-1.93150605636844,2.22135170164654,0.0416766614977175));
#98696=CARTESIAN_POINT('Ctrl Pts',(-2.00382190342501,2.15408026297865,0.0470079435289461));
#98697=CARTESIAN_POINT('Ctrl Pts',(-2.07390541239702,2.08888544514359,0.0521746527258335));
#98698=CARTESIAN_POINT('Ctrl Pts',(-2.14080775230235,2.0202639299885,0.0573413619227208));
#98699=CARTESIAN_POINT('Ctrl Pts',(-2.20419800366129,1.94855719973923,0.0625080711196082));
#98700=CARTESIAN_POINT('Ctrl Pts',(-2.26759963803479,1.87683759308174,0.0676757081046758));
#98701=CARTESIAN_POINT('Ctrl Pts',(-2.32748765382612,1.8020319790956,0.0728433450897433));
#98702=CARTESIAN_POINT('Ctrl Pts',(-2.38357059315908,1.72451594003282,0.0780109820748108));
#98703=CARTESIAN_POINT('Ctrl Pts',(-2.43967598230067,1.64696887156495,0.0831806876472737));
#98704=CARTESIAN_POINT('Ctrl Pts',(-2.49197302046287,1.5667095543312,0.0883503932197366));
#98705=CARTESIAN_POINT('Ctrl Pts',(-2.54021329705219,1.48414298687129,0.0935200987921995));
#98706=CARTESIAN_POINT('Ctrl Pts',(-2.58848353796475,1.4015251334012,0.0986930155139297));
#98707=CARTESIAN_POINT('Ctrl Pts',(-2.63269179296663,1.31659753470971,0.10386593223566));
#98708=CARTESIAN_POINT('Ctrl Pts',(-2.67263571909581,1.22978954013002,0.10903884895739));
#98709=CARTESIAN_POINT('Ctrl Pts',(-2.71263977449153,1.14285086983691,0.114219552687521));
#98710=CARTESIAN_POINT('Ctrl Pts',(-2.74836651135852,1.05402652900781,0.119400256417653));
#98711=CARTESIAN_POINT('Ctrl Pts',(-2.7796617792108,0.963765735640482,0.124580960147784));
#98712=CARTESIAN_POINT('Ctrl Pts',(-2.81098456103485,0.873425587370955,
0.129766218615609));
#98713=CARTESIAN_POINT('Ctrl Pts',(-2.83786799345476,0.781646866830215,
0.134951477083434));
#98714=CARTESIAN_POINT('Ctrl Pts',(-2.86020837059367,0.688891919524305,
0.140136735551259));
#98715=CARTESIAN_POINT('Ctrl Pts',(-2.88258671205671,0.595979348250766,
0.145330805635463));
#98716=CARTESIAN_POINT('Ctrl Pts',(-2.90040650544948,0.502087643872117,
0.150524875719667));
#98717=CARTESIAN_POINT('Ctrl Pts',(-2.91361546104576,0.407687312968051,
0.155718945803871));
#98718=CARTESIAN_POINT('Ctrl Pts',(-2.91636701024738,0.388022839631122,
0.156800919264163));
#98719=CARTESIAN_POINT('Ctrl Pts',(-2.91891866257042,0.368336303150983,
0.157882892724454));
#98720=CARTESIAN_POINT('Ctrl Pts',(-2.92127022970174,0.348631962187004,
0.158964866184746));
#98721=CARTESIAN_POINT('Ctrl Pts',(-2.93493299361991,0.234148409849401,
0.165251205093298));
#98722=CARTESIAN_POINT('Ctrl Pts',(-2.94187489336978,0.118783007009487,
0.171537544001849));
#98723=CARTESIAN_POINT('Ctrl Pts',(-2.94199832420144,0.00314012673363615,
0.1778238829104));
#98724=CARTESIAN_POINT('',(-2.94185727375763,0.00142673463472898,1.1778238505128));
#98725=CARTESIAN_POINT('Ctrl Pts',(-2.94199832420208,0.00314012613217657,
0.177823882943095));
#98726=CARTESIAN_POINT('Ctrl Pts',(-2.94209516594599,-0.0875913401540299,
0.182756039124081));
#98727=CARTESIAN_POINT('Ctrl Pts',(-2.93799066139926,-0.178517496165705,
0.187688195305066));
#98728=CARTESIAN_POINT('Ctrl Pts',(-2.92965745352971,-0.269204764032533,
0.192620351486051));
#98729=CARTESIAN_POINT('Ctrl Pts',(-2.92133503561485,-0.359774608750091,
0.19754612144188));
#98730=CARTESIAN_POINT('Ctrl Pts',(-2.90879482451379,-0.450105719668528,
0.202471891397708));
#98731=CARTESIAN_POINT('Ctrl Pts',(-2.89206147248208,-0.539763317931814,
0.207397661353537));
#98732=CARTESIAN_POINT('Ctrl Pts',(-2.87534435746252,-0.629333917994769,
0.212318651646183));
#98733=CARTESIAN_POINT('Ctrl Pts',(-2.85444226635288,-0.718231847586187,
0.21723964193883));
#98734=CARTESIAN_POINT('Ctrl Pts',(-2.82943163687848,-0.806027674606241,
0.222160632231477));
#98735=CARTESIAN_POINT('Ctrl Pts',(-2.80443376779796,-0.893778708298135,
0.227079111840637));
#98736=CARTESIAN_POINT('Ctrl Pts',(-2.77533164599731,-0.98042830775922,
0.231997591449797));
#98737=CARTESIAN_POINT('Ctrl Pts',(-2.74225248475926,-1.06555868436782,
0.236916071058958));
#98738=CARTESIAN_POINT('Ctrl Pts',(-2.70918004756733,-1.15067175640891,
0.241833550882074));
#98739=CARTESIAN_POINT('Ctrl Pts',(-2.67213234464307,-1.23426578455603,
0.24675103070519));
#98740=CARTESIAN_POINT('Ctrl Pts',(-2.63128551283259,-1.31594093710824,
0.251668510528306));
#98741=CARTESIAN_POINT('Ctrl Pts',(-2.59043444759753,-1.39762455459111,
0.256586500006127));
#98742=CARTESIAN_POINT('Ctrl Pts',(-2.54578368257135,-1.47738848615293,
0.261504489483948));
#98743=CARTESIAN_POINT('Ctrl Pts',(-2.49755562285416,-1.55485687789893,
0.266422478961768));
#98744=CARTESIAN_POINT('Ctrl Pts',(-2.44927774207178,-1.63240529687009,
0.271345548873588));
#98745=CARTESIAN_POINT('Ctrl Pts',(-2.39741543999569,-1.70765304858344,
0.276268618785408));
#98746=CARTESIAN_POINT('Ctrl Pts',(-2.3422344852868,-1.78025324488773,0.281191688697228));
#98747=CARTESIAN_POINT('Ctrl Pts',(-2.2870215635897,-1.85289549935559,0.286117610602433));
#98748=CARTESIAN_POINT('Ctrl Pts',(-2.22848646666738,-1.92288679334015,
0.291043532507638));
#98749=CARTESIAN_POINT('Ctrl Pts',(-2.1669336730891,-1.98991518825114,0.295969454412843));
#98750=CARTESIAN_POINT('Ctrl Pts',(-2.10528114624034,-2.05705218848532,
0.300903357731614));
#98751=CARTESIAN_POINT('Ctrl Pts',(-2.04060149944086,-2.12121638682871,
0.305837261050386));
#98752=CARTESIAN_POINT('Ctrl Pts',(-1.9732338943125,-2.18213473423076,0.310771164369158));
#98753=CARTESIAN_POINT('Ctrl Pts',(-1.94065282200704,-2.2115967446088,0.313157353702603));
#98754=CARTESIAN_POINT('Ctrl Pts',(-1.90744349998323,-2.24030018420665,
0.315543543036049));
#98755=CARTESIAN_POINT('Ctrl Pts',(-1.87364667060443,-2.26821783648152,
0.317929732369494));
#98756=CARTESIAN_POINT('Ctrl Pts',(-1.80198568799447,-2.3274129275878,0.322989280128001));
#98757=CARTESIAN_POINT('Ctrl Pts',(-1.72739011311397,-2.3833132220152,0.328048827886508));
#98758=CARTESIAN_POINT('Ctrl Pts',(-1.65019520011135,-2.43561487134758,
0.333108375645015));
#98759=CARTESIAN_POINT('Ctrl Pts',(-1.57310658002327,-2.48784450434459,
0.338160956699932));
#98760=CARTESIAN_POINT('Ctrl Pts',(-1.49342609802247,-2.53648509324391,
0.343213537754849));
#98761=CARTESIAN_POINT('Ctrl Pts',(-1.4115224133712,-2.58127264669014,0.348266118809766));
#98762=CARTESIAN_POINT('Ctrl Pts',(-1.32970640747573,-2.62601225458939,
0.353313291023526));
#98763=CARTESIAN_POINT('Ctrl Pts',(-1.24567231625463,-2.66690681484048,
0.358360463237286));
#98764=CARTESIAN_POINT('Ctrl Pts',(-1.15981723600913,-2.7037359299784,0.363407635451046));
#98765=CARTESIAN_POINT('Ctrl Pts',(-1.07402472071201,-2.74053820673143,
0.368451129652182));
#98766=CARTESIAN_POINT('Ctrl Pts',(-0.986414260068643,-2.77328075361311,
0.373494623853317));
#98767=CARTESIAN_POINT('Ctrl Pts',(-0.89740604689479,-2.80178985418191,
0.378538118054452));
#98768=CARTESIAN_POINT('Ctrl Pts',(-0.808430709768861,-2.83028842463755,
0.383579749392024));
#98769=CARTESIAN_POINT('Ctrl Pts',(-0.718059067082031,-2.85455652055424,
0.388621380729597));
#98770=CARTESIAN_POINT('Ctrl Pts',(-0.626728759781356,-2.87446952700197,
0.39366301206717));
#98771=CARTESIAN_POINT('Ctrl Pts',(-0.535406845971985,-2.89438070339294,
0.398704180065792));
#98772=CARTESIAN_POINT('Ctrl Pts',(-0.443126875368464,-2.90993749200716,
0.403745348064413));
#98773=CARTESIAN_POINT('Ctrl Pts',(-0.350337929466291,-2.92106612988773,
0.408786516063035));
#98774=CARTESIAN_POINT('Ctrl Pts',(-0.257531766689741,-2.93219683267332,
0.413828619444156));
#98775=CARTESIAN_POINT('Ctrl Pts',(-0.16421688069103,-2.93889770053683,
0.418870722825277));
#98776=CARTESIAN_POINT('Ctrl Pts',(-0.0708476160087499,-2.94114681974666,
0.423912826206398));
#98777=CARTESIAN_POINT('Ctrl Pts',(0.0226219382875447,-2.94339835477607,
0.428960345401852));
#98778=CARTESIAN_POINT('Ctrl Pts',(0.116145544535804,-2.94118858532501,
0.434007864597306));
#98779=CARTESIAN_POINT('Ctrl Pts',(0.209269017545923,-2.93454774680791,
0.43905538379276));
#98780=CARTESIAN_POINT('Ctrl Pts',(0.302448533360736,-2.92790291175583,
0.444105940644815));
#98781=CARTESIAN_POINT('Ctrl Pts',(0.395226997086348,-2.91682175051154,
0.449156497496869));
#98782=CARTESIAN_POINT('Ctrl Pts',(0.48715764938872,-2.90138612126033,0.454207054348924));
#98783=CARTESIAN_POINT('Ctrl Pts',(0.579234252341123,-2.88592598614446,
0.459265629549996));
#98784=CARTESIAN_POINT('Ctrl Pts',(0.670459924425042,-2.86609767494053,
0.464324204751068));
#98785=CARTESIAN_POINT('Ctrl Pts',(0.76040053390516,-2.84203360783027,0.46938277995214));
#98786=CARTESIAN_POINT('Ctrl Pts',(0.804920154320144,-2.83012215715652,
0.471886719486174));
#98787=CARTESIAN_POINT('Ctrl Pts',(0.849125183726759,-2.81717364719446,
0.474390659020208));
#98788=CARTESIAN_POINT('Ctrl Pts',(0.892964786050042,-2.8032084993583,0.476894598554242));
#98789=CARTESIAN_POINT('Ctrl Pts',(0.981572334246543,-2.77498247894782,
0.48195550082491));
#98790=CARTESIAN_POINT('Ctrl Pts',(1.06899313626838,-2.74250241713219,0.487016403095577));
#98791=CARTESIAN_POINT('Ctrl Pts',(1.15479018409174,-2.70588684736176,0.492077305366244));
#98792=CARTESIAN_POINT('Ctrl Pts',(1.24047196846654,-2.66932046852446,0.497131408602873));
#98793=CARTESIAN_POINT('Ctrl Pts',(1.32453393024678,-2.62862979536122,0.502185511839503));
#98794=CARTESIAN_POINT('Ctrl Pts',(1.40655463318329,-2.58398298443906,0.507239615076133));
#98795=CARTESIAN_POINT('Ctrl Pts',(1.48849023387733,-2.53938249772035,0.512288474325528));
#98796=CARTESIAN_POINT('Ctrl Pts',(1.5683883992688,-2.49083424348688,0.517337333574923));
#98797=CARTESIAN_POINT('Ctrl Pts',(1.64584908580887,-2.43855383101176,0.522386192824318));
#98798=CARTESIAN_POINT('Ctrl Pts',(1.72325702242345,-2.3863090209562,0.527431613852841));
#98799=CARTESIAN_POINT('Ctrl Pts',(1.79823041370787,-2.33033735128013,0.532477034881364));
#98800=CARTESIAN_POINT('Ctrl Pts',(1.87039606650381,-2.27089906301603,0.537522455909887));
#98801=CARTESIAN_POINT('Ctrl Pts',(1.94253719679688,-2.21148097238804,0.542566162461414));
#98802=CARTESIAN_POINT('Ctrl Pts',(2.01187214297372,-2.14859888467587,0.547609869012941));
#98803=CARTESIAN_POINT('Ctrl Pts',(2.07805966309663,-2.08255420976519,0.552653575564468));
#98804=CARTESIAN_POINT('Ctrl Pts',(2.14424302411208,-2.01651368498582,0.557696965178338));
#98805=CARTESIAN_POINT('Ctrl Pts',(2.2072790393132,-1.94731128091343,0.562740354792208));
#98806=CARTESIAN_POINT('Ctrl Pts',(2.26686312716272,-1.87528546165911,0.567783744406077));
#98807=CARTESIAN_POINT('Ctrl Pts',(2.32645997354199,-1.80324421977117,0.572828213943106));
#98808=CARTESIAN_POINT('Ctrl Pts',(2.38260314260021,-1.72837870293375,0.577872683480135));
#98809=CARTESIAN_POINT('Ctrl Pts',(2.4350288801728,-1.65105976655129,0.582917153017164));
#98810=CARTESIAN_POINT('Ctrl Pts',(2.48751304877621,-1.57365465445888,0.5879672448605));
#98811=CARTESIAN_POINT('Ctrl Pts',(2.53627126673176,-1.49379103128267,0.593017336703836));
#98812=CARTESIAN_POINT('Ctrl Pts',(2.581083772037,-1.41186775645854,0.598067428547172));
#98813=CARTESIAN_POINT('Ctrl Pts',(2.6259243092101,-1.32989323561727,0.603120679408428));
#98814=CARTESIAN_POINT('Ctrl Pts',(2.66681402620945,-1.24585689555878,0.608173930269683));
#98815=CARTESIAN_POINT('Ctrl Pts',(2.70358063846019,-1.1601791807058,0.613227181130939));
#98816=CARTESIAN_POINT('Ctrl Pts',(2.74040678082037,-1.07436274206433,0.618288613887625));
#98817=CARTESIAN_POINT('Ctrl Pts',(2.77309633592506,-0.986900036885405,
0.623350046644311));
#98818=CARTESIAN_POINT('Ctrl Pts',(2.80152640179825,-0.898228155886535,
0.628411479400998));
#98819=CARTESIAN_POINT('Ctrl Pts',(2.81547151207044,-0.854734089988602,
0.630894141180328));
#98820=CARTESIAN_POINT('Ctrl Pts',(2.82839258253587,-0.810949283268288,
0.633376802959659));
#98821=CARTESIAN_POINT('Ctrl Pts',(2.84027962227694,-0.766926115918837,
0.63585946473899));
#98822=CARTESIAN_POINT('Ctrl Pts',(2.86443637764123,-0.677462556682363,
0.640904711878893));
#98823=CARTESIAN_POINT('Ctrl Pts',(2.88440660936451,-0.586691594128352,
0.645949959018796));
#98824=CARTESIAN_POINT('Ctrl Pts',(2.90005137898637,-0.495041411640717,
0.6509952061587));
#98825=CARTESIAN_POINT('Ctrl Pts',(2.91567424617995,-0.403519537948771,
0.656033390032967));
#98826=CARTESIAN_POINT('Ctrl Pts',(2.92698360909852,-0.311121325401966,
0.661071573907234));
#98827=CARTESIAN_POINT('Ctrl Pts',(2.93389056820814,-0.218289105956563,
0.666109757781502));
#98828=CARTESIAN_POINT('Ctrl Pts',(2.94079000852528,-0.12555794200929,0.671142457178675));
#98829=CARTESIAN_POINT('Ctrl Pts',(2.94329653689728,-0.032394152113643,
0.67617515657585));
#98830=CARTESIAN_POINT('Ctrl Pts',(2.94137267422002,0.060751883524479,0.681207855973023));
#98831=CARTESIAN_POINT('Ctrl Pts',(2.93945023702623,0.153828902732275,0.686236826398321));
#98832=CARTESIAN_POINT('Ctrl Pts',(2.93310394246262,0.246887749584014,0.691265796823618));
#98833=CARTESIAN_POINT('Ctrl Pts',(2.92234835876399,0.339476170046479,0.696294767248916));
#98834=CARTESIAN_POINT('Ctrl Pts',(2.91159681473904,0.432029815361808,0.70132184885069));
#98835=CARTESIAN_POINT('Ctrl Pts',(2.8964393226185,0.524112943032413,0.706348930452465));
#98836=CARTESIAN_POINT('Ctrl Pts',(2.87694238148067,0.615277606971287,0.71137601205424));
#98837=CARTESIAN_POINT('Ctrl Pts',(2.85744726700986,0.706433729699323,0.7164026226691));
#98838=CARTESIAN_POINT('Ctrl Pts',(2.83361360512464,0.796671123973326,0.721429233283959));
#98839=CARTESIAN_POINT('Ctrl Pts',(2.80555894103354,0.885552386020586,0.726455843898819));
#98840=CARTESIAN_POINT('Ctrl Pts',(2.77749899685084,0.974450376167096,0.731483400558315));
#98841=CARTESIAN_POINT('Ctrl Pts',(2.7452166074292,1.06199130236983,0.736510957217811));
#98842=CARTESIAN_POINT('Ctrl Pts',(2.70887871331399,1.14775437988898,0.741538513877307));
#98843=CARTESIAN_POINT('Ctrl Pts',(2.67250091164686,1.23361164543283,0.746571591976152));
#98844=CARTESIAN_POINT('Ctrl Pts',(2.63205888894935,1.31768675387426,0.751604670074996));
#98845=CARTESIAN_POINT('Ctrl Pts',(2.58776700753775,1.39958062100728,0.75663774817384));
#98846=CARTESIAN_POINT('Ctrl Pts',(2.54344805401219,1.48152454336561,0.761673902594112));
#98847=CARTESIAN_POINT('Ctrl Pts',(2.49527478783876,1.56128418925326,0.766710057014383));
#98848=CARTESIAN_POINT('Ctrl Pts',(2.44350547838044,1.63848862587592,0.771746211434655));
#98849=CARTESIAN_POINT('Ctrl Pts',(2.39165167247806,1.71581907345813,0.776790585727756));
#98850=CARTESIAN_POINT('Ctrl Pts',(2.33619037114104,1.79058562837981,0.781834960020858));
#98851=CARTESIAN_POINT('Ctrl Pts',(2.27742062830142,1.86244980651485,0.78687933431396));
#98852=CARTESIAN_POINT('Ctrl Pts',(2.24656609739313,1.90017900862343,0.789527666517219));
#98853=CARTESIAN_POINT('Ctrl Pts',(2.21480028320741,1.93710882306337,0.792175998720478));
#98854=CARTESIAN_POINT('Ctrl Pts',(2.18217036558718,1.97319449004732,0.794824330923737));
#98855=CARTESIAN_POINT('Ctrl Pts',(2.11990642314893,2.04205264402996,0.79987784058258));
#98856=CARTESIAN_POINT('Ctrl Pts',(2.05426861974718,2.10808406357649,0.804931350241422));
#98857=CARTESIAN_POINT('Ctrl Pts',(1.98554367777261,2.17093995855648,0.809984859900264));
#98858=CARTESIAN_POINT('Ctrl Pts',(1.91691347614877,2.23370920392478,0.815031403074105));
#98859=CARTESIAN_POINT('Ctrl Pts',(1.84520491759781,2.29331132661815,0.820077946247946));
#98860=CARTESIAN_POINT('Ctrl Pts',(1.77074359213942,2.34943208688764,0.825124489421787));
#98861=CARTESIAN_POINT('Ctrl Pts',(1.69636193878188,2.40549279908727,0.830165632897272));
#98862=CARTESIAN_POINT('Ctrl Pts',(1.61923372570595,2.45807928711824,0.835206776372757));
#98863=CARTESIAN_POINT('Ctrl Pts',(1.53971902963432,2.50691629492928,0.840247919848242));
#98864=CARTESIAN_POINT('Ctrl Pts',(1.46026170981883,2.55571806290658,0.845285425732771));
#98865=CARTESIAN_POINT('Ctrl Pts',(1.37842170712222,2.60077549671088,0.850322931617301));
#98866=CARTESIAN_POINT('Ctrl Pts',(1.29458874332141,2.64185616294027,0.85536043750183));
#98867=CARTESIAN_POINT('Ctrl Pts',(1.21078631891674,2.68292186394974,0.860396108280206));
#98868=CARTESIAN_POINT('Ctrl Pts',(1.12499277404117,2.7200134802234,0.865431779058582));
#98869=CARTESIAN_POINT('Ctrl Pts',(1.03762222005052,2.75294462865809,0.870467449836958));
#98870=CARTESIAN_POINT('Ctrl Pts',(0.950259085454411,2.78587298062221,0.875502692992679));
#98871=CARTESIAN_POINT('Ctrl Pts',(0.861319623545659,2.8146414107707,0.880537936148401));
#98872=CARTESIAN_POINT('Ctrl Pts',(0.771236629574986,2.83911219595172,0.885573179304122));
#98873=CARTESIAN_POINT('Ctrl Pts',(0.681136119198972,2.86358773941368,0.89060940154986));
#98874=CARTESIAN_POINT('Ctrl Pts',(0.58989206370933,2.88376386222337,0.895645623795598));
#98875=CARTESIAN_POINT('Ctrl Pts',(0.497949957875531,2.89955338620481,0.900681846041336));
#98876=CARTESIAN_POINT('Ctrl Pts',(0.405907090868191,2.91536021423808,0.905723587582712));
#98877=CARTESIAN_POINT('Ctrl Pts',(0.313165084742484,2.92677077203526,0.910765329124089));
#98878=CARTESIAN_POINT('Ctrl Pts',(0.220176808105396,2.9337495075709,0.915807070665465));
#98879=CARTESIAN_POINT('Ctrl Pts',(0.127131573496098,2.94073251778116,0.920851900417366));
#98880=CARTESIAN_POINT('Ctrl Pts',(0.0338402115888993,2.9432782892246,0.925896730169267));
#98881=CARTESIAN_POINT('Ctrl Pts',(-0.0592443339899067,2.94140342504902,
0.930941559921168));
#98882=CARTESIAN_POINT('Ctrl Pts',(-0.15247932597867,2.93952553065416,0.935994543298575));
#98883=CARTESIAN_POINT('Ctrl Pts',(-0.245506391858317,2.93321276680787,
0.941047526675982));
#98884=CARTESIAN_POINT('Ctrl Pts',(-0.337877810556575,2.92253359007788,
0.946100510053389));
#98885=CARTESIAN_POINT('Ctrl Pts',(-0.384729005725857,2.91711706405419,
0.948663405738421));
#98886=CARTESIAN_POINT('Ctrl Pts',(-0.431411691090738,2.91057806867327,
0.951226301423452));
#98887=CARTESIAN_POINT('Ctrl Pts',(-0.4778687221613,2.90293049940572,0.953789197108484));
#98888=CARTESIAN_POINT('Ctrl Pts',(-0.569465358203213,2.88785223024682,
0.958842310014444));
#98889=CARTESIAN_POINT('Ctrl Pts',(-0.660511415684644,2.86840750677345,
0.963895422920404));
#98890=CARTESIAN_POINT('Ctrl Pts',(-0.75055847125516,2.84464865690424,0.968948535826364));
#98891=CARTESIAN_POINT('Ctrl Pts',(-0.8404816688065,2.82092248688297,0.973994698271244));
#98892=CARTESIAN_POINT('Ctrl Pts',(-0.929408169316603,2.79289409451912,
0.979040860716123));
#98893=CARTESIAN_POINT('Ctrl Pts',(-1.01689756881339,2.76066719010847,0.984087023161002));
#98894=CARTESIAN_POINT('Ctrl Pts',(-1.10429363537458,2.72847466508106,0.989127802403376));
#98895=CARTESIAN_POINT('Ctrl Pts',(-1.19025523370667,2.692092683341,0.994168581645751));
#98896=CARTESIAN_POINT('Ctrl Pts',(-1.27435607900167,2.65167505247372,0.999209360888125));
#98897=CARTESIAN_POINT('Ctrl Pts',(-1.35839667286267,2.61128637756056,1.00424652882104));
#98898=CARTESIAN_POINT('Ctrl Pts',(-1.44057876424077,2.56686799201402,1.00928369675396));
#98899=CARTESIAN_POINT('Ctrl Pts',(-1.52049603449511,2.51862180747421,1.01432086468688));
#98900=CARTESIAN_POINT('Ctrl Pts',(-1.60038445116335,2.47039304189071,1.01935621398463));
#98901=CARTESIAN_POINT('Ctrl Pts',(-1.67800929136593,2.41833945211539,1.02439156328237));
#98902=CARTESIAN_POINT('Ctrl Pts',(-1.75298976429711,2.36270837943864,1.02942691258012));
#98903=CARTESIAN_POINT('Ctrl Pts',(-1.82796412186676,2.30708184399817,1.03446185119785));
#98904=CARTESIAN_POINT('Ctrl Pts',(-1.90029418444405,2.24787867054407,1.03949678981559));
#98905=CARTESIAN_POINT('Ctrl Pts',(-1.96962997187994,2.18538824328132,1.04453172843332));
#98906=CARTESIAN_POINT('Ctrl Pts',(-2.03897948230982,2.1228854478637,1.0495676635701));
#98907=CARTESIAN_POINT('Ctrl Pts',(-2.10533321099665,2.05709440404767,1.05460359870687));
#98908=CARTESIAN_POINT('Ctrl Pts',(-2.16837681252091,1.98834252555279,1.05963953384365));
#98909=CARTESIAN_POINT('Ctrl Pts',(-2.23148986449097,1.91951490822802,1.06468101669553));
#98910=CARTESIAN_POINT('Ctrl Pts',(-2.29128520978513,1.84772027321607,1.0697224995474));
#98911=CARTESIAN_POINT('Ctrl Pts',(-2.34748792750901,1.77332017137331,1.07476398239928));
#98912=CARTESIAN_POINT('Ctrl Pts',(-2.403725248713,1.69887426209367,1.07980856924432));
#98913=CARTESIAN_POINT('Ctrl Pts',(-2.45636528844208,1.62182005880557,1.08485315608936));
#98914=CARTESIAN_POINT('Ctrl Pts',(-2.50517694724487,1.54254739408319,1.0898977429344));
#98915=CARTESIAN_POINT('Ctrl Pts',(-2.55406776315899,1.46314617410782,1.09495051050783));
#98916=CARTESIAN_POINT('Ctrl Pts',(-2.59911758937913,1.38151969871054,1.10000327808125));
#98917=CARTESIAN_POINT('Ctrl Pts',(-2.6401417594153,1.29808146515984,1.10505604565467));
#98918=CARTESIAN_POINT('Ctrl Pts',(-2.66097554208699,1.25570805400313,1.10762205153419));
#98919=CARTESIAN_POINT('Ctrl Pts',(-2.68077187101766,1.21286769363492,1.11018805741371));
#98920=CARTESIAN_POINT('Ctrl Pts',(-2.69951144407883,1.16961616066444,1.11275406329323));
#98921=CARTESIAN_POINT('Ctrl Pts',(-2.74022999787104,1.07563643838875,1.11832964647729));
#98922=CARTESIAN_POINT('Ctrl Pts',(-2.77608165791071,0.979425506923374,
1.12390522966136));
#98923=CARTESIAN_POINT('Ctrl Pts',(-2.80684144268218,0.881478936584314,
1.12948081284542));
#98924=CARTESIAN_POINT('Ctrl Pts',(-2.83751496533341,0.783807045632354,
1.13504075997641));
#98925=CARTESIAN_POINT('Ctrl Pts',(-2.8631249797981,0.684409483757163,1.1406007071074));
#98926=CARTESIAN_POINT('Ctrl Pts',(-2.88349448363252,0.583800961681977,
1.1461606542384));
#98927=CARTESIAN_POINT('Ctrl Pts',(-2.90376330266601,0.483689739349581,
1.15169311900288));
#98928=CARTESIAN_POINT('Ctrl Pts',(-2.91884317063577,0.382379762838641,
1.15722558376735));
#98929=CARTESIAN_POINT('Ctrl Pts',(-2.92860739691918,0.280397422795379,
1.16275804853183));
#98930=CARTESIAN_POINT('Ctrl Pts',(-2.9374705886954,0.187825926462083,1.16777998214742));
#98931=CARTESIAN_POINT('Ctrl Pts',(-2.94195441755449,0.0947008074507425,
1.172801915763));
#98932=CARTESIAN_POINT('Ctrl Pts',(-2.94199965400596,0.00142682472305235,
1.17782384937858));
#98933=CARTESIAN_POINT('',(-2.94199890897741,-0.00253368816290432,2.17782391179132));
#98934=CARTESIAN_POINT('Ctrl Pts',(-2.93779035503166,0.00142416137127735,
1.1778238829104));
#98935=CARTESIAN_POINT('Ctrl Pts',(-2.93530052620224,-0.579059729582153,
1.20912223176626));
#98936=CARTESIAN_POINT('Ctrl Pts',(-2.48777091207476,-2.14587530839216,
1.29340886935037));
#98937=CARTESIAN_POINT('Ctrl Pts',(0.062516362566841,-3.47815940114863,
1.43068379566273));
#98938=CARTESIAN_POINT('Ctrl Pts',(2.95837544317475,-1.83021987966787,1.58964866184748));
#98939=CARTESIAN_POINT('Ctrl Pts',(3.14027796553594,1.49678333878866,1.74861352803222));
#98940=CARTESIAN_POINT('Ctrl Pts',(0.441324113405188,3.45063445902487,1.90757839421697));
#98941=CARTESIAN_POINT('Ctrl Pts',(-2.35214246222887,2.36009024843845,2.0506485125097));
#98942=CARTESIAN_POINT('Ctrl Pts',(-2.93447401517848,0.684077783047056,
2.14073034207417));
#98943=CARTESIAN_POINT('Ctrl Pts',(-2.94008683942583,-0.00253150687518534,
2.1778238829104));
#98944=CARTESIAN_POINT('',(-2.9424770351591,-0.000169397631985995,3.1778238829104));
#98945=CARTESIAN_POINT('Ctrl Pts',(-2.94199890897741,-0.00253368816290432,
2.17782391179132));
#98946=CARTESIAN_POINT('Ctrl Pts',(-2.94190216531002,-0.114867860970932,
2.18388878241826));
#98947=CARTESIAN_POINT('Ctrl Pts',(-2.93536775276288,-0.226920986668357,
2.1899536530452));
#98948=CARTESIAN_POINT('Ctrl Pts',(-2.92251465713287,-0.338041534198877,
2.19601852367214));
#98949=CARTESIAN_POINT('Ctrl Pts',(-2.90948481331824,-0.450690145910656,
2.20216679482018));
#98950=CARTESIAN_POINT('Ctrl Pts',(-2.8899613801613,-0.562380351909379,
2.20831506596822));
#98951=CARTESIAN_POINT('Ctrl Pts',(-2.86411726493774,-0.672455420593505,
2.21446333711626));
#98952=CARTESIAN_POINT('Ctrl Pts',(-2.84864175944927,-0.738368581668222,
2.21814493360633));
#98953=CARTESIAN_POINT('Ctrl Pts',(-2.83090081430642,-0.803703035369289,
2.22182653009641));
#98954=CARTESIAN_POINT('Ctrl Pts',(-2.81093966913266,-0.86832147071023,
2.22550812658648));
#98955=CARTESIAN_POINT('Ctrl Pts',(-2.78354799893388,-0.956994082136707,
2.23056019529212));
#98956=CARTESIAN_POINT('Ctrl Pts',(-2.75190715797264,-1.0445286238472,2.23561226399775));
#98957=CARTESIAN_POINT('Ctrl Pts',(-2.71612972920927,-1.1304880778255,2.24066433270339));
#98958=CARTESIAN_POINT('Ctrl Pts',(-2.6804016769171,-1.21632889906102,2.24570942904311));
#98959=CARTESIAN_POINT('Ctrl Pts',(-2.64054855035648,-1.30059854550508,
2.25075452538283));
#98960=CARTESIAN_POINT('Ctrl Pts',(-2.59673275416955,-1.38287490519679,
2.25579962172254));
#98961=CARTESIAN_POINT('Ctrl Pts',(-2.55296388650603,-1.46506314351657,
2.26083931455617));
#98962=CARTESIAN_POINT('Ctrl Pts',(-2.50524099285918,-1.54526194844353,
2.26587900738979));
#98963=CARTESIAN_POINT('Ctrl Pts',(-2.45377419903128,-1.62306998622007,
2.27091870022342));
#98964=CARTESIAN_POINT('Ctrl Pts',(-2.40234454804303,-1.70082187106271,
2.27595475598372));
#98965=CARTESIAN_POINT('Ctrl Pts',(-2.34717661171069,-1.77618604868358,
2.28099081174402));
#98966=CARTESIAN_POINT('Ctrl Pts',(-2.28852546734672,-1.8487874905747,2.28602686750432));
#98967=CARTESIAN_POINT('Ctrl Pts',(-2.22989568477973,-1.92136248972068,
2.29106108904294));
#98968=CARTESIAN_POINT('Ctrl Pts',(-2.16778549339298,-1.99117640686272,
2.29609531058155));
#98969=CARTESIAN_POINT('Ctrl Pts',(-2.10249151778873,-2.05788566680135,
2.30112953212017));
#98970=CARTESIAN_POINT('Ctrl Pts',(-2.03720305329349,-2.12458929617453,
2.30616332874755));
#98971=CARTESIAN_POINT('Ctrl Pts',(-1.96873164977634,-2.18818847195827,
2.31119712537494));
#98972=CARTESIAN_POINT('Ctrl Pts',(-1.89741140531284,-2.24837584913838,
2.31623092200232));
#98973=CARTESIAN_POINT('Ctrl Pts',(-1.82607722448565,-2.30857498725936,
2.32126570226095));
#98974=CARTESIAN_POINT('Ctrl Pts',(-1.75189343691651,-2.36536071649472,
2.32630048251957));
#98975=CARTESIAN_POINT('Ctrl Pts',(-1.67522698116193,-2.41846615886745,
2.3313352627782));
#98976=CARTESIAN_POINT('Ctrl Pts',(-1.59847624074301,-2.47162998367538,
2.33637557811419));
#98977=CARTESIAN_POINT('Ctrl Pts',(-1.51923774978229,-2.52110519192561,
2.34141589345018));
#98978=CARTESIAN_POINT('Ctrl Pts',(-1.43790691383838,-2.56666860095646,
2.34645620878617));
#98979=CARTESIAN_POINT('Ctrl Pts',(-1.35652613571789,-2.61225998874583,
2.35149961918833));
#98980=CARTESIAN_POINT('Ctrl Pts',(-1.27305085199775,-2.65393459692558,
2.35654302959049));
#98981=CARTESIAN_POINT('Ctrl Pts',(-1.18789853504342,-2.69151650012436,
2.36158643999265));
#98982=CARTESIAN_POINT('Ctrl Pts',(-1.10260813749234,-2.72915934507795,
2.36663802864694));
#98983=CARTESIAN_POINT('Ctrl Pts',(-1.01563569170389,-2.76269607612556,
2.37168961730123));
#98984=CARTESIAN_POINT('Ctrl Pts',(-0.927415806383621,-2.79199998604402,
2.37674120595553));
#98985=CARTESIAN_POINT('Ctrl Pts',(-0.882407038325336,-2.80695050292502,
2.37931846822743));
#98986=CARTESIAN_POINT('Ctrl Pts',(-0.837073773584584,-2.82080006448637,
2.38189573049932));
#98987=CARTESIAN_POINT('Ctrl Pts',(-0.791474681886919,-2.83353698192418,
2.38447299277122));
#98988=CARTESIAN_POINT('Ctrl Pts',(-0.702089360760649,-2.85850444098862,
2.38952505427559));
#98989=CARTESIAN_POINT('Ctrl Pts',(-0.611360851967397,-2.87928305935194,
2.39457711577996));
#98990=CARTESIAN_POINT('Ctrl Pts',(-0.519717551769654,-2.89573093818859,
2.39962917728434));
#98991=CARTESIAN_POINT('Ctrl Pts',(-0.428200729617469,-2.91215611710539,
2.4046742663765));
#98992=CARTESIAN_POINT('Ctrl Pts',(-0.33577205834179,-2.92426235552378,
2.40971935546866));
#98993=CARTESIAN_POINT('Ctrl Pts',(-0.242874369756889,-2.93195771465333,
2.41476444456083));
#98994=CARTESIAN_POINT('Ctrl Pts',(-0.150076179228881,-2.93964483166953,
2.419804130111));
#98995=CARTESIAN_POINT('Ctrl Pts',(-0.0568104102683452,-2.94293042308684,
2.42484381566117));
#98996=CARTESIAN_POINT('Ctrl Pts',(0.0364717442503167,-2.94177392263093,
2.42988350121133));
#98997=CARTESIAN_POINT('Ctrl Pts',(0.12968657787327,-2.94061825681103,2.43491954966557));
#98998=CARTESIAN_POINT('Ctrl Pts',(0.22291733056244,-2.93502687660495,2.4399555981198));
#98999=CARTESIAN_POINT('Ctrl Pts',(0.315710594910331,-2.92501125130509,
2.44499164657403));
#99000=CARTESIAN_POINT('Ctrl Pts',(0.408470062032939,-2.91499927390303,
2.4500258607953));
#99001=CARTESIAN_POINT('Ctrl Pts',(0.50079191607328,-2.90056630024354,2.45506007501656));
#99002=CARTESIAN_POINT('Ctrl Pts',(0.592226706455157,-2.88177575952073,
2.46009428923783));
#99003=CARTESIAN_POINT('Ctrl Pts',(0.683653779273689,-2.86298680481554,
2.46512807854571));
#99004=CARTESIAN_POINT('Ctrl Pts',(0.774193502125792,-2.83984110392919,
2.47016186785358));
#99005=CARTESIAN_POINT('Ctrl Pts',(0.863406602989814,-2.81245320635092,
2.47519565716146));
#99006=CARTESIAN_POINT('Ctrl Pts',(0.952637136727754,-2.78505995698284,
2.48023043010754));
#99007=CARTESIAN_POINT('Ctrl Pts',(1.04054010903926,-2.75342299535612,2.48526520305361));
#99008=CARTESIAN_POINT('Ctrl Pts',(1.12669249679957,-2.7177063891553,2.49029997599969));
#99009=CARTESIAN_POINT('Ctrl Pts',(1.21293959884157,-2.68195051680309,2.49534028407852));
#99010=CARTESIAN_POINT('Ctrl Pts',(1.29743186360145,-2.64210621750187,2.50038059215735));
#99011=CARTESIAN_POINT('Ctrl Pts',(1.37976759867321,-2.5983851472889,2.50542090023618));
#99012=CARTESIAN_POINT('Ctrl Pts',(1.46215389340231,-2.55463722940977,2.51046430340184));
#99013=CARTESIAN_POINT('Ctrl Pts',(1.5423806403506,-2.50700802797234,2.5155077065675));
#99014=CARTESIAN_POINT('Ctrl Pts',(1.62007393732598,-2.45575333402952,2.52055110973316));
#99015=CARTESIAN_POINT('Ctrl Pts',(1.69789322133219,-2.40441552575178,2.52560269125416));
#99016=CARTESIAN_POINT('Ctrl Pts',(1.77317049537466,-2.34944074974798,2.53065427277516));
#99017=CARTESIAN_POINT('Ctrl Pts',(1.84556396510959,-2.29112584785056,2.53570585429616));
#99018=CARTESIAN_POINT('Ctrl Pts',(1.88249937124613,-2.26137337717496,2.53828318918276));
#99019=CARTESIAN_POINT('Ctrl Pts',(1.91868467709676,-2.23075205745533,2.54086052406937));
#99020=CARTESIAN_POINT('Ctrl Pts',(1.95407829257496,-2.19930489620865,2.54343785895597));
#99021=CARTESIAN_POINT('Ctrl Pts',(2.02345639223248,-2.13766258424246,2.54848991691042));
#99022=CARTESIAN_POINT('Ctrl Pts',(2.09003949319129,-2.07262344160913,2.55354197486487));
#99023=CARTESIAN_POINT('Ctrl Pts',(2.15347638948948,-2.00447086282424,2.55859403281932));
#99024=CARTESIAN_POINT('Ctrl Pts',(2.21682573467604,-1.93641234340198,2.56363911828117));
#99025=CARTESIAN_POINT('Ctrl Pts',(2.27703720352976,-1.86524924876456,2.56868420374302));
#99026=CARTESIAN_POINT('Ctrl Pts',(2.33379378359529,-1.79130415498094,2.57372928920488));
#99027=CARTESIAN_POINT('Ctrl Pts',(2.39048957364674,-1.71743826123521,2.57876897104981));
#99028=CARTESIAN_POINT('Ctrl Pts',(2.44373756094513,-1.64079664148663,2.58380865289474));
#99029=CARTESIAN_POINT('Ctrl Pts',(2.49325940237114,-1.56173671036059,2.58884833473968));
#99030=CARTESIAN_POINT('Ctrl Pts',(2.54274550335376,-1.48273383763365,2.59388437939224));
#99031=CARTESIAN_POINT('Ctrl Pts',(2.58851056843526,-1.40131649803873,2.59892042404481));
#99032=CARTESIAN_POINT('Ctrl Pts',(2.63031880851819,-1.31787213551067,2.60395646869737));
#99033=CARTESIAN_POINT('Ctrl Pts',(2.6721118206787,-1.2344581661366,2.60899067905849));
#99034=CARTESIAN_POINT('Ctrl Pts',(2.70995067210863,-1.14901903738044,2.61402488941961));
#99035=CARTESIAN_POINT('Ctrl Pts',(2.74364540472195,-1.06196699249464,2.61905909978072));
#99036=CARTESIAN_POINT('Ctrl Pts',(2.77733729296488,-0.97492229618355,2.62409288517456));
#99037=CARTESIAN_POINT('Ctrl Pts',(2.80688559771618,-0.886265368862106,
2.62912667056839));
#99038=CARTESIAN_POINT('Ctrl Pts',(2.83214885381344,-0.796427567229569,
2.63416045596223));
#99039=CARTESIAN_POINT('Ctrl Pts',(2.85741704628676,-0.706572211518826,
2.63919522494494));
#99040=CARTESIAN_POINT('Ctrl Pts',(2.87839840733941,-0.615535951036533,
2.64422999392765));
#99041=CARTESIAN_POINT('Ctrl Pts',(2.89500190357574,-0.523763284597973,
2.64926476291037));
#99042=CARTESIAN_POINT('Ctrl Pts',(2.91162365322265,-0.431889725905328,
2.65430506697461));
#99043=CARTESIAN_POINT('Ctrl Pts',(2.92385785167403,-0.339278583109973,
2.65934537103886));
#99044=CARTESIAN_POINT('Ctrl Pts',(2.9316650254743,-0.246382179572217,2.66438567510311));
#99045=CARTESIAN_POINT('Ctrl Pts',(2.93947699335174,-0.153428732021019,
2.66942907421907));
#99046=CARTESIAN_POINT('Ctrl Pts',(2.94285650858153,-0.0601901186905315,
2.67447247333503));
#99047=CARTESIAN_POINT('Ctrl Pts',(2.94181625057161,0.0328808131405041,
2.67951587245099));
#99048=CARTESIAN_POINT('Ctrl Pts',(2.94077430568675,0.126102668128605,2.68456744990687));
#99049=CARTESIAN_POINT('Ctrl Pts',(2.93529830536063,0.219155855786866,2.68961902736274));
#99050=CARTESIAN_POINT('Ctrl Pts',(2.9254528257311,0.311592304818211,2.69467060481862));
#99051=CARTESIAN_POINT('Ctrl Pts',(2.92042954776898,0.358754453823466,2.69724797825932));
#99052=CARTESIAN_POINT('Ctrl Pts',(2.91426965086572,0.405756209443027,2.69982535170001));
#99053=CARTESIAN_POINT('Ctrl Pts',(2.90698678445479,0.452539318739461,2.70240272514071));
#99054=CARTESIAN_POINT('Ctrl Pts',(2.89271120775524,0.544241655061684,2.70745478708446));
#99055=CARTESIAN_POINT('Ctrl Pts',(2.87406653123876,0.635432610317872,2.7125068490282));
#99056=CARTESIAN_POINT('Ctrl Pts',(2.85110093070811,0.725663477732859,2.71755891097195));
#99057=CARTESIAN_POINT('Ctrl Pts',(2.82816702538286,0.815769816034299,2.72260400048139));
#99058=CARTESIAN_POINT('Ctrl Pts',(2.80092415463223,0.904918272664531,2.72764908999083));
#99059=CARTESIAN_POINT('Ctrl Pts',(2.76947194826134,0.992667682456494,2.73269417950027));
#99060=CARTESIAN_POINT('Ctrl Pts',(2.73805342890985,1.0803231078699,2.73773386544514));
#99061=CARTESIAN_POINT('Ctrl Pts',(2.70243468419276,1.16658204884566,2.74277355139));
#99062=CARTESIAN_POINT('Ctrl Pts',(2.66276556900507,1.25101699609602,2.74781323733487));
#99063=CARTESIAN_POINT('Ctrl Pts',(2.62312508294012,1.33539100681032,2.75284928614826));
#99064=CARTESIAN_POINT('Ctrl Pts',(2.57944022493256,1.41794323929442,2.75788533496165));
#99065=CARTESIAN_POINT('Ctrl Pts',(2.53190913403474,1.49826570974292,2.76292138377504));
#99066=CARTESIAN_POINT('Ctrl Pts',(2.48439535515141,1.57855892473471,2.76795559833324));
#99067=CARTESIAN_POINT('Ctrl Pts',(2.43303835243074,1.65662360909303,2.77298981289144));
#99068=CARTESIAN_POINT('Ctrl Pts',(2.37808192542616,1.7320768908918,2.77802402744964));
#99069=CARTESIAN_POINT('Ctrl Pts',(2.32313013727259,1.80752380370788,2.78305781707172));
#99070=CARTESIAN_POINT('Ctrl Pts',(2.26457979063128,1.88035939318863,2.78809160669379));
#99071=CARTESIAN_POINT('Ctrl Pts',(2.20271700564477,1.95023121527765,2.79312539631587));
#99072=CARTESIAN_POINT('Ctrl Pts',(2.14084213251709,2.0201166904935,2.79816016955288));
#99073=CARTESIAN_POINT('Ctrl Pts',(2.07565383037372,2.08703691577986,2.8031949427899));
#99074=CARTESIAN_POINT('Ctrl Pts',(2.00747656861298,2.15067473748818,2.80822971602691));
#99075=CARTESIAN_POINT('Ctrl Pts',(1.93922435458943,2.21438252092002,2.81327002435931));
#99076=CARTESIAN_POINT('Ctrl Pts',(1.86797694701256,2.27480039393622,2.81831033269171));
#99077=CARTESIAN_POINT('Ctrl Pts',(1.79409330408111,2.33165032032063,2.82335064102411));
#99078=CARTESIAN_POINT('Ctrl Pts',(1.72016429195138,2.38853515613128,2.82839404442246));
#99079=CARTESIAN_POINT('Ctrl Pts',(1.6435961860873,2.44184742988604,2.83343744782082));
#99080=CARTESIAN_POINT('Ctrl Pts',(1.56477661589871,2.49135267321521,2.83848085121917));
#99081=CARTESIAN_POINT('Ctrl Pts',(1.48582923287356,2.54093819363241,2.84353243293787));
#99082=CARTESIAN_POINT('Ctrl Pts',(1.40462348339911,2.58670414117156,2.84858401465657));
#99083=CARTESIAN_POINT('Ctrl Pts',(1.3215710731625,2.62846226881424,2.85363559637527));
#99084=CARTESIAN_POINT('Ctrl Pts',(1.27919749248292,2.6497673866989,2.85621292802534));
#99085=CARTESIAN_POINT('Ctrl Pts',(1.23634353110035,2.67003001851766,2.8587902596754));
#99086=CARTESIAN_POINT('Ctrl Pts',(1.19306555526398,2.68923010931431,2.86136759132546));
#99087=CARTESIAN_POINT('Ctrl Pts',(1.10823248422076,2.72686594220878,2.86641965198094));
#99088=CARTESIAN_POINT('Ctrl Pts',(1.02146437177055,2.76055131467093,2.87147171263642));
#99089=CARTESIAN_POINT('Ctrl Pts',(0.933164579460419,2.79008384598751,2.8765237732919));
#99090=CARTESIAN_POINT('Ctrl Pts',(0.844986651378412,2.81957561889415,2.88156886150207));
#99091=CARTESIAN_POINT('Ctrl Pts',(0.755281661707406,2.84492579996593,2.88661394971225));
#99092=CARTESIAN_POINT('Ctrl Pts',(0.66447448324842,2.86597935462064,2.89165903792242));
#99093=CARTESIAN_POINT('Ctrl Pts',(0.573764564393398,2.88701035973222,2.8966987225589));
#99094=CARTESIAN_POINT('Ctrl Pts',(0.481955233668257,2.90375378561528,2.90173840719537));
#99095=CARTESIAN_POINT('Ctrl Pts',(0.389487068874256,2.91610422021912,2.90677809183185));
#99096=CARTESIAN_POINT('Ctrl Pts',(0.297085638339161,2.92844574151639,2.91181413932877));
#99097=CARTESIAN_POINT('Ctrl Pts',(0.204026757938821,2.93640051452241,2.9168501868257));
#99098=CARTESIAN_POINT('Ctrl Pts',(0.110760724522029,2.93991429499286,2.92188623432262));
#99099=CARTESIAN_POINT('Ctrl Pts',(0.0175286610244393,2.94342679565292,
2.92692044755984));
#99100=CARTESIAN_POINT('Ctrl Pts',(-0.0759099620612917,2.94250150043816,
2.93195466079707));
#99101=CARTESIAN_POINT('Ctrl Pts',(-0.169101246227653,2.93713615083201,
2.93698887403429));
#99102=CARTESIAN_POINT('Ctrl Pts',(-0.262284664097959,2.93177125411615,
2.94202266233251));
#99103=CARTESIAN_POINT('Ctrl Pts',(-0.35522034100107,2.92196707388151,2.94705645063072));
#99104=CARTESIAN_POINT('Ctrl Pts',(-0.44745705450973,2.90777340664115,2.95209023892894));
#99105=CARTESIAN_POINT('Ctrl Pts',(-0.539711791282198,2.89357696592589,
2.95712501084085));
#99106=CARTESIAN_POINT('Ctrl Pts',(-0.631266854362369,2.8749894027189,2.96215978275276));
#99107=CARTESIAN_POINT('Ctrl Pts',(-0.721679935661107,2.85211186149214,
2.96719455466467));
#99108=CARTESIAN_POINT('Ctrl Pts',(-0.81219241482694,2.82920916927209,2.97223486167816));
#99109=CARTESIAN_POINT('Ctrl Pts',(-0.901559974745023,2.80200719387074,
2.97727516869166));
#99110=CARTESIAN_POINT('Ctrl Pts',(-0.989354529215947,2.7706572533462,2.98231547570515));
#99111=CARTESIAN_POINT('Ctrl Pts',(-1.07720299509999,2.73928806197398,2.98735887778616));
#99112=CARTESIAN_POINT('Ctrl Pts',(-1.16347612203295,2.7037660037187,2.99240227986716));
#99113=CARTESIAN_POINT('Ctrl Pts',(-1.24776693683108,2.66429008768775,2.99744568194817));
#99114=CARTESIAN_POINT('Ctrl Pts',(-1.33219443686009,2.62475015786467,3.00249726236486));
#99115=CARTESIAN_POINT('Ctrl Pts',(-1.41463281490386,2.5812437774486,3.00754884278154));
#99116=CARTESIAN_POINT('Ctrl Pts',(-1.49470092919749,2.53401521942078,3.01260042319823));
#99117=CARTESIAN_POINT('Ctrl Pts',(-1.53555213192007,2.50991894320259,3.01517776796889));
#99118=CARTESIAN_POINT('Ctrl Pts',(-1.57578681340149,2.48485443600691,3.01775511273955));
#99119=CARTESIAN_POINT('Ctrl Pts',(-1.61535759876261,2.45885823668627,3.02033245751021));
#99120=CARTESIAN_POINT('Ctrl Pts',(-1.69279677129895,2.40798423592767,3.02537626557617));
#99121=CARTESIAN_POINT('Ctrl Pts',(-1.76797166233162,2.35335543275332,3.03042007364213));
#99122=CARTESIAN_POINT('Ctrl Pts',(-1.84049449808849,2.29520020967801,3.0354638817081));
#99123=CARTESIAN_POINT('Ctrl Pts',(-1.91291716172288,2.23712531346898,3.04050072301725));
#99124=CARTESIAN_POINT('Ctrl Pts',(-1.98269470377326,2.17553395208789,3.04553756432641));
#99125=CARTESIAN_POINT('Ctrl Pts',(-2.04946744717991,2.11069826904507,3.05057440563557));
#99126=CARTESIAN_POINT('Ctrl Pts',(-2.11616878274353,2.04593192232185,3.05560586046583));
#99127=CARTESIAN_POINT('Ctrl Pts',(-2.17987138803306,1.97792845857669,3.06063731529608));
#99128=CARTESIAN_POINT('Ctrl Pts',(-2.24024876236389,1.90700012656714,3.06566877012634));
#99129=CARTESIAN_POINT('Ctrl Pts',(-2.30058291089747,1.83612257407114,3.07069662280184));
#99130=CARTESIAN_POINT('Ctrl Pts',(-2.35759627164869,1.76232465365258,3.07572447547733));
#99131=CARTESIAN_POINT('Ctrl Pts',(-2.41100007869985,1.68595451317921,3.08075232815283));
#99132=CARTESIAN_POINT('Ctrl Pts',(-2.46438478843362,1.60961168283393,3.08577838285729));
#99133=CARTESIAN_POINT('Ctrl Pts',(-2.51416225325748,1.5306988247474,3.09080443756175));
#99134=CARTESIAN_POINT('Ctrl Pts',(-2.56008545935699,1.44959526792443,3.09583049226621));
#99135=CARTESIAN_POINT('Ctrl Pts',(-2.60600520700394,1.36849781896778,3.10085616846112));
#99136=CARTESIAN_POINT('Ctrl Pts',(-2.64807105353741,1.28521038748975,3.10588184465604));
#99137=CARTESIAN_POINT('Ctrl Pts',(-2.68608120570729,1.20013822385011,3.11090752085096));
#99138=CARTESIAN_POINT('Ctrl Pts',(-2.72409922529679,1.11504845179871,3.11593423727069));
#99139=CARTESIAN_POINT('Ctrl Pts',(-2.75805970201213,1.02817362130149,3.12096095369042));
#99140=CARTESIAN_POINT('Ctrl Pts',(-2.78780885240135,0.939939254671624,
3.12598767011016));
#99141=CARTESIAN_POINT('Ctrl Pts',(-2.81759078275611,0.851607664441793,
3.1310199253634));
#99142=CARTESIAN_POINT('Ctrl Pts',(-2.84315198266542,0.761913971385346,
3.13605218061663));
#99143=CARTESIAN_POINT('Ctrl Pts',(-2.86438856994763,0.671298830889301,
3.14108443586987));
#99144=CARTESIAN_POINT('Ctrl Pts',(-2.88563851571135,0.58062669061914,3.14611985656998));
#99145=CARTESIAN_POINT('Ctrl Pts',(-2.90255835329817,0.489032387258456,
3.15115527727009));
#99146=CARTESIAN_POINT('Ctrl Pts',(-2.91509573348633,0.396964563418193,
3.1561906979702));
#99147=CARTESIAN_POINT('Ctrl Pts',(-2.92765312232409,0.304749806741967,
3.16123415479642));
#99148=CARTESIAN_POINT('Ctrl Pts',(-2.93581405508617,0.212060464610946,
3.16627761162265));
#99149=CARTESIAN_POINT('Ctrl Pts',(-2.93957821840217,0.119347802223257,
3.17132106844887));
#99150=CARTESIAN_POINT('Ctrl Pts',(-2.94119600136931,0.0795012404625306,
3.17348867326938));
#99151=CARTESIAN_POINT('Ctrl Pts',(-2.94200228753483,0.039650337272543,
3.17565627808989));
#99152=CARTESIAN_POINT('Ctrl Pts',(-2.9419999951247,-0.000169370168916156,
3.1778238829104));
#99153=CARTESIAN_POINT('',(-2.94199882825472,0.00262574710428596,4.1778238829104));
#99154=CARTESIAN_POINT('Ctrl Pts',(-2.94684115129537,-0.00016964887300896,
3.1778238829104));
#99155=CARTESIAN_POINT('Ctrl Pts',(-2.94684868498682,-0.00920704813743015,
3.17831502983859));
#99156=CARTESIAN_POINT('Ctrl Pts',(-2.94681071471912,-0.0182443822752739,
3.17880617676677));
#99157=CARTESIAN_POINT('Ctrl Pts',(-2.93770067493934,-1.00224504924923,
3.23228561242321));
#99158=CARTESIAN_POINT('Ctrl Pts',(-1.8559090678843,-2.94232426067285,3.33826218987969));
#99159=CARTESIAN_POINT('Ctrl Pts',(1.46936377327205,-3.15319532053511,3.49722705606445));
#99160=CARTESIAN_POINT('Ctrl Pts',(3.44666251240458,-0.471368358035674,
3.6561919222492));
#99161=CARTESIAN_POINT('Ctrl Pts',(2.26204048071215,2.64288544059278,3.81515678843395));
#99162=CARTESIAN_POINT('Ctrl Pts',(-0.997746363252262,3.33259250407305,
3.9741216546187));
#99163=CARTESIAN_POINT('Ctrl Pts',(-2.78065560741015,1.53211675139101,4.09501045424348));
#99164=CARTESIAN_POINT('Ctrl Pts',(-2.94296032021889,0.278545523598026,
4.16291096514003));
#99165=CARTESIAN_POINT('Ctrl Pts',(-2.94059221637238,0.00263736173236185,
4.17782318730832));
#99166=CARTESIAN_POINT('',(-2.94172483514234,-0.00113785794874115,5.17782393613833));
#99167=CARTESIAN_POINT('Ctrl Pts',(-2.94199882825472,0.00262574710428596,
4.1778238829104));
#99168=CARTESIAN_POINT('Ctrl Pts',(-2.94208135216831,-0.089837558549181,
4.18281897121202));
#99169=CARTESIAN_POINT('Ctrl Pts',(-2.93780060605179,-0.182391783495091,
4.18781405951365));
#99170=CARTESIAN_POINT('Ctrl Pts',(-2.92915763932824,-0.274589737544923,
4.19280914781527));
#99171=CARTESIAN_POINT('Ctrl Pts',(-2.92051856511877,-0.366746168603293,
4.19780198648987));
#99172=CARTESIAN_POINT('Ctrl Pts',(-2.90752121322561,-0.458546197651342,
4.20279482516447));
#99173=CARTESIAN_POINT('Ctrl Pts',(-2.89021866431506,-0.549545332474808,
4.20778766383907));
#99174=CARTESIAN_POINT('Ctrl Pts',(-2.87291886798999,-0.640529990651052,
4.21277970822519));
#99175=CARTESIAN_POINT('Ctrl Pts',(-2.85131531996351,-0.730713563401275,
4.21777175261131));
#99176=CARTESIAN_POINT('Ctrl Pts',(-2.82551242969851,-0.819660606360478,
4.22276379699744));
#99177=CARTESIAN_POINT('Ctrl Pts',(-2.79970612822732,-0.908619408339702,
4.22775650134423));
#99178=CARTESIAN_POINT('Ctrl Pts',(-2.76969950941865,-0.996340921799696,
4.23274920569102));
#99179=CARTESIAN_POINT('Ctrl Pts',(-2.73564681545867,-1.08240496168062,
4.23774191003781));
#99180=CARTESIAN_POINT('Ctrl Pts',(-2.70155783753926,-1.16856070485338,
4.24273993423043));
#99181=CARTESIAN_POINT('Ctrl Pts',(-2.66341434533288,-1.25305502767173,
4.24773795842306));
#99182=CARTESIAN_POINT('Ctrl Pts',(-2.62141855177141,-1.33548821650686,
4.25273598261568));
#99183=CARTESIAN_POINT('Ctrl Pts',(-2.57939850044922,-1.41796902069584,
4.25773689378494));
#99184=CARTESIAN_POINT('Ctrl Pts',(-2.53352194388529,-1.49838592910131,
4.2627378049542));
#99185=CARTESIAN_POINT('Ctrl Pts',(-2.4840356721738,-1.5763663214393,4.26773871612346));
#99186=CARTESIAN_POINT('Ctrl Pts',(-2.43446682871423,-1.6544768302134,4.27274797170751));
#99187=CARTESIAN_POINT('Ctrl Pts',(-2.3812765059411,-1.73014233713128,4.27775722729155));
#99188=CARTESIAN_POINT('Ctrl Pts',(-2.3247530445471,-1.80302170865162,4.2827664828756));
#99189=CARTESIAN_POINT('Ctrl Pts',(-2.28983002984959,-1.84805022070626,
4.28586145091313));
#99190=CARTESIAN_POINT('Ctrl Pts',(-2.25363540625622,-1.89201583751354,
4.28895641895067));
#99191=CARTESIAN_POINT('Ctrl Pts',(-2.21624406221831,-1.93484527977874,
4.2920513869882));
#99192=CARTESIAN_POINT('Ctrl Pts',(-2.15520842775417,-2.00475777556257,
4.29710344763693));
#99193=CARTESIAN_POINT('Ctrl Pts',(-2.09075174052333,-2.07190496479329,
4.30215550828566));
#99194=CARTESIAN_POINT('Ctrl Pts',(-2.02315432548813,-2.13593318604742,
4.30720756893439));
#99195=CARTESIAN_POINT('Ctrl Pts',(-1.95565020298429,-2.19987304068521,
4.31225265713416));
#99196=CARTESIAN_POINT('Ctrl Pts',(-1.8850142857745,-2.26070217812353,4.31729774533392));
#99197=CARTESIAN_POINT('Ctrl Pts',(-1.8115663767167,-2.31810078787561,4.32234283353369));
#99198=CARTESIAN_POINT('Ctrl Pts',(-1.73819713456054,-2.3754379204414,4.32738251815611));
#99199=CARTESIAN_POINT('Ctrl Pts',(-1.6620222351466,-2.42935155639337,4.33242220277854));
#99200=CARTESIAN_POINT('Ctrl Pts',(-1.58339665538604,-2.4795602496637,4.33746188740096));
#99201=CARTESIAN_POINT('Ctrl Pts',(-1.50482781977722,-2.52973270727486,
4.34249793487845));
#99202=CARTESIAN_POINT('Ctrl Pts',(-1.42381219265337,-2.57620529842616,
4.34753398235595));
#99203=CARTESIAN_POINT('Ctrl Pts',(-1.34073514975917,-2.61873886789047,
4.35257002983344));
#99204=CARTESIAN_POINT('Ctrl Pts',(-1.2576883657436,-2.66125694549239,4.35760424304789));
#99205=CARTESIAN_POINT('Ctrl Pts',(-1.17258205262342,-2.69983864929842,
4.36263845626234));
#99206=CARTESIAN_POINT('Ctrl Pts',(-1.08582678373008,-2.73429043734099,
4.36767266947679));
#99207=CARTESIAN_POINT('Ctrl Pts',(-0.999078837924667,-2.76873931727808,
4.37270645774891));
#99208=CARTESIAN_POINT('Ctrl Pts',(-0.910682626085935,-2.79905881074814,
4.37774024602103));
#99209=CARTESIAN_POINT('Ctrl Pts',(-0.82106825667028,-2.82510370037782,
4.38277403429315));
#99210=CARTESIAN_POINT('Ctrl Pts',(-0.731436376461401,-2.85115367922119,
4.38780880617567));
#99211=CARTESIAN_POINT('Ctrl Pts',(-0.640586292675597,-2.87292727175354,
4.39284357805819));
#99212=CARTESIAN_POINT('Ctrl Pts',(-0.548961694685599,-2.89032957597709,
4.3978783499407));
#99213=CARTESIAN_POINT('Ctrl Pts',(-0.457236367006165,-2.90775101183929,
4.4029186569199));
#99214=CARTESIAN_POINT('Ctrl Pts',(-0.364735262637199,-2.9207914836135,
4.4079589638991));
#99215=CARTESIAN_POINT('Ctrl Pts',(-0.271910344332595,-2.9294075791267,
4.4129992708783));
#99216=CARTESIAN_POINT('Ctrl Pts',(-0.179028425704788,-2.93802896546307,
4.41804267292219));
#99217=CARTESIAN_POINT('Ctrl Pts',(-0.0858227408153346,-2.9422205468955,
4.42308607496607));
#99218=CARTESIAN_POINT('Ctrl Pts',(0.00725376937796118,-2.94199105757135,
4.42812947700996));
#99219=CARTESIAN_POINT('Ctrl Pts',(0.100481211533062,-2.94176119610956,
4.43318105738545));
#99220=CARTESIAN_POINT('Ctrl Pts',(0.193578617611841,-2.93709597365207,
4.43823263776094));
#99221=CARTESIAN_POINT('Ctrl Pts',(0.286097370379745,-2.92805606071021,
4.44328421813642));
#99222=CARTESIAN_POINT('Ctrl Pts',(0.333300963761295,-2.92344384575977,
4.4458615631486));
#99223=CARTESIAN_POINT('Ctrl Pts',(0.380354074264874,-2.91769368304617,
4.44843890816077));
#99224=CARTESIAN_POINT('Ctrl Pts',(0.427198334233323,-2.91081871356295,
4.45101625317294));
#99225=CARTESIAN_POINT('Ctrl Pts',(0.519021524882117,-2.89734253453937,
4.45606831382199));
#99226=CARTESIAN_POINT('Ctrl Pts',(0.610371415746862,-2.87949296899236,
4.46112037447104));
#99227=CARTESIAN_POINT('Ctrl Pts',(0.700798897592339,-2.85731428182714,
4.46617243512009));
#99228=CARTESIAN_POINT('Ctrl Pts',(0.791101578678766,-2.83516620390744,
4.47121752332016));
#99229=CARTESIAN_POINT('Ctrl Pts',(0.880483952658862,-2.80870098174539,
4.47626261152022));
#99230=CARTESIAN_POINT('Ctrl Pts',(0.968504003358442,-2.77801439799701,
4.48130769972029));
#99231=CARTESIAN_POINT('Ctrl Pts',(1.05642977956102,-2.74736068133089,4.48634738434301));
#99232=CARTESIAN_POINT('Ctrl Pts',(1.14299571542804,-2.71249473532883,4.49138706896572));
#99233=CARTESIAN_POINT('Ctrl Pts',(1.22777301259506,-2.67356268479781,4.49642675358844));
#99234=CARTESIAN_POINT('Ctrl Pts',(1.31248912591017,-2.6346587315628,4.50146280106621));
#99235=CARTESIAN_POINT('Ctrl Pts',(1.39541876368871,-2.59169469141985,4.50649884854399));
#99236=CARTESIAN_POINT('Ctrl Pts',(1.47615223166918,-2.54486514160144,4.51153489602176));
#99237=CARTESIAN_POINT('Ctrl Pts',(1.55685629436347,-2.49805264835632,4.51656910923649));
#99238=CARTESIAN_POINT('Ctrl Pts',(1.6353653924079,-2.44737766511334,4.52160332245121));
#99239=CARTESIAN_POINT('Ctrl Pts',(1.71129454468778,-2.39308064663978,4.52663753566593));
#99240=CARTESIAN_POINT('Ctrl Pts',(1.78721728772137,-2.33878821142513,4.5316713239383));
#99241=CARTESIAN_POINT('Ctrl Pts',(1.86056015667526,-2.28087460744231,4.53670511221068));
#99242=CARTESIAN_POINT('Ctrl Pts',(1.93096822846941,-2.21962287351742,4.54173890048305));
#99243=CARTESIAN_POINT('Ctrl Pts',(2.00139005811468,-2.15835917090463,4.5467736723658));
#99244=CARTESIAN_POINT('Ctrl Pts',(2.0688756167543,-2.09375633480824,4.55180844424854));
#99245=CARTESIAN_POINT('Ctrl Pts',(2.13310493629589,-2.02613605928874,4.55684321613129));
#99246=CARTESIAN_POINT('Ctrl Pts',(2.19740486787352,-1.95844144380478,4.56188352311072));
#99247=CARTESIAN_POINT('Ctrl Pts',(2.25844110810705,-1.8877230898025,4.56692383009015));
#99248=CARTESIAN_POINT('Ctrl Pts',(2.31593250440341,-1.81433751960537,4.57196413706958));
#99249=CARTESIAN_POINT('Ctrl Pts',(2.37345920402358,-1.7409068860646,4.57700753911368));
#99250=CARTESIAN_POINT('Ctrl Pts',(2.42743646936108,-1.66480613785273,4.58205094115778));
#99251=CARTESIAN_POINT('Ctrl Pts',(2.47762646424981,-1.58642084695361,4.58709434320188));
#99252=CARTESIAN_POINT('Ctrl Pts',(2.52789784674495,-1.50790844723094,4.59214592357756));
#99253=CARTESIAN_POINT('Ctrl Pts',(2.5743694769285,-1.42710449368637,4.59719750395325));
#99254=CARTESIAN_POINT('Ctrl Pts',(2.61684952849433,-1.34441903631978,4.60224908432894));
#99255=CARTESIAN_POINT('Ctrl Pts',(2.63852309216503,-1.30223244617172,4.60482642933852));
#99256=CARTESIAN_POINT('Ctrl Pts',(2.65915838336976,-1.25955640685416,4.6074037743481));
#99257=CARTESIAN_POINT('Ctrl Pts',(2.67873485657155,-1.21644710866877,4.60998111935769));
#99258=CARTESIAN_POINT('Ctrl Pts',(2.71710827168217,-1.13194511602972,4.61503318000808));
#99259=CARTESIAN_POINT('Ctrl Pts',(2.7515482331647,-1.04547374152125,4.62008524065846));
#99260=CARTESIAN_POINT('Ctrl Pts',(2.78184885414436,-0.957434568362622,
4.62513730130885));
#99261=CARTESIAN_POINT('Ctrl Pts',(2.81210765663692,-0.869516899810421,
4.63018238951028));
#99262=CARTESIAN_POINT('Ctrl Pts',(2.83823832728488,-0.780036148702834,
4.63522747771172));
#99263=CARTESIAN_POINT('Ctrl Pts',(2.86008213615458,-0.689415821148189,
4.64027256591315));
#99264=CARTESIAN_POINT('Ctrl Pts',(2.88190254905858,-0.598892553135136,
4.64531225053724));
#99265=CARTESIAN_POINT('Ctrl Pts',(2.89944512284491,-0.507232564302514,
4.65035193516134));
#99266=CARTESIAN_POINT('Ctrl Pts',(2.91260061141582,-0.414875497444982,
4.65539161978543));
#99267=CARTESIAN_POINT('Ctrl Pts',(2.92574660565883,-0.322585084765346,
4.66042766726462));
#99268=CARTESIAN_POINT('Ctrl Pts',(2.93451174538845,-0.229599032598319,
4.66546371474381));
#99269=CARTESIAN_POINT('Ctrl Pts',(2.93883786570519,-0.136367148160329,
4.670499762223));
#99270=CARTESIAN_POINT('Ctrl Pts',(2.94316241033333,-0.0431692212654586,
4.67553397543915));
#99271=CARTESIAN_POINT('Ctrl Pts',(2.94305112692431,0.0502739166469684,
4.6805681886553));
#99272=CARTESIAN_POINT('Ctrl Pts',(2.93849780295818,0.143508403969707,4.68560240187145));
#99273=CARTESIAN_POINT('Ctrl Pts',(2.93394486334212,0.236735021287823,4.69063619014526));
#99274=CARTESIAN_POINT('Ctrl Pts',(2.92495065051577,0.329752579268602,4.69566997841907));
#99275=CARTESIAN_POINT('Ctrl Pts',(2.91156102832598,0.422109438811009,4.70070376669288));
#99276=CARTESIAN_POINT('Ctrl Pts',(2.89816878978224,0.514484345033981,4.70573853857711));
#99277=CARTESIAN_POINT('Ctrl Pts',(2.88037950026913,0.606197856795858,4.71077331046133));
#99278=CARTESIAN_POINT('Ctrl Pts',(2.85829044730042,0.696806801682629,4.71580808234556));
#99279=CARTESIAN_POINT('Ctrl Pts',(2.83617711020399,0.787515359676054,4.72084838932645));
#99280=CARTESIAN_POINT('Ctrl Pts',(2.80975467926251,0.877116494502331,4.72588869630734));
#99281=CARTESIAN_POINT('Ctrl Pts',(2.77917073756452,0.965180818015509,4.73092900328823));
#99282=CARTESIAN_POINT('Ctrl Pts',(2.74856801540762,1.0532992185481,4.73597240533382));
#99283=CARTESIAN_POINT('Ctrl Pts',(2.71379886059695,1.13987851705496,4.7410158073794));
#99284=CARTESIAN_POINT('Ctrl Pts',(2.6750587293848,1.22451002214852,4.74605920942499));
#99285=CARTESIAN_POINT('Ctrl Pts',(2.63625577755367,1.30927876486542,4.75111078980215));
#99286=CARTESIAN_POINT('Ctrl Pts',(2.5934691976648,1.39209301428078,4.75616237017931));
#99287=CARTESIAN_POINT('Ctrl Pts',(2.54693993315464,1.47256951513408,4.76121395055647));
#99288=CARTESIAN_POINT('Ctrl Pts',(2.52320043817133,1.51362908287912,4.76379129555179));
#99289=CARTESIAN_POINT('Ctrl Pts',(2.49848737801963,1.55408058727492,4.76636864054711));
#99290=CARTESIAN_POINT('Ctrl Pts',(2.47283687747492,1.59387633692206,4.76894598554244));
#99291=CARTESIAN_POINT('Ctrl Pts',(2.42255727397671,1.67188317775094,4.77399804619198));
#99292=CARTESIAN_POINT('Ctrl Pts',(2.36849255924784,1.74764871196324,4.77905010684153));
#99293=CARTESIAN_POINT('Ctrl Pts',(2.31086894656018,1.82078244494608,4.78410216749107));
#99294=CARTESIAN_POINT('Ctrl Pts',(2.25332486136184,1.89381524461534,4.78914725569163));
#99295=CARTESIAN_POINT('Ctrl Pts',(2.19223191093946,1.96422311472191,4.7941923438922));
#99296=CARTESIAN_POINT('Ctrl Pts',(2.12786026825709,2.03164334438229,4.79923743209277));
#99297=CARTESIAN_POINT('Ctrl Pts',(2.06355757127691,2.09899136312989,4.80427711671601));
#99298=CARTESIAN_POINT('Ctrl Pts',(1.99598346714828,2.16335778214007,4.80931680133925));
#99299=CARTESIAN_POINT('Ctrl Pts',(1.92544848290709,2.22441276288166,4.8143564859625));
#99300=CARTESIAN_POINT('Ctrl Pts',(1.85496440382756,2.28542368018864,4.81939253344081));
#99301=CARTESIAN_POINT('Ctrl Pts',(1.78152402691584,2.34312761946754,4.82442858091912));
#99302=CARTESIAN_POINT('Ctrl Pts',(1.7054740763129,2.39723219046981,4.82946462839743));
#99303=CARTESIAN_POINT('Ctrl Pts',(1.62945182513385,2.45131705514176,4.83449884161269));
#99304=CARTESIAN_POINT('Ctrl Pts',(1.55082225014268,2.5018048986372,4.83953305482796));
#99305=CARTESIAN_POINT('Ctrl Pts',(1.46996360669441,2.54844481890308,4.84456726804323));
#99306=CARTESIAN_POINT('Ctrl Pts',(1.38911178859481,2.59508080225258,4.84960105631616));
#99307=CARTESIAN_POINT('Ctrl Pts',(1.30603166109351,2.63786928631908,4.8546348445891));
#99308=CARTESIAN_POINT('Ctrl Pts',(1.22112780010209,2.67660435922417,4.85966863286203));
#99309=CARTESIAN_POINT('Ctrl Pts',(1.13620734875875,2.71534700102523,4.86470340474534));
#99310=CARTESIAN_POINT('Ctrl Pts',(1.04946286054611,2.75003447459957,4.86973817662866));
#99311=CARTESIAN_POINT('Ctrl Pts',(0.96131962835742,2.780508689455,4.87477294851197));
#99312=CARTESIAN_POINT('Ctrl Pts',(0.873079493801843,2.81101640686616,4.87981325549197));
#99313=CARTESIAN_POINT('Ctrl Pts',(0.783437966308261,2.83730147420214,4.88485356247197));
#99314=CARTESIAN_POINT('Ctrl Pts',(0.692835973951886,2.85925555227198,4.88989386945197));
#99315=CARTESIAN_POINT('Ctrl Pts',(0.602178346288217,2.88122311152306,4.89493727149666));
#99316=CARTESIAN_POINT('Ctrl Pts',(0.510559515593608,2.89885430307471,4.89998067354135));
#99317=CARTESIAN_POINT('Ctrl Pts',(0.418428921662,2.91209224399173,4.90502407558604));
#99318=CARTESIAN_POINT('Ctrl Pts',(0.326148929657618,2.92535165142466,4.91007565596231));
#99319=CARTESIAN_POINT('Ctrl Pts',(0.233355959421926,2.93420354369714,4.91512723633859));
#99320=CARTESIAN_POINT('Ctrl Pts',(0.14050268594035,2.93864305339106,4.92017881671486));
#99321=CARTESIAN_POINT('Ctrl Pts',(0.0931284183453548,2.9409081164561,4.92275616171897));
#99322=CARTESIAN_POINT('Ctrl Pts',(0.0457384281583306,2.94202543260133,
4.92533350672308));
#99323=CARTESIAN_POINT('Ctrl Pts',(-0.00160762990463156,2.94199956076239,
4.92791085172719));
#99324=CARTESIAN_POINT('Ctrl Pts',(-0.0944144355417648,2.94194884729591,
4.93296291237685));
#99325=CARTESIAN_POINT('Ctrl Pts',(-0.187385601049113,2.93750228257937,
4.9380149730265));
#99326=CARTESIAN_POINT('Ctrl Pts',(-0.280070337951304,2.92863869499121,
4.94306703367616));
#99327=CARTESIAN_POINT('Ctrl Pts',(-0.372627158812504,2.91978734021583,
4.94811212187687));
#99328=CARTESIAN_POINT('Ctrl Pts',(-0.464897898150164,2.90653111802456,
4.95315721007757));
#99329=CARTESIAN_POINT('Ctrl Pts',(-0.556431333062393,2.88890085873268,
4.95820229827827));
#99330=CARTESIAN_POINT('Ctrl Pts',(-0.647866730442982,2.87128948245447,
4.96324198290164));
#99331=CARTESIAN_POINT('Ctrl Pts',(-0.738565959096744,2.84931346445757,
4.968281667525));
#99332=CARTESIAN_POINT('Ctrl Pts',(-0.828083592084304,2.82305535980447,
4.97332135214837));
#99333=CARTESIAN_POINT('Ctrl Pts',(-0.917536620115285,2.79681620564922,
4.9783573996268));
#99334=CARTESIAN_POINT('Ctrl Pts',(-1.00580932234237,2.76630123209306,4.98339344710522));
#99335=CARTESIAN_POINT('Ctrl Pts',(-1.09246816554048,2.7316437006463,4.98842949458364));
#99336=CARTESIAN_POINT('Ctrl Pts',(-1.17909544527248,2.6969987923985,4.99346370779902));
#99337=CARTESIAN_POINT('Ctrl Pts',(-1.26410962160118,2.65821448851637,4.99849792101439));
#99338=CARTESIAN_POINT('Ctrl Pts',(-1.34709497755487,2.61547302059235,5.00353213422977));
#99339=CARTESIAN_POINT('Ctrl Pts',(-1.43007332864213,2.57273516051298,5.00856592250281));
#99340=CARTESIAN_POINT('Ctrl Pts',(-1.51102280493738,2.52604100410974,5.01359971077585));
#99341=CARTESIAN_POINT('Ctrl Pts',(-1.58955127083903,2.47561926745088,5.01863349904888));
#99342=CARTESIAN_POINT('Ctrl Pts',(-1.66809508132968,2.42518767830329,5.02366827093228));
#99343=CARTESIAN_POINT('Ctrl Pts',(-1.74421656826335,2.37102730269974,5.02870304281567));
#99344=CARTESIAN_POINT('Ctrl Pts',(-1.817552591216,2.3134101621122,5.03373781469906));
#99345=CARTESIAN_POINT('Ctrl Pts',(-1.89096923787689,2.25572967874514,5.03877812167917));
#99346=CARTESIAN_POINT('Ctrl Pts',(-1.9615939579699,2.19458511947457,5.04381842865927));
#99347=CARTESIAN_POINT('Ctrl Pts',(-2.02909697978266,2.1302885829476,5.04885873563937));
#99348=CARTESIAN_POINT('Ctrl Pts',(-2.09664145268573,2.06595256431345,5.05390213768417));
#99349=CARTESIAN_POINT('Ctrl Pts',(-2.16106010456226,1.99846103636965,5.05894553972897));
#99350=CARTESIAN_POINT('Ctrl Pts',(-2.22206182195982,1.92816110825538,5.06398894177377));
#99351=CARTESIAN_POINT('Ctrl Pts',(-2.28316245914736,1.8577471824633,5.06904052215014));
#99352=CARTESIAN_POINT('Ctrl Pts',(-2.34083482556924,1.78451611341707,5.07409210252651));
#99353=CARTESIAN_POINT('Ctrl Pts',(-2.39482979249436,1.70884588684334,5.07914368290288));
#99354=CARTESIAN_POINT('Ctrl Pts',(-2.42237833133254,1.67023850740831,5.0817210279059));
#99355=CARTESIAN_POINT('Ctrl Pts',(-2.44897032649087,1.63099662472023,5.08429837290891));
#99356=CARTESIAN_POINT('Ctrl Pts',(-2.47457731972873,1.59117286574532,5.08687571791193));
#99357=CARTESIAN_POINT('Ctrl Pts',(-2.52593063722472,1.51130866148183,5.09204443159132));
#99358=CARTESIAN_POINT('Ctrl Pts',(-2.57349750309413,1.42882627654237,5.09721314527072));
#99359=CARTESIAN_POINT('Ctrl Pts',(-2.61700801586616,1.34411050322966,5.10238185895011));
#99360=CARTESIAN_POINT('Ctrl Pts',(-2.66044994472782,1.25952826405923,5.10754242538938));
#99361=CARTESIAN_POINT('Ctrl Pts',(-2.69984804730073,1.17272000538954,5.11270299182864));
#99362=CARTESIAN_POINT('Ctrl Pts',(-2.73497600826104,1.08409881202615,5.11786355826791));
#99363=CARTESIAN_POINT('Ctrl Pts',(-2.77004439535526,0.995627912245485,
5.12301537285009));
#99364=CARTESIAN_POINT('Ctrl Pts',(-2.80085690770018,0.905350584992716,
5.12816718743227));
#99365=CARTESIAN_POINT('Ctrl Pts',(-2.82723399079956,0.813702624591811,
5.13331900201445));
#99366=CARTESIAN_POINT('Ctrl Pts',(-2.85358474443882,0.72214614668383,5.13846567408349));
#99367=CARTESIAN_POINT('Ctrl Pts',(-2.87550875792413,0.629222154936498,
5.14361234615252));
#99368=CARTESIAN_POINT('Ctrl Pts',(-2.89287532254258,0.535384318246417,
5.14875901822156));
#99369=CARTESIAN_POINT('Ctrl Pts',(-2.91022669374542,0.441628577082012,
5.15390118764258));
#99370=CARTESIAN_POINT('Ctrl Pts',(-2.9230284755394,0.346960990963471,5.1590433570636));
#99371=CARTESIAN_POINT('Ctrl Pts',(-2.93120059672715,0.251847298469479,
5.16418552648463));
#99372=CARTESIAN_POINT('Ctrl Pts',(-2.93842545277446,0.167758636467438,
5.16873164529322));
#99373=CARTESIAN_POINT('Ctrl Pts',(-2.94203242052034,0.0833216685275416,
5.17327776410181));
#99374=CARTESIAN_POINT('Ctrl Pts',(-2.94199978029974,-0.0011369768179453,
5.1778238829104));
#99375=CARTESIAN_POINT('',(-2.9447614944152,-0.00213938116747883,6.1778238829104));
#99376=CARTESIAN_POINT('Ctrl Pts',(-2.9375628487339,-0.00115119607926536,
5.17782474187691));
#99377=CARTESIAN_POINT('Ctrl Pts',(-2.93901668938036,-0.421720246351829,
5.2004966892835));
#99378=CARTESIAN_POINT('Ctrl Pts',(-2.65772642519255,-1.82337310569149,
5.27615692541833));
#99379=CARTESIAN_POINT('Ctrl Pts',(-0.501375558914218,-3.44242547455181,
5.40480545028144));
#99380=CARTESIAN_POINT('Ctrl Pts',(2.62307973245116,-2.28497774958579,5.56377031646618));
#99381=CARTESIAN_POINT('Ctrl Pts',(3.34115776752328,0.968677124442226,5.72273518265092));
#99382=CARTESIAN_POINT('Ctrl Pts',(0.994103636774833,3.33368093228121,5.88170004883567));
#99383=CARTESIAN_POINT('Ctrl Pts',(-2.1159090271005,2.67211129893139,6.0333962822555));
#99384=CARTESIAN_POINT('Ctrl Pts',(-2.93786789722844,0.840699408537156,
6.13210422694707));
#99385=CARTESIAN_POINT('Ctrl Pts',(-2.9447614944152,-0.00213938116747883,
6.1778238829104));
#99386=CARTESIAN_POINT('',(-2.94432271303247,0.00230217249621089,7.1778238829104));
#99387=CARTESIAN_POINT('Ctrl Pts',(-2.9447614944152,-0.00213938116747883,
6.1778238829104));
#99388=CARTESIAN_POINT('Ctrl Pts',(-2.94585745686995,-0.136136138433291,
6.18509251567532));
#99389=CARTESIAN_POINT('Ctrl Pts',(-2.8766146460885,-1.24582928930445,6.24534943716847));
#99390=CARTESIAN_POINT('Ctrl Pts',(-1.46591682683645,-3.1547992734402,6.35859464738994));
#99391=CARTESIAN_POINT('Ctrl Pts',(1.85912357706067,-2.94029422407329,6.51755951357464));
#99392=CARTESIAN_POINT('Ctrl Pts',(3.47862959055127,-0.0284037082704225,
6.67652437975942));
#99393=CARTESIAN_POINT('Ctrl Pts',(1.90688867921259,2.90954397870054,6.83548924594416));
#99394=CARTESIAN_POINT('Ctrl Pts',(-1.4142056700595,3.17831605125627,6.99445411212891));
#99395=CARTESIAN_POINT('Ctrl Pts',(-2.86691655368935,1.2782107101568,7.10856565778431));
#99396=CARTESIAN_POINT('Ctrl Pts',(-2.94561300180491,0.152327949348626,
7.16968891471148));
#99397=CARTESIAN_POINT('Ctrl Pts',(-2.94432271303247,0.00230217249621089,
7.1778238829104));
#99398=CARTESIAN_POINT('',(-2.94164226802472,0.000891056651905342,8.17782382888466));
#99399=CARTESIAN_POINT('Ctrl Pts',(-2.94432271303247,0.00230217249621089,
7.1778238829104));
#99400=CARTESIAN_POINT('Ctrl Pts',(-2.93720851977804,-0.824886587469865,
7.22267720343973));
#99401=CARTESIAN_POINT('Ctrl Pts',(-2.14156346621365,-2.64127142281798,
7.32051881269732));
#99402=CARTESIAN_POINT('Ctrl Pts',(0.939534373351018,-3.34946947443834,
7.47134871068315));
#99403=CARTESIAN_POINT('Ctrl Pts',(3.32489445249589,-1.02310677774301,7.63031357686789));
#99404=CARTESIAN_POINT('Ctrl Pts',(2.66004210726286,2.24184000019857,7.78927844305266));
#99405=CARTESIAN_POINT('Ctrl Pts',(-0.445096268358593,3.45015360684055,
7.94824330923738));
#99406=CARTESIAN_POINT('Ctrl Pts',(-2.64229580147289,1.85586383567465,8.07775822408788));
#99407=CARTESIAN_POINT('Ctrl Pts',(-2.93857546330054,0.437603748156834,
8.15428485021008));
#99408=CARTESIAN_POINT('Ctrl Pts',(-2.93739762163734,0.000901669888460307,
8.17782318760405));
#99409=CARTESIAN_POINT('',(-2.94199878001864,-0.00267924781501915,9.17782388293972));
#99410=CARTESIAN_POINT('Ctrl Pts',(-2.94199986533152,0.000890162522109321,
8.17782388291041));
#99411=CARTESIAN_POINT('Ctrl Pts',(-2.94202891373335,-0.0951152209337257,
8.18299050364209));
#99412=CARTESIAN_POINT('Ctrl Pts',(-2.93735424679165,-0.191077943521917,
8.18815712437376));
#99413=CARTESIAN_POINT('Ctrl Pts',(-2.92801456306122,-0.286521759211059,
8.19332374510544));
#99414=CARTESIAN_POINT('Ctrl Pts',(-2.91866794100087,-0.382036478873143,
8.19849420405265));
#99415=CARTESIAN_POINT('Ctrl Pts',(-2.90464944199645,-0.477031115879893,
8.20366466299987));
#99416=CARTESIAN_POINT('Ctrl Pts',(-2.88604933563209,-0.571036979798659,
8.20883512194709));
#99417=CARTESIAN_POINT('Ctrl Pts',(-2.86741566602941,-0.66521247399547,
8.21401491080578));
#99418=CARTESIAN_POINT('Ctrl Pts',(-2.84418395519744,-0.758395227740191,
8.21919469966447));
#99419=CARTESIAN_POINT('Ctrl Pts',(-2.81649520403065,-0.850128675949902,
8.22437448852317));
#99420=CARTESIAN_POINT('Ctrl Pts',(-2.78877986988186,-0.941950194170039,
8.22955925031232));
#99421=CARTESIAN_POINT('Ctrl Pts',(-2.75659910502718,-1.03231924749004,
8.23474401210148));
#99422=CARTESIAN_POINT('Ctrl Pts',(-2.72014243688788,-1.12079843104891,
8.23992877389063));
#99423=CARTESIAN_POINT('Ctrl Pts',(-2.6836082499766,-1.20946575022204,8.2451245601751));
#99424=CARTESIAN_POINT('Ctrl Pts',(-2.64278016627184,-1.29623479789819,
8.25032034645956));
#99425=CARTESIAN_POINT('Ctrl Pts',(-2.59789436989746,-1.3806914365111,8.25551613274402));
#99426=CARTESIAN_POINT('Ctrl Pts',(-2.56720643580305,-1.43843352797297,
8.25906843569831));
#99427=CARTESIAN_POINT('Ctrl Pts',(-2.5346227496621,-1.49509527446311,8.2626207386526));
#99428=CARTESIAN_POINT('Ctrl Pts',(-2.50023013796568,-1.55055256512255,
8.26617304160688));
#99429=CARTESIAN_POINT('Ctrl Pts',(-2.45131720389756,-1.62942353966689,
8.27122510225662));
#99430=CARTESIAN_POINT('Ctrl Pts',(-2.39858068495313,-1.70611949212522,
8.27627716290635));
#99431=CARTESIAN_POINT('Ctrl Pts',(-2.3422399568583,-1.78024604605555,8.28132922355608));
#99432=CARTESIAN_POINT('Ctrl Pts',(-2.28597698571825,-1.85427029646059,
8.28637431175685));
#99433=CARTESIAN_POINT('Ctrl Pts',(-2.22611995635826,-1.92573184417074,
8.29141939995761));
#99434=CARTESIAN_POINT('Ctrl Pts',(-2.16293268157365,-1.99426332638912,
8.29646448815837));
#99435=CARTESIAN_POINT('Ctrl Pts',(-2.09981308396582,-2.06272140747962,
8.3015041727818));
#99436=CARTESIAN_POINT('Ctrl Pts',(-2.03337063018068,-2.12825533594879,
8.30654385740523));
#99437=CARTESIAN_POINT('Ctrl Pts',(-1.96391005366405,-2.19052991331259,
8.31158354202866));
#99438=CARTESIAN_POINT('Ctrl Pts',(-1.89449960690803,-2.25275954705785,
8.31661958950715));
#99439=CARTESIAN_POINT('Ctrl Pts',(-1.82207569671189,-2.31173420942861,
8.32165563698566));
#99440=CARTESIAN_POINT('Ctrl Pts',(-1.74697990055814,-2.3671555139124,8.32669168446415));
#99441=CARTESIAN_POINT('Ctrl Pts',(-1.67191145629963,-2.42255663247644,
8.33172589767961));
#99442=CARTESIAN_POINT('Ctrl Pts',(-1.59417341651241,-2.47440670069988,
8.33676011089507));
#99443=CARTESIAN_POINT('Ctrl Pts',(-1.51413960791633,-2.52244826463081,
8.34179432411054));
#99444=CARTESIAN_POINT('Ctrl Pts',(-1.43411255504405,-2.5704857733313,8.34682811238366));
#99445=CARTESIAN_POINT('Ctrl Pts',(-1.35179049968913,-2.6147151883972,8.35186190065678));
#99446=CARTESIAN_POINT('Ctrl Pts',(-1.26757436895377,-2.65492358066507,
8.3568956889299));
#99447=CARTESIAN_POINT('Ctrl Pts',(-1.18334178224989,-2.695139829718,8.36193046081341));
#99448=CARTESIAN_POINT('Ctrl Pts',(-1.09721478622076,-2.73133330445973,
8.36696523269692));
#99449=CARTESIAN_POINT('Ctrl Pts',(-1.00961585495202,-2.76333852892285,
8.37200000458044));
#99450=CARTESIAN_POINT('Ctrl Pts',(-0.921920619706692,-2.79537893909364,
8.37704031156063));
#99451=CARTESIAN_POINT('Ctrl Pts',(-0.832750637045269,-2.82322175520524,
8.38208061854082));
#99452=CARTESIAN_POINT('Ctrl Pts',(-0.742544880631375,-2.84675097264375,
8.38712092552101));
#99453=CARTESIAN_POINT('Ctrl Pts',(-0.652283732224084,-2.87029463849784,
8.39216432756589));
#99454=CARTESIAN_POINT('Ctrl Pts',(-0.560985978304944,-2.88951934092225,
8.39720772961076));
#99455=CARTESIAN_POINT('Ctrl Pts',(-0.46909999943738,-2.90436037545754,
8.40225113165564));
#99456=CARTESIAN_POINT('Ctrl Pts',(-0.377065019162338,-2.91922547606973,
8.4073027120321));
#99457=CARTESIAN_POINT('Ctrl Pts',(-0.284440350611836,-2.92969266759963,
8.41235429240856));
#99458=CARTESIAN_POINT('Ctrl Pts',(-0.191678515266118,-2.93574919684659,
8.41740587278502));
#99459=CARTESIAN_POINT('Ctrl Pts',(-0.144350899964211,-2.93883927247086,
8.41998321778722));
#99460=CARTESIAN_POINT('Ctrl Pts',(-0.0969875683649003,-2.94078204929621,
8.42256056278943));
#99461=CARTESIAN_POINT('Ctrl Pts',(-0.0496482455559902,-2.94158104625951,
8.42513790779164));
#99462=CARTESIAN_POINT('Ctrl Pts',(0.0431453578393812,-2.94314722428927,
8.43018996844137));
#99463=CARTESIAN_POINT('Ctrl Pts',(0.136179880851625,-2.94032108173428,
8.4352420290911));
#99464=CARTESIAN_POINT('Ctrl Pts',(0.229004972276714,-2.93307359653189,
8.44029408974083));
#99465=CARTESIAN_POINT('Ctrl Pts',(0.321701953954428,-2.92583611372739,
8.44533917794158));
#99466=CARTESIAN_POINT('Ctrl Pts',(0.4141896393011,-2.91418944793322,8.45038426614234));
#99467=CARTESIAN_POINT('Ctrl Pts',(0.506016336772334,-2.89815656356235,
8.45542935434309));
#99468=CARTESIAN_POINT('Ctrl Pts',(0.597744682611139,-2.88214085132543,
8.46046903896652));
#99469=CARTESIAN_POINT('Ctrl Pts',(0.688813012414029,-2.8617483342539,8.46550872358996));
#99470=CARTESIAN_POINT('Ctrl Pts',(0.778774528568876,-2.83705379463491,
8.47054840821339));
#99471=CARTESIAN_POINT('Ctrl Pts',(0.868671119416541,-2.81237707708738,
8.47558445569189));
#99472=CARTESIAN_POINT('Ctrl Pts',(0.95746205709736,-2.78340462542002,8.48062050317039));
#99473=CARTESIAN_POINT('Ctrl Pts',(1.04471155249861,-2.75026212788453,8.48565655064889));
#99474=CARTESIAN_POINT('Ctrl Pts',(1.13192926930258,-2.71713170173212,8.49069076386435));
#99475=CARTESIAN_POINT('Ctrl Pts',(1.21760624424501,-2.67983440465244,8.49572497707981));
#99476=CARTESIAN_POINT('Ctrl Pts',(1.30132364860379,-2.63854519794233,8.50075919029527));
#99477=CARTESIAN_POINT('Ctrl Pts',(1.38503398630335,-2.59725947649022,8.5057929785684));
#99478=CARTESIAN_POINT('Ctrl Pts',(1.46678468389312,-2.55198271204595,8.51082676684153));
#99479=CARTESIAN_POINT('Ctrl Pts',(1.54617968058766,-2.50293675416257,8.51586055511465));
#99480=CARTESIAN_POINT('Ctrl Pts',(1.62559019119318,-2.45388121261956,8.52089532699816));
#99481=CARTESIAN_POINT('Ctrl Pts',(1.70264370895385,-2.40105524874215,8.52593009888167));
#99482=CARTESIAN_POINT('Ctrl Pts',(1.77697240939263,-2.3447245160695,8.53096487076518));
#99483=CARTESIAN_POINT('Ctrl Pts',(1.8513828248629,-2.28833185486094,8.53600517774537));
#99484=CARTESIAN_POINT('Ctrl Pts',(1.92306208877641,-2.22842700245585,8.54104548472556));
#99485=CARTESIAN_POINT('Ctrl Pts',(1.99167504207716,-2.16531626483683,8.54608579170575));
#99486=CARTESIAN_POINT('Ctrl Pts',(2.06033012803545,-2.10216677326587,8.55112919375062));
#99487=CARTESIAN_POINT('Ctrl Pts',(2.12591484279603,-2.03580779313716,8.55617259579548));
#99488=CARTESIAN_POINT('Ctrl Pts',(2.18813206974124,-1.96658130911741,8.56121599784034));
#99489=CARTESIAN_POINT('Ctrl Pts',(2.25045018753521,-1.89724256810593,8.5662675782168));
#99490=CARTESIAN_POINT('Ctrl Pts',(2.30938963527,-1.82502738394544,8.57131915859326));
#99491=CARTESIAN_POINT('Ctrl Pts',(2.36469473674397,-1.75030934466321,8.57637073896973));
#99492=CARTESIAN_POINT('Ctrl Pts',(2.3929117136618,-1.71218777660562,8.57894808397194));
#99493=CARTESIAN_POINT('Ctrl Pts',(2.42018334642052,-1.67341513665586,8.58152542897416));
#99494=CARTESIAN_POINT('Ctrl Pts',(2.44648026422972,-1.63404354799206,8.58410277397638));
#99495=CARTESIAN_POINT('Ctrl Pts',(2.49802696192011,-1.55686813933131,8.58915483462612));
#99496=CARTESIAN_POINT('Ctrl Pts',(2.54601089762617,-1.47711256605875,8.59420689527585));
#99497=CARTESIAN_POINT('Ctrl Pts',(2.59016389066404,-1.39513978493201,8.59925895592559));
#99498=CARTESIAN_POINT('Ctrl Pts',(2.63425594728163,-1.31328013606424,8.60430404412635));
#99499=CARTESIAN_POINT('Ctrl Pts',(2.67452735859163,-1.22920974772194,8.60934913232711));
#99500=CARTESIAN_POINT('Ctrl Pts',(2.71075292990872,-1.14332084429144,8.61439422052787));
#99501=CARTESIAN_POINT('Ctrl Pts',(2.74693970157195,-1.05752393277721,8.61943390515131));
#99502=CARTESIAN_POINT('Ctrl Pts',(2.77908907461641,-0.969912784751068,
8.62447358977474));
#99503=CARTESIAN_POINT('Ctrl Pts',(2.80702207324564,-0.880903559030014,
8.62951327439817));
#99504=CARTESIAN_POINT('Ctrl Pts',(2.8349349126046,-0.791958571347312,8.63454932187667));
#99505=CARTESIAN_POINT('Ctrl Pts',(2.85863729319264,-0.701617934177094,
8.63958536935518));
#99506=CARTESIAN_POINT('Ctrl Pts',(2.8779990012029,-0.610316105862478,8.64462141683368));
#99507=CARTESIAN_POINT('Ctrl Pts',(2.8973536571618,-0.519047532113093,8.64965563004914));
#99508=CARTESIAN_POINT('Ctrl Pts',(2.91237068925402,-0.426818896907573,
8.6546898432646));
#99509=CARTESIAN_POINT('Ctrl Pts',(2.92297049446232,-0.334077069705039,
8.65972405648006));
#99510=CARTESIAN_POINT('Ctrl Pts',(2.9335694049318,-0.241343070921145,8.66475784475319));
#99511=CARTESIAN_POINT('Ctrl Pts',(2.93975177957361,-0.14809640771684,8.66979163302631));
#99512=CARTESIAN_POINT('Ctrl Pts',(2.94148976463434,-0.0547901866340656,
8.67482542129943));
#99513=CARTESIAN_POINT('Ctrl Pts',(2.94322808930017,0.0385342666353106,
8.67986019318294));
#99514=CARTESIAN_POINT('Ctrl Pts',(2.94052029175772,0.13191785668895,8.68489496506644));
#99515=CARTESIAN_POINT('Ctrl Pts',(2.93339063425293,0.224907507382898,8.68992973694994));
#99516=CARTESIAN_POINT('Ctrl Pts',(2.92625313858892,0.317999388469715,8.69497004393013));
#99517=CARTESIAN_POINT('Ctrl Pts',(2.91468411325629,0.41069602201003,8.70001035091032));
#99518=CARTESIAN_POINT('Ctrl Pts',(2.89875968411325,0.502549792318768,8.70505065789051));
#99519=CARTESIAN_POINT('Ctrl Pts',(2.88282547637173,0.594459966604765,8.71009405993538));
#99520=CARTESIAN_POINT('Ctrl Pts',(2.86253063701528,0.685525813932192,8.71513746198024));
#99521=CARTESIAN_POINT('Ctrl Pts',(2.83800188406911,0.775312392536198,8.72018086402512));
#99522=CARTESIAN_POINT('Ctrl Pts',(2.8134333555363,0.865244568180685,8.72523244440157));
#99523=CARTESIAN_POINT('Ctrl Pts',(2.78461734403574,0.953892911672233,8.73028402477803));
#99524=CARTESIAN_POINT('Ctrl Pts',(2.75172957247402,1.04084021827174,8.73533560515448));
#99525=CARTESIAN_POINT('Ctrl Pts',(2.73495004461305,1.08520122797968,8.7379129501567));
#99526=CARTESIAN_POINT('Ctrl Pts',(2.7171113578613,1.12911979827709,8.74049029515891));
#99527=CARTESIAN_POINT('Ctrl Pts',(2.69824144008475,1.17254301883102,8.74306764016113));
#99528=CARTESIAN_POINT('Ctrl Pts',(2.66125300082632,1.25766035611273,8.74811970081085));
#99529=CARTESIAN_POINT('Ctrl Pts',(2.6201665468077,1.34117869451823,8.75317176146058));
#99530=CARTESIAN_POINT('Ctrl Pts',(2.57514209313475,1.42267607000525,8.75822382211031));
#99531=CARTESIAN_POINT('Ctrl Pts',(2.53017977860204,1.50406096935028,8.76326891031107));
#99532=CARTESIAN_POINT('Ctrl Pts',(2.48129047722312,1.58343006267773,8.76831399851184));
#99533=CARTESIAN_POINT('Ctrl Pts',(2.42868208167767,1.66038168688341,8.7733590867126));
#99534=CARTESIAN_POINT('Ctrl Pts',(2.37613003272558,1.73725089150886,8.77839877133604));
#99535=CARTESIAN_POINT('Ctrl Pts',(2.31986705651522,1.81170740870906,8.78343845595948));
#99536=CARTESIAN_POINT('Ctrl Pts',(2.26014618899899,1.88337548151009,8.78847814058292));
#99537=CARTESIAN_POINT('Ctrl Pts',(2.20046842208674,1.95499183139829,8.79351418806142));
#99538=CARTESIAN_POINT('Ctrl Pts',(2.13733800774534,2.02382339650421,8.79855023553992));
#99539=CARTESIAN_POINT('Ctrl Pts',(2.07104976382865,2.08952551449971,8.80358628301842));
#99540=CARTESIAN_POINT('Ctrl Pts',(2.00478566386137,2.15520370202852,8.80862049623388));
#99541=CARTESIAN_POINT('Ctrl Pts',(1.93536633447734,2.21775439437172,8.81365470944934));
#99542=CARTESIAN_POINT('Ctrl Pts',(1.86312442507697,2.27686876580132,8.8186889226648));
#99543=CARTESIAN_POINT('Ctrl Pts',(1.7908886136794,2.33597814733508,8.82372271093792));
#99544=CARTESIAN_POINT('Ctrl Pts',(1.71583103993865,2.39165150343185,8.82875649921104));
#99545=CARTESIAN_POINT('Ctrl Pts',(1.63831760978349,2.44362014426819,8.83379028748416));
#99546=CARTESIAN_POINT('Ctrl Pts',(1.56078903337859,2.49559893986109,8.83882505936766));
#99547=CARTESIAN_POINT('Ctrl Pts',(1.48080401674281,2.5438713354159,8.84385983125116));
#99548=CARTESIAN_POINT('Ctrl Pts',(1.39875665099451,2.58821247800458,8.84889460313465));
#99549=CARTESIAN_POINT('Ctrl Pts',(1.31661908451552,2.63260236808717,8.85393491011484));
#99550=CARTESIAN_POINT('Ctrl Pts',(1.23241503460177,2.67305216654127,8.85897521709503));
#99551=CARTESIAN_POINT('Ctrl Pts',(1.1465620752108,2.70938358445022,8.86401552407522));
#99552=CARTESIAN_POINT('Ctrl Pts',(1.0606563967169,2.74573731212896,8.86905892612009));
#99553=CARTESIAN_POINT('Ctrl Pts',(0.973100209637635,2.77796747126774,8.87410232816496));
#99554=CARTESIAN_POINT('Ctrl Pts',(0.884327817268211,2.80594517259437,8.87914573020983));
#99555=CARTESIAN_POINT('Ctrl Pts',(0.795411472452718,2.83396824228872,8.88419731058629));
#99556=CARTESIAN_POINT('Ctrl Pts',(0.705275414195521,2.85772497448137,8.88924889096275));
#99557=CARTESIAN_POINT('Ctrl Pts',(0.614365558734634,2.87713728560885,8.89430047133921));
#99558=CARTESIAN_POINT('Ctrl Pts',(0.567982834089371,2.88704155701254,8.89687781634143));
#99559=CARTESIAN_POINT('Ctrl Pts',(0.521398793615352,2.89581576553078,8.89945516134366));
#99560=CARTESIAN_POINT('Ctrl Pts',(0.474673043194979,2.90345475288733,8.90203250634588));
#99561=CARTESIAN_POINT('Ctrl Pts',(0.383082152249367,2.9184285446748,8.90708456699561));
#99562=CARTESIAN_POINT('Ctrl Pts',(0.290617456125183,2.92909107366691,8.91213662764533));
#99563=CARTESIAN_POINT('Ctrl Pts',(0.197720370061504,2.93534847254338,8.91718868829506));
#99564=CARTESIAN_POINT('Ctrl Pts',(0.10495149310619,2.94159723545973,8.92223377649582));
#99565=CARTESIAN_POINT('Ctrl Pts',(0.0117518514684078,2.94345291957198,
8.92727886469659));
#99566=CARTESIAN_POINT('Ctrl Pts',(-0.0814282926911858,2.94087290326349,
8.93232395289735));
#99567=CARTESIAN_POINT('Ctrl Pts',(-0.174508635599422,2.93829565029967,
8.93736363752078));
#99568=CARTESIAN_POINT('Ctrl Pts',(-0.267569080796354,2.93129215222189,
8.9424033221442));
#99569=CARTESIAN_POINT('Ctrl Pts',(-0.360156712281988,2.9198717681772,8.94744300676762));
#99570=CARTESIAN_POINT('Ctrl Pts',(-0.452677523190822,2.90845962623393,
8.95247905424613));
#99571=CARTESIAN_POINT('Ctrl Pts',(-0.544725758939587,2.89263698848272,
8.95751510172463));
#99572=CARTESIAN_POINT('Ctrl Pts',(-0.63585203185653,2.87246517708813,8.96255114920313));
#99573=CARTESIAN_POINT('Ctrl Pts',(-0.72694511415023,2.85230071280618,8.9675853624186));
#99574=CARTESIAN_POINT('Ctrl Pts',(-0.817116467355787,2.82779031774977,
8.97261957563406));
#99575=CARTESIAN_POINT('Ctrl Pts',(-0.905926357638238,2.79904652239585,
8.97765378884953));
#99576=CARTESIAN_POINT('Ctrl Pts',(-0.994728751400297,2.7703051533308,8.98268757712266));
#99577=CARTESIAN_POINT('Ctrl Pts',(-1.08216948807129,2.73733123143188,8.98772136539578));
#99578=CARTESIAN_POINT('Ctrl Pts',(-1.16782457910494,2.70028697594133,8.99275515366891));
#99579=CARTESIAN_POINT('Ctrl Pts',(-1.25349640728163,2.66323548194347,8.99778992555239));
#99580=CARTESIAN_POINT('Ctrl Pts',(-1.3373814892415,2.62211225148476,9.00282469743588));
#99581=CARTESIAN_POINT('Ctrl Pts',(-1.41907743876359,2.57712693183556,9.00785946931936));
#99582=CARTESIAN_POINT('Ctrl Pts',(-1.50086320267885,2.53209215650087,9.01289977629955));
#99583=CARTESIAN_POINT('Ctrl Pts',(-1.58045464032414,2.48318703130501,9.01794008327975));
#99584=CARTESIAN_POINT('Ctrl Pts',(-1.65747580624598,2.43066615389881,9.02298039025994));
#99585=CARTESIAN_POINT('Ctrl Pts',(-1.7345442679953,2.37811302537921,9.0280237923048));
#99586=CARTESIAN_POINT('Ctrl Pts',(-1.80903896143313,2.32193999178175,9.03306719434966));
#99587=CARTESIAN_POINT('Ctrl Pts',(-1.88061642186181,2.26244245757183,9.03811059639453));
#99588=CARTESIAN_POINT('Ctrl Pts',(-1.95230995160258,2.20284844274043,9.04316217677098));
#99589=CARTESIAN_POINT('Ctrl Pts',(-2.0210764769293,2.13991946438324,9.04821375714744));
#99590=CARTESIAN_POINT('Ctrl Pts',(-2.08660896569403,2.0739881928992,9.05326533752389));
#99591=CARTESIAN_POINT('Ctrl Pts',(-2.12004401370196,2.04034968368269,9.05584268252614));
#99592=CARTESIAN_POINT('Ctrl Pts',(-2.15263785010515,2.0059301922487,9.05842002752838));
#99593=CARTESIAN_POINT('Ctrl Pts',(-2.18435387262118,1.97077704450931,9.06099737253063));
#99594=CARTESIAN_POINT('Ctrl Pts',(-2.24587576570944,1.90258790774585,9.06599683750452));
#99595=CARTESIAN_POINT('Ctrl Pts',(-2.304323743165,1.83137957052598,9.0709963024784));
#99596=CARTESIAN_POINT('Ctrl Pts',(-2.35938251168991,1.75746355965972,9.07599576745229));
#99597=CARTESIAN_POINT('Ctrl Pts',(-2.41437124025441,1.68364157694944,9.08098887263393));
#99598=CARTESIAN_POINT('Ctrl Pts',(-2.46597904899703,1.60711911752429,9.08598197781558));
#99599=CARTESIAN_POINT('Ctrl Pts',(-2.51392844109951,1.52824336839097,9.09097508299722));
#99600=CARTESIAN_POINT('Ctrl Pts',(-2.56183092720743,1.44944477863962,9.09596330372561));
#99601=CARTESIAN_POINT('Ctrl Pts',(-2.60608186788051,1.36829785550792,9.10095152445399));
#99602=CARTESIAN_POINT('Ctrl Pts',(-2.64644571237268,1.28518056764964,9.10593974518238));
#99603=CARTESIAN_POINT('Ctrl Pts',(-2.68678192713052,1.2021201749809,9.1109245513893));
#99604=CARTESIAN_POINT('Ctrl Pts',(-2.72323613318865,1.11709250390312,9.11590935759621));
#99605=CARTESIAN_POINT('Ctrl Pts',(-2.75561822778716,1.03050093774199,9.12089416380313));
#99606=CARTESIAN_POINT('Ctrl Pts',(-2.78799587501206,0.94392126411135,9.12587828539419));
#99607=CARTESIAN_POINT('Ctrl Pts',(-2.81630234981916,0.855778542245091,
9.13086240698524));
#99608=CARTESIAN_POINT('Ctrl Pts',(-2.84039569224437,0.766496126200019,
9.1358465285763));
#99609=CARTESIAN_POINT('Ctrl Pts',(-2.86448612171046,0.677224504673327,
9.14083004757174));
#99610=CARTESIAN_POINT('Ctrl Pts',(-2.88436431870589,0.586813903109782,
9.14581356656718));
#99611=CARTESIAN_POINT('Ctrl Pts',(-2.8999386703983,0.495701228492089,9.15079708556263));
#99612=CARTESIAN_POINT('Ctrl Pts',(-2.9155237877027,0.404525573165936,9.15578404936483));
#99613=CARTESIAN_POINT('Ctrl Pts',(-2.92679904500027,0.312647324569952,
9.16077101316702));
#99614=CARTESIAN_POINT('Ctrl Pts',(-2.93372438166545,0.220511343068046,
9.16575797696922));
#99615=CARTESIAN_POINT('Ctrl Pts',(-2.93930964116251,0.146204000250804,
9.16977994561628));
#99616=CARTESIAN_POINT('Ctrl Pts',(-2.94206654305182,0.0717292485551678,
9.17380191426335));
#99617=CARTESIAN_POINT('Ctrl Pts',(-2.94199878001913,-0.00267924727273255,
9.17782388291041));
#99618=CARTESIAN_POINT('',(-2.941999963151,0.000465638797190243,10.1778238829398));
#99619=CARTESIAN_POINT('Ctrl Pts',(-2.94199878001864,-0.00267924781502314,
9.17782388293972));
#99620=CARTESIAN_POINT('Ctrl Pts',(-2.94189214524261,-0.119771582166532,
9.18415302173411));
#99621=CARTESIAN_POINT('Ctrl Pts',(-2.93479142724456,-0.236551798411417,
9.19048216052851));
#99622=CARTESIAN_POINT('Ctrl Pts',(-2.92082967268118,-0.352303879037908,
9.19681129932291));
#99623=CARTESIAN_POINT('Ctrl Pts',(-2.90659295952955,-0.470335546268701,
9.20326508227));
#99624=CARTESIAN_POINT('Ctrl Pts',(-2.8852223297207,-0.587298377518235,
9.20971886521709));
#99625=CARTESIAN_POINT('Ctrl Pts',(-2.85690708185129,-0.70245706322021,
9.21617264816419));
#99626=CARTESIAN_POINT('Ctrl Pts',(-2.85136494753718,-0.724997035553822,
9.21743584501458));
#99627=CARTESIAN_POINT('Ctrl Pts',(-2.84555690974658,-0.747467957434179,
9.21869904186498));
#99628=CARTESIAN_POINT('Ctrl Pts',(-2.83948459964082,-0.769864409102424,
9.21996223871538));
#99629=CARTESIAN_POINT('Ctrl Pts',(-2.81519885278461,-0.859437330481364,
9.22501429936511));
#99630=CARTESIAN_POINT('Ctrl Pts',(-2.78662687917521,-0.94802091743699,
9.23006636001484));
#99631=CARTESIAN_POINT('Ctrl Pts',(-2.75386596675008,-1.03517449600328,
9.23511842066457));
#99632=CARTESIAN_POINT('Ctrl Pts',(-2.72115026830903,-1.12220779218968,
9.24016350886534));
#99633=CARTESIAN_POINT('Ctrl Pts',(-2.68425727404025,-1.20781458945974,
9.24520859706611));
#99634=CARTESIAN_POINT('Ctrl Pts',(-2.64333458266587,-1.29156737496835,
9.25025368526688));
#99635=CARTESIAN_POINT('Ctrl Pts',(-2.60245572182898,-1.37523045646481,
9.25529336989032));
#99636=CARTESIAN_POINT('Ctrl Pts',(-2.55755593663263,-1.45704307612064,
9.26033305451376));
#99637=CARTESIAN_POINT('Ctrl Pts',(-2.50883124192735,-1.53659682400078,
9.2653727391372));
#99638=CARTESIAN_POINT('Ctrl Pts',(-2.46014171187815,-1.61609315786937,
9.2704087866157));
#99639=CARTESIAN_POINT('Ctrl Pts',(-2.40763299045645,-1.69333348247071,
9.2754448340942));
#99640=CARTESIAN_POINT('Ctrl Pts',(-2.35154693323202,-1.76793411099143,
9.28048088157271));
#99641=CARTESIAN_POINT('Ctrl Pts',(-2.29548130404812,-1.8425075679701,9.28551509478817));
#99642=CARTESIAN_POINT('Ctrl Pts',(-2.2358411942451,-1.91444288410493,9.29054930800362));
#99643=CARTESIAN_POINT('Ctrl Pts',(-2.17291107731279,-1.98338635925817,
9.29558352121908));
#99644=CARTESIAN_POINT('Ctrl Pts',(-2.1099862723666,-2.05232401483247,9.30061730949221));
#99645=CARTESIAN_POINT('Ctrl Pts',(-2.04377231210823,-2.11827000350394,
9.30565109776534));
#99646=CARTESIAN_POINT('Ctrl Pts',(-1.97459238301976,-2.1809055277385,9.31068488603846));
#99647=CARTESIAN_POINT('Ctrl Pts',(-1.90539893606111,-2.24355329105593,
9.31571965792197));
#99648=CARTESIAN_POINT('Ctrl Pts',(-1.83323869886711,-2.30288900734021,
9.32075442980548));
#99649=CARTESIAN_POINT('Ctrl Pts',(-1.75846908832904,-2.35863317737016,
9.32578920168899));
#99650=CARTESIAN_POINT('Ctrl Pts',(-1.68361727803433,-2.41443863108444,
9.33082950866918));
#99651=CARTESIAN_POINT('Ctrl Pts',(-1.60615072490937,-2.46664439095639,
9.33586981564937));
#99652=CARTESIAN_POINT('Ctrl Pts',(-1.52645681789169,-2.51501363477656,
9.34091012262956));
#99653=CARTESIAN_POINT('Ctrl Pts',(-1.44671397381565,-2.56341258034679,
9.34595352467444));
#99654=CARTESIAN_POINT('Ctrl Pts',(-1.36474144303353,-2.60797010778216,
9.35099692671931));
#99655=CARTESIAN_POINT('Ctrl Pts',(-1.28095031429092,-2.64849585469149,
9.35604032876418));
#99656=CARTESIAN_POINT('Ctrl Pts',(-1.19702331067083,-2.68908731775692,
9.36109190914064));
#99657=CARTESIAN_POINT('Ctrl Pts',(-1.11127222992197,-2.72563377412438,
9.3661434895171));
#99658=CARTESIAN_POINT('Ctrl Pts',(-1.02412700143469,-2.75799345266307,
9.37119506989356));
#99659=CARTESIAN_POINT('Ctrl Pts',(-0.979665010855948,-2.77450354446379,
9.37377241489575));
#99660=CARTESIAN_POINT('Ctrl Pts',(-0.934840340388964,-2.78992458461901,
9.37634975989794));
#99661=CARTESIAN_POINT('Ctrl Pts',(-0.889711222666078,-2.80424284616401,
9.37892710490012));
#99662=CARTESIAN_POINT('Ctrl Pts',(-0.801250019524294,-2.8323092189867,
9.38397916554985));
#99663=CARTESIAN_POINT('Ctrl Pts',(-0.711300509577873,-2.85623609120711,
9.38903122619958));
#99664=CARTESIAN_POINT('Ctrl Pts',(-0.620285885191738,-2.87586672511643,
9.39408328684931));
#99665=CARTESIAN_POINT('Ctrl Pts',(-0.529396871891344,-2.89547026639909,
9.39912837505008));
#99666=CARTESIAN_POINT('Ctrl Pts',(-0.437446095727711,-2.91078925878916,
9.40417346325084));
#99667=CARTESIAN_POINT('Ctrl Pts',(-0.344872916438735,-2.92171639135407,
9.40921855145161));
#99668=CARTESIAN_POINT('Ctrl Pts',(-0.252398888306911,-2.93263182033651,
9.41425823607504));
#99669=CARTESIAN_POINT('Ctrl Pts',(-0.159304220935015,-2.93916468743556,
9.41929792069848));
#99670=CARTESIAN_POINT('Ctrl Pts',(-0.06603841983787,-2.94125873175165,
9.42433760532191));
#99671=CARTESIAN_POINT('Ctrl Pts',(0.0271600712465363,-2.94335126479407,
9.42937365280041));
#99672=CARTESIAN_POINT('Ctrl Pts',(0.120529007658576,-2.94101133250171,
9.43440970027891));
#99673=CARTESIAN_POINT('Ctrl Pts',(0.213614857808199,-2.93423460079858,
9.43944574775741));
#99674=CARTESIAN_POINT('Ctrl Pts',(0.306666803604203,-2.92746033736218,
9.44447996097287));
#99675=CARTESIAN_POINT('Ctrl Pts',(0.399435425289394,-2.91625251708545,
9.44951417418833));
#99676=CARTESIAN_POINT('Ctrl Pts',(0.491469335450193,-2.9006588721034,9.45454838740379));
#99677=CARTESIAN_POINT('Ctrl Pts',(0.583495476948213,-2.88506654339455,
9.45958217567691));
#99678=CARTESIAN_POINT('Ctrl Pts',(0.674786592197164,-2.86508920043962,
9.46461596395003));
#99679=CARTESIAN_POINT('Ctrl Pts',(0.76489968515994,-2.84082601924902,9.46964975222316));
#99680=CARTESIAN_POINT('Ctrl Pts',(0.855030386367092,-2.8165580969935,9.47468452410666));
#99681=CARTESIAN_POINT('Ctrl Pts',(0.943982179233714,-2.78800278917391,
9.47971929599017));
#99682=CARTESIAN_POINT('Ctrl Pts',(1.03132658157492,-2.75530932603528,9.48475406787368));
#99683=CARTESIAN_POINT('Ctrl Pts',(1.11876700807031,-2.72257992055734,9.48979437485387));
#99684=CARTESIAN_POINT('Ctrl Pts',(1.20459609988353,-2.68570343461613,9.49483468183406));
#99685=CARTESIAN_POINT('Ctrl Pts',(1.28840503465784,-2.64487740106575,9.49987498881425));
#99686=CARTESIAN_POINT('Ctrl Pts',(1.37226543337574,-2.60402629776961,9.50491839085912));
#99687=CARTESIAN_POINT('Ctrl Pts',(1.45410281602812,-2.55922103184496,9.50996179290399));
#99688=CARTESIAN_POINT('Ctrl Pts',(1.53353459597083,-2.51070421255882,9.51500519494886));
#99689=CARTESIAN_POINT('Ctrl Pts',(1.61309518171351,-2.46210871887151,9.52005677532532));
#99690=CARTESIAN_POINT('Ctrl Pts',(1.69024200976055,-2.40978990538259,9.52510835570178));
#99691=CARTESIAN_POINT('Ctrl Pts',(1.76462315164894,-2.35403252582978,9.53015993607824));
#99692=CARTESIAN_POINT('Ctrl Pts',(1.80257283274249,-2.32558479406713,9.53273728108045));
#99693=CARTESIAN_POINT('Ctrl Pts',(1.83980313298703,-2.29624260080055,9.53531462608267));
#99694=CARTESIAN_POINT('Ctrl Pts',(1.87627098868146,-2.26604747898897,9.53789197108488));
#99695=CARTESIAN_POINT('Ctrl Pts',(1.94775455746084,-2.20685959898569,9.54294403173461));
#99696=CARTESIAN_POINT('Ctrl Pts',(2.01656316091093,-2.1441795730994,9.54799609238434));
#99697=CARTESIAN_POINT('Ctrl Pts',(2.08233593309237,-2.07827838889605,9.55304815303407));
#99698=CARTESIAN_POINT('Ctrl Pts',(2.14801793096823,-2.01246815622223,9.55809324123484));
#99699=CARTESIAN_POINT('Ctrl Pts',(2.21067211210061,-1.94344591088365,9.56313832943561));
#99700=CARTESIAN_POINT('Ctrl Pts',(2.26997041831439,-1.87152298943336,9.56818341763638));
#99701=CARTESIAN_POINT('Ctrl Pts',(2.32920521265868,-1.79967710153584,9.57322310225981));
#99702=CARTESIAN_POINT('Ctrl Pts',(2.38509099522403,-1.72493705368548,9.57826278688325));
#99703=CARTESIAN_POINT('Ctrl Pts',(2.43733714000599,-1.64765034699338,9.58330247150668));
#99704=CARTESIAN_POINT('Ctrl Pts',(2.48954557869818,-1.57041941818715,9.58833851898518));
#99705=CARTESIAN_POINT('Ctrl Pts',(2.53811935247468,-1.49064585069163,9.59337456646368));
#99706=CARTESIAN_POINT('Ctrl Pts',(2.58280931736585,-1.40870863918986,9.59841061394218));
#99707=CARTESIAN_POINT('Ctrl Pts',(2.6274830049778,-1.32680127140968,9.60344482715764));
#99708=CARTESIAN_POINT('Ctrl Pts',(2.6682754813901,-1.24273221483784,9.60847904037309));
#99709=CARTESIAN_POINT('Ctrl Pts',(2.7049825418681,-1.15690684507821,9.61351325358855));
#99710=CARTESIAN_POINT('Ctrl Pts',(2.74168650387106,-1.07108871991301,9.61854704186167));
#99711=CARTESIAN_POINT('Ctrl Pts',(2.77430556103156,-0.983514984895593,
9.6235808301348));
#99712=CARTESIAN_POINT('Ctrl Pts',(2.80268330622685,-0.894611806873418,
9.62861461840792));
#99713=CARTESIAN_POINT('Ctrl Pts',(2.83106659647952,-0.805691257026247,
9.63364939029142));
#99714=CARTESIAN_POINT('Ctrl Pts',(2.85520679410711,-0.715441171611568,
9.63868416217493));
#99715=CARTESIAN_POINT('Ctrl Pts',(2.87499743529214,-0.624302608567035,
9.64371893405843));
#99716=CARTESIAN_POINT('Ctrl Pts',(2.8948098337911,-0.533063850167109,9.64875924103862));
#99717=CARTESIAN_POINT('Ctrl Pts',(2.91026303636294,-0.440935099241388,
9.65379954801881));
#99718=CARTESIAN_POINT('Ctrl Pts',(2.92130183523695,-0.348367029784977,
9.658839854999));
#99719=CARTESIAN_POINT('Ctrl Pts',(2.93234741262598,-0.255742117726806,
9.66388325704388));
#99720=CARTESIAN_POINT('Ctrl Pts',(2.93897315828224,-0.162677792937583,
9.66892665908875));
#99721=CARTESIAN_POINT('Ctrl Pts',(2.94117596738647,-0.0696270699389575,
9.67397006113362));
#99722=CARTESIAN_POINT('Ctrl Pts',(2.94338234854446,0.0235745432049082,
9.67902164151007));
#99723=CARTESIAN_POINT('Ctrl Pts',(2.94115148528214,0.116762066896197,9.68407322188653));
#99724=CARTESIAN_POINT('Ctrl Pts',(2.93453230439372,0.209485451689823,9.68912480226299));
#99725=CARTESIAN_POINT('Ctrl Pts',(2.93115516070598,0.256793449301686,9.6917021472652));
#99726=CARTESIAN_POINT('Ctrl Pts',(2.92663652552509,0.303980751598852,9.69427949226741));
#99727=CARTESIAN_POINT('Ctrl Pts',(2.92098801012808,0.3509886674638,9.69685683726962));
#99728=CARTESIAN_POINT('Ctrl Pts',(2.9099159020703,0.443132653528412,9.70190889791935));
#99729=CARTESIAN_POINT('Ctrl Pts',(2.89445953293827,0.534917784171193,9.70696095856908));
#99730=CARTESIAN_POINT('Ctrl Pts',(2.87465141666587,0.625893946815999,9.71201301921881));
#99731=CARTESIAN_POINT('Ctrl Pts',(2.85487063796707,0.716744551456834,9.71705810741957));
#99732=CARTESIAN_POINT('Ctrl Pts',(2.8307501403396,0.806787976309188,9.72210319562034));
#99733=CARTESIAN_POINT('Ctrl Pts',(2.80237412322733,0.895579853204544,9.7271482838211));
#99734=CARTESIAN_POINT('Ctrl Pts',(2.77402849844848,0.984276628933381,9.73218796844454));
#99735=CARTESIAN_POINT('Ctrl Pts',(2.74143654819952,1.07172410016375,9.73722765306797));
#99736=CARTESIAN_POINT('Ctrl Pts',(2.7047331422842,1.15748979651202,9.74226733769141));
#99737=CARTESIAN_POINT('Ctrl Pts',(2.66805622525,1.24319359567996,9.74730338516991));
#99738=CARTESIAN_POINT('Ctrl Pts',(2.62727392464204,1.32721762514166,9.75233943264841));
#99739=CARTESIAN_POINT('Ctrl Pts',(2.58257004536095,1.40914724596273,9.75737548012691));
#99740=CARTESIAN_POINT('Ctrl Pts',(2.53788244842707,1.49104702582694,9.76240969334237));
#99741=CARTESIAN_POINT('Ctrl Pts',(2.48927632295869,1.57085352287876,9.76744390655783));
#99742=CARTESIAN_POINT('Ctrl Pts',(2.43698198151407,1.64817560404701,9.77247811977329));
#99743=CARTESIAN_POINT('Ctrl Pts',(2.38469205428051,1.72549115839084,9.77751190804642));
#99744=CARTESIAN_POINT('Ctrl Pts',(2.32871477911046,1.80032234586958,9.78254569631954));
#99745=CARTESIAN_POINT('Ctrl Pts',(2.26932382353795,1.87230696840104,9.78757948459266));
#99746=CARTESIAN_POINT('Ctrl Pts',(2.20992126287648,1.9443056568444,9.79261425647617));
#99747=CARTESIAN_POINT('Ctrl Pts',(2.14710398010003,2.01345633322179,9.79764902835968));
#99748=CARTESIAN_POINT('Ctrl Pts',(2.08118519819989,2.07943073238655,9.80268380024319));
#99749=CARTESIAN_POINT('Ctrl Pts',(2.01519394691296,2.14547766208227,9.80772410722339));
#99750=CARTESIAN_POINT('Ctrl Pts',(1.9460947048205,2.20834102946829,9.81276441420358));
#99751=CARTESIAN_POINT('Ctrl Pts',(1.87423652558705,2.26773046153095,9.81780472118377));
#99752=CARTESIAN_POINT('Ctrl Pts',(1.80233422092363,2.32715636243061,9.82284812322864));
#99753=CARTESIAN_POINT('Ctrl Pts',(1.72766996168055,2.38310381497015,9.82789152527352));
#99754=CARTESIAN_POINT('Ctrl Pts',(1.65062297318189,2.43532498866254,9.83293492731839));
#99755=CARTESIAN_POINT('Ctrl Pts',(1.57345104603785,2.48763084370106,9.83798650769485));
#99756=CARTESIAN_POINT('Ctrl Pts',(1.49388905472915,2.53619812550275,9.84303808807131));
#99757=CARTESIAN_POINT('Ctrl Pts',(1.41234189653937,2.58082435808398,9.84808966844777));
#99758=CARTESIAN_POINT('Ctrl Pts',(1.37073607322446,2.60359291543411,9.85066701344997));
#99759=CARTESIAN_POINT('Ctrl Pts',(1.3286138363626,2.62533634487202,9.85324435845217));
#99760=CARTESIAN_POINT('Ctrl Pts',(1.28603082018315,2.6460326395453,9.85582170345437));
#99761=CARTESIAN_POINT('Ctrl Pts',(1.20256043488224,2.68660110664024,9.8608737641041));
#99762=CARTESIAN_POINT('Ctrl Pts',(1.11701855354975,2.72328892603511,9.86592582475383));
#99763=CARTESIAN_POINT('Ctrl Pts',(1.02980124215722,2.75587978722793,9.87097788540356));
#99764=CARTESIAN_POINT('Ctrl Pts',(0.942704301103581,2.78842566912772,9.87602297360433));
#99765=CARTESIAN_POINT('Ctrl Pts',(0.853936937372214,2.81688567441796,9.88106806180509));
#99766=CARTESIAN_POINT('Ctrl Pts',(0.763918364614622,2.84109006055854,9.88611315000585));
#99767=CARTESIAN_POINT('Ctrl Pts',(0.673996206884852,2.86526852242048,9.89115283462929));
#99768=CARTESIAN_POINT('Ctrl Pts',(0.582825930556004,2.88520031009069,9.89619251925272));
#99769=CARTESIAN_POINT('Ctrl Pts',(0.49084417353772,2.90076472629272,9.90123220387616));
#99770=CARTESIAN_POINT('Ctrl Pts',(0.398928799836315,2.91631790964156,9.90626825135466));
#99771=CARTESIAN_POINT('Ctrl Pts',(0.306203546308772,2.92750991250561,9.91130429883316));
#99772=CARTESIAN_POINT('Ctrl Pts',(0.213116546639057,2.93427083575267,9.91634034631166));
#99773=CARTESIAN_POINT('Ctrl Pts',(0.120063451741682,2.94102929649084,9.92137455952712));
#99774=CARTESIAN_POINT('Ctrl Pts',(0.0266493151385261,2.94335985166373,
9.92640877274257));
#99775=CARTESIAN_POINT('Ctrl Pts',(-0.0666723188913893,2.94124443083088,
9.93144298595803));
#99776=CARTESIAN_POINT('Ctrl Pts',(-0.159986075560635,2.93912918856254,
9.93647677423115));
#99777=CARTESIAN_POINT('Ctrl Pts',(-0.253206900996718,2.93256872669209,
9.94151056250427));
#99778=CARTESIAN_POINT('Ctrl Pts',(-0.345882111839208,2.92159709143983,
9.9465443507774));
#99779=CARTESIAN_POINT('Ctrl Pts',(-0.438575431567919,2.91062331231228,
9.9515791226609));
#99780=CARTESIAN_POINT('Ctrl Pts',(-0.530722483815477,2.89523670056958,
9.95661389454439));
#99781=CARTESIAN_POINT('Ctrl Pts',(-0.62187770524449,2.87552292978509,9.96164866642789));
#99782=CARTESIAN_POINT('Ctrl Pts',(-0.713133140342792,2.85578748619597,
9.96668897340808));
#99783=CARTESIAN_POINT('Ctrl Pts',(-0.803394133122073,2.83171548172278,
9.97172928038827));
#99784=CARTESIAN_POINT('Ctrl Pts',(-0.892227585511837,2.80344322854088,
9.97676958736846));
#99785=CARTESIAN_POINT('Ctrl Pts',(-0.981115587214204,2.77515361442191,
9.98181298941333));
#99786=CARTESIAN_POINT('Ctrl Pts',(-1.06857388721276,2.74265877151817,9.98685639145821));
#99787=CARTESIAN_POINT('Ctrl Pts',(-1.1541888261347,2.70614340965622,9.99189979350308));
#99788=CARTESIAN_POINT('Ctrl Pts',(-1.23994259740693,2.66956883483947,9.99695137387954));
#99789=CARTESIAN_POINT('Ctrl Pts',(-1.32384664060778,2.62896091865108,10.002002954256));
#99790=CARTESIAN_POINT('Ctrl Pts',(-1.40551153516136,2.58455050725041,10.0070545346325));
#99791=CARTESIAN_POINT('Ctrl Pts',(-1.44717742823815,2.56189206309235,10.0096318796347));
#99792=CARTESIAN_POINT('Ctrl Pts',(-1.48826090623292,2.53824449666673,10.0122092246369));
#99793=CARTESIAN_POINT('Ctrl Pts',(-1.52871335004053,2.51364267416987,10.0147865696391));
#99794=CARTESIAN_POINT('Ctrl Pts',(-1.60800742955645,2.46541866875304,10.0198386302888));
#99795=CARTESIAN_POINT('Ctrl Pts',(-1.68515987810307,2.41335227616514,10.0248906909386));
#99796=CARTESIAN_POINT('Ctrl Pts',(-1.75977442314413,2.35765942825671,10.0299427515883));
#99797=CARTESIAN_POINT('Ctrl Pts',(-1.83428599117365,2.3020434431508,10.0349878397891));
#99798=CARTESIAN_POINT('Ctrl Pts',(-1.90626626284834,2.2428112115994,10.0400329279898));
#99799=CARTESIAN_POINT('Ctrl Pts',(-1.97534559114506,2.18022333616164,10.0450780161906));
#99800=CARTESIAN_POINT('Ctrl Pts',(-2.04435093153967,2.11770249590958,10.050117700814));
#99801=CARTESIAN_POINT('Ctrl Pts',(-2.11046117683206,2.05183345224717,10.0551573854375));
#99802=CARTESIAN_POINT('Ctrl Pts',(-2.17333848661742,1.98291800702588,10.0601970700609));
#99803=CARTESIAN_POINT('Ctrl Pts',(-2.23617041779166,1.91405229814351,10.0652331175394));
#99804=CARTESIAN_POINT('Ctrl Pts',(-2.29577375243484,1.84214488497022,10.0702691650179));
#99805=CARTESIAN_POINT('Ctrl Pts',(-2.35184713975556,1.76753473267814,10.0753052124964));
#99806=CARTESIAN_POINT('Ctrl Pts',(-2.40790010365047,1.69295175539695,10.0803394257119));
#99807=CARTESIAN_POINT('Ctrl Pts',(-2.46042540772903,1.6156683494408,10.0853736389273));
#99808=CARTESIAN_POINT('Ctrl Pts',(-2.50916235127285,1.53605608457338,10.0904078521428));
#99809=CARTESIAN_POINT('Ctrl Pts',(-2.55789518088868,1.45645053984681,10.0954416404159));
#99810=CARTESIAN_POINT('Ctrl Pts',(-2.60284005393637,1.37451690608349,10.100475428689));
#99811=CARTESIAN_POINT('Ctrl Pts',(-2.64378055671563,1.29065424027213,10.1055092169621));
#99812=CARTESIAN_POINT('Ctrl Pts',(-2.68472905933543,1.20677518756004,10.1105439888456));
#99813=CARTESIAN_POINT('Ctrl Pts',(-2.72167144314922,1.12096675360975,10.1155787607291));
#99814=CARTESIAN_POINT('Ctrl Pts',(-2.75443855814882,1.0336499549572,10.1206135326126));
#99815=CARTESIAN_POINT('Ctrl Pts',(-2.78724169645872,0.94623716249711,10.1256538395928));
#99816=CARTESIAN_POINT('Ctrl Pts',(-2.81586024702623,0.857313111868039,
10.130694146573));
#99817=CARTESIAN_POINT('Ctrl Pts',(-2.84017438558591,0.767315749520159,
10.1357344535532));
#99818=CARTESIAN_POINT('Ctrl Pts',(-2.86450345455197,0.67726312314598,10.1407778555981));
#99819=CARTESIAN_POINT('Ctrl Pts',(-2.88452275420294,0.586136306590904,
10.145821257643));
#99820=CARTESIAN_POINT('Ctrl Pts',(-2.90016367653447,0.494383099741565,
10.1508646596878));
#99821=CARTESIAN_POINT('Ctrl Pts',(-2.91582996203316,0.40248110678653,10.1559162400643));
#99822=CARTESIAN_POINT('Ctrl Pts',(-2.92710364230719,0.309951136205699,
10.1609678204407));
#99823=CARTESIAN_POINT('Ctrl Pts',(-2.93396802256676,0.21724558121101,10.1660194008172));
#99824=CARTESIAN_POINT('Ctrl Pts',(-2.93747026836645,0.169946680463769,
10.1685967458194));
#99825=CARTESIAN_POINT('Ctrl Pts',(-2.93982557003811,0.122602070252842,
10.1711740908216));
#99826=CARTESIAN_POINT('Ctrl Pts',(-2.94103692609892,0.0752715040544825,
10.1737514358238));
#99827=CARTESIAN_POINT('Ctrl Pts',(-2.94167494486841,0.0503425912581443,
10.175108918186));
#99828=CARTESIAN_POINT('Ctrl Pts',(-2.94199601583779,0.0254055319659734,
10.1764664005482));
#99829=CARTESIAN_POINT('Ctrl Pts',(-2.94199996315092,0.000465639337999335,
10.1778238829104));
#99830=CARTESIAN_POINT('',(-2.94199900023815,0.00242540671930449,11.1778238494769));
#99831=CARTESIAN_POINT('Ctrl Pts',(-2.941999963151,0.000465638797186323,
10.1778238829398));
#99832=CARTESIAN_POINT('Ctrl Pts',(-2.94201459018696,-0.0919509285156992,
10.1828541315448));
#99833=CARTESIAN_POINT('Ctrl Pts',(-2.9376703396371,-0.184540249590128,
10.1878843801497));
#99834=CARTESIAN_POINT('Ctrl Pts',(-2.92894441554051,-0.276854854886246,
10.1929146287547));
#99835=CARTESIAN_POINT('Ctrl Pts',(-2.92023046815804,-0.369042754331495,
10.1979379731225));
#99836=CARTESIAN_POINT('Ctrl Pts',(-2.90714683721503,-0.460956244507401,
10.2029613174902));
#99837=CARTESIAN_POINT('Ctrl Pts',(-2.88972272958064,-0.552147214196571,
10.207984661858));
#99838=CARTESIAN_POINT('Ctrl Pts',(-2.87169574924409,-0.646493383994814,
10.213181813531));
#99839=CARTESIAN_POINT('Ctrl Pts',(-2.84902243369197,-0.740065636381678,
10.2183789652039));
#99840=CARTESIAN_POINT('Ctrl Pts',(-2.8217937359022,-0.832372580052397,
10.2235761168768));
#99841=CARTESIAN_POINT('Ctrl Pts',(-2.79552210425161,-0.921435011228237,
10.2285905929799));
#99842=CARTESIAN_POINT('Ctrl Pts',(-2.76501010197364,-1.00931912350969,
10.2336050690829));
#99843=CARTESIAN_POINT('Ctrl Pts',(-2.73039119609779,-1.09559477740251,
10.238619545186));
#99844=CARTESIAN_POINT('Ctrl Pts',(-2.69578363629902,-1.18184215512096,
10.2436323778335));
#99845=CARTESIAN_POINT('Ctrl Pts',(-2.65707201338557,-1.266481705588,10.248645210481));
#99846=CARTESIAN_POINT('Ctrl Pts',(-2.61443869955637,-1.34910128836273,
10.2536580431285));
#99847=CARTESIAN_POINT('Ctrl Pts',(-2.5718071616241,-1.43171742960666,10.2586706669657));
#99848=CARTESIAN_POINT('Ctrl Pts',(-2.52525446385776,-1.51231337209969,
10.263683290803));
#99849=CARTESIAN_POINT('Ctrl Pts',(-2.47500934673925,-1.59050078074592,
10.2686959146402));
#99850=CARTESIAN_POINT('Ctrl Pts',(-2.42475194795028,-1.66870730113954,
10.2737097637386));
#99851=CARTESIAN_POINT('Ctrl Pts',(-2.37080058059845,-1.74450374171304,
10.2787236128371));
#99852=CARTESIAN_POINT('Ctrl Pts',(-2.31342711202098,-1.8175310168925,10.2837374619356));
#99853=CARTESIAN_POINT('Ctrl Pts',(-2.25598943837909,-1.89064001487909,
10.2887569218941));
#99854=CARTESIAN_POINT('Ctrl Pts',(-2.19512230010199,-1.96097331145026,
10.2937763818527));
#99855=CARTESIAN_POINT('Ctrl Pts',(-2.1311373570192,-2.0282055037686,10.2987958418112));
#99856=CARTESIAN_POINT('Ctrl Pts',(-2.06710957764277,-2.09548270633143,
10.3038186621706));
#99857=CARTESIAN_POINT('Ctrl Pts',(-1.99996016392209,-2.15965436438974,
10.3088414825301));
#99858=CARTESIAN_POINT('Ctrl Pts',(-1.93003544668252,-2.22043400589817,
10.3138643028895));
#99859=CARTESIAN_POINT('Ctrl Pts',(-1.86000269536138,-2.28130755229472,
10.3188948835347));
#99860=CARTESIAN_POINT('Ctrl Pts',(-1.78718643750142,-2.33877835063966,
10.3239254641799));
#99861=CARTESIAN_POINT('Ctrl Pts',(-1.71196329883252,-2.39260227857672,
10.328956044825));
#99862=CARTESIAN_POINT('Ctrl Pts',(-1.69322070776798,-2.40601304404945,
10.3302094638862));
#99863=CARTESIAN_POINT('Ctrl Pts',(-1.67432881903902,-2.41919763059321,
10.3314628829474));
#99864=CARTESIAN_POINT('Ctrl Pts',(-1.65529369110195,-2.43215270823978,
10.3327163020086));
#99865=CARTESIAN_POINT('Ctrl Pts',(-1.57857025215669,-2.48436975201975,
10.3377683626583));
#99866=CARTESIAN_POINT('Ctrl Pts',(-1.49923571003575,-2.53304664572001,
10.342820423308));
#99867=CARTESIAN_POINT('Ctrl Pts',(-1.41765067150871,-2.57791205698932,
10.3478724839577));
#99868=CARTESIAN_POINT('Ctrl Pts',(-1.33617823010909,-2.622715548616,10.3529175721585));
#99869=CARTESIAN_POINT('Ctrl Pts',(-1.25246185014146,-2.66371779843324,
10.3579626603593));
#99870=CARTESIAN_POINT('Ctrl Pts',(-1.16689177935965,-2.70069020349667,
10.3630077485601));
#99871=CARTESIAN_POINT('Ctrl Pts',(-1.08141335900638,-2.73762300900458,
10.3680474331835));
#99872=CARTESIAN_POINT('Ctrl Pts',(-0.994085599788648,-2.77053437354037,
10.3730871178069));
#99873=CARTESIAN_POINT('Ctrl Pts',(-0.905323085611669,-2.79924170279356,
10.3781268024303));
#99874=CARTESIAN_POINT('Ctrl Pts',(-0.816624631421044,-2.82792831394139,
10.3831628499088));
#99875=CARTESIAN_POINT('Ctrl Pts',(-0.72649390191969,-2.85241678407349,
10.3881988973874));
#99876=CARTESIAN_POINT('Ctrl Pts',(-0.635364204627327,-2.87257311960519,
10.3932349448659));
#99877=CARTESIAN_POINT('Ctrl Pts',(-0.544267699205483,-2.89272211366095,
10.3982691580813));
#99878=CARTESIAN_POINT('Ctrl Pts',(-0.452173382196428,-2.90854201187061,
10.4033033712968));
#99879=CARTESIAN_POINT('Ctrl Pts',(-0.359527412653276,-2.91994932140112,
10.4083375845122));
#99880=CARTESIAN_POINT('Ctrl Pts',(-0.266889263437537,-2.93135566803063,
10.4133713727854));
#99881=CARTESIAN_POINT('Ctrl Pts',(-0.173699995264317,-2.93835011241512,
10.4184051610585));
#99882=CARTESIAN_POINT('Ctrl Pts',(-0.0804124548388498,-2.94090085468837,
10.4234389493316));
#99883=CARTESIAN_POINT('Ctrl Pts',(0.0128933141230999,-2.94345209538079,
10.4284737212151));
#99884=CARTESIAN_POINT('Ctrl Pts',(0.106296949352597,-2.94155789773219,
10.4335084930986));
#99885=CARTESIAN_POINT('Ctrl Pts',(0.19934518054053,-2.93523857616298,10.4385432649821));
#99886=CARTESIAN_POINT('Ctrl Pts',(0.292495706523349,-2.9289123072967,10.4435835719623));
#99887=CARTESIAN_POINT('Ctrl Pts',(0.385289604563623,-2.91815123377434,
10.4486238789425));
#99888=CARTESIAN_POINT('Ctrl Pts',(0.477278612801847,-2.90302757922861,
10.4536641859227));
#99889=CARTESIAN_POINT('Ctrl Pts',(0.569324108061952,-2.88789463781024,
10.4587075879675));
#99890=CARTESIAN_POINT('Ctrl Pts',(0.660563295389788,-2.86839387501129,
10.4637509900124));
#99891=CARTESIAN_POINT('Ctrl Pts',(0.750560145639077,-2.84464821511874,
10.4687943920573));
#99892=CARTESIAN_POINT('Ctrl Pts',(0.840702933903302,-2.82086404949562,
10.4738459724338));
#99893=CARTESIAN_POINT('Ctrl Pts',(0.929598940040217,-2.79282137816211,
10.4788975528102));
#99894=CARTESIAN_POINT('Ctrl Pts',(1.01682944435761,-2.76069228294053,10.4839491331867));
#99895=CARTESIAN_POINT('Ctrl Pts',(1.06133494315002,-2.7442998360577,10.4865264781889));
#99896=CARTESIAN_POINT('Ctrl Pts',(1.10540724602397,-2.72684441622875,10.4891038231911));
#99897=CARTESIAN_POINT('Ctrl Pts',(1.14899320136477,-2.70835348933952,10.4916811681934));
#99898=CARTESIAN_POINT('Ctrl Pts',(1.23442952815362,-2.67210794051572,10.4967332288431));
#99899=CARTESIAN_POINT('Ctrl Pts',(1.31830261598088,-2.63175060298992,10.5017852894928));
#99900=CARTESIAN_POINT('Ctrl Pts',(1.40018912286786,-2.58743780991979,10.5068373501426));
#99901=CARTESIAN_POINT('Ctrl Pts',(1.48196261656491,-2.54318617381301,10.5118824383433));
#99902=CARTESIAN_POINT('Ctrl Pts',(1.5617545900905,-2.49499013947571,10.5169275265441));
#99903=CARTESIAN_POINT('Ctrl Pts',(1.63916158455543,-2.44305409267125,10.5219726147449));
#99904=CARTESIAN_POINT('Ctrl Pts',(1.71648567171248,-2.39117367233636,10.5270122993683));
#99905=CARTESIAN_POINT('Ctrl Pts',(1.79142949017917,-2.33556144778772,10.5320519839918));
#99906=CARTESIAN_POINT('Ctrl Pts',(1.86361509295472,-2.27646717202585,10.5370916686152));
#99907=CARTESIAN_POINT('Ctrl Pts',(1.93574859931567,-2.21741554465607,10.5421277160937));
#99908=CARTESIAN_POINT('Ctrl Pts',(2.00512750378226,-2.15488714163099,10.5471637635722));
#99909=CARTESIAN_POINT('Ctrl Pts',(2.07140458884285,-2.08917376714355,10.5521998110507));
#99910=CARTESIAN_POINT('Ctrl Pts',(2.13765753401841,-2.0234843272227,10.5572340242662));
#99911=CARTESIAN_POINT('Ctrl Pts',(2.20081058898781,-1.95461253290325,10.5622682374816));
#99912=CARTESIAN_POINT('Ctrl Pts',(2.26055204191595,-1.88288833067435,10.5673024506971));
#99913=CARTESIAN_POINT('Ctrl Pts',(2.32028845201586,-1.81117018274801,10.5723362389702));
#99914=CARTESIAN_POINT('Ctrl Pts',(2.37661354841684,-1.73660044712834,10.5773700272433));
#99915=CARTESIAN_POINT('Ctrl Pts',(2.4292554639561,-1.65954267520887,10.5824038155165));
#99916=CARTESIAN_POINT('Ctrl Pts',(2.48190766581084,-1.58246984607609,10.5874385874));
#99917=CARTESIAN_POINT('Ctrl Pts',(2.53087500717596,-1.50290838217252,10.5924733592835));
#99918=CARTESIAN_POINT('Ctrl Pts',(2.57592921058967,-1.42125040089031,10.597508131167));
#99919=CARTESIAN_POINT('Ctrl Pts',(2.6210329454177,-1.33950264695657,10.6025484381472));
#99920=CARTESIAN_POINT('Ctrl Pts',(2.66221473998287,-1.25565416448217,10.6075887451274));
#99921=CARTESIAN_POINT('Ctrl Pts',(2.69929267450065,-1.17012095844282,10.6126290521076));
#99922=CARTESIAN_POINT('Ctrl Pts',(2.73639337719623,-1.0845352296492,10.6176724541524));
#99923=CARTESIAN_POINT('Ctrl Pts',(2.76938504597688,-0.997263133048711,
10.6227158561973));
#99924=CARTESIAN_POINT('Ctrl Pts',(2.79813501309297,-0.908737832657571,
10.6277592582422));
#99925=CARTESIAN_POINT('Ctrl Pts',(2.82693160087547,-0.820068980502306,
10.6328108386186));
#99926=CARTESIAN_POINT('Ctrl Pts',(2.85147263839126,-0.730143295627111,
10.6378624189951));
#99927=CARTESIAN_POINT('Ctrl Pts',(2.87167616050725,-0.639405997136669,
10.6429139993716));
#99928=CARTESIAN_POINT('Ctrl Pts',(2.88198411225141,-0.593111312038459,
10.6454913443738));
#99929=CARTESIAN_POINT('Ctrl Pts',(2.89116379772252,-0.546605474376901,
10.648068689376));
#99930=CARTESIAN_POINT('Ctrl Pts',(2.89920953959236,-0.499948042837104,
10.6506460343781));
#99931=CARTESIAN_POINT('Ctrl Pts',(2.91498064352448,-0.408491069207567,
10.6556980950279));
#99932=CARTESIAN_POINT('Ctrl Pts',(2.9264482602729,-0.316122766635949,10.6607501556776));
#99933=CARTESIAN_POINT('Ctrl Pts',(2.93351468075643,-0.223283715900937,
10.6658022163273));
#99934=CARTESIAN_POINT('Ctrl Pts',(2.94057134873308,-0.130572794178757,
10.6708473045281));
#99935=CARTESIAN_POINT('Ctrl Pts',(2.94323885714092,-0.0373928544717329,
10.6758923927288));
#99936=CARTESIAN_POINT('Ctrl Pts',(2.94147066358924,0.0558062294362782,
10.6809374809296));
#99937=CARTESIAN_POINT('Ctrl Pts',(2.93970436387373,0.148905491807847,10.685977165553));
#99938=CARTESIAN_POINT('Ctrl Pts',(2.93351181366009,0.242023415793992,10.6910168501765));
#99939=CARTESIAN_POINT('Ctrl Pts',(2.92289842623039,0.334707021049594,10.6960565347999));
#99940=CARTESIAN_POINT('Ctrl Pts',(2.91229269849198,0.427323736463604,10.7010925822784));
#99941=CARTESIAN_POINT('Ctrl Pts',(2.89727252553217,0.519506316022336,10.7061286297569));
#99942=CARTESIAN_POINT('Ctrl Pts',(2.87789531241531,0.610804854907006,10.7111646772354));
#99943=CARTESIAN_POINT('Ctrl Pts',(2.85852515699718,0.702070140424593,10.7161988904509));
#99944=CARTESIAN_POINT('Ctrl Pts',(2.83480120620408,0.792451590753148,10.7212331036663));
#99945=CARTESIAN_POINT('Ctrl Pts',(2.80683215556769,0.881508508450836,10.7262673168818));
#99946=CARTESIAN_POINT('Ctrl Pts',(2.7788654658233,0.970557908776306,10.7313011051549));
#99947=CARTESIAN_POINT('Ctrl Pts',(2.74665452197561,1.05828257492776,10.736334893428));
#99948=CARTESIAN_POINT('Ctrl Pts',(2.71035784359889,1.14425712129835,10.7413686817011));
#99949=CARTESIAN_POINT('Ctrl Pts',(2.67405407279247,1.23024846723444,10.7464034535846));
#99950=CARTESIAN_POINT('Ctrl Pts',(2.63366315505343,1.31448860507283,10.7514382254681));
#99951=CARTESIAN_POINT('Ctrl Pts',(2.58939122436995,1.39657333755012,10.7564729973516));
#99952=CARTESIAN_POINT('Ctrl Pts',(2.54507062228231,1.47874831183814,10.7615133043318));
#99953=CARTESIAN_POINT('Ctrl Pts',(2.49686070164771,1.55876275909157,10.766553611312));
#99954=CARTESIAN_POINT('Ctrl Pts',(2.44501277546394,1.63623853023272,10.7715939182922));
#99955=CARTESIAN_POINT('Ctrl Pts',(2.39313301140087,1.7137618763577,10.7766373203371));
#99956=CARTESIAN_POINT('Ctrl Pts',(2.33761105861865,1.78874308609211,10.781680722382));
#99957=CARTESIAN_POINT('Ctrl Pts',(2.27873931833247,1.86083613439918,10.7867241244268));
#99958=CARTESIAN_POINT('Ctrl Pts',(2.21977211220626,1.93304608809045,10.7917757048033));
#99959=CARTESIAN_POINT('Ctrl Pts',(2.15744457093765,2.00235820046636,10.7968272851797));
#99960=CARTESIAN_POINT('Ctrl Pts',(2.09208667763803,2.06846255302084,10.8018788655562));
#99961=CARTESIAN_POINT('Ctrl Pts',(2.05874070922855,2.1021893691822,10.8044562105584));
#99962=CARTESIAN_POINT('Ctrl Pts',(2.02460646014681,2.13508180906774,10.8070335555606));
#99963=CARTESIAN_POINT('Ctrl Pts',(1.98973093565381,2.16710285951134,10.8096109005629));
#99964=CARTESIAN_POINT('Ctrl Pts',(1.92136862297226,2.22986988867118,10.8146629612126));
#99965=CARTESIAN_POINT('Ctrl Pts',(1.8499105348167,2.28951174638045,10.8197150218623));
#99966=CARTESIAN_POINT('Ctrl Pts',(1.77567423197015,2.34570778698397,10.8247670825121));
#99967=CARTESIAN_POINT('Ctrl Pts',(1.70154038411552,2.4018262703188,10.8298121707128));
#99968=CARTESIAN_POINT('Ctrl Pts',(1.62463629189386,2.45450812074662,10.8348572589136));
#99969=CARTESIAN_POINT('Ctrl Pts',(1.54531502676182,2.50347068448267,10.8399023471144));
#99970=CARTESIAN_POINT('Ctrl Pts',(1.46607871923073,2.55238080651919,10.8449420317378));
#99971=CARTESIAN_POINT('Ctrl Pts',(1.38443076070111,2.59757932766267,10.8499817163612));
#99972=CARTESIAN_POINT('Ctrl Pts',(1.30075495866742,2.63882559815955,10.8550214009847));
#99973=CARTESIAN_POINT('Ctrl Pts',(1.21713954553546,2.68004210118585,10.8600574484632));
#99974=CARTESIAN_POINT('Ctrl Pts',(1.13149959516399,2.71731182710678,10.8650934959417));
#99975=CARTESIAN_POINT('Ctrl Pts',(1.04424447257713,2.75043950696832,10.8701295434202));
#99976=CARTESIAN_POINT('Ctrl Pts',(0.95702113063717,2.78355512084375,10.8751637566356));
#99977=CARTESIAN_POINT('Ctrl Pts',(0.868184200127716,2.81253152818451,10.8801979698511));
#99978=CARTESIAN_POINT('Ctrl Pts',(0.778163068161974,2.83722157036576,10.8852321830665));
#99979=CARTESIAN_POINT('Ctrl Pts',(0.688149534958645,2.86190952843897,10.8902659713397));
#99980=CARTESIAN_POINT('Ctrl Pts',(0.596952427566446,2.88231172337541,10.8952997596128));
#99981=CARTESIAN_POINT('Ctrl Pts',(0.505015228620273,2.89833117825786,10.9003335478859));
#99982=CARTESIAN_POINT('Ctrl Pts',(0.41306006499664,2.91435376336773,10.9053683197694));
#99983=CARTESIAN_POINT('Ctrl Pts',(0.320364960359397,2.92599183172582,10.9104030916529));
#99984=CARTESIAN_POINT('Ctrl Pts',(0.227381355662065,2.93319991120573,10.9154378635364));
#99985=CARTESIAN_POINT('Ctrl Pts',(0.134295527218521,2.94041591505993,10.9204781705166));
#99986=CARTESIAN_POINT('Ctrl Pts',(0.0409210092667924,2.94319217407971,
10.9255184774968));
#99987=CARTESIAN_POINT('Ctrl Pts',(-0.0522882034994405,2.94153530384641,
10.930558784477));
#99988=CARTESIAN_POINT('Ctrl Pts',(-0.145554652569598,2.93987741619085,
10.9356021865218));
#99989=CARTESIAN_POINT('Ctrl Pts',(-0.238655151344086,2.93378100889542,
10.9406455885667));
#99990=CARTESIAN_POINT('Ctrl Pts',(-0.33114047449463,2.92330463451065,10.9456889906116));
#99991=CARTESIAN_POINT('Ctrl Pts',(-0.423775770943575,2.91281127173932,
10.950740570988));
#99992=CARTESIAN_POINT('Ctrl Pts',(-0.515793462184951,2.89792383336941,
10.9557921513645));
#99993=CARTESIAN_POINT('Ctrl Pts',(-0.606754338829127,2.87875201646686,
10.960843731741));
#99994=CARTESIAN_POINT('Ctrl Pts',(-0.653163094772113,2.86897044658276,
10.9634210767432));
#99995=CARTESIAN_POINT('Ctrl Pts',(-0.699296987943584,2.85807441689912,
10.9659984217454));
#99996=CARTESIAN_POINT('Ctrl Pts',(-0.745099452472975,2.84608341513816,
10.9685757667476));
#99997=CARTESIAN_POINT('Ctrl Pts',(-0.83488053669317,2.8225788908719,10.9736278273974));
#99998=CARTESIAN_POINT('Ctrl Pts',(-0.923709662851784,2.79477968405277,
10.9786798880471));
#99999=CARTESIAN_POINT('Ctrl Pts',(-1.01114532619468,2.76277924006147,10.9837319486969));
#100000=CARTESIAN_POINT('Ctrl Pts',(-1.09846031784684,2.73082296051673,
10.9887770368976));
#100001=CARTESIAN_POINT('Ctrl Pts',(-1.18438525459698,2.69467711691828,
10.9938221250984));
#100002=CARTESIAN_POINT('Ctrl Pts',(-1.26849135403759,2.65448557817365,
10.9988672132992));
#100003=CARTESIAN_POINT('Ctrl Pts',(-1.35250737104688,2.6143370868602,11.0039068979226));
#100004=CARTESIAN_POINT('Ctrl Pts',(-1.4347080241103,2.57015170373841,11.0089465825461));
#100005=CARTESIAN_POINT('Ctrl Pts',(-1.51468321123573,2.52212187841917,
11.0139862671695));
#100006=CARTESIAN_POINT('Ctrl Pts',(-1.59460068019626,2.4741267162683,11.019022314648));
#100007=CARTESIAN_POINT('Ctrl Pts',(-1.67229549580595,2.42229285477578,
11.0240583621265));
#100008=CARTESIAN_POINT('Ctrl Pts',(-1.74738187892169,2.36685879790411,
11.029094409605));
#100009=CARTESIAN_POINT('Ctrl Pts',(-1.8224409135706,2.31144493159701,11.0341286228205));
#100010=CARTESIAN_POINT('Ctrl Pts',(-1.89489304603083,2.25243373853424,
11.0391628360359));
#100011=CARTESIAN_POINT('Ctrl Pts',(-1.96438211143745,2.19010660020569,
11.0441970492514));
#100012=CARTESIAN_POINT('Ctrl Pts',(-2.03386531121143,2.12778472296528,
11.0492308375245));
#100013=CARTESIAN_POINT('Ctrl Pts',(-2.10038561058346,2.06214775376033,
11.0542646257976));
#100014=CARTESIAN_POINT('Ctrl Pts',(-2.1636214087255,1.99351608965282,11.0592984140708));
#100015=CARTESIAN_POINT('Ctrl Pts',(-2.22686956324487,1.92487101480704,
11.0643331859543));
#100016=CARTESIAN_POINT('Ctrl Pts',(-2.28683164115361,1.85323040989809,
11.0693679578378));
#100017=CARTESIAN_POINT('Ctrl Pts',(-2.34322504025233,1.77894924343963,
11.0744027297213));
#100018=CARTESIAN_POINT('Ctrl Pts',(-2.39968043678087,1.70458641420722,
11.0794430367014));
#100019=CARTESIAN_POINT('Ctrl Pts',(-2.45255905399601,1.62757758316637,
11.0844833436816));
#100020=CARTESIAN_POINT('Ctrl Pts',(-2.50162070399376,1.54830806151417,
11.0895236506618));
#100021=CARTESIAN_POINT('Ctrl Pts',(-2.55071248092226,1.46898986340307,
11.0945670527067));
#100022=CARTESIAN_POINT('Ctrl Pts',(-2.59598240905828,1.38740859925202,
11.0996104547515));
#100023=CARTESIAN_POINT('Ctrl Pts',(-2.63723655209584,1.30397368389459,
11.1046538567964));
#100024=CARTESIAN_POINT('Ctrl Pts',(-2.67855759244963,1.2204034712917,11.1097054371728));
#100025=CARTESIAN_POINT('Ctrl Pts',(-2.71584966976585,1.13497401330425,
11.1147570175493));
#100026=CARTESIAN_POINT('Ctrl Pts',(-2.74896727302769,1.04811398799116,
11.1198085979258));
#100027=CARTESIAN_POINT('Ctrl Pts',(-2.76586406232745,1.00379750969158,
11.122385942928));
#100028=CARTESIAN_POINT('Ctrl Pts',(-2.78167500073675,0.959108878155302,
11.1249632879302));
#100029=CARTESIAN_POINT('Ctrl Pts',(-2.79638585452687,0.914106204224653,
11.1275406329324));
#100030=CARTESIAN_POINT('Ctrl Pts',(-2.83087452683876,0.808600263067428,
11.1335830563351));
#100031=CARTESIAN_POINT('Ctrl Pts',(-2.85941468770278,0.701059871883707,
11.1396254797378));
#100032=CARTESIAN_POINT('Ctrl Pts',(-2.88180167265537,0.592100599122085,
11.1456679031406));
#100033=CARTESIAN_POINT('Ctrl Pts',(-2.90393651237435,0.484368537677298,
11.1516422705606));
#100034=CARTESIAN_POINT('Ctrl Pts',(-2.9200559557708,0.375249434849865,
11.1576166379806));
#100035=CARTESIAN_POINT('Ctrl Pts',(-2.93000827999668,0.265359151247653,
11.1635910054007));
#100036=CARTESIAN_POINT('Ctrl Pts',(-2.93791148095195,0.178094611364554,
11.1683352867594));
#100037=CARTESIAN_POINT('Ctrl Pts',(-2.94192651932955,0.0903441705776652,
11.1730795681182));
#100038=CARTESIAN_POINT('Ctrl Pts',(-2.94199900023815,0.00242540671930449,
11.1778238494769));
#100039=CARTESIAN_POINT('',(-2.9380472957324,-0.00162286220386191,12.1778238829104));
#100040=CARTESIAN_POINT('Ctrl Pts',(-2.93966322424947,0.00242286200588204,
11.1778238829104));
#100041=CARTESIAN_POINT('Ctrl Pts',(-2.93447022488878,-0.668394196839997,
11.2140510883126));
#100042=CARTESIAN_POINT('Ctrl Pts',(-2.37356269205824,-2.3282443459899,
11.3032665824432));
#100043=CARTESIAN_POINT('Ctrl Pts',(0.384920002627215,-3.45738444354686,
11.4454703653018));
#100044=CARTESIAN_POINT('Ctrl Pts',(3.11541549378935,-1.54785558110535,
11.6044352314866));
#100045=CARTESIAN_POINT('Ctrl Pts',(2.98787167512539,1.78165469490725,11.7634000976714));
#100046=CARTESIAN_POINT('Ctrl Pts',(0.119295491036091,3.47669946712688,
11.922364963856));
#100047=CARTESIAN_POINT('Ctrl Pts',(-2.4686154660414,2.17803105228073,12.0605062256025));
#100048=CARTESIAN_POINT('Ctrl Pts',(-2.93506592488484,0.594792322390365,
12.1456591986206));
#100049=CARTESIAN_POINT('Ctrl Pts',(-2.9380472957324,-0.00162286220386191,
12.1778238829104));
#100050=CARTESIAN_POINT('',(-2.94199950407814,-0.00170821660887623,13.1778238829104));
#100051=CARTESIAN_POINT('Ctrl Pts',(-2.9380472957324,-0.00162286220386191,
12.1778238829104));
#100052=CARTESIAN_POINT('Ctrl Pts',(-2.93997745262914,-0.38774553554093,
12.1986474873488));
#100053=CARTESIAN_POINT('Ctrl Pts',(-2.68948523871683,-1.75400101947579,
12.2724593805155));
#100054=CARTESIAN_POINT('Ctrl Pts',(-0.62100113389732,-3.42286841561285,
12.3992595624103));
#100055=CARTESIAN_POINT('Ctrl Pts',(2.54188151956999,-2.37497556605756,
12.558224428595));
#100056=CARTESIAN_POINT('Ctrl Pts',(3.37287704005805,0.851687191139494,
12.7171892947799));
#100057=CARTESIAN_POINT('Ctrl Pts',(1.10964157051829,3.29702383732351,12.8761541609645));
#100058=CARTESIAN_POINT('Ctrl Pts',(-2.05967935882506,2.73746974758015,
13.0296985506708));
#100059=CARTESIAN_POINT('Ctrl Pts',(-2.93954203332316,0.874568473683911,
13.1302546516486));
#100060=CARTESIAN_POINT('Ctrl Pts',(-2.94560408402907,-0.00168416984504231,
13.1778224638982));
#100061=CARTESIAN_POINT('',(-2.94199888698872,0.00255909303077856,14.1778238829104));
#100062=CARTESIAN_POINT('Ctrl Pts',(-2.94199950407814,-0.00170821660887623,
13.1778238829104));
#100063=CARTESIAN_POINT('Ctrl Pts',(-2.9419416035759,-0.101428151412843,
13.183243886385));
#100064=CARTESIAN_POINT('Ctrl Pts',(-2.93681405116898,-0.200999029500833,
13.1886638898595));
#100065=CARTESIAN_POINT('Ctrl Pts',(-2.92665961476548,-0.300045828667542,
13.194083893334));
#100066=CARTESIAN_POINT('Ctrl Pts',(-2.91719452331025,-0.392368728256213,
13.1991359539837));
#100067=CARTESIAN_POINT('Ctrl Pts',(-2.90333958420986,-0.484409209656405,
13.2041880146334));
#100068=CARTESIAN_POINT('Ctrl Pts',(-2.88511946458446,-0.575716662148895,
13.2092400752831));
#100069=CARTESIAN_POINT('Ctrl Pts',(-2.86692449090703,-0.666898099417747,
13.2142851634838));
#100070=CARTESIAN_POINT('Ctrl Pts',(-2.84437639424497,-0.75734808616101,
13.2193302516846));
#100071=CARTESIAN_POINT('Ctrl Pts',(-2.81755161946311,-0.846620854728244,
13.2243753398853));
#100072=CARTESIAN_POINT('Ctrl Pts',(-2.79075557554563,-0.935798007066586,
13.2294150245088));
#100073=CARTESIAN_POINT('Ctrl Pts',(-2.75969208521324,-1.02380002416844,
13.2344547091322));
#100074=CARTESIAN_POINT('Ctrl Pts',(-2.72448846328387,-1.11019215158148,
13.2394943937556));
#100075=CARTESIAN_POINT('Ctrl Pts',(-2.68931024784018,-1.19652192971826,
13.2445304412341));
#100076=CARTESIAN_POINT('Ctrl Pts',(-2.64999800690478,-1.2812437172495,
13.2495664887126));
#100077=CARTESIAN_POINT('Ctrl Pts',(-2.60672829362551,-1.36393973591659,
13.2546025361911));
#100078=CARTESIAN_POINT('Ctrl Pts',(-2.56347434033188,-1.44660563448424,
13.2596367494066));
#100079=CARTESIAN_POINT('Ctrl Pts',(-2.51626598398431,-1.52724683670544,
13.2646709626221));
#100080=CARTESIAN_POINT('Ctrl Pts',(-2.46532668784965,-1.60546825635896,
13.2697051758376));
#100081=CARTESIAN_POINT('Ctrl Pts',(-2.41439169154547,-1.68368307327412,
13.2747389641107));
#100082=CARTESIAN_POINT('Ctrl Pts',(-2.35972662421619,-1.7594781415096,
13.2797727523838));
#100083=CARTESIAN_POINT('Ctrl Pts',(-2.30159880163073,-1.83248655010943,
13.284806540657));
#100084=CARTESIAN_POINT('Ctrl Pts',(-2.24345962077456,-1.9055092246706,
13.2898413125405));
#100085=CARTESIAN_POINT('Ctrl Pts',(-2.18185661789604,-1.97574381084583,
13.294876084424));
#100086=CARTESIAN_POINT('Ctrl Pts',(-2.11709724939872,-2.04285663632776,
13.2999108563076));
#100087=CARTESIAN_POINT('Ctrl Pts',(-2.0522666861434,-2.11004324389683,
13.3049511632878));
#100088=CARTESIAN_POINT('Ctrl Pts',(-1.98427313965147,-2.17410091987957,
13.309991470268));
#100089=CARTESIAN_POINT('Ctrl Pts',(-1.91346055171977,-2.23473325410714,
13.3150317772482));
#100090=CARTESIAN_POINT('Ctrl Pts',(-1.84260448041671,-2.29540282039165,
13.3200751792931));
#100091=CARTESIAN_POINT('Ctrl Pts',(-1.76892627206687,-2.35264258513913,
13.325118581338));
#100092=CARTESIAN_POINT('Ctrl Pts',(-1.69280077672489,-2.40619814859866,
13.3301619833829));
#100093=CARTESIAN_POINT('Ctrl Pts',(-1.61655183702189,-2.45984055723772,
13.3352135637594));
#100094=CARTESIAN_POINT('Ctrl Pts',(-1.53784806233757,-2.50978659985422,
13.3402651441359));
#100095=CARTESIAN_POINT('Ctrl Pts',(-1.45709076095764,-2.55582677705902,
13.3453167245123));
#100096=CARTESIAN_POINT('Ctrl Pts',(-1.41588792707355,-2.57931673698771,
13.3478940695146));
#100097=CARTESIAN_POINT('Ctrl Pts',(-1.3741508982027,-2.60179072157022,
13.3504714145168));
#100098=CARTESIAN_POINT('Ctrl Pts',(-1.3319349167263,-2.62322575803252,
13.353048759519));
#100099=CARTESIAN_POINT('Ctrl Pts',(-1.24918398558434,-2.66524229215738,
13.3581008201687));
#100100=CARTESIAN_POINT('Ctrl Pts',(-1.16429426401653,-2.70341485725333,
13.3631528808185));
#100101=CARTESIAN_POINT('Ctrl Pts',(-1.07765798931138,-2.7375202753721,
13.3682049414682));
#100102=CARTESIAN_POINT('Ctrl Pts',(-0.991141283044934,-2.77157862392781,
13.373250029669));
#100103=CARTESIAN_POINT('Ctrl Pts',(-0.902883223327401,-2.80158081817814,
13.3782951178697));
#100104=CARTESIAN_POINT('Ctrl Pts',(-0.813300002922856,-2.82734983778903,
13.3833402060705));
#100105=CARTESIAN_POINT('Ctrl Pts',(-0.723812731258834,-2.85309125730959,
13.3883798906939));
#100106=CARTESIAN_POINT('Ctrl Pts',(-0.633003544705303,-2.87460839194949,
13.3934195753174));
#100107=CARTESIAN_POINT('Ctrl Pts',(-0.541306912108402,-2.89177295562838,
13.3984592599408));
#100108=CARTESIAN_POINT('Ctrl Pts',(-0.449676457053898,-2.90892513162618,
13.4034953074193));
#100109=CARTESIAN_POINT('Ctrl Pts',(-0.35716026443591,-2.92173089881644,
13.4085313548978));
#100110=CARTESIAN_POINT('Ctrl Pts',(-0.26420518213739,-2.93011256127333,
13.4135674023763));
#100111=CARTESIAN_POINT('Ctrl Pts',(-0.171283956563379,-2.93849117090481,
13.4186016155917));
#100112=CARTESIAN_POINT('Ctrl Pts',(-0.0779246009367638,-2.94244883710017,
13.4236358288072));
#100113=CARTESIAN_POINT('Ctrl Pts',(0.0154197241241465,-2.94195959049541,
13.4286700420226));
#100114=CARTESIAN_POINT('Ctrl Pts',(0.108756169909025,-2.94147038518838,
13.4337038302957));
#100115=CARTESIAN_POINT('Ctrl Pts',(0.202077143355244,-2.93653501590194,
13.4387376185689));
#100116=CARTESIAN_POINT('Ctrl Pts',(0.294929436653915,-2.92717963702179,
13.443771406842));
#100117=CARTESIAN_POINT('Ctrl Pts',(0.387799873441089,-2.91782243008545,
13.4488061787255));
#100118=CARTESIAN_POINT('Ctrl Pts',(0.480201006199476,-2.90404354319927,
13.4538409506089));
#100119=CARTESIAN_POINT('Ctrl Pts',(0.571685846608818,-2.88592087431155,
13.4588757224924));
#100120=CARTESIAN_POINT('Ctrl Pts',(0.663271263061884,-2.86777828183508,
13.4639160294726));
#100121=CARTESIAN_POINT('Ctrl Pts',(0.753937939861054,-2.84528246144413,
13.4689563364528));
#100122=CARTESIAN_POINT('Ctrl Pts',(0.843250469833347,-2.81856215917369,
13.473996643433));
#100123=CARTESIAN_POINT('Ctrl Pts',(0.932617843301892,-2.79182544896141,
13.4790400454778));
#100124=CARTESIAN_POINT('Ctrl Pts',(1.02062899572037,-2.76085923989495,
13.4840834475227));
#100125=CARTESIAN_POINT('Ctrl Pts',(1.10686711247742,-2.72584100697673,
13.4891268495676));
#100126=CARTESIAN_POINT('Ctrl Pts',(1.19324507212386,-2.69076598883339,
13.494178429944));
#100127=CARTESIAN_POINT('Ctrl Pts',(1.27784385347303,-2.65162601544494,
13.4992300103205));
#100128=CARTESIAN_POINT('Ctrl Pts',(1.36027007324264,-2.6086451134335,13.5042815906969));
#100129=CARTESIAN_POINT('Ctrl Pts',(1.4023243987688,-2.58671601308594,13.5068589356991));
#100130=CARTESIAN_POINT('Ctrl Pts',(1.443813630136,-2.56378779373677,13.5094362807013));
#100131=CARTESIAN_POINT('Ctrl Pts',(1.48468854817802,-2.53989446924652,
13.5120136257035));
#100132=CARTESIAN_POINT('Ctrl Pts',(1.56481075332511,-2.49305924759577,
13.5170656863532));
#100133=CARTESIAN_POINT('Ctrl Pts',(1.64285859476912,-2.44234491037467,
13.5221177470029));
#100134=CARTESIAN_POINT('Ctrl Pts',(1.71843209814497,-2.38796045278499,
13.5271698076527));
#100135=CARTESIAN_POINT('Ctrl Pts',(1.79390130103201,-2.33365105226236,
13.5322148958534));
#100136=CARTESIAN_POINT('Ctrl Pts',(1.86690259413939,-2.27568185380676,
13.5372599840542));
#100137=CARTESIAN_POINT('Ctrl Pts',(1.93706184631927,-2.21430698041942,
13.5423050722549));
#100138=CARTESIAN_POINT('Ctrl Pts',(2.00714595393684,-2.15299784302348,
13.5473447568784));
#100139=CARTESIAN_POINT('Ctrl Pts',(2.07439373838678,-2.0882905719314,13.5523844415018));
#100140=CARTESIAN_POINT('Ctrl Pts',(2.13846215253643,-2.02048103731989,
13.5574241261253));
#100141=CARTESIAN_POINT('Ctrl Pts',(2.20248432845386,-1.9527204409106,13.5624601736038));
#100142=CARTESIAN_POINT('Ctrl Pts',(2.26333139055242,-1.88186235313072,
13.5674962210823));
#100143=CARTESIAN_POINT('Ctrl Pts',(2.32069612831383,-1.80824043756056,
13.5725322685608));
#100144=CARTESIAN_POINT('Ctrl Pts',(2.3780399723051,-1.73464533705904,13.5775664817762));
#100145=CARTESIAN_POINT('Ctrl Pts',(2.4319037388655,-1.65828875871343,13.5826006949917));
#100146=CARTESIAN_POINT('Ctrl Pts',(2.48202029334157,-1.5795376739542,13.5876349082072));
#100147=CARTESIAN_POINT('Ctrl Pts',(2.5321326174355,-1.50079323664281,13.5926686964803));
#100148=CARTESIAN_POINT('Ctrl Pts',(2.57849811993762,-1.4196550697134,13.5977024847534));
#100149=CARTESIAN_POINT('Ctrl Pts',(2.62089346760739,-1.33651839921975,
13.6027362730265));
#100150=CARTESIAN_POINT('Ctrl Pts',(2.66329709939676,-1.25336548368603,
13.6077710449101));
#100151=CARTESIAN_POINT('Ctrl Pts',(2.70172883416518,-1.16821368498781,
13.6128058167936));
#100152=CARTESIAN_POINT('Ctrl Pts',(2.73601221261071,-1.0814810088231,13.6178405886771));
#100153=CARTESIAN_POINT('Ctrl Pts',(2.77033328130693,-0.994652981019935,
13.6228808956573));
#100154=CARTESIAN_POINT('Ctrl Pts',(2.80049672657653,-0.906241020367979,
13.6279212026375));
#100155=CARTESIAN_POINT('Ctrl Pts',(2.82637511242025,-0.816680919264938,
13.6329615096177));
#100156=CARTESIAN_POINT('Ctrl Pts',(2.85226938921632,-0.727065822641398,
13.6380049116626));
#100157=CARTESIAN_POINT('Ctrl Pts',(2.87387326539693,-0.636301613902794,
13.6430483137074));
#100158=CARTESIAN_POINT('Ctrl Pts',(2.89111034178361,-0.544834829679486,
13.6480917157523));
#100159=CARTESIAN_POINT('Ctrl Pts',(2.9083753696453,-0.453219723810628,
13.6531432961288));
#100160=CARTESIAN_POINT('Ctrl Pts',(2.92125939962182,-0.360900207487329,
13.6581948765052));
#100161=CARTESIAN_POINT('Ctrl Pts',(2.92973785784498,-0.268328314402158,
13.6632464568817));
#100162=CARTESIAN_POINT('Ctrl Pts',(2.93406361539006,-0.221097608720155,
13.6658238018839));
#100163=CARTESIAN_POINT('Ctrl Pts',(2.93724339923687,-0.173801218406553,
13.6684011468862));
#100164=CARTESIAN_POINT('Ctrl Pts',(2.93927916642012,-0.126498940108793,
13.6709784918884));
#100165=CARTESIAN_POINT('Ctrl Pts',(2.94326963695069,-0.0337779506314332,
13.6760305525381));
#100166=CARTESIAN_POINT('Ctrl Pts',(2.94287558236983,0.0592986537052232,
13.6810826131878));
#100167=CARTESIAN_POINT('Ctrl Pts',(2.93805622221528,0.152281433871947,
13.6861346738376));
#100168=CARTESIAN_POINT('Ctrl Pts',(2.93324351335512,0.245135886662127,
13.6911797620383));
#100169=CARTESIAN_POINT('Ctrl Pts',(2.92401765796111,0.337896332743346,
13.6962248502391));
#100170=CARTESIAN_POINT('Ctrl Pts',(2.91038980926908,0.430110634724023,
13.7012699384399));
#100171=CARTESIAN_POINT('Ctrl Pts',(2.89677655678059,0.522226169925629,
13.7063096230633));
#100172=CARTESIAN_POINT('Ctrl Pts',(2.87877074691709,0.61379628654003,13.7113493076867));
#100173=CARTESIAN_POINT('Ctrl Pts',(2.856435460979,0.704372385362796,13.7163889923102));
#100174=CARTESIAN_POINT('Ctrl Pts',(2.83411629443691,0.794883115333414,
13.7214250397887));
#100175=CARTESIAN_POINT('Ctrl Pts',(2.80747396842548,0.88440082327186,13.7264610872672));
#100176=CARTESIAN_POINT('Ctrl Pts',(2.77662274049373,0.972486584469465,
13.7314971347457));
#100177=CARTESIAN_POINT('Ctrl Pts',(2.74578274940346,1.06054026247942,13.7365313479611));
#100178=CARTESIAN_POINT('Ctrl Pts',(2.71073704855245,1.14716261096171,13.7415655611766));
#100179=CARTESIAN_POINT('Ctrl Pts',(2.67164959490775,1.23193037223264,13.746599774392));
#100180=CARTESIAN_POINT('Ctrl Pts',(2.63256544066916,1.3166909781828,13.7516335626651));
#100181=CARTESIAN_POINT('Ctrl Pts',(2.5894403981624,1.39959690477271,13.7566673509383));
#100182=CARTESIAN_POINT('Ctrl Pts',(2.54248589155738,1.48024642922444,13.7617011392114));
#100183=CARTESIAN_POINT('Ctrl Pts',(2.49552220996571,1.56091171272386,13.7667359110949));
#100184=CARTESIAN_POINT('Ctrl Pts',(2.44472780203968,1.63931933468942,13.7717706829784));
#100185=CARTESIAN_POINT('Ctrl Pts',(2.3903586188314,1.71509465434956,13.7768054548619));
#100186=CARTESIAN_POINT('Ctrl Pts',(2.33592966356338,1.79095327941667,13.7818457618421));
#100187=CARTESIAN_POINT('Ctrl Pts',(2.27791834762396,1.86417346406433,13.7868860688222));
#100188=CARTESIAN_POINT('Ctrl Pts',(2.21662211421995,1.93441215948181,13.7919263758024));
#100189=CARTESIAN_POINT('Ctrl Pts',(2.15528824108331,2.00469398586459,13.7969697778473));
#100190=CARTESIAN_POINT('Ctrl Pts',(2.09066574225995,2.0719903579793,13.8020131798922));
#100191=CARTESIAN_POINT('Ctrl Pts',(2.02308872155946,2.13599532412852,13.807056581937));
#100192=CARTESIAN_POINT('Ctrl Pts',(1.95540211862103,2.20010408010686,13.8121081623135));
#100193=CARTESIAN_POINT('Ctrl Pts',(1.88475176539237,2.26091048528984,13.8171597426899));
#100194=CARTESIAN_POINT('Ctrl Pts',(1.81150444114801,2.31814918840463,13.8222113230664));
#100195=CARTESIAN_POINT('Ctrl Pts',(1.77413324025682,2.34735269986285,13.8247886680686));
#100196=CARTESIAN_POINT('Ctrl Pts',(1.73608648663172,2.37562820340534,13.8273660130708));
#100197=CARTESIAN_POINT('Ctrl Pts',(1.69741551815161,2.40294497621941,13.829943358073));
#100198=CARTESIAN_POINT('Ctrl Pts',(1.62161345130467,2.45649077350038,13.8349954187228));
#100199=CARTESIAN_POINT('Ctrl Pts',(1.54313900094964,2.50654244875047,13.8400474793725));
#100200=CARTESIAN_POINT('Ctrl Pts',(1.4623479919621,2.5528224282947,13.8450995400222));
#100201=CARTESIAN_POINT('Ctrl Pts',(1.38166848424622,2.59903853592253,13.850144628223));
#100202=CARTESIAN_POINT('Ctrl Pts',(1.29867915315312,2.64149307266085,13.8551897164238));
#100203=CARTESIAN_POINT('Ctrl Pts',(1.21376620447723,2.67995067134993,13.8602348046245));
#100204=CARTESIAN_POINT('Ctrl Pts',(1.12894420241449,2.71836707975643,13.865274489248));
#100205=CARTESIAN_POINT('Ctrl Pts',(1.04220308046915,2.75279487680003,13.8703141738714));
#100206=CARTESIAN_POINT('Ctrl Pts',(0.953954178457664,2.78304427298654,
13.8753538584948));
#100207=CARTESIAN_POINT('Ctrl Pts',(0.865768965758247,2.81327183815657,
13.8803899059733));
#100208=CARTESIAN_POINT('Ctrl Pts',(0.776078554954986,2.83932685264125,
13.8854259534518));
#100209=CARTESIAN_POINT('Ctrl Pts',(0.68531385336078,2.86106779409223,13.8904620009303));
#100210=CARTESIAN_POINT('Ctrl Pts',(0.594582210695881,2.88280081691149,
13.8954962141458));
#100211=CARTESIAN_POINT('Ctrl Pts',(0.502777486209641,2.90022278484671,
13.9005304273613));
#100212=CARTESIAN_POINT('Ctrl Pts',(0.410344316623877,2.91324244473653,
13.9055646405767));
#100213=CARTESIAN_POINT('Ctrl Pts',(0.317918949402688,2.92626100562549,
13.9105984288499));
#100214=CARTESIAN_POINT('Ctrl Pts',(0.224865682536686,2.93487793550296,
13.915632217123));
#100215=CARTESIAN_POINT('Ctrl Pts',(0.131636739981672,2.93905354981616,
13.9206660053961));
#100216=CARTESIAN_POINT('Ctrl Pts',(0.0383895803403089,2.94322998005117,
13.9257007772796));
#100217=CARTESIAN_POINT('Ctrl Pts',(-0.0550328793156447,2.94296335168255,
13.9307355491631));
#100218=CARTESIAN_POINT('Ctrl Pts',(-0.148177083553659,2.93826607915443,
13.9357703210467));
#100219=CARTESIAN_POINT('Ctrl Pts',(-0.241423688096629,2.9335636425676,
13.9408106280268));
#100220=CARTESIAN_POINT('Ctrl Pts',(-0.334390982164589,2.92442086123227,
13.945850935007));
#100221=CARTESIAN_POINT('Ctrl Pts',(-0.426629513650132,2.91090213818374,
13.9508912419872));
#100222=CARTESIAN_POINT('Ctrl Pts',(-0.518924685380454,2.89737511379118,
13.9559346440321));
#100223=CARTESIAN_POINT('Ctrl Pts',(-0.610489767911087,2.87946688341686,
13.960978046077));
#100224=CARTESIAN_POINT('Ctrl Pts',(-0.700886656682442,2.85729275617402,
13.9660214481219));
#100225=CARTESIAN_POINT('Ctrl Pts',(-0.791430132167314,2.83508267158262,
13.9710730284983));
#100226=CARTESIAN_POINT('Ctrl Pts',(-0.880801206608649,2.80859300612958,
13.9761246088748));
#100227=CARTESIAN_POINT('Ctrl Pts',(-0.968578225849275,2.77798852056856,
13.9811761892513));
#100228=CARTESIAN_POINT('Ctrl Pts',(-1.01336255965936,2.76237393819486,
13.9837535342535));
#100229=CARTESIAN_POINT('Ctrl Pts',(-1.05773228245566,2.74568899705179,
13.9863308792557));
#100230=CARTESIAN_POINT('Ctrl Pts',(-1.10163377217885,2.72796023284706,
13.9889082242579));
#100231=CARTESIAN_POINT('Ctrl Pts',(-1.18768860321842,2.6932086602285,13.9939602849076));
#100232=CARTESIAN_POINT('Ctrl Pts',(-1.27225206830103,2.65431868816531,
13.9990123455573));
#100233=CARTESIAN_POINT('Ctrl Pts',(-1.35489816605842,2.61143925060713,
14.004064406207));
#100234=CARTESIAN_POINT('Ctrl Pts',(-1.43743020229941,2.56861899181,14.0091094944078));
#100235=CARTESIAN_POINT('Ctrl Pts',(-1.51804973857495,2.5218204113224,14.0141545826086));
#100236=CARTESIAN_POINT('Ctrl Pts',(-1.59634981641415,2.47124083481042,
14.0191996708093));
#100237=CARTESIAN_POINT('Ctrl Pts',(-1.67456603040223,2.42071543191092,
14.0242393554328));
#100238=CARTESIAN_POINT('Ctrl Pts',(-1.75046735260485,2.36641732205891,
14.0292790400562));
#100239=CARTESIAN_POINT('Ctrl Pts',(-1.82367154217766,2.30858963574113,
14.0343187246796));
#100240=CARTESIAN_POINT('Ctrl Pts',(-1.89682290022091,2.25080368371666,
14.0393547721581));
#100241=CARTESIAN_POINT('Ctrl Pts',(-1.96728064697167,2.18949349294338,
14.0443908196366));
#100242=CARTESIAN_POINT('Ctrl Pts',(-2.03469253379327,2.12494477408848,
14.0494268671151));
#100243=CARTESIAN_POINT('Ctrl Pts',(-2.10207986740462,2.06041956560156,
14.0544610803306));
#100244=CARTESIAN_POINT('Ctrl Pts',(-2.16642322439926,1.99265847931019,
14.059495293546));
#100245=CARTESIAN_POINT('Ctrl Pts',(-2.22740519191158,1.92198598097003,
14.0645295067615));
#100246=CARTESIAN_POINT('Ctrl Pts',(-2.28838201188272,1.85131944815723,
14.0695632950346));
#100247=CARTESIAN_POINT('Ctrl Pts',(-2.34599771638028,1.77774232841077,
14.0745970833077));
#100248=CARTESIAN_POINT('Ctrl Pts',(-2.39997414569756,1.70161338146573,
14.0796308715808));
#100249=CARTESIAN_POINT('Ctrl Pts',(-2.45396112209656,1.62546955880117,
14.0846656434643));
#100250=CARTESIAN_POINT('Ctrl Pts',(-2.50430715436889,1.54677328129533,
14.0897004153478));
#100251=CARTESIAN_POINT('Ctrl Pts',(-2.55077716821508,1.46591262976777,
14.0947351872313));
#100252=CARTESIAN_POINT('Ctrl Pts',(-2.59729826998059,1.38496308215219,
14.0997754942115));
#100253=CARTESIAN_POINT('Ctrl Pts',(-2.6399346257115,1.30184479663781,14.1048158011917));
#100254=CARTESIAN_POINT('Ctrl Pts',(-2.67849709557925,1.21697054564747,
14.1098561081719));
#100255=CARTESIAN_POINT('Ctrl Pts',(-2.71708324522266,1.13204417654257,
14.1148995102168));
#100256=CARTESIAN_POINT('Ctrl Pts',(-2.75159036456666,1.04536010783004,
14.1199429122616));
#100257=CARTESIAN_POINT('Ctrl Pts',(-2.78187825939687,0.957349126439784,
14.1249863143065));
#100258=CARTESIAN_POINT('Ctrl Pts',(-2.81221526878206,0.869195427300135,
14.130037894683));
#100259=CARTESIAN_POINT('Ctrl Pts',(-2.83831927037654,0.779710945833389,
14.1350894750594));
#100260=CARTESIAN_POINT('Ctrl Pts',(-2.86010055486284,0.689339405571228,
14.1401410554359));
#100261=CARTESIAN_POINT('Ctrl Pts',(-2.87121348993049,0.643231332398185,
14.1427184004381));
#100262=CARTESIAN_POINT('Ctrl Pts',(-2.88120200867619,0.596892482010356,
14.1452957454403));
#100263=CARTESIAN_POINT('Ctrl Pts',(-2.89005939699962,0.550382305142697,
14.1478730904426));
#100264=CARTESIAN_POINT('Ctrl Pts',(-2.91574538419712,0.415505097104356,
14.155347263225));
#100265=CARTESIAN_POINT('Ctrl Pts',(-2.93199546254514,0.278777808809255,
14.1628214360074));
#100266=CARTESIAN_POINT('Ctrl Pts',(-2.93860597986145,0.141275953801512,
14.1702956087899));
#100267=CARTESIAN_POINT('Ctrl Pts',(-2.940825435574,0.0951102359037864,
14.1728050334967));
#100268=CARTESIAN_POINT('Ctrl Pts',(-2.94195861445419,0.0488574301164584,
14.1753144582036));
#100269=CARTESIAN_POINT('Ctrl Pts',(-2.94199888698872,0.00255909303077856,
14.1778238829104));
#100270=CARTESIAN_POINT('',(-2.94153552810316,0.000339057197988907,15.1778238581128));
#100271=CARTESIAN_POINT('Ctrl Pts',(-2.94332536232247,0.00254738520742678,
14.1778245797126));
#100272=CARTESIAN_POINT('Ctrl Pts',(-2.93605737211391,-0.791240222849468,
14.2208290386842));
#100273=CARTESIAN_POINT('Ctrl Pts',(-2.19483961771011,-2.57505010203599,
14.3168217863839));
#100274=CARTESIAN_POINT('Ctrl Pts',(0.822272561487176,-3.38016840313126,
14.4658028228121));
#100275=CARTESIAN_POINT('Ctrl Pts',(3.28723225708272,-1.1383209946658,14.6247676889968));
#100276=CARTESIAN_POINT('Ctrl Pts',(2.73653030818804,2.14780643244915,14.7837325551815));
#100277=CARTESIAN_POINT('Ctrl Pts',(-0.32462689424278,3.46356578953478,
14.9426974213664));
#100278=CARTESIAN_POINT('Ctrl Pts',(-2.60817372378361,1.92514024732049,
15.0740611115662));
#100279=CARTESIAN_POINT('Ctrl Pts',(-2.93766532742435,0.471430358787691,
15.152436513038));
#100280=CARTESIAN_POINT('Ctrl Pts',(-2.93718401591717,0.000342867480166743,
15.1778236257814));
#100281=CARTESIAN_POINT('',(-2.94199875963773,-0.00270153476367689,16.1778238829104));
#100282=CARTESIAN_POINT('Ctrl Pts',(-2.94199998050915,0.000338650512990829,
15.1778238829104));
#100283=CARTESIAN_POINT('Ctrl Pts',(-2.94201116901371,-0.0968606122596855,
15.1830534200964));
#100284=CARTESIAN_POINT('Ctrl Pts',(-2.93720105751752,-0.193984951321332,
15.1882829572824));
#100285=CARTESIAN_POINT('Ctrl Pts',(-2.92761780337622,-0.290547754000271,
15.1935124944683));
#100286=CARTESIAN_POINT('Ctrl Pts',(-2.91802323889267,-0.387224521970202,
15.1987482036554));
#100287=CARTESIAN_POINT('Ctrl Pts',(-2.903644344505,-0.48333804304514,15.2039839128426));
#100288=CARTESIAN_POINT('Ctrl Pts',(-2.88458066522055,-0.578410222796756,
15.2092196220297));
#100289=CARTESIAN_POINT('Ctrl Pts',(-2.8654748648745,-0.673692463842373,
15.2144668994784));
#100290=CARTESIAN_POINT('Ctrl Pts',(-2.84166367815638,-0.767928381784394,
15.2197141769271));
#100291=CARTESIAN_POINT('Ctrl Pts',(-2.81329716202206,-0.860652704729742,
15.2249614543758));
#100292=CARTESIAN_POINT('Ctrl Pts',(-2.78489523094661,-0.953492791853635,
15.2302152829294));
#100293=CARTESIAN_POINT('Ctrl Pts',(-2.75192676404131,-1.04481715309615,
15.235469111483));
#100294=CARTESIAN_POINT('Ctrl Pts',(-2.71459004383728,-1.13418027398625,
15.2407229400366));
#100295=CARTESIAN_POINT('Ctrl Pts',(-2.67717267079504,-1.2237364324354,
15.245988117637));
#100296=CARTESIAN_POINT('Ctrl Pts',(-2.63536836176582,-1.31132253321761,
15.2512532952374));
#100297=CARTESIAN_POINT('Ctrl Pts',(-2.58942164066141,-1.39651694113404,
15.2565184728377));
#100298=CARTESIAN_POINT('Ctrl Pts',(-2.57747013401016,-1.41867742415413,
15.2578880331371));
#100299=CARTESIAN_POINT('Ctrl Pts',(-2.56523857520824,-1.44067623877505,
15.2592575934365));
#100300=CARTESIAN_POINT('Ctrl Pts',(-2.55273173589492,-1.46250630239836,
15.2606271537359));
#100301=CARTESIAN_POINT('Ctrl Pts',(-2.50659626396544,-1.54303346535945,
15.2656792143856));
#100302=CARTESIAN_POINT('Ctrl Pts',(-2.45656375314834,-1.62152013566208,
15.2707312750353));
#100303=CARTESIAN_POINT('Ctrl Pts',(-2.40283970639844,-1.69756453348762,
15.2757833356851));
#100304=CARTESIAN_POINT('Ctrl Pts',(-2.34918980526959,-1.77350398093349,
15.2808284238858));
#100305=CARTESIAN_POINT('Ctrl Pts',(-2.29185874625095,-1.84700749402453,
15.2858735120866));
#100306=CARTESIAN_POINT('Ctrl Pts',(-2.23109738351376,-1.91769874205467,
15.2909186002873));
#100307=CARTESIAN_POINT('Ctrl Pts',(-2.17040109966286,-1.98831427572481,
15.2959582849108));
#100308=CARTESIAN_POINT('Ctrl Pts',(-2.10628210285226,-2.05612319618261,
15.3009979695342));
#100309=CARTESIAN_POINT('Ctrl Pts',(-2.03903326362832,-2.12077989188347,
15.3060376541577));
#100310=CARTESIAN_POINT('Ctrl Pts',(-1.97183295795236,-2.18538992478866,
15.3110737016362));
#100311=CARTESIAN_POINT('Ctrl Pts',(-1.90150761891054,-2.24685194768499,
15.3161097491147));
#100312=CARTESIAN_POINT('Ctrl Pts',(-1.82838822120408,-2.30485585505085,
15.3211457965932));
#100313=CARTESIAN_POINT('Ctrl Pts',(-1.75529545553588,-2.36283863584389,
15.3261800098086));
#100314=CARTESIAN_POINT('Ctrl Pts',(-1.67941100063365,-2.41736552745628,
15.3312142230241));
#100315=CARTESIAN_POINT('Ctrl Pts',(-1.60109948689982,-2.46816620855427,
15.3362484362395));
#100316=CARTESIAN_POINT('Ctrl Pts',(-1.52279458350912,-2.51896260152248,
15.3412822245127));
#100317=CARTESIAN_POINT('Ctrl Pts',(-1.44206340145464,-2.56603316768702,
15.3463160127858));
#100318=CARTESIAN_POINT('Ctrl Pts',(-1.35929920625946,-2.60915113932911,
15.3513498010589));
#100319=CARTESIAN_POINT('Ctrl Pts',(-1.27651883880636,-2.65227753629276,
15.3563845729424));
#100320=CARTESIAN_POINT('Ctrl Pts',(-1.19170506344987,-2.69144959991829,
15.3614193448259));
#100321=CARTESIAN_POINT('Ctrl Pts',(-1.10527433282822,-2.72648723620543,
15.3664541167094));
#100322=CARTESIAN_POINT('Ctrl Pts',(-1.01874858251935,-2.76156339195454,
15.3714944236896));
#100323=CARTESIAN_POINT('Ctrl Pts',(-0.930602740949971,-2.79249588022971,
15.3765347306698));
#100324=CARTESIAN_POINT('Ctrl Pts',(-0.841271473842247,-2.81915347352699,
15.38157503765));
#100325=CARTESIAN_POINT('Ctrl Pts',(-0.751885351732374,-2.84582743625891,
15.3866184396949));
#100326=CARTESIAN_POINT('Ctrl Pts',(-0.661312785928075,-2.86822117149054,
15.3916618417397));
#100327=CARTESIAN_POINT('Ctrl Pts',(-0.56999963057609,-2.88625439300543,
15.3967052437846));
#100328=CARTESIAN_POINT('Ctrl Pts',(-0.478538402701799,-2.90431685701647,
15.4017568241611));
#100329=CARTESIAN_POINT('Ctrl Pts',(-0.38633462669517,-2.91800462574334,
15.4068084045375));
#100330=CARTESIAN_POINT('Ctrl Pts',(-0.293840105025006,-2.92728918842654,
15.411859984914));
#100331=CARTESIAN_POINT('Ctrl Pts',(-0.24664887467922,-2.93202622504591,
15.4144373299162));
#100332=CARTESIAN_POINT('Ctrl Pts',(-0.199381979216108,-2.93561790365231,
15.4170146749183));
#100333=CARTESIAN_POINT('Ctrl Pts',(-0.152099230062562,-2.93806566029665,
15.4195920199205));
#100334=CARTESIAN_POINT('Ctrl Pts',(-0.0594165212255564,-2.94286370441279,
15.4246440805702));
#100335=CARTESIAN_POINT('Ctrl Pts',(0.0336599841104272,-2.94328048767179,
15.42969614122));
#100336=CARTESIAN_POINT('Ctrl Pts',(0.126681219222801,-2.93927131593806,
15.4347482018697));
#100337=CARTESIAN_POINT('Ctrl Pts',(0.219574073886284,-2.93526767734163,
15.4397932900704));
#100338=CARTESIAN_POINT('Ctrl Pts',(0.312411369872398,-2.92685024074075,
15.4448383782712));
#100339=CARTESIAN_POINT('Ctrl Pts',(0.404740889785965,-2.91402622022096,
15.449883466472));
#100340=CARTESIAN_POINT('Ctrl Pts',(0.496971519515494,-2.90121593495887,
15.4549231510954));
#100341=CARTESIAN_POINT('Ctrl Pts',(0.588695016458655,-2.88400850766301,
15.4599628357188));
#100342=CARTESIAN_POINT('Ctrl Pts',(0.679462248909604,-2.86246310933551,
15.4650025203423));
#100343=CARTESIAN_POINT('Ctrl Pts',(0.770163974567093,-2.84093326034139,
15.4700385678208));
#100344=CARTESIAN_POINT('Ctrl Pts',(0.859910376427894,-2.8150717653556,
15.4750746152993));
#100345=CARTESIAN_POINT('Ctrl Pts',(0.948261551100615,-2.78498905396489,
15.4801106627778));
#100346=CARTESIAN_POINT('Ctrl Pts',(1.03658054591503,-2.75491729950139,
15.4851448759933));
#100347=CARTESIAN_POINT('Ctrl Pts',(1.1235049029231,-2.72062752604819,15.4901790892087));
#100348=CARTESIAN_POINT('Ctrl Pts',(1.20860995221491,-2.68227999720519,
15.4952133024242));
#100349=CARTESIAN_POINT('Ctrl Pts',(1.29370781771518,-2.64393570531059,
15.5002470906973));
#100350=CARTESIAN_POINT('Ctrl Pts',(1.3769862758226,-2.60153452171618,15.5052808789704));
#100351=CARTESIAN_POINT('Ctrl Pts',(1.45804177721246,-2.55528436302169,
15.5103146672436));
#100352=CARTESIAN_POINT('Ctrl Pts',(1.53911311697834,-2.5090251669714,15.5153494391271));
#100353=CARTESIAN_POINT('Ctrl Pts',(1.61796025167456,-2.45891572266182,
15.5203842110106));
#100354=CARTESIAN_POINT('Ctrl Pts',(1.6942063250659,-2.40520870780618,15.5254189828941));
#100355=CARTESIAN_POINT('Ctrl Pts',(1.77053622139873,-2.35144264886128,
15.5304592898742));
#100356=CARTESIAN_POINT('Ctrl Pts',(1.84425898462451,-2.29407138079774,
15.5354995968544));
#100357=CARTESIAN_POINT('Ctrl Pts',(1.91502898781745,-2.23338934711771,
15.5405399038346));
#100358=CARTESIAN_POINT('Ctrl Pts',(1.98584244823186,-2.17267005086233,
15.5455833058795));
#100359=CARTESIAN_POINT('Ctrl Pts',(2.0536992160296,-2.10863624636823,15.5506267079244));
#100360=CARTESIAN_POINT('Ctrl Pts',(2.11829044062721,-2.04161935951523,
15.5556701099692));
#100361=CARTESIAN_POINT('Ctrl Pts',(2.18298640572505,-1.97449379873173,
15.5607216903457));
#100362=CARTESIAN_POINT('Ctrl Pts',(2.24440596360011,-1.90437583218216,
15.5657732707222));
#100363=CARTESIAN_POINT('Ctrl Pts',(2.3022805779055,-1.8316299136559,15.5708248510986));
#100364=CARTESIAN_POINT('Ctrl Pts',(2.33180853486532,-1.79451453281014,
15.5734021961008));
#100365=CARTESIAN_POINT('Ctrl Pts',(2.36041440409863,-1.75671554066214,
15.5759795411031));
#100366=CARTESIAN_POINT('Ctrl Pts',(2.38806701673623,-1.71828400550564,
15.5785568861053));
#100367=CARTESIAN_POINT('Ctrl Pts',(2.44227112059056,-1.64295127111975,
15.583608946755));
#100368=CARTESIAN_POINT('Ctrl Pts',(2.49300451506521,-1.56491581610779,
15.5886610074047));
#100369=CARTESIAN_POINT('Ctrl Pts',(2.53998653730253,-1.48453103380222,
15.5937130680545));
#100370=CARTESIAN_POINT('Ctrl Pts',(2.58690371872048,-1.40425719212675,
15.5987581562552));
#100371=CARTESIAN_POINT('Ctrl Pts',(2.6300795936601,-1.32164084635823,15.603803244456));
#100372=CARTESIAN_POINT('Ctrl Pts',(2.66927543951866,-1.23706613727096,
15.6088483326568));
#100373=CARTESIAN_POINT('Ctrl Pts',(2.70842930438981,-1.15258201252289,
15.6138880172802));
#100374=CARTESIAN_POINT('Ctrl Pts',(2.74361142736925,-1.06614409452229,
15.6189277019036));
#100375=CARTESIAN_POINT('Ctrl Pts',(2.7746284428391,-0.97816205415477,15.6239673865271));
#100376=CARTESIAN_POINT('Ctrl Pts',(2.80562307330092,-0.890243510505094,
15.6290034340056));
#100377=CARTESIAN_POINT('Ctrl Pts',(2.83245842371054,-0.800783477315732,
15.6340394814841));
#100378=CARTESIAN_POINT('Ctrl Pts',(2.85498922330515,-0.710211612698273,
15.6390755289626));
#100379=CARTESIAN_POINT('Ctrl Pts',(2.87751181658058,-0.61967273677373,
15.644109742178));
#100380=CARTESIAN_POINT('Ctrl Pts',(2.8957328665444,-0.528023264636981,
15.6491439553935));
#100381=CARTESIAN_POINT('Ctrl Pts',(2.9095572501116,-0.435707021200076,
15.654178168609));
#100382=CARTESIAN_POINT('Ctrl Pts',(2.9233804667505,-0.343398570257963,
15.6592119568821));
#100383=CARTESIAN_POINT('Ctrl Pts',(2.93280768924939,-0.250423899347588,
15.6642457451552));
#100384=CARTESIAN_POINT('Ctrl Pts',(2.93779529508008,-0.157234869559293,
15.6692795334283));
#100385=CARTESIAN_POINT('Ctrl Pts',(2.94278387549704,-0.0640276304835271,
15.6743143053118));
#100386=CARTESIAN_POINT('Ctrl Pts',(2.94333109299994,0.0293936069942164,
15.6793490771953));
#100387=CARTESIAN_POINT('Ctrl Pts',(2.93944541048168,0.122575196504791,
15.6843838490788));
#100388=CARTESIAN_POINT('Ctrl Pts',(2.93555545614557,0.215859227420616,
15.689424156059));
#100389=CARTESIAN_POINT('Ctrl Pts',(2.92722289237642,0.308902639857464,
15.6944644630392));
#100390=CARTESIAN_POINT('Ctrl Pts',(2.91450820443112,0.401255437724781,
15.6995047700194));
#100391=CARTESIAN_POINT('Ctrl Pts',(2.90178570886979,0.493664946003564,
15.7045481720643));
#100392=CARTESIAN_POINT('Ctrl Pts',(2.88467581350687,0.585382559004776,
15.7095915741092));
#100393=CARTESIAN_POINT('Ctrl Pts',(2.86329000659806,0.675969184294437,
15.714634976154));
#100394=CARTESIAN_POINT('Ctrl Pts',(2.84186952067322,0.766702703972665,
15.7196865565305));
#100395=CARTESIAN_POINT('Ctrl Pts',(2.81615940307745,0.856301148020783,
15.724738136907));
#100396=CARTESIAN_POINT('Ctrl Pts',(2.78632073513565,0.944341442992474,
15.7297897172834));
#100397=CARTESIAN_POINT('Ctrl Pts',(2.77109687726129,0.989260101576055,
15.7323670622856));
#100398=CARTESIAN_POINT('Ctrl Pts',(2.75479908941012,1.03377348914806,15.7349444072878));
#100399=CARTESIAN_POINT('Ctrl Pts',(2.73745343916241,1.07782775452198,15.73752175229));
#100400=CARTESIAN_POINT('Ctrl Pts',(2.70345283893801,1.16418205336739,15.7425738129398));
#100401=CARTESIAN_POINT('Ctrl Pts',(2.66530100448761,1.24908109389148,15.7476258735895));
#100402=CARTESIAN_POINT('Ctrl Pts',(2.62314315306257,1.33209759347465,15.7526779342392));
#100403=CARTESIAN_POINT('Ctrl Pts',(2.58104348452323,1.41499952034257,15.75772302244));
#100404=CARTESIAN_POINT('Ctrl Pts',(2.53494898479218,1.49602367636708,15.7627681106407));
#100405=CARTESIAN_POINT('Ctrl Pts',(2.48505342689035,1.57476139954614,15.7678131988415));
#100406=CARTESIAN_POINT('Ctrl Pts',(2.43521130997793,1.65341479013114,15.772852883465));
#100407=CARTESIAN_POINT('Ctrl Pts',(2.38157646343374,1.72978624213928,15.7778925680884));
#100408=CARTESIAN_POINT('Ctrl Pts',(2.32438867868526,1.80349141123538,15.7829322527118));
#100409=CARTESIAN_POINT('Ctrl Pts',(2.26724216641271,1.87714338724433,15.7879683001903));
#100410=CARTESIAN_POINT('Ctrl Pts',(2.2065480841259,1.94813255504624,15.7930043476688));
#100411=CARTESIAN_POINT('Ctrl Pts',(2.14258906308966,2.01610419044467,15.7980403951473));
#100412=CARTESIAN_POINT('Ctrl Pts',(2.07865333763776,2.08405106875741,15.8030746083628));
#100413=CARTESIAN_POINT('Ctrl Pts',(2.01145534001924,2.14898227482019,15.8081088215782));
#100414=CARTESIAN_POINT('Ctrl Pts',(1.94131675858346,2.21057758127667,15.8131430347937));
#100415=CARTESIAN_POINT('Ctrl Pts',(1.87118409760659,2.27216768841954,15.8181768230668));
#100416=CARTESIAN_POINT('Ctrl Pts',(1.79811168028328,2.33042216276658,15.8232106113399));
#100417=CARTESIAN_POINT('Ctrl Pts',(1.72245582958902,2.3850597298841,15.828244399613));
#100418=CARTESIAN_POINT('Ctrl Pts',(1.64678519561889,2.43970797327081,15.8332791714965));
#100419=CARTESIAN_POINT('Ctrl Pts',(1.56853048612015,2.49073764601253,15.83831394338));
#100420=CARTESIAN_POINT('Ctrl Pts',(1.4880777193723,2.53791030202167,15.8433487152635));
#100421=CARTESIAN_POINT('Ctrl Pts',(1.40753650495438,2.58513481841653,15.8483890222437));
#100422=CARTESIAN_POINT('Ctrl Pts',(1.32479279354661,2.62849362881679,15.8534293292239));
#100423=CARTESIAN_POINT('Ctrl Pts',(1.2402576942461,2.66779400476561,15.8584696362041));
#100424=CARTESIAN_POINT('Ctrl Pts',(1.15567068509158,2.70711851361066,15.863513038249));
#100425=CARTESIAN_POINT('Ctrl Pts',(1.06929050916347,2.74237945886987,15.8685564402938));
#100426=CARTESIAN_POINT('Ctrl Pts',(0.981546715764777,2.77343289891271,
15.8735998423387));
#100427=CARTESIAN_POINT('Ctrl Pts',(0.893660637886069,2.80453669491121,
15.8786514227152));
#100428=CARTESIAN_POINT('Ctrl Pts',(0.804406952963284,2.83141923664927,
15.8837030030916));
#100429=CARTESIAN_POINT('Ctrl Pts',(0.714228586201955,2.85398695278236,
15.8887545834681));
#100430=CARTESIAN_POINT('Ctrl Pts',(0.668219071246137,2.86550112974337,
15.8913319284703));
#100431=CARTESIAN_POINT('Ctrl Pts',(0.621968992648011,2.87589294342898,
15.8939092734725));
#100432=CARTESIAN_POINT('Ctrl Pts',(0.57553774039783,2.88515516209748,15.8964866184747));
#100433=CARTESIAN_POINT('Ctrl Pts',(0.484524118935146,2.90331077976762,
15.9015386791245));
#100434=CARTESIAN_POINT('Ctrl Pts',(0.392487023563346,2.91718819413048,
15.9065907397742));
#100435=CARTESIAN_POINT('Ctrl Pts',(0.299864331334389,2.9266782164757,15.911642800424));
#100436=CARTESIAN_POINT('Ctrl Pts',(0.207369469517258,2.93615514145314,
15.9166878886247));
#100437=CARTESIAN_POINT('Ctrl Pts',(0.114291054966479,2.94125666178667,
15.9217329768255));
#100438=CARTESIAN_POINT('Ctrl Pts',(0.0210775916233303,2.94192449514452,
15.9267780650263));
#100439=CARTESIAN_POINT('Ctrl Pts',(-0.0720360347817216,2.94259161321474,
15.9318177496498));
#100440=CARTESIAN_POINT('Ctrl Pts',(-0.165283980577547,2.93883447993254,
15.9368574342732));
#100441=CARTESIAN_POINT('Ctrl Pts',(-0.25821327864767,2.93064666971814,
15.9418971188966));
#100442=CARTESIAN_POINT('Ctrl Pts',(-0.351075509559587,2.92246476865375,
15.9469331663751));
#100443=CARTESIAN_POINT('Ctrl Pts',(-0.443619108526811,2.90985858524784,
15.9519692138537));
#100444=CARTESIAN_POINT('Ctrl Pts',(-0.535392824290577,2.8928737483164,
15.9570052613322));
#100445=CARTESIAN_POINT('Ctrl Pts',(-0.627133113615048,2.87589509771637,
15.9620394745476));
#100446=CARTESIAN_POINT('Ctrl Pts',(-0.718103640360218,2.85454104263448,
15.9670736877631));
#100447=CARTESIAN_POINT('Ctrl Pts',(-0.807861017208068,2.82890872544088,
15.9721079009785));
#100448=CARTESIAN_POINT('Ctrl Pts',(-0.89761081755764,2.80327857189348,
15.9771416892517));
#100449=CARTESIAN_POINT('Ctrl Pts',(-0.986147244435183,2.77337099641894,
15.9821754775248));
#100450=CARTESIAN_POINT('Ctrl Pts',(-1.07304091515667,2.73933334853568,
15.987209265798));
#100451=CARTESIAN_POINT('Ctrl Pts',(-1.1599515650417,2.70528904964109,15.9922440376815));
#100452=CARTESIAN_POINT('Ctrl Pts',(-1.24521840773356,2.66711323797731,
15.997278809565));
#100453=CARTESIAN_POINT('Ctrl Pts',(-1.32843199742465,2.62500141489836,
16.0023135814485));
#100454=CARTESIAN_POINT('Ctrl Pts',(-1.41173706996259,2.58284329518112,
16.0073538884287));
#100455=CARTESIAN_POINT('Ctrl Pts',(-1.49298398661229,2.5367407274459,16.0123941954089));
#100456=CARTESIAN_POINT('Ctrl Pts',(-1.57178816026574,2.48693505730416,
16.017434502389));
#100457=CARTESIAN_POINT('Ctrl Pts',(-1.65064072462551,2.43709880335645,
16.0224779044339));
#100458=CARTESIAN_POINT('Ctrl Pts',(-1.72704719620449,2.38355517483878,
16.0275213064788));
#100459=CARTESIAN_POINT('Ctrl Pts',(-1.80065402727287,2.32658743099545,
16.0325647085237));
#100460=CARTESIAN_POINT('Ctrl Pts',(-1.87438021846099,2.26952730881402,
16.0376162889001));
#100461=CARTESIAN_POINT('Ctrl Pts',(-1.94529736818064,2.20903227432121,
16.0426678692766));
#100462=CARTESIAN_POINT('Ctrl Pts',(-2.01308704083513,2.14542409933833,
16.0477194496531));
#100463=CARTESIAN_POINT('Ctrl Pts',(-2.04767371688367,2.11297084715366,
16.0502967946552));
#100464=CARTESIAN_POINT('Ctrl Pts',(-2.08144690046443,2.07970778005639,
16.0528741396574));
#100465=CARTESIAN_POINT('Ctrl Pts',(-2.11436836273714,2.04568092004992,
16.0554514846596));
#100466=CARTESIAN_POINT('Ctrl Pts',(-2.17949801956193,1.97836441701341,
16.0605503345867));
#100467=CARTESIAN_POINT('Ctrl Pts',(-2.24154457972021,1.9077946655625,16.0656491845138));
#100468=CARTESIAN_POINT('Ctrl Pts',(-2.30016070585547,1.83429134197337,
16.0707480344409));
#100469=CARTESIAN_POINT('Ctrl Pts',(-2.35739165283549,1.76252500235759,
16.075726391577));
#100470=CARTESIAN_POINT('Ctrl Pts',(-2.41135216583501,1.68796256164301,
16.0807047487132));
#100471=CARTESIAN_POINT('Ctrl Pts',(-2.46175467667096,1.61094007085573,
16.0856831058493));
#100472=CARTESIAN_POINT('Ctrl Pts',(-2.51210957595231,1.53399033756533,
16.0906567602966));
#100473=CARTESIAN_POINT('Ctrl Pts',(-2.55891289594708,1.45458554692395,
16.095630414744));
#100474=CARTESIAN_POINT('Ctrl Pts',(-2.601917966428,1.37309391375069,16.1006040691913));
#100475=CARTESIAN_POINT('Ctrl Pts',(-2.6448951938005,1.2916550413415,16.1055745035068));
#100476=CARTESIAN_POINT('Ctrl Pts',(-2.68407884249686,1.20813241238184,
16.1105449378222));
#100477=CARTESIAN_POINT('Ctrl Pts',(-2.71926683982214,1.12292112538846,
16.1155153721376));
#100478=CARTESIAN_POINT('Ctrl Pts',(-2.75602606398772,1.03390495401982,
16.1207077480353));
#100479=CARTESIAN_POINT('Ctrl Pts',(-2.78842422023279,0.943046257073344,
16.1259001239331));
#100480=CARTESIAN_POINT('Ctrl Pts',(-2.81628627618475,0.850820551334667,
16.1310924998308));
#100481=CARTESIAN_POINT('Ctrl Pts',(-2.84295512294477,0.762544466543243,
16.1360625091286));
#100482=CARTESIAN_POINT('Ctrl Pts',(-2.86546831287009,0.673016534318072,
16.1410325184264));
#100483=CARTESIAN_POINT('Ctrl Pts',(-2.88372341249344,0.582669100122154,
16.1460025277242));
#100484=CARTESIAN_POINT('Ctrl Pts',(-2.90198198245374,0.492304490668651,
16.1509734818323));
#100485=CARTESIAN_POINT('Ctrl Pts',(-2.91598077466729,0.401120519722664,
16.1559444359405));
#100486=CARTESIAN_POINT('Ctrl Pts',(-2.92566878415543,0.309558016240055,
16.1609153900486));
#100487=CARTESIAN_POINT('Ctrl Pts',(-2.93536485446695,0.217919328978934,
16.1658904801955));
#100488=CARTESIAN_POINT('Ctrl Pts',(-2.94074295664986,0.125901936329462,
16.1708655703425));
#100489=CARTESIAN_POINT('Ctrl Pts',(-2.9418041153148,0.0339491843337573,
16.1758406604894));
#100490=CARTESIAN_POINT('Ctrl Pts',(-2.94194511869995,0.0217307953837703,
16.1765017346297));
#100491=CARTESIAN_POINT('Ctrl Pts',(-2.94200997631809,0.00951354392413586,
16.1771628087701));
#100492=CARTESIAN_POINT('Ctrl Pts',(-2.94199875963773,-0.00270153476367689,
16.1778238829104));
#100493=CARTESIAN_POINT('',(-2.9422462097844,0.00107083704094043,17.1778238829104));
#100494=CARTESIAN_POINT('Ctrl Pts',(-2.94208124408393,-0.00270161050626413,
16.1778238829104));
#100495=CARTESIAN_POINT('Ctrl Pts',(-2.94416292838268,-0.228090639137221,
16.1900213722217));
#100496=CARTESIAN_POINT('Ctrl Pts',(-2.81747124271292,-1.43029794424299,
16.2552071502614));
#100497=CARTESIAN_POINT('Ctrl Pts',(-1.16691403270231,-3.27719121187224,
16.3733812170289));
#100498=CARTESIAN_POINT('Ctrl Pts',(2.12388606133514,-2.75513676563843,
16.5323460832138));
#100499=CARTESIAN_POINT('Ctrl Pts',(3.46626230468908,0.294442242197471,
16.6913109493985));
#100500=CARTESIAN_POINT('Ctrl Pts',(1.62873720110606,3.07390398819469,16.8502758155833));
#100501=CARTESIAN_POINT('Ctrl Pts',(-1.7029690014089,3.03340850845079,17.0092406817681));
#100502=CARTESIAN_POINT('Ctrl Pts',(-2.91827323464354,1.0942644108035,17.118423370877));
#100503=CARTESIAN_POINT('Ctrl Pts',(-2.94665605505738,0.0600914372647645,
17.1746177712579));
#100504=CARTESIAN_POINT('Ctrl Pts',(-2.9463796754372,0.00107234142494241,
17.1778238829104));
#100505=CARTESIAN_POINT('',(-2.94199923877503,0.00211637595187146,18.1778238442168));
#100506=CARTESIAN_POINT('Ctrl Pts',(-2.94199980514957,0.00107074736142649,
17.1778238829104));
#100507=CARTESIAN_POINT('Ctrl Pts',(-2.94203329402139,-0.0909437258276088,
17.1828298628248));
#100508=CARTESIAN_POINT('Ctrl Pts',(-2.9377457510742,-0.183133975815443,
17.1878358427392));
#100509=CARTESIAN_POINT('Ctrl Pts',(-2.92911390110944,-0.275055911275205,
17.1928418226536));
#100510=CARTESIAN_POINT('Ctrl Pts',(-2.92049354800805,-0.366855414818711,
17.1978411350439));
#100511=CARTESIAN_POINT('Ctrl Pts',(-2.90754042312244,-0.458386866549597,
17.2028404474343));
#100512=CARTESIAN_POINT('Ctrl Pts',(-2.89028326165503,-0.549205487405925,
17.2078397598246));
#100513=CARTESIAN_POINT('Ctrl Pts',(-2.87304432078033,-0.639928219427667,
17.2128337938014));
#100514=CARTESIAN_POINT('Ctrl Pts',(-2.85151045925375,-0.729939173642679,
17.2178278277782));
#100515=CARTESIAN_POINT('Ctrl Pts',(-2.82576214795534,-0.818799293589582,
17.222821861755));
#100516=CARTESIAN_POINT('Ctrl Pts',(-2.80002863466342,-0.907608344065715,
17.2278130255728));
#100517=CARTESIAN_POINT('Ctrl Pts',(-2.77008560583347,-0.995267439275946,
17.2328041893907));
#100518=CARTESIAN_POINT('Ctrl Pts',(-2.73606426772405,-1.0813493065997,
17.2377953532085));
#100519=CARTESIAN_POINT('Ctrl Pts',(-2.70205254225591,-1.16740685171399,
17.2427851067858));
#100520=CARTESIAN_POINT('Ctrl Pts',(-2.66396496251153,-1.25188763292986,
17.2477748603632));
#100521=CARTESIAN_POINT('Ctrl Pts',(-2.62198166987877,-1.33438230009985,
17.2527646139405));
#100522=CARTESIAN_POINT('Ctrl Pts',(-2.57999797332518,-1.41687776095018,
17.2577544155243));
#100523=CARTESIAN_POINT('Ctrl Pts',(-2.53411869616048,-1.49738666660656,
17.262744217108));
#100524=CARTESIAN_POINT('Ctrl Pts',(-2.48457035483657,-1.57552345329014,
17.2677340186917));
#100525=CARTESIAN_POINT('Ctrl Pts',(-2.43497377683174,-1.65373630829703,
17.2727286779853));
#100526=CARTESIAN_POINT('Ctrl Pts',(-2.38170124307166,-1.72957204808033,
17.2777233372789));
#100527=CARTESIAN_POINT('Ctrl Pts',(-2.3250229238281,-1.80267368197183,
17.2827179965725));
#100528=CARTESIAN_POINT('Ctrl Pts',(-2.26831796501701,-1.87580967460821,
17.2877150034227));
#100529=CARTESIAN_POINT('Ctrl Pts',(-2.20820432795751,-1.94620865790778,
17.292712010273));
#100530=CARTESIAN_POINT('Ctrl Pts',(-2.14499132103499,-2.01354816994393,
17.2977090171232));
#100531=CARTESIAN_POINT('Ctrl Pts',(-2.08166776344506,-2.08100544932516,
17.3027147630363));
#100532=CARTESIAN_POINT('Ctrl Pts',(-2.01523433286974,-2.14539225199398,
17.3077205089494));
#100533=CARTESIAN_POINT('Ctrl Pts',(-1.94603592045869,-2.20642430105465,
17.3127262548625));
#100534=CARTESIAN_POINT('Ctrl Pts',(-1.87947821472108,-2.26512728310883,
17.3175409746208));
#100535=CARTESIAN_POINT('Ctrl Pts',(-1.8103630377244,-2.32072672154925,
17.3223556943792));
#100536=CARTESIAN_POINT('Ctrl Pts',(-1.73902209390058,-2.37300782909068,
17.3271704141375));
#100537=CARTESIAN_POINT('Ctrl Pts',(-1.66416440890601,-2.42786612601998,
17.3322224747872));
#100538=CARTESIAN_POINT('Ctrl Pts',(-1.58657387127427,-2.47927738960965,
17.337274535437));
#100539=CARTESIAN_POINT('Ctrl Pts',(-1.50660141597608,-2.52695788911863,
17.3423265960867));
#100540=CARTESIAN_POINT('Ctrl Pts',(-1.42673933224742,-2.57457258382585,
17.3473716842875));
#100541=CARTESIAN_POINT('Ctrl Pts',(-1.34450224148032,-2.61846652039016,
17.3524167724883));
#100542=CARTESIAN_POINT('Ctrl Pts',(-1.26027219027686,-2.65839763888226,
17.357461860689));
#100543=CARTESIAN_POINT('Ctrl Pts',(-1.17613235426424,-2.69828598886806,
17.3625015453125));
#100544=CARTESIAN_POINT('Ctrl Pts',(-1.09000419990067,-2.73421976784508,
17.3675412299359));
#100545=CARTESIAN_POINT('Ctrl Pts',(-1.00229569805139,-2.76600204874611,
17.3725809145594));
#100546=CARTESIAN_POINT('Ctrl Pts',(-0.914650495507,-2.79776139234635,17.3776169620379));
#100547=CARTESIAN_POINT('Ctrl Pts',(-0.825427628969259,-2.82537504217137,
17.3826530095164));
#100548=CARTESIAN_POINT('Ctrl Pts',(-0.735055474742115,-2.84869399006837,
17.3876890569949));
#100549=CARTESIAN_POINT('Ctrl Pts',(-0.644716236468095,-2.87200444458151,
17.3927232702103));
#100550=CARTESIAN_POINT('Ctrl Pts',(-0.553228971873109,-2.8910231937955,
17.3977574834258));
#100551=CARTESIAN_POINT('Ctrl Pts',(-0.461036660377981,-2.90565125192056,
17.4027916966413));
#100552=CARTESIAN_POINT('Ctrl Pts',(-0.368852130916373,-2.92027807527846,
17.4078254849144));
#100553=CARTESIAN_POINT('Ctrl Pts',(-0.275963111721861,-2.93051487497566,
17.4128592731875));
#100554=CARTESIAN_POINT('Ctrl Pts',(-0.182821066728011,-2.93631409381906,
17.4178930614606));
#100555=CARTESIAN_POINT('Ctrl Pts',(-0.089660821627973,-2.94211444583919,
17.4229278333441));
#100556=CARTESIAN_POINT('Ctrl Pts',(0.00375210402130081,-2.94347546768573,
17.4279626052276));
#100557=CARTESIAN_POINT('Ctrl Pts',(0.0969640073408292,-2.94040167005809,
17.4329973771111));
#100558=CARTESIAN_POINT('Ctrl Pts',(0.19027838539218,-2.93732449317763,
17.4380376840913));
#100559=CARTESIAN_POINT('Ctrl Pts',(0.283390855220886,-2.92980277932503,
17.4430779910715));
#100560=CARTESIAN_POINT('Ctrl Pts',(0.375850910903049,-2.9178930913886,
17.4481182980517));
#100561=CARTESIAN_POINT('Ctrl Pts',(0.468367742859676,-2.90597609015666,
17.4531617000966));
#100562=CARTESIAN_POINT('Ctrl Pts',(0.560230925968129,-2.88966582825894,
17.4582051021415));
#100563=CARTESIAN_POINT('Ctrl Pts',(0.651000413242353,-2.86906996463284,
17.4632485041864));
#100564=CARTESIAN_POINT('Ctrl Pts',(0.741917091432303,-2.84844070295506,
17.4683000845628));
#100565=CARTESIAN_POINT('Ctrl Pts',(0.831736105545388,-2.82351208433317,
17.4733516649393));
#100566=CARTESIAN_POINT('Ctrl Pts',(0.920032994952805,-2.79444149843903,
17.4784032453158));
#100567=CARTESIAN_POINT('Ctrl Pts',(0.965082569474462,-2.77960952038844,
17.4809805903179));
#100568=CARTESIAN_POINT('Ctrl Pts',(1.0097362437424,-2.76370012265316,17.4835579353201));
#100569=CARTESIAN_POINT('Ctrl Pts',(1.05393994152964,-2.74673890270781,
17.4861352803223));
#100570=CARTESIAN_POINT('Ctrl Pts',(1.14058715483423,-2.71349185515119,
17.491187340972));
#100571=CARTESIAN_POINT('Ctrl Pts',(1.22581532789134,-2.67608105362047,
17.4962394016217));
#100572=CARTESIAN_POINT('Ctrl Pts',(1.30919592925609,-2.63464798764831,
17.5012914622715));
#100573=CARTESIAN_POINT('Ctrl Pts',(1.39246145540148,-2.59327210427111,
17.5063365504722));
#100574=CARTESIAN_POINT('Ctrl Pts',(1.47388408232774,-2.54788518336495,
17.511381638673));
#100575=CARTESIAN_POINT('Ctrl Pts',(1.55305347551471,-2.49867743060037,
17.5164267268737));
#100576=CARTESIAN_POINT('Ctrl Pts',(1.63213807376387,-2.44952238214699,
17.5214664114971));
#100577=CARTESIAN_POINT('Ctrl Pts',(1.70897385981901,-2.39655486920936,
17.5265060961205));
#100578=CARTESIAN_POINT('Ctrl Pts',(1.78317441502162,-2.34001132595812,
17.531545780744));
#100579=CARTESIAN_POINT('Ctrl Pts',(1.85732141961698,-2.28350859023278,
17.5365818282224));
#100580=CARTESIAN_POINT('Ctrl Pts',(1.92883662116874,-2.22343522244948,
17.5416178757009));
#100581=CARTESIAN_POINT('Ctrl Pts',(1.99736284684045,-2.16007075302209,
17.5466539231794));
#100582=CARTESIAN_POINT('Ctrl Pts',(2.06586411342986,-2.09672936262746,
17.5516881363949));
#100583=CARTESIAN_POINT('Ctrl Pts',(2.13137824099259,-2.03009955327481,
17.5567223496103));
#100584=CARTESIAN_POINT('Ctrl Pts',(2.19358221198335,-1.96050021149457,
17.5617565628258));
#100585=CARTESIAN_POINT('Ctrl Pts',(2.2557809322827,-1.89090674465542,17.5667903510989));
#100586=CARTESIAN_POINT('Ctrl Pts',(2.31466975560202,-1.81834457515237,
17.571824139372));
#100587=CARTESIAN_POINT('Ctrl Pts',(2.36996431412626,-1.74316756216034,
17.5768579276451));
#100588=CARTESIAN_POINT('Ctrl Pts',(2.42526967729674,-1.66797585945829,
17.5818926995286));
#100589=CARTESIAN_POINT('Ctrl Pts',(2.47697911791386,-1.59016865664336,
17.5869274714121));
#100590=CARTESIAN_POINT('Ctrl Pts',(2.52485083619738,-1.51012988016045,
17.5919622432956));
#100591=CARTESIAN_POINT('Ctrl Pts',(2.57277518339745,-1.43000311113747,
17.5970025502758));
#100592=CARTESIAN_POINT('Ctrl Pts',(2.61685315800773,-1.34764025317901,
17.602042857256));
#100593=CARTESIAN_POINT('Ctrl Pts',(2.65688845756911,-1.26345072085777,
17.6070831642362));
#100594=CARTESIAN_POINT('Ctrl Pts',(2.69694834131592,-1.17920949088231,
17.612126566281));
#100595=CARTESIAN_POINT('Ctrl Pts',(2.7329604365705,-1.09313976304902,17.6171699683259));
#100596=CARTESIAN_POINT('Ctrl Pts',(2.76477706520972,-1.00566981643594,
17.6222133703707));
#100597=CARTESIAN_POINT('Ctrl Pts',(2.7966452873838,-0.918058029410124,
17.6272649507472));
#100598=CARTESIAN_POINT('Ctrl Pts',(2.82430432917473,-0.829041914409659,
17.6323165311236));
#100599=CARTESIAN_POINT('Ctrl Pts',(2.84765676431199,-0.739063564700747,
17.6373681115001));
#100600=CARTESIAN_POINT('Ctrl Pts',(2.85957130936675,-0.693156099579488,
17.6399454565024));
#100601=CARTESIAN_POINT('Ctrl Pts',(2.8703656293677,-0.646998302644535,
17.6425228015047));
#100602=CARTESIAN_POINT('Ctrl Pts',(2.88003197548053,-0.60064949863438,
17.645100146507));
#100603=CARTESIAN_POINT('Ctrl Pts',(2.89897975576582,-0.509797490582921,
17.6501522071567));
#100604=CARTESIAN_POINT('Ctrl Pts',(2.91365841091782,-0.417884778530722,
17.6552042678065));
#100605=CARTESIAN_POINT('Ctrl Pts',(2.92395494186897,-0.325348271733616,
17.6602563284562));
#100606=CARTESIAN_POINT('Ctrl Pts',(2.9342372623738,-0.232939476402446,
17.665301416657));
#100607=CARTESIAN_POINT('Ctrl Pts',(2.9401494277896,-0.139909034798525,
17.6703465048577));
#100608=CARTESIAN_POINT('Ctrl Pts',(2.94162925092124,-0.0467049261270682,
17.6753915930585));
#100609=CARTESIAN_POINT('Ctrl Pts',(2.94310748907788,0.0463993556257909,
17.6804312776819));
#100610=CARTESIAN_POINT('Ctrl Pts',(2.94016281386149,0.139676492875248,
17.6854709623053));
#100611=CARTESIAN_POINT('Ctrl Pts',(2.932784853981,0.232673591667947,17.6905106469288));
#100612=CARTESIAN_POINT('Ctrl Pts',(2.92541221878078,0.325603574370818,
17.6955466944073));
#100613=CARTESIAN_POINT('Ctrl Pts',(2.91361269340193,0.41825347869182,17.7005827418858));
#100614=CARTESIAN_POINT('Ctrl Pts',(2.89742797392138,0.5101716730061,17.7056187893643));
#100615=CARTESIAN_POINT('Ctrl Pts',(2.88124914934808,0.602056388258219,
17.7106530025797));
#100616=CARTESIAN_POINT('Ctrl Pts',(2.86068838064425,0.693209485819634,
17.7156872157952));
#100617=CARTESIAN_POINT('Ctrl Pts',(2.83583894399186,0.783186748955274,
17.7207214290106));
#100618=CARTESIAN_POINT('Ctrl Pts',(2.81099160490214,0.87315641703148,17.7257552172838));
#100619=CARTESIAN_POINT('Ctrl Pts',(2.78185643606895,0.961950019796551,
17.7307890055569));
#100620=CARTESIAN_POINT('Ctrl Pts',(2.74857704091671,1.04913690724593,17.73582279383));
#100621=CARTESIAN_POINT('Ctrl Pts',(2.71529114291672,1.13634083115442,17.7408575657135));
#100622=CARTESIAN_POINT('Ctrl Pts',(2.67785956913586,1.22193700129747,17.745892337597));
#100623=CARTESIAN_POINT('Ctrl Pts',(2.63647424668415,1.30551428432293,17.7509271094805));
#100624=CARTESIAN_POINT('Ctrl Pts',(2.59504342629008,1.38918345003001,17.7559674164607));
#100625=CARTESIAN_POINT('Ctrl Pts',(2.54965037823171,1.47082889941229,17.7610077234409));
#100626=CARTESIAN_POINT('Ctrl Pts',(2.50053308868983,1.55006395750862,17.7660480304211));
#100627=CARTESIAN_POINT('Ctrl Pts',(2.45138563805086,1.62934767090134,17.771091432466));
#100628=CARTESIAN_POINT('Ctrl Pts',(2.39850964474591,1.70621768056698,17.7761348345108));
#100629=CARTESIAN_POINT('Ctrl Pts',(2.34218527739306,1.7803179846205,17.7811782365557));
#100630=CARTESIAN_POINT('Ctrl Pts',(2.28576957499525,1.85453844900462,17.7862298169322));
#100631=CARTESIAN_POINT('Ctrl Pts',(2.2258946200785,1.92597990123178,17.7912813973086));
#100632=CARTESIAN_POINT('Ctrl Pts',(2.16287939825066,1.99432111472121,17.7963329776851));
#100633=CARTESIAN_POINT('Ctrl Pts',(2.13072867413291,2.02918919003758,17.7989103226873));
#100634=CARTESIAN_POINT('Ctrl Pts',(2.09776107921285,2.06325085833496,17.8014876676895));
#100635=CARTESIAN_POINT('Ctrl Pts',(2.0640223007228,2.09646749130984,17.8040650126918));
#100636=CARTESIAN_POINT('Ctrl Pts',(1.99788821505217,2.16157807767854,17.8091170733415));
#100637=CARTESIAN_POINT('Ctrl Pts',(1.92855135602194,2.22367324281825,17.8141691339912));
#100638=CARTESIAN_POINT('Ctrl Pts',(1.85631792073174,2.28242147228995,17.819221194641));
#100639=CARTESIAN_POINT('Ctrl Pts',(1.78418417623612,2.34108862216667,17.8242662828418));
#100640=CARTESIAN_POINT('Ctrl Pts',(1.70916214093243,2.39641773732234,17.8293113710426));
#100641=CARTESIAN_POINT('Ctrl Pts',(1.63159482462775,2.4481140349763,17.8343564592434));
#100642=CARTESIAN_POINT('Ctrl Pts',(1.55411058734505,2.49975496294553,17.8393961438668));
#100643=CARTESIAN_POINT('Ctrl Pts',(1.47408685538507,2.54777056216937,17.8444358284902));
#100644=CARTESIAN_POINT('Ctrl Pts',(1.39189881930388,2.59190695759328,17.8494755131137));
#100645=CARTESIAN_POINT('Ctrl Pts',(1.3097700984023,2.63601149974089,17.8545115605922));
#100646=CARTESIAN_POINT('Ctrl Pts',(1.22548056832853,2.67624219312077,17.8595476080707));
#100647=CARTESIAN_POINT('Ctrl Pts',(1.13943254266561,2.71238962553586,17.8645836555492));
#100648=CARTESIAN_POINT('Ctrl Pts',(1.05341585799265,2.74852389209029,17.8696178687647));
#100649=CARTESIAN_POINT('Ctrl Pts',(0.965642359340677,2.78057768030859,
17.8746520819802));
#100650=CARTESIAN_POINT('Ctrl Pts',(0.876536046332958,2.80838896157192,
17.8796862951956));
#100651=CARTESIAN_POINT('Ctrl Pts',(0.787437254866824,2.83619789526074,
17.8847200834688));
#100652=CARTESIAN_POINT('Ctrl Pts',(0.697006296905316,2.85976490179861,
17.8897538717419));
#100653=CARTESIAN_POINT('Ctrl Pts',(0.605683007306596,2.87897761274033,
17.894787660015));
#100654=CARTESIAN_POINT('Ctrl Pts',(0.514341872989364,2.89819407787686,
17.8998224318986));
#100655=CARTESIAN_POINT('Ctrl Pts',(0.422108495585902,2.91305446655337,
17.9048572037821));
#100656=CARTESIAN_POINT('Ctrl Pts',(0.329432457806434,2.92349760659105,
17.9098919756656));
#100657=CARTESIAN_POINT('Ctrl Pts',(0.236654534412013,2.93395222754408,
17.9149322826458));
#100658=CARTESIAN_POINT('Ctrl Pts',(0.143433421422785,2.9399798564246,17.919972589626));
#100659=CARTESIAN_POINT('Ctrl Pts',(0.0502230684115907,2.94157128817225,
17.9250128966062));
#100660=CARTESIAN_POINT('Ctrl Pts',(-0.043044521604017,2.94316369715882,
17.9300562986511));
#100661=CARTESIAN_POINT('Ctrl Pts',(-0.136300894717583,2.94031449942311,
17.935099700696));
#100662=CARTESIAN_POINT('Ctrl Pts',(-0.229095058405284,2.93306656150424,
17.9401431027408));
#100663=CARTESIAN_POINT('Ctrl Pts',(-0.32203969620398,2.92580687039991,
17.9451946831173));
#100664=CARTESIAN_POINT('Ctrl Pts',(-0.414520187991462,2.91413425452411,
17.9502462634938));
#100665=CARTESIAN_POINT('Ctrl Pts',(-0.506093769289275,2.89814304282701,
17.9552978438702));
#100666=CARTESIAN_POINT('Ctrl Pts',(-0.552815130624427,2.88998423578573,
17.9578751888723));
#100667=CARTESIAN_POINT('Ctrl Pts',(-0.599300622475556,2.88070206959699,
17.9604525338744));
#100668=CARTESIAN_POINT('Ctrl Pts',(-0.645493034382045,2.87031404946641,
17.9630298788766));
#100669=CARTESIAN_POINT('Ctrl Pts',(-0.736038485735576,2.84995165805682,
17.9680819395263));
#100670=CARTESIAN_POINT('Ctrl Pts',(-0.825782178460994,2.82526402613562,
17.973134000176));
#100671=CARTESIAN_POINT('Ctrl Pts',(-0.914279620297822,2.79632916086574,
17.9781860608258));
#100672=CARTESIAN_POINT('Ctrl Pts',(-1.00265492506214,2.76743422917658,
17.9832311490265));
#100673=CARTESIAN_POINT('Ctrl Pts',(-1.08978697810545,2.73430384889857,
17.9882762372273));
#100674=CARTESIAN_POINT('Ctrl Pts',(-1.1752422450961,2.69706686334275,17.993321325428));
#100675=CARTESIAN_POINT('Ctrl Pts',(-1.26060598461976,2.65986976072318,
17.9983610100514));
#100676=CARTESIAN_POINT('Ctrl Pts',(-1.34429610264826,2.61857497182734,
18.0034006946749));
#100677=CARTESIAN_POINT('Ctrl Pts',(-1.42589604143235,2.57336054198154,
18.0084403792983));
#100678=CARTESIAN_POINT('Ctrl Pts',(-1.50743708946725,2.52817874343043,
18.0134764267768));
#100679=CARTESIAN_POINT('Ctrl Pts',(-1.58689056906333,2.47908314128601,
18.0185124742553));
#100680=CARTESIAN_POINT('Ctrl Pts',(-1.66386262607719,2.42629865464734,
18.0235485217338));
#100681=CARTESIAN_POINT('Ctrl Pts',(-1.74080664781156,2.37353339352887,
18.0285827349492));
#100682=CARTESIAN_POINT('Ctrl Pts',(-1.81527067640061,2.31708216811217,
18.0336169481647));
#100683=CARTESIAN_POINT('Ctrl Pts',(-1.88688896020049,2.25721378072028,
18.0386511613802));
#100684=CARTESIAN_POINT('Ctrl Pts',(-1.95850119863849,2.19735044687123,
18.0436849496533));
#100685=CARTESIAN_POINT('Ctrl Pts',(-2.02726782910982,2.13407080963618,
18.0487187379264));
#100686=CARTESIAN_POINT('Ctrl Pts',(-2.0928562837699,2.06768386739483,18.0537525261996));
#100687=CARTESIAN_POINT('Ctrl Pts',(-2.15845755451999,2.00128395303772,
18.0587872980831));
#100688=CARTESIAN_POINT('Ctrl Pts',(-2.22087910413052,1.93177584413635,
18.0638220699666));
#100689=CARTESIAN_POINT('Ctrl Pts',(-2.27982613528375,1.85950444820043,
18.06885684185));
#100690=CARTESIAN_POINT('Ctrl Pts',(-2.33883797126325,1.78715359897963,
18.0738971488302));
#100691=CARTESIAN_POINT('Ctrl Pts',(-2.39436738273153,1.71203374355614,
18.0789374558104));
#100692=CARTESIAN_POINT('Ctrl Pts',(-2.44616090381604,1.63452159136607,
18.0839777627906));
#100693=CARTESIAN_POINT('Ctrl Pts',(-2.4979862293717,1.55696184185195,18.0890211648355));
#100694=CARTESIAN_POINT('Ctrl Pts',(-2.5460708686889,1.47700725151648,18.0940645668803));
#100695=CARTESIAN_POINT('Ctrl Pts',(-2.59020673967435,1.39506023014978,
18.0991079689252));
#100696=CARTESIAN_POINT('Ctrl Pts',(-2.6344141809579,1.31298032429216,18.1041595493017));
#100697=CARTESIAN_POINT('Ctrl Pts',(-2.67465987886471,1.22890193751765,
18.1092111296781));
#100698=CARTESIAN_POINT('Ctrl Pts',(-2.71078347608639,1.14324841822633,
18.1142627100546));
#100699=CARTESIAN_POINT('Ctrl Pts',(-2.72921394057933,1.09954750615196,
18.1168400550568));
#100700=CARTESIAN_POINT('Ctrl Pts',(-2.74657217872128,1.0554368370274,18.119417400059));
#100701=CARTESIAN_POINT('Ctrl Pts',(-2.76284194091274,1.01097399053265,
18.1219947450613));
#100702=CARTESIAN_POINT('Ctrl Pts',(-2.79968270885509,0.910293636972882,
18.1278308087982));
#100703=CARTESIAN_POINT('Ctrl Pts',(-2.83104886874699,0.807508598495934,
18.1336668725351));
#100704=CARTESIAN_POINT('Ctrl Pts',(-2.85672911385411,0.703180467631383,
18.1395029362721));
#100705=CARTESIAN_POINT('Ctrl Pts',(-2.88229461777721,0.599318482366823,
18.1453129240561));
#100706=CARTESIAN_POINT('Ctrl Pts',(-2.90222479222233,0.493927308134397,
18.1511229118401));
#100707=CARTESIAN_POINT('Ctrl Pts',(-2.91635794815504,0.387582659871288,
18.1569328996241));
#100708=CARTESIAN_POINT('Ctrl Pts',(-2.93038160278863,0.282061951936535,
18.1626978726065));
#100709=CARTESIAN_POINT('Ctrl Pts',(-2.93869761945983,0.175602649068792,
18.1684628455889));
#100710=CARTESIAN_POINT('Ctrl Pts',(-2.941195752608,0.068786225660934,18.1742278185713));
#100711=CARTESIAN_POINT('Ctrl Pts',(-2.94171517399957,0.0465765466729996,
18.1754264937864));
#100712=CARTESIAN_POINT('Ctrl Pts',(-2.9419832435771,0.0243514897462521,
18.1766251690016));
#100713=CARTESIAN_POINT('Ctrl Pts',(-2.94199923877503,0.00211637595187146,
18.1778238442168));
#100714=CARTESIAN_POINT('',(-2.94199929009827,-0.00204378601551511,19.1778239218877));
#100715=CARTESIAN_POINT('Ctrl Pts',(-2.9388439218794,0.0021133891354786,
18.1778238829104));
#100716=CARTESIAN_POINT('Ctrl Pts',(-2.93462424779457,-0.634919682450241,
18.2122024590223));
#100717=CARTESIAN_POINT('Ctrl Pts',(-2.41790829107791,-2.26005798993625,
18.2995693238623));
#100718=CARTESIAN_POINT('Ctrl Pts',(0.264235245208259,-3.46869576845375,
18.4399244774308));
#100719=CARTESIAN_POINT('Ctrl Pts',(3.05959885035108,-1.65545325329123,
18.5988893436155));
#100720=CARTESIAN_POINT('Ctrl Pts',(3.04812856639187,1.67647929949768,18.7578542098002));
#100721=CARTESIAN_POINT('Ctrl Pts',(0.240347074017613,3.4704328091634,18.916819075985));
#100722=CARTESIAN_POINT('Ctrl Pts',(-2.4264532086293,2.24655052879084,19.0568089670217));
#100723=CARTESIAN_POINT('Ctrl Pts',(-2.93467894617267,0.628302831224356,
19.1438105693302));
#100724=CARTESIAN_POINT('Ctrl Pts',(-2.93869762167607,-0.00204077003662013,
19.1778238829104));
#100725=CARTESIAN_POINT('',(-2.94219292041373,-0.00118371768616264,20.1778238829104));
#100726=CARTESIAN_POINT('Ctrl Pts',(-2.94199929009827,-0.00204378601551511,
19.1778239218877));
#100727=CARTESIAN_POINT('Ctrl Pts',(-2.94192528935904,-0.108566739313825,
19.183565473421));
#100728=CARTESIAN_POINT('Ctrl Pts',(-2.93606185133819,-0.214861265836627,
19.1893070249543));
#100729=CARTESIAN_POINT('Ctrl Pts',(-2.92450720316344,-0.320346091977305,
19.1950485764876));
#100730=CARTESIAN_POINT('Ctrl Pts',(-2.91289326540157,-0.426372185294256,
19.2008195892572));
#100731=CARTESIAN_POINT('Ctrl Pts',(-2.89552968666625,-0.531580070789771,
19.2065906020268));
#100732=CARTESIAN_POINT('Ctrl Pts',(-2.87256561562812,-0.63539813023885,
19.2123616147964));
#100733=CARTESIAN_POINT('Ctrl Pts',(-2.84946366066775,-0.73983954785524,
19.2181672786465));
#100734=CARTESIAN_POINT('Ctrl Pts',(-2.82069386446977,-0.842874227815561,
19.2239729424967));
#100735=CARTESIAN_POINT('Ctrl Pts',(-2.7864562018921,-0.943941648057266,
19.2297786063469));
#100736=CARTESIAN_POINT('Ctrl Pts',(-2.77668596695865,-0.972782765281283,
19.2314353403494));
#100737=CARTESIAN_POINT('Ctrl Pts',(-2.76647075879212,-1.00146382400338,
19.233092074352));
#100738=CARTESIAN_POINT('Ctrl Pts',(-2.75581591881844,-1.02997214602478,
19.2347488083546));
#100739=CARTESIAN_POINT('Ctrl Pts',(-2.72332494701671,-1.11690569821321,
19.2398008690043));
#100740=CARTESIAN_POINT('Ctrl Pts',(-2.68665801747615,-1.20245653591761,
19.2448529296541));
#100741=CARTESIAN_POINT('Ctrl Pts',(-2.64595288127318,-1.28619491138869,
19.2499049903038));
#100742=CARTESIAN_POINT('Ctrl Pts',(-2.60530392303494,-1.36981771786916,
19.2549500785046));
#100743=CARTESIAN_POINT('Ctrl Pts',(-2.56062802532435,-1.45163263661067,
19.2599951667053));
#100744=CARTESIAN_POINT('Ctrl Pts',(-2.51211181202702,-1.53122769171483,
19.2650402549061));
#100745=CARTESIAN_POINT('Ctrl Pts',(-2.46364756236242,-1.61073749597335,
19.2700799395295));
#100746=CARTESIAN_POINT('Ctrl Pts',(-2.41135140268535,-1.68803178508086,
19.275119624153));
#100747=CARTESIAN_POINT('Ctrl Pts',(-2.35545639196684,-1.76272209538048,
19.2801593087764));
#100748=CARTESIAN_POINT('Ctrl Pts',(-2.29960172072789,-1.83735850161591,
19.2851953562549));
#100749=CARTESIAN_POINT('Ctrl Pts',(-2.24015362635919,-1.90939430969625,
19.2902314037334));
#100750=CARTESIAN_POINT('Ctrl Pts',(-2.17738851721032,-1.97846992525048,
19.2952674512119));
#100751=CARTESIAN_POINT('Ctrl Pts',(-2.11464626879112,-2.04752038162,19.3003016644273));
#100752=CARTESIAN_POINT('Ctrl Pts',(-2.0485897041775,-2.11361245887728,
19.3053358776428));
#100753=CARTESIAN_POINT('Ctrl Pts',(-1.97953488388095,-2.17642037380154,
19.3103700908583));
#100754=CARTESIAN_POINT('Ctrl Pts',(-1.91048589256215,-2.23922298705479,
19.3154038791314));
#100755=CARTESIAN_POINT('Ctrl Pts',(-1.83843947755403,-2.29874169032879,
19.3204376674045));
#100756=CARTESIAN_POINT('Ctrl Pts',(-1.76374700737692,-2.3546890440075,
19.3254714556776));
#100757=CARTESIAN_POINT('Ctrl Pts',(-1.68903994217004,-2.41064732988982,
19.3305062275611));
#100758=CARTESIAN_POINT('Ctrl Pts',(-1.61168615075386,-2.46303261420156,
19.3355409994446));
#100759=CARTESIAN_POINT('Ctrl Pts',(-1.53206743860281,-2.51159976181975,
19.3405757713281));
#100760=CARTESIAN_POINT('Ctrl Pts',(-1.45236119571956,-2.56022030289127,
19.3456160783083));
#100761=CARTESIAN_POINT('Ctrl Pts',(-1.37038544164988,-2.6050140966754,
19.3506563852885));
#100762=CARTESIAN_POINT('Ctrl Pts',(-1.28654786537196,-2.64578128160792,
19.3556966922687));
#100763=CARTESIAN_POINT('Ctrl Pts',(-1.2026588075628,-2.68657350014945,
19.3607400943136));
#100764=CARTESIAN_POINT('Ctrl Pts',(-1.11690605957456,-2.72333401247518,
19.3657834963584));
#100765=CARTESIAN_POINT('Ctrl Pts',(-1.02971659775859,-2.75591141517656,
19.3708268984033));
#100766=CARTESIAN_POINT('Ctrl Pts',(-0.942385750361367,-2.78854164507656,
19.3758784787797));
#100767=CARTESIAN_POINT('Ctrl Pts',(-0.853613960632055,-2.81697508790143,
19.3809300591562));
#100768=CARTESIAN_POINT('Ctrl Pts',(-0.763842456347477,-2.8411104698482,
19.3859816395327));
#100769=CARTESIAN_POINT('Ctrl Pts',(-0.718040524939103,-2.85342447881185,
19.3885589845348));
#100770=CARTESIAN_POINT('Ctrl Pts',(-0.671978512543133,-2.86462048595629,
19.391136329537));
#100771=CARTESIAN_POINT('Ctrl Pts',(-0.625715674144197,-2.87469022594266,
19.3937136745392));
#100772=CARTESIAN_POINT('Ctrl Pts',(-0.53503217417749,-2.89442873091386,
19.3987657351889));
#100773=CARTESIAN_POINT('Ctrl Pts',(-0.44325082061425,-2.90990751290563,
19.4038177958386));
#100774=CARTESIAN_POINT('Ctrl Pts',(-0.350807521757551,-2.92100977106862,
19.4088698564884));
#100775=CARTESIAN_POINT('Ctrl Pts',(-0.258491805728526,-2.93209670678522,
19.4139149446891));
#100776=CARTESIAN_POINT('Ctrl Pts',(-0.165516397063802,-2.9388190686146,
19.4189600328899));
#100777=CARTESIAN_POINT('Ctrl Pts',(-0.0723287162357964,-2.94111076921759,
19.4240051210907));
#100778=CARTESIAN_POINT('Ctrl Pts',(0.0207591552688803,-2.94340001527847,
19.4290448057141));
#100779=CARTESIAN_POINT('Ctrl Pts',(0.11405840525815,-2.94126802159644,
19.4340844903375));
#100780=CARTESIAN_POINT('Ctrl Pts',(0.207116247311439,-2.93470047195615,
19.439124174961));
#100781=CARTESIAN_POINT('Ctrl Pts',(0.300106929436197,-2.92813766212235,
19.4441602224394));
#100782=CARTESIAN_POINT('Ctrl Pts',(0.392856107996778,-2.91714569022534,
19.4491962699179));
#100783=CARTESIAN_POINT('Ctrl Pts',(0.484911805276166,-2.90176231643872,
19.4542323173964));
#100784=CARTESIAN_POINT('Ctrl Pts',(0.576933973411127,-2.88638454568784,
19.4592665306119));
#100785=CARTESIAN_POINT('Ctrl Pts',(0.668262724265773,-2.86661862369939,
19.4643007438274));
#100786=CARTESIAN_POINT('Ctrl Pts',(0.758453045399138,-2.84255395338853,
19.4693349570428));
#100787=CARTESIAN_POINT('Ctrl Pts',(0.848635753488712,-2.81849131439751,
19.4743687453159));
#100788=CARTESIAN_POINT('Ctrl Pts',(0.937679793678511,-2.79013076324602,
19.4794025335891));
#100789=CARTESIAN_POINT('Ctrl Pts',(1.02515328132509,-2.75761214636656,
19.4844363218622));
#100790=CARTESIAN_POINT('Ctrl Pts',(1.11264386143281,-2.72508717529671,
19.4894710937457));
#100791=CARTESIAN_POINT('Ctrl Pts',(1.19856286321372,-2.68840268004576,
19.4945058656292));
#100792=CARTESIAN_POINT('Ctrl Pts',(1.28249749697171,-2.6477469989146,19.4995406375127));
#100793=CARTESIAN_POINT('Ctrl Pts',(1.36652440627345,-2.60704662198965,
19.5045809444929));
#100794=CARTESIAN_POINT('Ctrl Pts',(1.44856219239176,-2.56236653844383,
19.5096212514731));
#100795=CARTESIAN_POINT('Ctrl Pts',(1.52822212185677,-2.51394135696671,
19.5146615584533));
#100796=CARTESIAN_POINT('Ctrl Pts',(1.60793096751581,-2.46548643939027,
19.5197049604981));
#100797=CARTESIAN_POINT('Ctrl Pts',(1.68525868167522,-2.41328209400741,
19.524748362543));
#100798=CARTESIAN_POINT('Ctrl Pts',(1.75984683531133,-2.35760537754831,
19.5297917645879));
#100799=CARTESIAN_POINT('Ctrl Pts',(1.8345559403702,-2.30183837626859,19.5348433449644));
#100800=CARTESIAN_POINT('Ctrl Pts',(1.90651627348025,-2.24258804478179,
19.5398949253408));
#100801=CARTESIAN_POINT('Ctrl Pts',(1.97540384145417,-2.18017055827476,
19.5449465057173));
#100802=CARTESIAN_POINT('Ctrl Pts',(2.01055066993215,-2.14832480211279,
19.5475238507195));
#100803=CARTESIAN_POINT('Ctrl Pts',(2.04489823803742,-2.1156551812504,19.5501011957218));
#100804=CARTESIAN_POINT('Ctrl Pts',(2.07840752093473,-2.08220704468167,
19.552678540724));
#100805=CARTESIAN_POINT('Ctrl Pts',(2.14409175388668,-2.01664266955247,
19.5577306013737));
#100806=CARTESIAN_POINT('Ctrl Pts',(2.20678858050854,-1.94784937420141,
19.5627826620234));
#100807=CARTESIAN_POINT('Ctrl Pts',(2.2661638315503,-1.87613045617123,19.5678347226731));
#100808=CARTESIAN_POINT('Ctrl Pts',(2.32545713763209,-1.80451051884032,
19.5728798108738));
#100809=CARTESIAN_POINT('Ctrl Pts',(2.38143769656555,-1.72997332150707,
19.5779248990745));
#100810=CARTESIAN_POINT('Ctrl Pts',(2.43380774867689,-1.65285929300723,
19.5829699872752));
#100811=CARTESIAN_POINT('Ctrl Pts',(2.48612170947426,-1.57582785803192,
19.5880096718986));
#100812=CARTESIAN_POINT('Ctrl Pts',(2.53483260151494,-1.49622544323132,
19.593049356522));
#100813=CARTESIAN_POINT('Ctrl Pts',(2.57968329096128,-1.41442501333057,
19.5980890411454));
#100814=CARTESIAN_POINT('Ctrl Pts',(2.62450161162462,-1.33268361887382,
19.6031250886239));
#100815=CARTESIAN_POINT('Ctrl Pts',(2.66546505407691,-1.24874775078289,
19.6081611361024));
#100816=CARTESIAN_POINT('Ctrl Pts',(2.70236070937266,-1.16301788311225,
19.6131971835808));
#100817=CARTESIAN_POINT('Ctrl Pts',(2.73924292628499,-1.0773192405499,19.6182313967962));
#100818=CARTESIAN_POINT('Ctrl Pts',(2.77206012391477,-0.989828304194625,
19.6232656100117));
#100819=CARTESIAN_POINT('Ctrl Pts',(2.80064658618208,-0.900967646093179,
19.6282998232271));
#100820=CARTESIAN_POINT('Ctrl Pts',(2.82923063544113,-0.812114488797507,
19.6333336115002));
#100821=CARTESIAN_POINT('Ctrl Pts',(2.85358452347601,-0.721892262642336,
19.6383673997732));
#100822=CARTESIAN_POINT('Ctrl Pts',(2.87359205454985,-0.630739806915627,
19.6434011880463));
#100823=CARTESIAN_POINT('Ctrl Pts',(2.89360349512767,-0.539569539851416,
19.6484359599298));
#100824=CARTESIAN_POINT('Ctrl Pts',(2.90926679717675,-0.447469116249552,
19.6534707318133));
#100825=CARTESIAN_POINT('Ctrl Pts',(2.920516874367,-0.354887568868786,19.6585055036967));
#100826=CARTESIAN_POINT('Ctrl Pts',(2.93177931959824,-0.262204239753328,
19.6635458106769));
#100827=CARTESIAN_POINT('Ctrl Pts',(2.93861880151689,-0.169039172781787,
19.668586117657));
#100828=CARTESIAN_POINT('Ctrl Pts',(2.94102216089823,-0.0758462201135838,
19.6736264246372));
#100829=CARTESIAN_POINT('Ctrl Pts',(2.94342699609299,0.0174039588738806,
19.678669826682));
#100830=CARTESIAN_POINT('Ctrl Pts',(2.94139029538589,0.110681613776166,
19.6837132287268));
#100831=CARTESIAN_POINT('Ctrl Pts',(2.93495099493572,0.203535395756719,
19.6887566307717));
#100832=CARTESIAN_POINT('Ctrl Pts',(2.92850125257871,0.296539748524878,
19.6938082111481));
#100833=CARTESIAN_POINT('Ctrl Pts',(2.91763470955827,0.389118415426352,
19.6988597915245));
#100834=CARTESIAN_POINT('Ctrl Pts',(2.9024418341689,0.480827827050681,19.7039113719009));
#100835=CARTESIAN_POINT('Ctrl Pts',(2.89469034284498,0.527618489799412,
19.7064887169035));
#100836=CARTESIAN_POINT('Ctrl Pts',(2.88581348025684,0.574183077988833,
19.7090660619061));
#100837=CARTESIAN_POINT('Ctrl Pts',(2.87582825256554,0.620464230835137,
19.7116434069087));
#100838=CARTESIAN_POINT('Ctrl Pts',(2.85625540692478,0.71118363040637,19.7166954675585));
#100839=CARTESIAN_POINT('Ctrl Pts',(2.83235050049138,0.801138980456197,
19.7217475282084));
#100840=CARTESIAN_POINT('Ctrl Pts',(2.8041876653406,0.889885126042465,19.7267995888582));
#100841=CARTESIAN_POINT('Ctrl Pts',(2.77606369827642,0.978508791315476,
19.7318446770591));
#100842=CARTESIAN_POINT('Ctrl Pts',(2.74369361293433,1.06592614851754,19.7368897652599));
#100843=CARTESIAN_POINT('Ctrl Pts',(2.70720247106711,1.15170255736805,19.7419348534608));
#100844=CARTESIAN_POINT('Ctrl Pts',(2.67075041329496,1.23738709479044,19.7469745380843));
#100845=CARTESIAN_POINT('Ctrl Pts',(2.63018624522835,1.32143377060214,19.7520142227079));
#100846=CARTESIAN_POINT('Ctrl Pts',(2.58568437665739,1.40342449184482,19.7570539073314));
#100847=CARTESIAN_POINT('Ctrl Pts',(2.54121462512511,1.48535604031002,19.76208995481));
#100848=CARTESIAN_POINT('Ctrl Pts',(2.4928130329673,1.56523419406149,19.7671260022886));
#100849=CARTESIAN_POINT('Ctrl Pts',(2.44070107974723,1.64266315455139,19.7721620497672));
#100850=CARTESIAN_POINT('Ctrl Pts',(2.38860810709281,1.72006391334518,19.7771962629827));
#100851=CARTESIAN_POINT('Ctrl Pts',(2.3328077059137,1.79501688282123,19.7822304761983));
#100852=CARTESIAN_POINT('Ctrl Pts',(2.27356548214273,1.86715398358279,19.7872646894138));
#100853=CARTESIAN_POINT('Ctrl Pts',(2.21432825905962,1.93928499518866,19.7922984776871));
#100854=CARTESIAN_POINT('Ctrl Pts',(2.15165007313315,2.00860026741789,19.7973322659603));
#100855=CARTESIAN_POINT('Ctrl Pts',(2.08583701390335,2.07476455325195,19.8023660542335));
#100856=CARTESIAN_POINT('Ctrl Pts',(2.02001109469515,2.14094176769465,19.8074008261171));
#100857=CARTESIAN_POINT('Ctrl Pts',(1.95104939921749,2.20396645822157,19.8124355980007));
#100858=CARTESIAN_POINT('Ctrl Pts',(1.87929425381006,2.2635408340908,19.8174703698843));
#100859=CARTESIAN_POINT('Ctrl Pts',(1.80746022267026,2.32318070447258,19.8225106768646));
#100860=CARTESIAN_POINT('Ctrl Pts',(1.73282695377717,2.37936240426445,19.8275509838449));
#100861=CARTESIAN_POINT('Ctrl Pts',(1.65576893424291,2.43182919556372,19.8325912908251));
#100862=CARTESIAN_POINT('Ctrl Pts',(1.57866359625056,2.48432820476426,19.8376346928701));
#100863=CARTESIAN_POINT('Ctrl Pts',(1.49913092188043,2.53310753196164,19.8426780949151));
#100864=CARTESIAN_POINT('Ctrl Pts',(1.41757149297742,2.57795559742556,19.84772149696));
#100865=CARTESIAN_POINT('Ctrl Pts',(1.33587980809967,2.62287638807519,19.8527730773366));
#100866=CARTESIAN_POINT('Ctrl Pts',(1.25215520600279,2.66385299514138,19.8578246577131));
#100867=CARTESIAN_POINT('Ctrl Pts',(1.16681962209446,2.70072137946426,19.8628762380897));
#100868=CARTESIAN_POINT('Ctrl Pts',(1.12328092247561,2.71953183855939,19.865453583091));
#100869=CARTESIAN_POINT('Ctrl Pts',(1.07932314081581,2.73727368152657,19.8680309280922));
#100870=CARTESIAN_POINT('Ctrl Pts',(1.03500371305417,2.75393015778616,19.8706082730935));
#100871=CARTESIAN_POINT('Ctrl Pts',(0.948129648114924,2.78657985281419,
19.8756603337431));
#100872=CARTESIAN_POINT('Ctrl Pts',(0.859553040888233,2.81517345709628,
19.8807123943928));
#100873=CARTESIAN_POINT('Ctrl Pts',(0.769688317028746,2.83953233731005,
19.8857644550424));
#100874=CARTESIAN_POINT('Ctrl Pts',(0.67994761725451,2.86385759935078,19.8908095432431));
#100875=CARTESIAN_POINT('Ctrl Pts',(0.588922758559964,2.88395963567448,
19.8958546314438));
#100876=CARTESIAN_POINT('Ctrl Pts',(0.497046894193138,2.89970832756899,
19.9008997196445));
#100877=CARTESIAN_POINT('Ctrl Pts',(0.405269434119334,2.91544015171589,
19.9059394042678));
#100878=CARTESIAN_POINT('Ctrl Pts',(0.312643215620222,2.92682782452305,
19.9109790888912));
#100879=CARTESIAN_POINT('Ctrl Pts',(0.219614190971859,2.9337916775265,19.9160187735146));
#100880=CARTESIAN_POINT('Ctrl Pts',(0.126652305454438,2.94075050471097,
19.921054820993));
#100881=CARTESIAN_POINT('Ctrl Pts',(0.033288633389895,2.94329182489224,
19.9260908684714));
#100882=CARTESIAN_POINT('Ctrl Pts',(-0.0600241394538181,2.94138761517125,
19.9311269159499));
#100883=CARTESIAN_POINT('Ctrl Pts',(-0.153302925292624,2.93948409901432,
19.9361611291652));
#100884=CARTESIAN_POINT('Ctrl Pts',(-0.246530404979054,2.93313827867081,
19.9411953423806));
#100885=CARTESIAN_POINT('Ctrl Pts',(-0.339253313795942,2.92237423836826,
19.946229555596));
#100886=CARTESIAN_POINT('Ctrl Pts',(-0.431968395791085,2.91161110666776,
19.9512633438691));
#100887=CARTESIAN_POINT('Ctrl Pts',(-0.524178550279414,2.89643054791783,
19.9562971321421));
#100888=CARTESIAN_POINT('Ctrl Pts',(-0.615436204776654,2.87690845837161,
19.9613309204152));
#100889=CARTESIAN_POINT('Ctrl Pts',(-0.706711691167461,2.85738255417746,
19.9663656922986));
#100890=CARTESIAN_POINT('Ctrl Pts',(-0.797033873563027,2.83351352767994,
19.9714004641821));
#100891=CARTESIAN_POINT('Ctrl Pts',(-0.885967058427973,2.80542801928342,
19.9764352360655));
#100892=CARTESIAN_POINT('Ctrl Pts',(-0.974998014113154,2.77731163441264,
19.9814755430456));
#100893=CARTESIAN_POINT('Ctrl Pts',(-1.06263649979134,2.74496964862536,
19.9865158500257));
#100894=CARTESIAN_POINT('Ctrl Pts',(-1.14846393133775,2.70857796609517,
19.9915561570059));
#100895=CARTESIAN_POINT('Ctrl Pts',(-1.23434406631143,2.67216393678891,
19.9965995590507));
#100896=CARTESIAN_POINT('Ctrl Pts',(-1.31841053314281,2.63169545265336,
20.0016429610955));
#100897=CARTESIAN_POINT('Ctrl Pts',(-1.40026859257394,2.587394803398,20.0066863631403));
#100898=CARTESIAN_POINT('Ctrl Pts',(-1.4822593922362,2.54302231664171,20.0117379435167));
#100899=CARTESIAN_POINT('Ctrl Pts',(-1.56203425538677,2.49480548833797,
20.0167895238931));
#100900=CARTESIAN_POINT('Ctrl Pts',(-1.63922685724251,2.44301029684585,
20.0218411042695));
#100901=CARTESIAN_POINT('Ctrl Pts',(-1.67861096119261,2.4165840959302,20.0244184492724));
#100902=CARTESIAN_POINT('Ctrl Pts',(-1.71732339786238,2.38922707104951,
20.0269957942753));
#100903=CARTESIAN_POINT('Ctrl Pts',(-1.75531899247482,2.36097844857957,
20.0295731392782));
#100904=CARTESIAN_POINT('Ctrl Pts',(-1.82907976954247,2.30613945038183,
20.034576534333));
#100905=CARTESIAN_POINT('Ctrl Pts',(-1.90041320610856,2.24773250319076,
20.0395799293878));
#100906=CARTESIAN_POINT('Ctrl Pts',(-1.96894869439112,2.18600206744081,
20.0445833244426));
#100907=CARTESIAN_POINT('Ctrl Pts',(-2.03738930140254,2.12435709197368,
20.0495797927432));
#100908=CARTESIAN_POINT('Ctrl Pts',(-2.10303931960925,2.05939806735333,
20.0545762610437));
#100909=CARTESIAN_POINT('Ctrl Pts',(-2.16555842516025,1.99141173724006,
20.0595727293443));
#100910=CARTESIAN_POINT('Ctrl Pts',(-2.22800653052416,1.92350261619936,
20.0645635233765));
#100911=CARTESIAN_POINT('Ctrl Pts',(-2.28733048517625,1.8525733552444,20.0695543174087));
#100912=CARTESIAN_POINT('Ctrl Pts',(-2.34322528180016,1.77894892527374,
20.0745451114409));
#100913=CARTESIAN_POINT('Ctrl Pts',(-2.39908531028227,1.70537029177743,
20.0795328010582));
#100914=CARTESIAN_POINT('Ctrl Pts',(-2.45152014164691,1.62910017771565,
20.0845204906756));
#100915=CARTESIAN_POINT('Ctrl Pts',(-2.50026434729797,1.55049740200707,
20.089508180293));
#100916=CARTESIAN_POINT('Ctrl Pts',(-2.54899251987054,1.47192048054014,
20.0944942293457));
#100917=CARTESIAN_POINT('Ctrl Pts',(-2.59403223871125,1.39101280656167,
20.0994802783985));
#100918=CARTESIAN_POINT('Ctrl Pts',(-2.63516153465743,1.30816194955437,
20.1044663274512));
#100919=CARTESIAN_POINT('Ctrl Pts',(-2.67628935711786,1.22531406073689,
20.1094521978753));
#100920=CARTESIAN_POINT('Ctrl Pts',(-2.71350683455284,1.14052353429524,
20.1144380682993));
#100921=CARTESIAN_POINT('Ctrl Pts',(-2.7466386640879,1.05420114254228,20.1194239387234));
#100922=CARTESIAN_POINT('Ctrl Pts',(-2.77979990513923,0.967802121382922,
20.1244142351635));
#100923=CARTESIAN_POINT('Ctrl Pts',(-2.80886809048247,0.879868943068014,
20.1294045316036));
#100924=CARTESIAN_POINT('Ctrl Pts',(-2.83371684144385,0.7908304891173,20.1343948280437));
#100925=CARTESIAN_POINT('Ctrl Pts',(-2.8585763585795,0.701753457633498,
20.1393872866207));
#100926=CARTESIAN_POINT('Ctrl Pts',(-2.87921269939872,0.61157063956846,
20.1443797451977));
#100927=CARTESIAN_POINT('Ctrl Pts',(-2.89555049922398,0.520721908933904,
20.1493722037747));
#100928=CARTESIAN_POINT('Ctrl Pts',(-2.91191514662537,0.429723888417112,
20.154372866358));
#100929=CARTESIAN_POINT('Ctrl Pts',(-2.92396708264555,0.338058219848184,
20.1593735289412));
#100930=CARTESIAN_POINT('Ctrl Pts',(-2.93168279631951,0.246170635462961,
20.1643741915245));
#100931=CARTESIAN_POINT('Ctrl Pts',(-2.93860014417155,0.163790908669531,
20.1688574219864));
#100932=CARTESIAN_POINT('Ctrl Pts',(-2.94203292020321,0.0812330863468883,
20.1733406524484));
#100933=CARTESIAN_POINT('Ctrl Pts',(-2.94199976189605,-0.00118363997366727,
20.1778238829104));
#100934=CARTESIAN_POINT('',(-2.94199876947892,0.00269079626312435,21.1778238829104));
#100935=CARTESIAN_POINT('Ctrl Pts',(-2.94627313971723,-0.00118535926028303,
20.1778238829104));
#100936=CARTESIAN_POINT('Ctrl Pts',(-2.94660879883213,-0.0669346369190534,
20.1813952570946));
#100937=CARTESIAN_POINT('Ctrl Pts',(-2.91478035335495,-1.10787161819102,
20.2379549200069));
#100938=CARTESIAN_POINT('Ctrl Pts',(-1.68204367473694,-3.04506152239431,
20.3475028716478));
#100939=CARTESIAN_POINT('Ctrl Pts',(1.64986237125127,-3.06261730478403,
20.5064677378324));
#100940=CARTESIAN_POINT('Ctrl Pts',(3.46820737751736,-0.270570109276814,
20.6654326040173));
#100941=CARTESIAN_POINT('Ctrl Pts',(2.1048666544717,2.76969438133523,20.8243974702019));
#100942=CARTESIAN_POINT('Ctrl Pts',(-1.18944977837209,3.26907935485098,
20.9833623363867));
#100943=CARTESIAN_POINT('Ctrl Pts',(-2.82218977905123,1.41660932964794,
21.1011711406229));
#100944=CARTESIAN_POINT('Ctrl Pts',(-2.94431188226859,0.221291506348862,
21.1659916561308));
#100945=CARTESIAN_POINT('Ctrl Pts',(-2.94228710142995,0.00269105997585707,
21.1778238829104));
#100946=CARTESIAN_POINT('',(-2.94152579413549,-0.000227484859817469,22.177823899892));
#100947=CARTESIAN_POINT('Ctrl Pts',(-2.94199876947892,0.00269079626312435,
21.1778238829104));
#100948=CARTESIAN_POINT('Ctrl Pts',(-2.94208568955751,-0.092343810318554,
21.182968390654));
#100949=CARTESIAN_POINT('Ctrl Pts',(-2.93756295517028,-0.187514566962741,
21.1881128983975));
#100950=CARTESIAN_POINT('Ctrl Pts',(-2.92842156909576,-0.282331566876175,
21.1932574061411));
#100951=CARTESIAN_POINT('Ctrl Pts',(-2.91959119562788,-0.373922657495653,
21.1982268849831));
#100952=CARTESIAN_POINT('Ctrl Pts',(-2.90645140284425,-0.465183175120309,
21.2031963638252));
#100953=CARTESIAN_POINT('Ctrl Pts',(-2.8890470071336,-0.555672017085965,
21.2081658426672));
#100954=CARTESIAN_POINT('Ctrl Pts',(-2.8716495703139,-0.646124678422679,
21.2131333345364));
#100955=CARTESIAN_POINT('Ctrl Pts',(-2.8499910018557,-0.735805828061689,
21.2181008264056));
#100956=CARTESIAN_POINT('Ctrl Pts',(-2.82416761979265,-0.824282266771967,
21.2230683182748));
#100957=CARTESIAN_POINT('Ctrl Pts',(-2.79834688003636,-0.912749652373244,
21.228035301859));
#100958=CARTESIAN_POINT('Ctrl Pts',(-2.76836230204739,-1.0000121330932,
21.2330022854432));
#100959=CARTESIAN_POINT('Ctrl Pts',(-2.7343603456571,-1.08565072656817,
21.2379692690275));
#100960=CARTESIAN_POINT('Ctrl Pts',(-2.70035175188033,-1.17130603721188,
21.2429372221968));
#100961=CARTESIAN_POINT('Ctrl Pts',(-2.66232439333023,-1.2553364070001,
21.2479051753661));
#100962=CARTESIAN_POINT('Ctrl Pts',(-2.62047271950662,-1.33734315952248,
21.2528731285354));
#100963=CARTESIAN_POINT('Ctrl Pts',(-2.57857604001892,-1.41943809892057,
21.2578464240485));
#100964=CARTESIAN_POINT('Ctrl Pts',(-2.53284704979247,-1.49950467242914,
21.2628197195616));
#100965=CARTESIAN_POINT('Ctrl Pts',(-2.48352571060707,-1.57716963093818,
21.2677930150748));
#100966=CARTESIAN_POINT('Ctrl Pts',(-2.43417250807282,-1.6548847637877,
21.2727695235146));
#100967=CARTESIAN_POINT('Ctrl Pts',(-2.38122260415856,-1.7301948231818,
21.2777460319545));
#100968=CARTESIAN_POINT('Ctrl Pts',(-2.32495739514281,-1.80275819531371,
21.2827225403944));
#100969=CARTESIAN_POINT('Ctrl Pts',(-2.26860603184925,-1.87543267775751,
21.2877066689515));
#100970=CARTESIAN_POINT('Ctrl Pts',(-2.20892953587721,-1.94535173976802,
21.2926907975087));
#100971=CARTESIAN_POINT('Ctrl Pts',(-2.1462469970462,-2.01220968779851,
21.2976749260658));
#100972=CARTESIAN_POINT('Ctrl Pts',(-2.13108341765969,-2.02838334351645,
21.2988806402959));
#100973=CARTESIAN_POINT('Ctrl Pts',(-2.11574407572406,-2.04437804425921,
21.3000863545261));
#100974=CARTESIAN_POINT('Ctrl Pts',(-2.10023377245074,-2.06018982160803,
21.3012920687562));
#100975=CARTESIAN_POINT('Ctrl Pts',(-2.03524408410839,-2.12644271582489,
21.3063441293552));
#100976=CARTESIAN_POINT('Ctrl Pts',(-1.96699957376989,-2.18973644539041,
21.3113961899542));
#100977=CARTESIAN_POINT('Ctrl Pts',(-1.89580061639637,-2.24973421160615,
21.3164482505532));
#100978=CARTESIAN_POINT('Ctrl Pts',(-1.82469992211389,-2.30964917371659,
21.3214933387033));
#100979=CARTESIAN_POINT('Ctrl Pts',(-1.75065322006327,-2.36627692772359,
21.3265384268534));
#100980=CARTESIAN_POINT('Ctrl Pts',(-1.67399833226664,-2.41931675965933,
21.3315835150036));
#100981=CARTESIAN_POINT('Ctrl Pts',(-1.59742554622715,-2.47229978290973,
21.3366231995765));
#100982=CARTESIAN_POINT('Ctrl Pts',(-1.51825049035633,-2.52170227089869,
21.3416628841494));
#100983=CARTESIAN_POINT('Ctrl Pts',(-1.43684387523728,-2.56726385052123,
21.3467025687224));
#100984=CARTESIAN_POINT('Ctrl Pts',(-1.35549601133922,-2.61279254831435,
21.3517386161508));
#100985=CARTESIAN_POINT('Ctrl Pts',(-1.27192017590671,-2.65448563107063,
21.3567746635793));
#100986=CARTESIAN_POINT('Ctrl Pts',(-1.18651497306713,-2.69212670925562,
21.3618107110077));
#100987=CARTESIAN_POINT('Ctrl Pts',(-1.10114087707972,-2.72975407755626,
21.3668449241734));
#100988=CARTESIAN_POINT('Ctrl Pts',(-1.01393914351902,-2.76333219419435,
21.3718791373391));
#100989=CARTESIAN_POINT('Ctrl Pts',(-0.925330884779896,-2.79269166820694,
21.3769133505048));
#100990=CARTESIAN_POINT('Ctrl Pts',(-0.836730105535406,-2.82204866396263,
21.3819471387285));
#100991=CARTESIAN_POINT('Ctrl Pts',(-0.746723458975725,-2.84718758552121,
21.3869809269522));
#100992=CARTESIAN_POINT('Ctrl Pts',(-0.655748755508701,-2.8679884186741,
21.3920147151759));
#100993=CARTESIAN_POINT('Ctrl Pts',(-0.564756275429846,-2.88879331634519,
21.3970494870103));
#100994=CARTESIAN_POINT('Ctrl Pts',(-0.472795795954753,-2.90525834347357,
21.4020842588448));
#100995=CARTESIAN_POINT('Ctrl Pts',(-0.380315765807076,-2.91731450451928,
21.4071190306793));
#100996=CARTESIAN_POINT('Ctrl Pts',(-0.287734065512315,-2.92938391979582,
21.4121593376114));
#100997=CARTESIAN_POINT('Ctrl Pts',(-0.194632115655815,-2.93703473625338,
21.4171996445435));
#100998=CARTESIAN_POINT('Ctrl Pts',(-0.101463636534064,-2.94024984150349,
21.4222399514755));
#100999=CARTESIAN_POINT('Ctrl Pts',(-0.00823794611273068,-2.94346692103021,
21.4272833534727));
#101000=CARTESIAN_POINT('Ctrl Pts',(0.0850539109652886,-2.94224287261987,
21.4323267554699));
#101001=CARTESIAN_POINT('Ctrl Pts',(0.177960263810673,-2.93661269909814,
21.4373701574671));
#101002=CARTESIAN_POINT('Ctrl Pts',(0.271017272714683,-2.93097339574054,
21.4424217377971));
#101003=CARTESIAN_POINT('Ctrl Pts',(0.363687088218949,-2.92091375109494,
21.447473318127));
#101004=CARTESIAN_POINT('Ctrl Pts',(0.455525369650964,-2.90652036593662,
21.4525248984569));
#101005=CARTESIAN_POINT('Ctrl Pts',(0.502381791884863,-2.89917677760028,
21.4551022439516));
#101006=CARTESIAN_POINT('Ctrl Pts',(0.549021951560869,-2.89070589085695,
21.4576795894463));
#101007=CARTESIAN_POINT('Ctrl Pts',(0.595388341891801,-2.88112421154301,
21.460256934941));
#101008=CARTESIAN_POINT('Ctrl Pts',(0.686274804721182,-2.86234239707365,
21.4653089955786));
#101009=CARTESIAN_POINT('Ctrl Pts',(0.776434985139052,-2.8392220303162,
21.4703610562162));
#101010=CARTESIAN_POINT('Ctrl Pts',(0.865423099306033,-2.81183336262794,
21.4754131168539));
#101011=CARTESIAN_POINT('Ctrl Pts',(0.95428839920448,-2.78448249458539,
21.480458205042));
#101012=CARTESIAN_POINT('Ctrl Pts',(1.04198442625007,-2.75287516083567,
21.4855032932302));
#101013=CARTESIAN_POINT('Ctrl Pts',(1.12807546719918,-2.71713263207804,
21.4905483814183));
#101014=CARTESIAN_POINT('Ctrl Pts',(1.21407429972261,-2.6814283856117,21.4955880660287));
#101015=CARTESIAN_POINT('Ctrl Pts',(1.29847115483984,-2.64159791691911,
21.500627750639));
#101016=CARTESIAN_POINT('Ctrl Pts',(1.38084643611309,-2.59781198701403,
21.5056674352493));
#101017=CARTESIAN_POINT('Ctrl Pts',(1.46316226706027,-2.55405765746004,
21.510703482714));
#101018=CARTESIAN_POINT('Ctrl Pts',(1.54345903287469,-2.50635374865088,
21.5157395301788));
#101019=CARTESIAN_POINT('Ctrl Pts',(1.62133902064147,-2.454918283802,21.5207755776435));
#101020=CARTESIAN_POINT('Ctrl Pts',(1.69919064242934,-2.40350155312802,
21.5258097908447));
#101021=CARTESIAN_POINT('Ctrl Pts',(1.77462686451415,-2.34835621107149,
21.530844004046));
#101022=CARTESIAN_POINT('Ctrl Pts',(1.84727730767968,-2.28974464701454,
21.5358782172472));
#101023=CARTESIAN_POINT('Ctrl Pts',(1.9199216183521,-2.23113803041553,21.5409120055057));
#101024=CARTESIAN_POINT('Ctrl Pts',(1.98978027194905,-2.16906605265924,
21.5459457937642));
#101025=CARTESIAN_POINT('Ctrl Pts',(2.05651536771951,-2.10383187121345,
21.5509795820228));
#101026=CARTESIAN_POINT('Ctrl Pts',(2.12326350363077,-2.03858494290784,
21.5560143538913));
#101027=CARTESIAN_POINT('Ctrl Pts',(2.18688655211979,-1.97017489458745,
21.5610491257598));
#101028=CARTESIAN_POINT('Ctrl Pts',(2.24708375161924,-1.89894144543975,
21.5660838976283));
#101029=CARTESIAN_POINT('Ctrl Pts',(2.30734713034196,-1.82762968410519,
21.5711242045931));
#101030=CARTESIAN_POINT('Ctrl Pts',(2.36417685486138,-1.75348866590415,
21.5761645115578));
#101031=CARTESIAN_POINT('Ctrl Pts',(2.41731293472768,-1.67689062720209,
21.5812048185226));
#101032=CARTESIAN_POINT('Ctrl Pts',(2.47048164347745,-1.60024555250332,
21.5862482205517));
#101033=CARTESIAN_POINT('Ctrl Pts',(2.51995195677038,-1.52114083008159,
21.5912916225808));
#101034=CARTESIAN_POINT('Ctrl Pts',(2.56550881329504,-1.43997518343389,
21.5963350246099));
#101035=CARTESIAN_POINT('Ctrl Pts',(2.61113954437165,-1.35867791936926,
21.6013866049704));
#101036=CARTESIAN_POINT('Ctrl Pts',(2.65284395100615,-1.27531345605971,
21.6064381853308));
#101037=CARTESIAN_POINT('Ctrl Pts',(2.69045432463521,-1.19030228389755,
21.6114897656912));
#101038=CARTESIAN_POINT('Ctrl Pts',(2.70964335201929,-1.14692909843915,
21.6140671108361));
#101039=CARTESIAN_POINT('Ctrl Pts',(2.72776745447538,-1.10312753770133,
21.6166444559809));
#101040=CARTESIAN_POINT('Ctrl Pts',(2.74480938171181,-1.05895488953347,
21.6192218011258));
#101041=CARTESIAN_POINT('Ctrl Pts',(2.77821462964113,-0.972368540274324,
21.6242738619854));
#101042=CARTESIAN_POINT('Ctrl Pts',(2.80757877179907,-0.884044379248353,
21.629325922845));
#101043=CARTESIAN_POINT('Ctrl Pts',(2.83271957144272,-0.79439526028633,
21.6343779837046));
#101044=CARTESIAN_POINT('Ctrl Pts',(2.85782567377613,-0.704869867830115,
21.639423072116));
#101045=CARTESIAN_POINT('Ctrl Pts',(2.87871989703247,-0.614023575165785,
21.6444681605274));
#101046=CARTESIAN_POINT('Ctrl Pts',(2.89526835409674,-0.522288385631872,
21.6495132489388));
#101047=CARTESIAN_POINT('Ctrl Pts',(2.91179908682151,-0.430651449707756,
21.6545529337733));
#101048=CARTESIAN_POINT('Ctrl Pts',(2.92399322651787,-0.338127944159667,
21.6595926186079));
#101049=CARTESIAN_POINT('Ctrl Pts',(2.9317672229085,-0.245163110355933,
21.6646323034424));
#101050=CARTESIAN_POINT('Ctrl Pts',(2.9395356087989,-0.152265369356827,
21.6696683511319));
#101051=CARTESIAN_POINT('Ctrl Pts',(2.94289015506298,-0.0589273746584211,
21.6747043988213));
#101052=CARTESIAN_POINT('Ctrl Pts',(2.94179889637111,0.0343984492339381,
21.6797404465107));
#101053=CARTESIAN_POINT('Ctrl Pts',(2.94070803514484,0.127690281365921,
21.684774659937));
#101054=CARTESIAN_POINT('Ctrl Pts',(2.93517459101143,0.220969507675514,
21.6898088733632));
#101055=CARTESIAN_POINT('Ctrl Pts',(2.92521869874725,0.31378267080806,21.6948430867894));
#101056=CARTESIAN_POINT('Ctrl Pts',(2.91526364686947,0.406587999492738,
21.6998768752729));
#101057=CARTESIAN_POINT('Ctrl Pts',(2.90088693663444,0.498926901469453,
21.7049106637563));
#101058=CARTESIAN_POINT('Ctrl Pts',(2.88216056246513,0.590351160048563,
21.7099444522398));
#101059=CARTESIAN_POINT('Ctrl Pts',(2.86343052913474,0.681793283062371,
21.7149792243329));
#101060=CARTESIAN_POINT('Ctrl Pts',(2.84034923342057,0.772319972569361,
21.720013996426));
#101061=CARTESIAN_POINT('Ctrl Pts',(2.81303951545293,0.861494448328216,
21.7250487685191));
#101062=CARTESIAN_POINT('Ctrl Pts',(2.7856997739086,0.950766960131055,21.7300890757066));
#101063=CARTESIAN_POINT('Ctrl Pts',(2.75412246119298,1.03868386528113,21.7351293828941));
#101064=CARTESIAN_POINT('Ctrl Pts',(2.71847982838235,1.12482506314461,21.7401696900816));
#101065=CARTESIAN_POINT('Ctrl Pts',(2.68281530876714,1.21101915708829,21.7452130923328));
#101066=CARTESIAN_POINT('Ctrl Pts',(2.64308068838097,1.29543497128397,21.750256494584));
#101067=CARTESIAN_POINT('Ctrl Pts',(2.59949480979731,1.37767584497837,21.7552998968352));
#101068=CARTESIAN_POINT('Ctrl Pts',(2.55583825281186,1.46005007960762,21.7603514774143));
#101069=CARTESIAN_POINT('Ctrl Pts',(2.50831819607966,1.54024195098564,21.7654030579935));
#101070=CARTESIAN_POINT('Ctrl Pts',(2.4571974166949,1.61788283116792,21.7704546385727));
#101071=CARTESIAN_POINT('Ctrl Pts',(2.43111532686805,1.65749561554877,21.7730319814852));
#101072=CARTESIAN_POINT('Ctrl Pts',(2.40409659879385,1.69644486793155,21.7756093243978));
#101073=CARTESIAN_POINT('Ctrl Pts',(2.37618006372778,1.73468507364958,21.7781866673104));
#101074=CARTESIAN_POINT('Ctrl Pts',(2.32145858420865,1.80964282284925,21.7832387275705));
#101075=CARTESIAN_POINT('Ctrl Pts',(2.26308843126375,1.88214339907823,21.7882907878305));
#101076=CARTESIAN_POINT('Ctrl Pts',(2.20131809666195,1.9518100925317,21.7933428480905));
#101077=CARTESIAN_POINT('Ctrl Pts',(2.13963301252477,2.021380637599,21.7983879359019));
#101078=CARTESIAN_POINT('Ctrl Pts',(2.07455736380772,2.08812474215966,21.8034330237133));
#101079=CARTESIAN_POINT('Ctrl Pts',(2.00638191565684,2.15169598422388,21.8084781115247));
#101080=CARTESIAN_POINT('Ctrl Pts',(1.93827948729521,2.21519913786591,21.8135177957597));
#101081=CARTESIAN_POINT('Ctrl Pts',(1.86708418180217,2.27553588228219,21.8185574799946));
#101082=CARTESIAN_POINT('Ctrl Pts',(1.79312514287188,2.3323949541192,21.8235971642295));
#101083=CARTESIAN_POINT('Ctrl Pts',(1.71921948020912,2.38921299074167,21.8286332113223));
#101084=CARTESIAN_POINT('Ctrl Pts',(1.64255439984473,2.44255807340714,21.8336692584152));
#101085=CARTESIAN_POINT('Ctrl Pts',(1.56349300852536,2.49215842439687,21.838705305508));
#101086=CARTESIAN_POINT('Ctrl Pts',(1.48446041344956,2.54174070963082,21.8437395183396));
#101087=CARTESIAN_POINT('Ctrl Pts',(1.40303361730671,2.58758073688774,21.8487737311713));
#101088=CARTESIAN_POINT('Ctrl Pts',(1.31960479743701,2.62944997643637,21.853807944003));
#101089=CARTESIAN_POINT('Ctrl Pts',(1.23618301982847,2.67131568178519,21.8588417318947));
#101090=CARTESIAN_POINT('Ctrl Pts',(1.15075995166674,2.70921106670083,21.8638755197864));
#101091=CARTESIAN_POINT('Ctrl Pts',(1.06375143579366,2.74295404315255,21.868909307678));
#101092=CARTESIAN_POINT('Ctrl Pts',(0.976725918265993,2.77670361305579,
21.8739440791829));
#101093=CARTESIAN_POINT('Ctrl Pts',(0.888114752116835,2.80629900278147,
21.8789788506878));
#101094=CARTESIAN_POINT('Ctrl Pts',(0.798351687265794,2.83160706727467,
21.8840136221926));
#101095=CARTESIAN_POINT('Ctrl Pts',(0.708489939122239,2.85694295482778,
21.8890539288007));
#101096=CARTESIAN_POINT('Ctrl Pts',(0.617474192739987,2.87798198789189,
21.8940942354088));
#101097=CARTESIAN_POINT('Ctrl Pts',(0.525750919889955,2.89464159616262,
21.8991345420169));
#101098=CARTESIAN_POINT('Ctrl Pts',(0.43397132313475,2.91131143448911,21.9041779436928));
#101099=CARTESIAN_POINT('Ctrl Pts',(0.341483775087955,2.92359643581221,
21.9092213453687));
#101100=CARTESIAN_POINT('Ctrl Pts',(0.248740258974479,2.9314658932973,21.9142647470446));
#101101=CARTESIAN_POINT('Ctrl Pts',(0.155846350712511,2.93934811183208,
21.9193163270606));
#101102=CARTESIAN_POINT('Ctrl Pts',(0.0626960891820613,2.94280047552177,
21.9243679070766));
#101103=CARTESIAN_POINT('Ctrl Pts',(-0.0302583310267743,2.94184439313222,
21.9294194870926));
#101104=CARTESIAN_POINT('Ctrl Pts',(-0.0776842775038254,2.94135659371254,
21.9319968358935));
#101105=CARTESIAN_POINT('Ctrl Pts',(-0.125059318147335,2.93972206567021,
21.9345741846944));
#101106=CARTESIAN_POINT('Ctrl Pts',(-0.17232416304451,2.9369488219632,21.9371515334952));
#101107=CARTESIAN_POINT('Ctrl Pts',(-0.264971640504095,2.93151277251895,
21.9422035941855));
#101108=CARTESIAN_POINT('Ctrl Pts',(-0.357528117153358,2.92167874159305,
21.9472556548757));
#101109=CARTESIAN_POINT('Ctrl Pts',(-0.449542335570193,2.90745175171147,
21.952307715566));
#101110=CARTESIAN_POINT('Ctrl Pts',(-0.54142956327939,2.89324439679005,
21.9573528038038));
#101111=CARTESIAN_POINT('Ctrl Pts',(-0.63277558461395,2.87465619775139,
21.9623978920416));
#101112=CARTESIAN_POINT('Ctrl Pts',(-0.723131726038894,2.8517441166409,
21.9674429802794));
#101113=CARTESIAN_POINT('Ctrl Pts',(-0.813391090819521,2.82885657569215,
21.9724826649364));
#101114=CARTESIAN_POINT('Ctrl Pts',(-0.902662254674683,2.80165446632487,
21.9775223495934));
#101115=CARTESIAN_POINT('Ctrl Pts',(-0.990505331762105,2.77024605184284,
21.9825620342505));
#101116=CARTESIAN_POINT('Ctrl Pts',(-1.07828501233058,2.7388603048744,21.9875980817573));
#101117=CARTESIAN_POINT('Ctrl Pts',(-1.16463823753488,2.70327443580654,
21.9926341292641));
#101118=CARTESIAN_POINT('Ctrl Pts',(-1.24913993761244,2.6636466387758,21.997670176771));
#101119=CARTESIAN_POINT('Ctrl Pts',(-1.33361085985892,2.62403327527292,
22.0027043900115));
#101120=CARTESIAN_POINT('Ctrl Pts',(-1.41623119483375,2.58038109689235,
22.0077386032521));
#101121=CARTESIAN_POINT('Ctrl Pts',(-1.49659650065452,2.53289615148917,
22.0127728164926));
#101122=CARTESIAN_POINT('Ctrl Pts',(-1.57695502271736,2.48541521436259,
22.0178066047875));
#101123=CARTESIAN_POINT('Ctrl Pts',(-1.65505851165594,2.43410237963196,
22.0228403930825));
#101124=CARTESIAN_POINT('Ctrl Pts',(-1.73052876463478,2.37920873291345,
22.0278741813774));
#101125=CARTESIAN_POINT('Ctrl Pts',(-1.80601376457456,2.3243043599229,22.0329089532795));
#101126=CARTESIAN_POINT('Ctrl Pts',(-1.8788641476136,2.26581804698184,22.0379437251816));
#101127=CARTESIAN_POINT('Ctrl Pts',(-1.94873317017218,2.20404242959856,
22.0429784970836));
#101128=CARTESIAN_POINT('Ctrl Pts',(-2.01867900483887,2.14219889777726,
22.0480188040774));
#101129=CARTESIAN_POINT('Ctrl Pts',(-2.0856366030939,2.07705913793298,22.0530591110711));
#101130=CARTESIAN_POINT('Ctrl Pts',(-2.14929485944968,2.00895385888854,
22.0580994180648));
#101131=CARTESIAN_POINT('Ctrl Pts',(-2.21299220593247,1.9408067589687,22.0631428201204));
#101132=CARTESIAN_POINT('Ctrl Pts',(-2.27338588976149,1.86969085298636,
22.068186222176));
#101133=CARTESIAN_POINT('Ctrl Pts',(-2.33020543016506,1.79596955799069,
22.0732296242315));
#101134=CARTESIAN_POINT('Ctrl Pts',(-2.38711710853098,1.72212871732719,
22.0782812046142));
#101135=CARTESIAN_POINT('Ctrl Pts',(-2.44044281894712,1.64567441712911,
22.083332784997));
#101136=CARTESIAN_POINT('Ctrl Pts',(-2.48995578633093,1.56699846270414,
22.0883843653797));
#101137=CARTESIAN_POINT('Ctrl Pts',(-2.51521758119624,1.52685754757558,
22.0909617101464));
#101138=CARTESIAN_POINT('Ctrl Pts',(-2.53948762525191,1.48613870506356,
22.0935390549132));
#101139=CARTESIAN_POINT('Ctrl Pts',(-2.56274056206897,1.44489612482227,
22.0961163996799));
#101140=CARTESIAN_POINT('Ctrl Pts',(-2.6103764335966,1.36040674314553,22.1013963376576));
#101141=CARTESIAN_POINT('Ctrl Pts',(-2.65389921416439,1.27343736533958,
22.1066762756352));
#101142=CARTESIAN_POINT('Ctrl Pts',(-2.69305519158291,1.18440606849522,
22.1119562136129));
#101143=CARTESIAN_POINT('Ctrl Pts',(-2.73376136689767,1.09184999361783,
22.1174451860543));
#101144=CARTESIAN_POINT('Ctrl Pts',(-2.76974753991899,0.997065665326674,
22.1229341584958));
#101145=CARTESIAN_POINT('Ctrl Pts',(-2.8007794475078,0.900554543832798,
22.1284231309372));
#101146=CARTESIAN_POINT('Ctrl Pts',(-2.83050512030054,0.808105892064405,
22.1336810545211));
#101147=CARTESIAN_POINT('Ctrl Pts',(-2.85568497940642,0.714073287878334,
22.1389389781049));
#101148=CARTESIAN_POINT('Ctrl Pts',(-2.87616093144695,0.618920266608081,
22.1441969016888));
#101149=CARTESIAN_POINT('Ctrl Pts',(-2.8966088623409,0.52389746134687,22.149447629854));
#101150=CARTESIAN_POINT('Ctrl Pts',(-2.91236561448378,0.427757666820328,
22.1546983580192));
#101151=CARTESIAN_POINT('Ctrl Pts',(-2.92332287558182,0.330979402833541,
22.1599490861844));
#101152=CARTESIAN_POINT('Ctrl Pts',(-2.93426307423731,0.234351840153816,
22.1651916380136));
#101153=CARTESIAN_POINT('Ctrl Pts',(-2.94041862569877,0.137088172150242,
22.1704341898429));
#101154=CARTESIAN_POINT('Ctrl Pts',(-2.94173245156721,0.0396759800933485,
22.1756767416722));
#101155=CARTESIAN_POINT('Ctrl Pts',(-2.9419118152177,0.0263772570361183,
22.1763924554182));
#101156=CARTESIAN_POINT('Ctrl Pts',(-2.94200101859664,0.0130757779320145,
22.1771081691643));
#101157=CARTESIAN_POINT('Ctrl Pts',(-2.94199999122659,-0.000227206362431655,
22.1778238829104));
#101158=CARTESIAN_POINT('',(-2.94312392831984,-0.00259505423936747,23.1778238829104));
#101159=CARTESIAN_POINT('Ctrl Pts',(-2.9371647108909,-0.000230046137197137,
22.1778240560681));
#101160=CARTESIAN_POINT('Ctrl Pts',(-2.93749219107628,-0.478103761682066,
22.2035764593337));
#101161=CARTESIAN_POINT('Ctrl Pts',(-2.6012367037522,-1.93881763980532,
22.2823171513272));
#101162=CARTESIAN_POINT('Ctrl Pts',(-0.300772375801865,-3.46571890274164,
22.4140461320495));
#101163=CARTESIAN_POINT('Ctrl Pts',(2.75125260656092,-2.12891426657218,
22.5730109982341));
#101164=CARTESIAN_POINT('Ctrl Pts',(3.279317883015,1.16092598313884,22.731975864419));
#101165=CARTESIAN_POINT('Ctrl Pts',(0.798979033620407,3.38575070070742,
22.8909407306036));
#101166=CARTESIAN_POINT('Ctrl Pts',(-2.20513524174184,2.56189931173273,
23.0395567367676));
#101167=CARTESIAN_POINT('Ctrl Pts',(-2.93587608380215,0.784594837198067,
23.1351844542031));
#101168=CARTESIAN_POINT('Ctrl Pts',(-2.94312392831984,-0.00259505423936747,
23.1778238829104));
#101169=CARTESIAN_POINT('',(-2.14321747322427,2.01117680924495,24.058));
#101170=CARTESIAN_POINT('Ctrl Pts',(-2.94312392831984,-0.00259505423936747,
23.1778238829104));
#101171=CARTESIAN_POINT('Ctrl Pts',(-2.94488302619335,-0.193651037946246,
23.1881727429313));
#101172=CARTESIAN_POINT('Ctrl Pts',(-2.84079414435847,-1.36104498058977,
23.2515098916811));
#101173=CARTESIAN_POINT('Ctrl Pts',(-1.28036762178996,-3.23455542907612,
23.3678353291575));
#101174=CARTESIAN_POINT('Ctrl Pts',(2.02658934189923,-2.82744350159193,
23.5268001953429));
#101175=CARTESIAN_POINT('Ctrl Pts',(3.47445766960654,0.173475693601123,
23.6857650615274));
#101176=CARTESIAN_POINT('Ctrl Pts',(1.73476021572655,3.01534707573969,23.8447299277121));
#101177=CARTESIAN_POINT('Ctrl Pts',(-0.865109513097841,3.07423831390616,
23.9688082405364));
#101178=CARTESIAN_POINT('Ctrl Pts',(-1.91559325183167,2.25747821289124,
24.0398982646323));
#101179=CARTESIAN_POINT('Ctrl Pts',(-2.14321747322427,2.01117680924495,
24.058));
#101180=CARTESIAN_POINT('',(0.261321691565681,2.93037113238532,24.0579967072125));
#101181=CARTESIAN_POINT('Origin',(0.,0.,24.058));
#101182=CARTESIAN_POINT('',(-2.94199917298087,-0.00220594195414625,23.3221761170896));
#101183=CARTESIAN_POINT('Ctrl Pts',(0.261321691565681,2.93037113238532,
24.0579967072125));
#101184=CARTESIAN_POINT('Ctrl Pts',(0.359057733722356,2.92165532585111,
24.0527226020593));
#101185=CARTESIAN_POINT('Ctrl Pts',(0.456247631980505,2.90805537680646,
24.0474484969061));
#101186=CARTESIAN_POINT('Ctrl Pts',(0.552404207582251,2.88967361330747,
24.0421743917529));
#101187=CARTESIAN_POINT('Ctrl Pts',(0.648847947472514,2.87123695407197,
24.0368845358865));
#101188=CARTESIAN_POINT('Ctrl Pts',(0.744251823606086,2.84798999998556,
24.03159468002));
#101189=CARTESIAN_POINT('Ctrl Pts',(0.838140963850976,2.82008576548923,
24.0263048241535));
#101190=CARTESIAN_POINT('Ctrl Pts',(0.932174041408198,2.79213875223801,
24.0210068586416));
#101191=CARTESIAN_POINT('Ctrl Pts',(1.02468739675793,2.75952034278332,24.0157088931297));
#101192=CARTESIAN_POINT('Ctrl Pts',(1.1152259313767,2.72243183973171,24.0104109276178));
#101193=CARTESIAN_POINT('Ctrl Pts',(1.20603083901619,2.68523421875994,24.0050973749851));
#101194=CARTESIAN_POINT('Ctrl Pts',(1.29484896517312,2.6435403648311,23.9997838223524));
#101195=CARTESIAN_POINT('Ctrl Pts',(1.3812482474766,2.5975983675008,23.9944702697197));
#101196=CARTESIAN_POINT('Ctrl Pts',(1.4529996823673,2.55944522383677,23.9900575591555));
#101197=CARTESIAN_POINT('Ctrl Pts',(1.52308332424415,2.51836314368226,23.9856448485912));
#101198=CARTESIAN_POINT('Ctrl Pts',(1.591268138782,2.47451605581723,23.981232138027));
#101199=CARTESIAN_POINT('Ctrl Pts',(1.66945284296764,2.42423841529911,23.9761722654958));
#101200=CARTESIAN_POINT('Ctrl Pts',(1.7453902427937,2.37016300472242,23.9711123929647));
#101201=CARTESIAN_POINT('Ctrl Pts',(1.81868893726781,2.31251692955093,23.9660525204335));
#101202=CARTESIAN_POINT('Ctrl Pts',(1.89188680650336,2.25495014882422,23.9609996079561));
#101203=CARTESIAN_POINT('Ctrl Pts',(1.96245283852198,2.19382273562446,23.9559466954787));
#101204=CARTESIAN_POINT('Ctrl Pts',(2.03002345584912,2.12940573134911,23.9508937830013));
#101205=CARTESIAN_POINT('Ctrl Pts',(2.09752182464432,2.06505760366796,23.9458462732496));
#101206=CARTESIAN_POINT('Ctrl Pts',(2.16203082654755,1.99742718056391,23.9407987634979));
#101207=CARTESIAN_POINT('Ctrl Pts',(2.2232197764767,1.92682584202176,23.9357512537462));
#101208=CARTESIAN_POINT('Ctrl Pts',(2.28436421696083,1.85627585958885,23.9307074156028));
#101209=CARTESIAN_POINT('Ctrl Pts',(2.34219311717723,1.78275959127877,23.9256635774594));
#101210=CARTESIAN_POINT('Ctrl Pts',(2.39641324748676,1.7066246064293,23.920619739316));
#101211=CARTESIAN_POINT('Ctrl Pts',(2.4506133994977,1.63051767476695,23.9155777596577));
#101212=CARTESIAN_POINT('Ctrl Pts',(2.5012071669494,1.55179430389707,23.9105357799994));
#101213=CARTESIAN_POINT('Ctrl Pts',(2.54794279767852,1.47083360709435,23.9054938003411));
#101214=CARTESIAN_POINT('Ctrl Pts',(2.59467416993196,1.3898802873004,23.9004522800999));
#101215=CARTESIAN_POINT('Ctrl Pts',(2.63754788331948,1.30669043042103,23.8954107598587));
#101216=CARTESIAN_POINT('Ctrl Pts',(2.67635715586578,1.22166950287139,23.8903692396175));
#101217=CARTESIAN_POINT('Ctrl Pts',(2.71517365562128,1.13663274240374,23.8853267805253));
#101218=CARTESIAN_POINT('Ctrl Pts',(2.74992402779534,1.04976463689369,23.8802843214332));
#101219=CARTESIAN_POINT('Ctrl Pts',(2.78044928756233,0.961491424451683,
23.8752418623411));
#101220=CARTESIAN_POINT('Ctrl Pts',(2.81100731255043,0.873123461257484,
23.8701939907713));
#101221=CARTESIAN_POINT('Ctrl Pts',(2.83733102728764,0.783347799512513,
23.8651461192015));
#101222=CARTESIAN_POINT('Ctrl Pts',(2.85931117778128,0.692606373501589,
23.8600982476317));
#101223=CARTESIAN_POINT('Ctrl Pts',(2.88130456619673,0.601810296913911,
23.8550473358948));
#101224=CARTESIAN_POINT('Ctrl Pts',(2.8989490981255,0.510047732412025,23.849996424158));
#101225=CARTESIAN_POINT('Ctrl Pts',(2.91218695661328,0.417769230235415,
23.8449455124211));
#101226=CARTESIAN_POINT('Ctrl Pts',(2.92544578927689,0.325344521213357,
23.8398865979767));
#101227=CARTESIAN_POINT('Ctrl Pts',(2.93428396748588,0.232402682732934,
23.8348276835322));
#101228=CARTESIAN_POINT('Ctrl Pts',(2.93869568164846,0.139397599192756,
23.8297687690878));
#101229=CARTESIAN_POINT('Ctrl Pts',(2.94085508511951,0.0938743642728768,
23.8272925802395));
#101230=CARTESIAN_POINT('Ctrl Pts',(2.94195478478335,0.0483359531580007,
23.8248163913912));
#101231=CARTESIAN_POINT('Ctrl Pts',(2.94199863385711,0.00283520421246993,
23.822340202543));
#101232=CARTESIAN_POINT('Ctrl Pts',(2.94208825862301,-0.0901654825415715,
23.8172790273149));
#101233=CARTESIAN_POINT('Ctrl Pts',(2.93776390565251,-0.18333064952558,
23.8122178520868));
#101234=CARTESIAN_POINT('Ctrl Pts',(2.92900549655993,-0.276207894749105,
23.8071566768588));
#101235=CARTESIAN_POINT('Ctrl Pts',(2.92025884316683,-0.368960478407758,
23.8021022948342));
#101236=CARTESIAN_POINT('Ctrl Pts',(2.90709000256503,-0.46142547144831,
23.7970479128096));
#101237=CARTESIAN_POINT('Ctrl Pts',(2.88953090489682,-0.553150205320539,
23.791993530785));
#101238=CARTESIAN_POINT('Ctrl Pts',(2.87199000635214,-0.644779871109348,
23.7869443873737));
#101239=CARTESIAN_POINT('Ctrl Pts',(2.85006797892551,-0.735670370570118,
23.7818952439624));
#101240=CARTESIAN_POINT('Ctrl Pts',(2.82384846507248,-0.825374973153284,
23.7768461005511));
#101241=CARTESIAN_POINT('Ctrl Pts',(2.79764677704639,-0.915018588384454,
23.7718003898944));
#101242=CARTESIAN_POINT('Ctrl Pts',(2.76715353378432,-1.0034774857748,23.7667546792377));
#101243=CARTESIAN_POINT('Ctrl Pts',(2.73250306386018,-1.09031692915167,
23.761708968581));
#101244=CARTESIAN_POINT('Ctrl Pts',(2.69786434134265,-1.17712693170844,
23.7566649685509));
#101245=CARTESIAN_POINT('Ctrl Pts',(2.6590713562346,-1.26231816054592,23.7516209685208));
#101246=CARTESIAN_POINT('Ctrl Pts',(2.61630737697131,-1.3454737861458,23.7465769684907));
#101247=CARTESIAN_POINT('Ctrl Pts',(2.57354605543116,-1.42862424373665,
23.7415332819383));
#101248=CARTESIAN_POINT('Ctrl Pts',(2.52681443305615,-1.50973895632797,
23.7364895953859));
#101249=CARTESIAN_POINT('Ctrl Pts',(2.47634223213565,-1.58842473833085,
23.7314459088336));
#101250=CARTESIAN_POINT('Ctrl Pts',(2.4258591936746,-1.66712741597801,23.7264011392859));
#101251=CARTESIAN_POINT('Ctrl Pts',(2.37163422037517,-1.74339975488208,
23.7213563697382));
#101252=CARTESIAN_POINT('Ctrl Pts',(2.31394031524762,-1.81687760112555,
23.7163116001905));
#101253=CARTESIAN_POINT('Ctrl Pts',(2.25618215362255,-1.89043728320652,
23.7112612120385));
#101254=CARTESIAN_POINT('Ctrl Pts',(2.19494762177065,-1.96119591149916,
23.7062108238865));
#101255=CARTESIAN_POINT('Ctrl Pts',(2.13054978681914,-2.02882271425694,
23.7011604357345));
#101256=CARTESIAN_POINT('Ctrl Pts',(2.06611164201707,-2.09649184803898,
23.6961068862901));
#101257=CARTESIAN_POINT('Ctrl Pts',(1.99850657162384,-2.16102494801463,
23.6910533368456));
#101258=CARTESIAN_POINT('Ctrl Pts',(1.92808265482739,-2.22212989632779,
23.6859997874012));
#101259=CARTESIAN_POINT('Ctrl Pts',(1.85754493690038,-2.28333358683703,
23.680938071702));
#101260=CARTESIAN_POINT('Ctrl Pts',(1.78417962593036,-2.34109779290347,
23.6758763560029));
#101261=CARTESIAN_POINT('Ctrl Pts',(1.70836568544675,-2.39517237057964,
23.6708146403037));
#101262=CARTESIAN_POINT('Ctrl Pts',(1.67158805140991,-2.42140415612968,
23.6683591825556));
#101263=CARTESIAN_POINT('Ctrl Pts',(1.63423459445879,-2.44676835059095,
23.6659037248074));
#101264=CARTESIAN_POINT('Ctrl Pts',(1.59635063320942,-2.4712403071842,23.6634482670592));
#101265=CARTESIAN_POINT('Ctrl Pts',(1.51850564244454,-2.52152594712721,
23.6584027259007));
#101266=CARTESIAN_POINT('Ctrl Pts',(1.43813897262431,-2.56822233179505,
23.6533571847421));
#101267=CARTESIAN_POINT('Ctrl Pts',(1.35561614290803,-2.61106661598037,
23.6483116435836));
#101268=CARTESIAN_POINT('Ctrl Pts',(1.27320874086602,-2.65385097231182,
23.6432731598064));
#101269=CARTESIAN_POINT('Ctrl Pts',(1.18865156332485,-2.69279373056832,
23.6382346760293));
#101270=CARTESIAN_POINT('Ctrl Pts',(1.10233885300424,-2.72767539365616,
23.6331961922521));
#101271=CARTESIAN_POINT('Ctrl Pts',(1.01612000238436,-2.76251912510628,
23.6281631875125));
#101272=CARTESIAN_POINT('Ctrl Pts',(0.928149824009637,-2.79331037246852,
23.6231301827729));
#101273=CARTESIAN_POINT('Ctrl Pts',(0.838845895604781,-2.81987616100903,
23.6180971780333));
#101274=CARTESIAN_POINT('Ctrl Pts',(0.749608033340722,-2.84642229644852,
23.6130678966595));
#101275=CARTESIAN_POINT('Ctrl Pts',(0.659038807994886,-2.86874905938527,
23.6080386152858));
#101276=CARTESIAN_POINT('Ctrl Pts',(0.567573443485155,-2.88673247569816,
23.6030093339121));
#101277=CARTESIAN_POINT('Ctrl Pts',(0.47614235849875,-2.90470915215993,
23.5979819374198));
#101278=CARTESIAN_POINT('Ctrl Pts',(0.383816238285809,-2.91834562964665,
23.5929545409275));
#101279=CARTESIAN_POINT('Ctrl Pts',(0.291042030199817,-2.9275687074187,
23.5879271444352));
#101280=CARTESIAN_POINT('Ctrl Pts',(0.198276447765538,-2.93679092767809,
23.5829002153634));
#101281=CARTESIAN_POINT('Ctrl Pts',(0.105063303727384,-2.94160052004931,
23.5778732862916));
#101282=CARTESIAN_POINT('Ctrl Pts',(0.0118550622816464,-2.9419761143657,
23.5728463572199));
#101283=CARTESIAN_POINT('Ctrl Pts',(-0.0813707797332918,-2.94235177960579,
23.56781847891));
#101284=CARTESIAN_POINT('Ctrl Pts',(-0.174591271718575,-2.93829178273634,
23.5627906006002));
#101285=CARTESIAN_POINT('Ctrl Pts',(-0.267354722522535,-2.92982686388546,
23.5577627222904));
#101286=CARTESIAN_POINT('Ctrl Pts',(-0.360219976310396,-2.92135265523358,
23.5527293261498));
#101287=CARTESIAN_POINT('Ctrl Pts',(-0.452626743240865,-2.90846391566424,
23.5476959300093));
#101288=CARTESIAN_POINT('Ctrl Pts',(-0.544129547265214,-2.89124316441785,
23.5426625338688));
#101289=CARTESIAN_POINT('Ctrl Pts',(-0.635688320105321,-2.87401187988711,
23.5376260589896));
#101290=CARTESIAN_POINT('Ctrl Pts',(-0.726341596185885,-2.85244341210413,
23.5325895841104));
#101291=CARTESIAN_POINT('Ctrl Pts',(-0.815657327205701,-2.82667067847948,
23.5275531092312));
#101292=CARTESIAN_POINT('Ctrl Pts',(-0.905118546569044,-2.80085596308656,
23.5225084303282));
#101293=CARTESIAN_POINT('Ctrl Pts',(-0.993237450076915,-2.77082345365114,
23.5174637514251));
#101294=CARTESIAN_POINT('Ctrl Pts',(-1.07960046519243,-2.73675480004261,
23.5124190725221));
#101295=CARTESIAN_POINT('Ctrl Pts',(-1.12446952612382,-2.71905476383421,
23.5097981588732));
#101296=CARTESIAN_POINT('Ctrl Pts',(-1.16886501045896,-2.70026605650189,
23.5071772452242));
#101297=CARTESIAN_POINT('Ctrl Pts',(-1.21273165315311,-2.68041898542756,
23.5045563315753));
#101298=CARTESIAN_POINT('Ctrl Pts',(-1.29731811114346,-2.64214859725665,
23.4995025187315));
#101299=CARTESIAN_POINT('Ctrl Pts',(-1.38024241671689,-2.59980191982492,
23.4944487058877));
#101300=CARTESIAN_POINT('Ctrl Pts',(-1.46108486777875,-2.55354557608591,
23.4893948930439));
#101301=CARTESIAN_POINT('Ctrl Pts',(-1.54181597956702,-2.50735293832865,
23.4843480405018));
#101302=CARTESIAN_POINT('Ctrl Pts',(-1.62047055244664,-2.4572615527917,
23.4793011879597));
#101303=CARTESIAN_POINT('Ctrl Pts',(-1.69664992645296,-2.40348559951316,
23.4742543354176));
#101304=CARTESIAN_POINT('Ctrl Pts',(-1.77274788113775,-2.34976712113105,
23.4692128768725));
#101305=CARTESIAN_POINT('Ctrl Pts',(-1.84637553453101,-2.29237215718286,
23.4641714183273));
#101306=CARTESIAN_POINT('Ctrl Pts',(-1.91716082674176,-2.23155962600304,
23.4591299597822));
#101307=CARTESIAN_POINT('Ctrl Pts',(-1.98789512770512,-2.17079090204257,
23.4540921329273));
#101308=CARTESIAN_POINT('Ctrl Pts',(-2.05579080156047,-2.10660979278462,
23.4490543060725));
#101309=CARTESIAN_POINT('Ctrl Pts',(-2.12050752097289,-2.03931651626162,
23.4440164792177));
#101310=CARTESIAN_POINT('Ctrl Pts',(-2.18520071905583,-1.97204769751927,
23.4389804833639));
#101311=CARTESIAN_POINT('Ctrl Pts',(-2.24671695063373,-1.90166927830933,
23.4339444875102));
#101312=CARTESIAN_POINT('Ctrl Pts',(-2.30475229808391,-1.82851875693878,
23.4289084916565));
#101313=CARTESIAN_POINT('Ctrl Pts',(-2.36278276014744,-1.7553743933427,
23.4238729197304));
#101314=CARTESIAN_POINT('Ctrl Pts',(-2.41733264491014,-1.67945873945854,
23.4188373478043));
#101315=CARTESIAN_POINT('Ctrl Pts',(-2.46813867034164,-1.60114193748219,
23.4138017758782));
#101316=CARTESIAN_POINT('Ctrl Pts',(-2.51895460740193,-1.52280985686392,
23.4087652215741));
#101317=CARTESIAN_POINT('Ctrl Pts',(-2.56602499328706,-1.44207607044779,
23.4037286672701));
#101318=CARTESIAN_POINT('Ctrl Pts',(-2.60913080260939,-1.35933824152595,
23.398692112966));
#101319=CARTESIAN_POINT('Ctrl Pts',(-2.65228381918497,-1.27650980241248,
23.3936500428881));
#101320=CARTESIAN_POINT('Ctrl Pts',(-2.6914633869885,-1.19167333417574,
23.3886079728102));
#101321=CARTESIAN_POINT('Ctrl Pts',(-2.72649739255411,-1.10524927884872,
23.3835659027323));
#101322=CARTESIAN_POINT('Ctrl Pts',(-2.76155287297451,-1.01877224801954,
23.3785207420081));
#101323=CARTESIAN_POINT('Ctrl Pts',(-2.79245758527019,-0.930706111303744,
23.3734755812838));
#101324=CARTESIAN_POINT('Ctrl Pts',(-2.81908905840467,-0.841487302805616,
23.3684304205595));
#101325=CARTESIAN_POINT('Ctrl Pts',(-2.84576348825401,-0.752124583871262,
23.3633771219629));
#101326=CARTESIAN_POINT('Ctrl Pts',(-2.86815081188743,-0.661605911771167,
23.3583238233662));
#101327=CARTESIAN_POINT('Ctrl Pts',(-2.88617953089253,-0.570378572052812,
23.3532705247695));
#101328=CARTESIAN_POINT('Ctrl Pts',(-2.89522502556831,-0.524607354725887,
23.3507351485434));
#101329=CARTESIAN_POINT('Ctrl Pts',(-2.90317414490181,-0.478657840198326,
23.3481997723174));
#101330=CARTESIAN_POINT('Ctrl Pts',(-2.91002279202621,-0.432586811967262,
23.3456643960914));
#101331=CARTESIAN_POINT('Ctrl Pts',(-2.93117191285364,-0.290316123318043,
23.3378349697574));
#101332=CARTESIAN_POINT('Ctrl Pts',(-2.94189101104494,-0.146458298840477,
23.3300055434235));
#101333=CARTESIAN_POINT('Ctrl Pts',(-2.94199917298087,-0.00220594195414625,
23.3221761170896));
#101334=CARTESIAN_POINT('',(-2.94164694255709,-0.000931396376265734,22.3221761729126));
#101335=CARTESIAN_POINT('Ctrl Pts',(-2.94442704671558,-0.00218612406040982,
23.3221749436185));
#101336=CARTESIAN_POINT('Ctrl Pts',(-2.93738112964605,0.830075128864581,
23.2770407826148));
#101337=CARTESIAN_POINT('Ctrl Pts',(-2.13351380414281,2.65076091012592,
23.1789426431165));
#101338=CARTESIAN_POINT('Ctrl Pts',(0.955635603265417,3.34439215967238,
23.0278805251237));
#101339=CARTESIAN_POINT('Ctrl Pts',(3.32881183697859,1.00834644561564,22.8689885896398));
#101340=CARTESIAN_POINT('Ctrl Pts',(2.65081929289952,-2.25190969884369,
22.7100966541558));
#101341=CARTESIAN_POINT('Ctrl Pts',(-0.456994034995296,-3.44805916202772,
22.5512047186722));
#101342=CARTESIAN_POINT('Ctrl Pts',(-2.64523118583122,-1.84941700741083,
22.4218981138432));
#101343=CARTESIAN_POINT('Ctrl Pts',(-2.93865671149535,-0.434669198947471,
22.3455554875091));
#101344=CARTESIAN_POINT('Ctrl Pts',(-2.9374317399157,-0.00094243306318272,
22.3221768396696));
#101345=CARTESIAN_POINT('',(-2.94199878572312,0.00267297655470239,21.3221761170605));
#101346=CARTESIAN_POINT('Ctrl Pts',(-2.9419998528588,-0.000930472349394172,
22.3221761170896));
#101347=CARTESIAN_POINT('Ctrl Pts',(-2.94203019000661,0.094990577261412,
22.3170138242079));
#101348=CARTESIAN_POINT('Ctrl Pts',(-2.93736506348151,0.190871573344608,
22.3118515313263));
#101349=CARTESIAN_POINT('Ctrl Pts',(-2.92804241566056,0.286236985892223,
22.3066892384446));
#101350=CARTESIAN_POINT('Ctrl Pts',(-2.91871313585854,0.381670239853906,
22.3015232731912));
#101351=CARTESIAN_POINT('Ctrl Pts',(-2.9047197783399,0.476586770599642,
22.2963573079377));
#101352=CARTESIAN_POINT('Ctrl Pts',(-2.88615187045034,0.570518519152539,
22.2911913426843));
#101353=CARTESIAN_POINT('Ctrl Pts',(-2.8675510357606,0.66461683854007,22.2860162165331));
#101354=CARTESIAN_POINT('Ctrl Pts',(-2.84435952707144,0.757726482815267,
22.2808410903819));
#101355=CARTESIAN_POINT('Ctrl Pts',(-2.81671762109817,0.849391454510266,
22.2756659642308));
#101356=CARTESIAN_POINT('Ctrl Pts',(-2.78904978270547,0.941142422246759,
22.270485983004));
#101357=CARTESIAN_POINT('Ctrl Pts',(-2.75692336416446,1.03144562881346,
22.2653060017773));
#101358=CARTESIAN_POINT('Ctrl Pts',(-2.72052719543667,1.11986417876879,
22.2601260205505));
#101359=CARTESIAN_POINT('Ctrl Pts',(-2.68405381864556,1.20847029310912,
22.2549350509057));
#101360=CARTESIAN_POINT('Ctrl Pts',(-2.64329276694592,1.29518338866856,
22.2497440812609));
#101361=CARTESIAN_POINT('Ctrl Pts',(-2.59847956311998,1.37958977962575,
22.2445531116161));
#101362=CARTESIAN_POINT('Ctrl Pts',(-2.56644493080924,1.43992752538238,
22.2408423569788));
#101363=CARTESIAN_POINT('Ctrl Pts',(-2.53234058057719,1.49908706191697,
22.2371316023416));
#101364=CARTESIAN_POINT('Ctrl Pts',(-2.49626575990915,1.55692686273479,
22.2334208477043));
#101365=CARTESIAN_POINT('Ctrl Pts',(-2.44714850223653,1.63567797910606,
22.228368512355));
#101366=CARTESIAN_POINT('Ctrl Pts',(-2.39421284353252,1.71224383471465,
22.2233161770058));
#101367=CARTESIAN_POINT('Ctrl Pts',(-2.33767924232075,1.78623060102068,
22.2182638416566));
#101368=CARTESIAN_POINT('Ctrl Pts',(-2.28122359605779,1.86011534597203,
22.213218473041));
#101369=CARTESIAN_POINT('Ctrl Pts',(-2.22118013331467,1.9314277185992,22.2081731044254));
#101370=CARTESIAN_POINT('Ctrl Pts',(-2.15781367650433,1.9998010244749,22.2031277358099));
#101371=CARTESIAN_POINT('Ctrl Pts',(-2.09451501869394,2.0681011742678,22.1980877654912));
#101372=CARTESIAN_POINT('Ctrl Pts',(-2.02790073414699,2.13346818371392,
22.1930477951725));
#101373=CARTESIAN_POINT('Ctrl Pts',(-1.958276479213,2.19556763297357,22.1880078248538));
#101374=CARTESIAN_POINT('Ctrl Pts',(-1.88870239469447,2.25762233410381,
22.1829714862782));
#101375=CARTESIAN_POINT('Ctrl Pts',(-1.816122981461,2.31641386022739,22.1779351477026));
#101376=CARTESIAN_POINT('Ctrl Pts',(-1.74088064128557,2.37164470205744,
22.172898809127));
#101377=CARTESIAN_POINT('Ctrl Pts',(-1.66566564784683,2.42685547030546,
22.1678643010025));
#101378=CARTESIAN_POINT('Ctrl Pts',(-1.58779000794011,2.47850786257356,
22.162829792878));
#101379=CARTESIAN_POINT('Ctrl Pts',(-1.50762826327053,2.52634538806314,
22.1577952847535));
#101380=CARTESIAN_POINT('Ctrl Pts',(-1.42747322991276,2.5741789084933,22.1527611981287));
#101381=CARTESIAN_POINT('Ctrl Pts',(-1.34503285391046,2.61819796967141,
22.1477271115039));
#101382=CARTESIAN_POINT('Ctrl Pts',(-1.26070865911788,2.65819067728882,
22.1426930248791));
#101383=CARTESIAN_POINT('Ctrl Pts',(-1.17636793669289,2.69819122351972,
22.137657951568));
#101384=CARTESIAN_POINT('Ctrl Pts',(-1.0901430637071,2.73416365887391,22.1326228782568));
#101385=CARTESIAN_POINT('Ctrl Pts',(-1.00245698571702,2.76594359880804,
22.1275878049457));
#101386=CARTESIAN_POINT('Ctrl Pts',(-0.914674577582191,2.79775845153885,
22.1225472002053));
#101387=CARTESIAN_POINT('Ctrl Pts',(-0.825428178482752,2.82537146355402,
22.1175065954648));
#101388=CARTESIAN_POINT('Ctrl Pts',(-0.735157102062007,2.84866776498906,
22.1124659907244));
#101389=CARTESIAN_POINT('Ctrl Pts',(-0.64483055526435,2.87197838169178,
22.1074222885993));
#101390=CARTESIAN_POINT('Ctrl Pts',(-0.553478512257664,2.89096691674169,
22.1023785864742));
#101391=CARTESIAN_POINT('Ctrl Pts',(-0.461549559709994,2.90556982430839,
22.0973348843492));
#101392=CARTESIAN_POINT('Ctrl Pts',(-0.369471830695332,2.92019636500629,
22.0922830195706));
#101393=CARTESIAN_POINT('Ctrl Pts',(-0.276815769208732,2.93042306002186,
22.0872311547921));
#101394=CARTESIAN_POINT('Ctrl Pts',(-0.184033963419593,2.93623832484832,
22.0821792900136));
#101395=CARTESIAN_POINT('Ctrl Pts',(-0.137198725494143,2.93917380675052,
22.0796291640825));
#101396=CARTESIAN_POINT('Ctrl Pts',(-0.0903314332698338,2.9409860316533,
22.0770790381515));
#101397=CARTESIAN_POINT('Ctrl Pts',(-0.0434899276352311,2.94167853889481,
22.0745289122205));
#101398=CARTESIAN_POINT('Ctrl Pts',(0.0493134496888117,2.94305054882409,
22.0694765490269));
#101399=CARTESIAN_POINT('Ctrl Pts',(0.142348327697592,2.94002910592505,
22.0644241858333));
#101400=CARTESIAN_POINT('Ctrl Pts',(0.235164237631819,2.932586193335,22.0593718226397));
#101401=CARTESIAN_POINT('Ctrl Pts',(0.327852170320183,2.92515354324687,
22.0543264257898));
#101402=CARTESIAN_POINT('Ctrl Pts',(0.42032129591086,2.91331157310301,22.0492810289399));
#101403=CARTESIAN_POINT('Ctrl Pts',(0.512119923029994,2.89708425566737,
22.04423563209));
#101404=CARTESIAN_POINT('Ctrl Pts',(0.603820337012713,2.88087429944715,
22.0391956331884));
#101405=CARTESIAN_POINT('Ctrl Pts',(0.69485124325998,2.86028839847612,22.0341556342869));
#101406=CARTESIAN_POINT('Ctrl Pts',(0.784765960818846,2.83540233242834,
22.0291156353853));
#101407=CARTESIAN_POINT('Ctrl Pts',(0.874615894393207,2.8105341969103,22.0240792678271));
#101408=CARTESIAN_POINT('Ctrl Pts',(0.96335081086689,2.7813721727628,22.0190429002689));
#101409=CARTESIAN_POINT('Ctrl Pts',(1.05053515120018,2.74804292107907,22.0140065327107));
#101410=CARTESIAN_POINT('Ctrl Pts',(1.13768780878291,2.71472578123061,22.0089719953662));
#101411=CARTESIAN_POINT('Ctrl Pts',(1.22329059510423,2.67724458077506,22.0039374580218));
#101412=CARTESIAN_POINT('Ctrl Pts',(1.30692502077597,2.63577521614984,21.9989029206773));
#101413=CARTESIAN_POINT('Ctrl Pts',(1.3905524477864,2.59430932174679,21.9938688046309));
#101414=CARTESIAN_POINT('Ctrl Pts',(1.47221144372437,2.54885612423029,21.9888346885845));
#101415=CARTESIAN_POINT('Ctrl Pts',(1.55150639027973,2.49963835802725,21.983800572538));
#101416=CARTESIAN_POINT('Ctrl Pts',(1.63081688125524,2.45041094352164,21.9787654696392));
#101417=CARTESIAN_POINT('Ctrl Pts',(1.70776202524664,2.39741772927431,21.9737303667403));
#101418=CARTESIAN_POINT('Ctrl Pts',(1.78197453581782,2.34092519181987,21.9686952638414));
#101419=CARTESIAN_POINT('Ctrl Pts',(1.85626857534372,2.28437059235602,21.9636546294401));
#101420=CARTESIAN_POINT('Ctrl Pts',(1.92782363501229,2.22430926548201,21.9586139950389));
#101421=CARTESIAN_POINT('Ctrl Pts',(1.9963051829809,2.16104826794859,21.9535733606376));
#101422=CARTESIAN_POINT('Ctrl Pts',(2.06482881286728,2.09774839652614,21.9485296287661));
#101423=CARTESIAN_POINT('Ctrl Pts',(2.13027485970737,2.0312452565218,21.9434858968945));
#101424=CARTESIAN_POINT('Ctrl Pts',(2.19234691041335,1.96188150111087,21.938442165023));
#101425=CARTESIAN_POINT('Ctrl Pts',(2.25451941509935,1.89240549122758,21.9333902706542));
#101426=CARTESIAN_POINT('Ctrl Pts',(2.31330674307987,1.82005996813581,21.9283383762854));
#101427=CARTESIAN_POINT('Ctrl Pts',(2.36845399122824,1.7452190955393,21.9232864819167));
#101428=CARTESIAN_POINT('Ctrl Pts',(2.39628837899023,1.70744477427684,21.9207366468566));
#101429=CARTESIAN_POINT('Ctrl Pts',(2.42319615647617,1.66903519809311,21.9181868117966));
#101430=CARTESIAN_POINT('Ctrl Pts',(2.44914897657549,1.63004088615569,21.9156369767366));
#101431=CARTESIAN_POINT('Ctrl Pts',(2.50057304152298,1.55277583280201,21.9105846208373));
#101432=CARTESIAN_POINT('Ctrl Pts',(2.54842948649866,1.47293629093071,21.905532264938));
#101433=CARTESIAN_POINT('Ctrl Pts',(2.59245074570147,1.39088573618105,21.9004799090386));
#101434=CARTESIAN_POINT('Ctrl Pts',(2.63641130662138,1.30894831603668,21.8954345195309));
#101435=CARTESIAN_POINT('Ctrl Pts',(2.6765469817218,1.22480632910527,21.8903891300231));
#101436=CARTESIAN_POINT('Ctrl Pts',(2.71263324413171,1.13885244120187,21.8853437405153));
#101437=CARTESIAN_POINT('Ctrl Pts',(2.74868089839694,1.05299051405911,21.8803037489933));
#101438=CARTESIAN_POINT('Ctrl Pts',(2.78068758024804,0.965320946466707,
21.8752637574712));
#101439=CARTESIAN_POINT('Ctrl Pts',(2.80847502456532,0.876260256084261,
21.8702237659491));
#101440=CARTESIAN_POINT('Ctrl Pts',(2.83624244773248,0.787263734879458,
21.8651874057947));
#101441=CARTESIAN_POINT('Ctrl Pts',(2.85979654387253,0.696878505994045,
21.8601510456403));
#101442=CARTESIAN_POINT('Ctrl Pts',(2.87900784223665,0.605539300409035,
21.8551146854859));
#101443=CARTESIAN_POINT('Ctrl Pts',(2.89821215916643,0.514233287722003,
21.8500801555575));
#101444=CARTESIAN_POINT('Ctrl Pts',(2.91307672221103,0.421974421338534,
21.845045625629));
#101445=CARTESIAN_POINT('Ctrl Pts',(2.92352269319776,0.329209754347786,
21.8400110957006));
#101446=CARTESIAN_POINT('Ctrl Pts',(2.93396779004153,0.23645285011844,21.8349769870733));
#101447=CARTESIAN_POINT('Ctrl Pts',(2.93999498046764,0.143190670907543,
21.829942878446));
#101448=CARTESIAN_POINT('Ctrl Pts',(2.94157718631606,0.0498764167204417,
21.8249087698186));
#101449=CARTESIAN_POINT('Ctrl Pts',(2.94315970233135,-0.0434561302754896,
21.8198736743326));
#101450=CARTESIAN_POINT('Ctrl Pts',(2.94029549606274,-0.136840328366542,
21.8148385788465));
#101451=CARTESIAN_POINT('Ctrl Pts',(2.93300960511188,-0.229823097885035,
21.8098034833604));
#101452=CARTESIAN_POINT('Ctrl Pts',(2.92571570987932,-0.322908018298392,
21.8047628563172));
#101453=CARTESIAN_POINT('Ctrl Pts',(2.91399046826226,-0.415590186266749,
21.7997222292739));
#101454=CARTESIAN_POINT('Ctrl Pts',(2.89791077156557,-0.507422072878408,
21.7946816022306));
#101455=CARTESIAN_POINT('Ctrl Pts',(2.88182119381464,-0.599310390644901,
21.7896378776967));
#101456=CARTESIAN_POINT('Ctrl Pts',(2.86137193120887,-0.690346953737875,
21.7845941531628));
#101457=CARTESIAN_POINT('Ctrl Pts',(2.83669044521521,-0.780096992703287,
21.779550428629));
#101458=CARTESIAN_POINT('Ctrl Pts',(2.81196901550317,-0.869992280227979,
21.7744985414945));
#101459=CARTESIAN_POINT('Ctrl Pts',(2.7830018265317,-0.95859646532433,21.76944665436));
#101460=CARTESIAN_POINT('Ctrl Pts',(2.74996531240784,-1.04549260186461,
21.7643947672255));
#101461=CARTESIAN_POINT('Ctrl Pts',(2.73329033706895,-1.08935288713628,
21.7618448585679));
#101462=CARTESIAN_POINT('Ctrl Pts',(2.71557938353974,-1.1327783733076,21.7592949499103));
#101463=CARTESIAN_POINT('Ctrl Pts',(2.69685956413281,-1.1757178621359,21.7567450412526));
#101464=CARTESIAN_POINT('Ctrl Pts',(2.65976838277848,-1.26079754868474,
21.7516926888554));
#101465=CARTESIAN_POINT('Ctrl Pts',(2.61858059949813,-1.34427296168509,
21.7466403364581));
#101466=CARTESIAN_POINT('Ctrl Pts',(2.57345680430365,-1.42572229988285,
21.7415879840608));
#101467=CARTESIAN_POINT('Ctrl Pts',(2.52839522836952,-1.50705933109143,
21.736542598135));
#101468=CARTESIAN_POINT('Ctrl Pts',(2.47940863847927,-1.58637545365499,
21.7314972122091));
#101469=CARTESIAN_POINT('Ctrl Pts',(2.42670547512277,-1.66326923166671,
21.7264518262833));
#101470=CARTESIAN_POINT('Ctrl Pts',(2.37405869889898,-1.74008074099873,
21.7214118384175));
#101471=CARTESIAN_POINT('Ctrl Pts',(2.31770350264379,-1.81447469265057,
21.7163718505518));
#101472=CARTESIAN_POINT('Ctrl Pts',(2.25789343583091,-1.88607561683822,
21.7113318626861));
#101473=CARTESIAN_POINT('Ctrl Pts',(2.19812646397875,-1.95762495039608,
21.706295506284));
#101474=CARTESIAN_POINT('Ctrl Pts',(2.13490985345959,-2.02638491657892,
21.7012591498818));
#101475=CARTESIAN_POINT('Ctrl Pts',(2.06853889501785,-2.09201119495053,
21.6962227934797));
#101476=CARTESIAN_POINT('Ctrl Pts',(2.00219205673494,-2.15761362379073,
21.6911882673618));
#101477=CARTESIAN_POINT('Ctrl Pts',(1.93269346342445,-2.22008431519057,
21.6861537412438));
#101478=CARTESIAN_POINT('Ctrl Pts',(1.86037619083133,-2.27911483444514,
21.6811192151259));
#101479=CARTESIAN_POINT('Ctrl Pts',(1.78806497068942,-2.33814041325707,
21.6760851103627));
#101480=CARTESIAN_POINT('Ctrl Pts',(1.71293588455987,-2.39372611160138,
21.6710510055994));
#101481=CARTESIAN_POINT('Ctrl Pts',(1.63535521318685,-2.44560367326814,
21.6660169008362));
#101482=CARTESIAN_POINT('Ctrl Pts',(1.55775933407516,-2.4974914042256,21.6609818092634));
#101483=CARTESIAN_POINT('Ctrl Pts',(1.47771128477066,-2.54566930828948,
21.6559467176906));
#101484=CARTESIAN_POINT('Ctrl Pts',(1.39560547561088,-2.58991300171356,
21.6509116261178));
#101485=CARTESIAN_POINT('Ctrl Pts',(1.31340946575208,-2.6342053008589,21.6458710030389));
#101486=CARTESIAN_POINT('Ctrl Pts',(1.22915157522609,-2.67455455091527,
21.6408303799601));
#101487=CARTESIAN_POINT('Ctrl Pts',(1.1432496373168,-2.71078296194568,21.6357897568812));
#101488=CARTESIAN_POINT('Ctrl Pts',(1.05729491279115,-2.74703363528217,
21.6307460363468));
#101489=CARTESIAN_POINT('Ctrl Pts',(0.969694546411809,-2.77915827554041,
21.6257023158124));
#101490=CARTESIAN_POINT('Ctrl Pts',(0.880883039653029,-2.80702851258259,
21.620658595278));
#101491=CARTESIAN_POINT('Ctrl Pts',(0.791927803389455,-2.83494385386312,
21.6156067121588));
#101492=CARTESIAN_POINT('Ctrl Pts',(0.701757942888001,-2.85859093399181,
21.6105548290395));
#101493=CARTESIAN_POINT('Ctrl Pts',(0.610819505872041,-2.87789220285372,
21.6055029459203));
#101494=CARTESIAN_POINT('Ctrl Pts',(0.564918172951121,-2.88763455159973,
21.6029529992031));
#101495=CARTESIAN_POINT('Ctrl Pts',(0.51882113440247,-2.89627052047224,
21.600403052486));
#101496=CARTESIAN_POINT('Ctrl Pts',(0.472586115470197,-2.90379516554884,
21.5978531057688));
#101497=CARTESIAN_POINT('Ctrl Pts',(0.380978007886807,-2.91870417849233,
21.592800749382));
#101498=CARTESIAN_POINT('Ctrl Pts',(0.288499320069357,-2.9293006517501,
21.5877483929951));
#101499=CARTESIAN_POINT('Ctrl Pts',(0.195591599580818,-2.93549108773531,
21.5826960366083));
#101500=CARTESIAN_POINT('Ctrl Pts',(0.102811984375719,-2.94167298807296,
21.5776506466344));
#101501=CARTESIAN_POINT('Ctrl Pts',(0.00960495143632237,-2.94346089414566,
21.5726052566605));
#101502=CARTESIAN_POINT('Ctrl Pts',(-0.0835791501822573,-2.94081256214245,
21.5675598666867));
#101503=CARTESIAN_POINT('Ctrl Pts',(-0.176663555147768,-2.93816706356073,
21.5625198747204));
#101504=CARTESIAN_POINT('Ctrl Pts',(-0.269724635881426,-2.93109477341955,
21.5574798827542));
#101505=CARTESIAN_POINT('Ctrl Pts',(-0.362309434755363,-2.91960543113059,
21.552439890788));
#101506=CARTESIAN_POINT('Ctrl Pts',(-0.454827524660897,-2.90812436711389,
21.5474035302242));
#101507=CARTESIAN_POINT('Ctrl Pts',(-0.546869575213149,-2.89223263129561,
21.5423671696604));
#101508=CARTESIAN_POINT('Ctrl Pts',(-0.637986201359988,-2.87199192319099,
21.5373308090966));
#101509=CARTESIAN_POINT('Ctrl Pts',(-0.729069715103207,-2.85175857069778,
21.5322962787806));
#101510=CARTESIAN_POINT('Ctrl Pts',(-0.819228039316954,-2.82717948188605,
21.5272617484646));
#101511=CARTESIAN_POINT('Ctrl Pts',(-0.908021485893451,-2.79836755647929,
21.5222272181486));
#101512=CARTESIAN_POINT('Ctrl Pts',(-0.996807501635577,-2.76955804224873,
21.5171931091561));
#101513=CARTESIAN_POINT('Ctrl Pts',(-1.08422844434704,-2.73651653300771,
21.5121590001635));
#101514=CARTESIAN_POINT('Ctrl Pts',(-1.16986041220074,-2.69940560419614,
21.507124891171));
#101515=CARTESIAN_POINT('Ctrl Pts',(-1.25550916647857,-2.66228740053375,
21.5020897953427));
#101516=CARTESIAN_POINT('Ctrl Pts',(-1.33936784198538,-2.62109836998623,
21.4970546995144));
#101517=CARTESIAN_POINT('Ctrl Pts',(-1.42103417753485,-2.5760484984328,
21.492019603686));
#101518=CARTESIAN_POINT('Ctrl Pts',(-1.5027902311323,-2.53094913541497,
21.4869789763377));
#101519=CARTESIAN_POINT('Ctrl Pts',(-1.58234874756784,-2.48198067978894,
21.4819383489894));
#101520=CARTESIAN_POINT('Ctrl Pts',(-1.65933394333949,-2.42939804570627,
21.4768977216411));
#101521=CARTESIAN_POINT('Ctrl Pts',(-1.73636644658095,-2.37678309954918,
21.4718539968228));
#101522=CARTESIAN_POINT('Ctrl Pts',(-1.81082212685152,-2.32054982106105,
21.4668102720046));
#101523=CARTESIAN_POINT('Ctrl Pts',(-1.88235771278168,-2.26099390559358,
21.4617665471864));
#101524=CARTESIAN_POINT('Ctrl Pts',(-1.95400906908359,-2.2013416071807,
21.4567146598028));
#101525=CARTESIAN_POINT('Ctrl Pts',(-2.02273056957333,-2.1383562366254,
21.4516627724192));
#101526=CARTESIAN_POINT('Ctrl Pts',(-2.08821540652036,-2.07237072358471,
21.4466108850356));
#101527=CARTESIAN_POINT('Ctrl Pts',(-2.12126842117285,-2.03906499616646,
21.4440609801187));
#101528=CARTESIAN_POINT('Ctrl Pts',(-2.15349747733302,-2.00499547140519,
21.4415110752018));
#101529=CARTESIAN_POINT('Ctrl Pts',(-2.18486715170584,-1.97020799140518,
21.4389611702849));
#101530=CARTESIAN_POINT('Ctrl Pts',(-2.24637569772523,-1.90199793321173,
21.4339614070722));
#101531=CARTESIAN_POINT('Ctrl Pts',(-2.30480892287151,-1.83076923906431,
21.4289616438594));
#101532=CARTESIAN_POINT('Ctrl Pts',(-2.35985162593047,-1.75683360156656,
21.4239618806467));
#101533=CARTESIAN_POINT('Ctrl Pts',(-2.41482437391578,-1.68299193061985,
21.4189684717513));
#101534=CARTESIAN_POINT('Ctrl Pts',(-2.46641488452217,-1.60645050518711,
21.4139750628559));
#101535=CARTESIAN_POINT('Ctrl Pts',(-2.51434576883271,-1.52755666171604,
21.4089816539605));
#101536=CARTESIAN_POINT('Ctrl Pts',(-2.56222981774856,-1.44873990892149,
21.4039931243465));
#101537=CARTESIAN_POINT('Ctrl Pts',(-2.6064611061311,-1.36757568765215,
21.3990045947326));
#101538=CARTESIAN_POINT('Ctrl Pts',(-2.6468042042926,-1.28444209839876,
21.3940160651187));
#101539=CARTESIAN_POINT('Ctrl Pts',(-2.6871197281023,-1.20136533063258,
21.3890309451455));
#101540=CARTESIAN_POINT('Ctrl Pts',(-2.72355214294089,-1.1163222758734,
21.3840458251723));
#101541=CARTESIAN_POINT('Ctrl Pts',(-2.75591147754233,-1.02971643084418,
21.3790607051992));
#101542=CARTESIAN_POINT('Ctrl Pts',(-2.78826639365761,-0.9431224113587,
21.3740762659162));
#101543=CARTESIAN_POINT('Ctrl Pts',(-2.81654916256314,-0.854966445684254,
21.3690918266333));
#101544=CARTESIAN_POINT('Ctrl Pts',(-2.84061796367395,-0.765671982282783,
21.3641073873503));
#101545=CARTESIAN_POINT('Ctrl Pts',(-2.86468387395497,-0.67638824376513,
21.3591235467331));
#101546=CARTESIAN_POINT('Ctrl Pts',(-2.88453671004305,-0.585966719553561,
21.3541397061159));
#101547=CARTESIAN_POINT('Ctrl Pts',(-2.9000850035322,-0.494844391993714,
21.3491558654986));
#101548=CARTESIAN_POINT('Ctrl Pts',(-2.91564403480524,-0.403659134578519,
21.3441685829986));
#101549=CARTESIAN_POINT('Ctrl Pts',(-2.92689251344888,-0.311772556206746,
21.3391813004986));
#101550=CARTESIAN_POINT('Ctrl Pts',(-2.93379052609947,-0.219629572164131,
21.3341940179986));
#101551=CARTESIAN_POINT('Ctrl Pts',(-2.93933126112593,-0.145616971000863,
21.3301880510289));
#101552=CARTESIAN_POINT('Ctrl Pts',(-2.94206612089074,-0.0714391666931478,
21.3261820840593));
#101553=CARTESIAN_POINT('Ctrl Pts',(-2.94199878572361,0.00267297601551483,
21.3221761170896));
#101554=CARTESIAN_POINT('',(-2.94199995448535,-0.000517501908736848,20.3221761170572));
#101555=CARTESIAN_POINT('Ctrl Pts',(-2.94199878572312,0.00267297655470376,
21.3221761170605));
#101556=CARTESIAN_POINT('Ctrl Pts',(-2.94189240953056,0.11975542114466,
21.3158474860343));
#101557=CARTESIAN_POINT('Ctrl Pts',(-2.93479312830803,0.236526265844601,
21.3095188550082));
#101558=CARTESIAN_POINT('Ctrl Pts',(-2.92083380798487,0.352269592971963,
21.3031902239821));
#101559=CARTESIAN_POINT('Ctrl Pts',(-2.90660046919479,0.470284936810828,
21.2967373632849));
#101560=CARTESIAN_POINT('Ctrl Pts',(-2.88523514508262,0.587232220707165,
21.2902845025877));
#101561=CARTESIAN_POINT('Ctrl Pts',(-2.85692692874275,0.702376340592786,
21.2838316418906));
#101562=CARTESIAN_POINT('Ctrl Pts',(-2.8514251294196,0.724754996783811,
21.2825775061941));
#101563=CARTESIAN_POINT('Ctrl Pts',(-2.84566121807922,0.747065607135637,
21.2813233704976));
#101564=CARTESIAN_POINT('Ctrl Pts',(-2.83963679003616,0.769302866674205,
21.2800692348011));
#101565=CARTESIAN_POINT('Ctrl Pts',(-2.81536704985242,0.858886891504768,
21.2750168800727));
#101566=CARTESIAN_POINT('Ctrl Pts',(-2.78681035035391,0.947482047980881,
21.2699645253443));
#101567=CARTESIAN_POINT('Ctrl Pts',(-2.75406396661295,1.03464760561465,
21.264912170616));
#101568=CARTESIAN_POINT('Ctrl Pts',(-2.72136273518789,1.12169297511333,
21.2598667823215));
#101569=CARTESIAN_POINT('Ctrl Pts',(-2.6844834539253,1.20731225054544,21.254821394027));
#101570=CARTESIAN_POINT('Ctrl Pts',(-2.643573709314,1.29107786110049,21.2497760057324));
#101571=CARTESIAN_POINT('Ctrl Pts',(-2.6027077337561,1.37475385140695,21.244736015464));
#101572=CARTESIAN_POINT('Ctrl Pts',(-2.55782005984269,1.45657972176175,
21.2396960251957));
#101573=CARTESIAN_POINT('Ctrl Pts',(-2.50910669122713,1.53614700209298,
21.2346560349273));
#101574=CARTESIAN_POINT('Ctrl Pts',(-2.46042842165539,1.61565695246453,
21.2296196760817));
#101575=CARTESIAN_POINT('Ctrl Pts',(-2.40793016759864,1.69291116964257,
21.2245833172361));
#101576=CARTESIAN_POINT('Ctrl Pts',(-2.35185377514653,1.76752590372221,
21.2195469583906));
#101577=CARTESIAN_POINT('Ctrl Pts',(-2.29579776137878,1.84211352211112,
21.2145124298048));
#101578=CARTESIAN_POINT('Ctrl Pts',(-2.23616645908777,1.91406320821207,
21.2094779012191));
#101579=CARTESIAN_POINT('Ctrl Pts',(-2.17324433457103,1.98302119561414,
21.2044433726333));
#101580=CARTESIAN_POINT('Ctrl Pts',(-2.11032747592742,2.05197341200932,
21.1994092653809));
#101581=CARTESIAN_POINT('Ctrl Pts',(-2.04412064219976,2.11793409946989,
21.1943751581285));
#101582=CARTESIAN_POINT('Ctrl Pts',(-1.97494701584284,2.18058439061951,
21.1893410508761));
#101583=CARTESIAN_POINT('Ctrl Pts',(-1.90575982949065,2.24324696300544,
21.1843059567957));
#101584=CARTESIAN_POINT('Ctrl Pts',(-1.83360502499238,2.30259755237567,
21.1792708627153));
#101585=CARTESIAN_POINT('Ctrl Pts',(-1.75884001937715,2.35835658589565,
21.1742357686349));
#101586=CARTESIAN_POINT('Ctrl Pts',(-1.68399287745445,2.4141768758963,21.1691951430357));
#101587=CARTESIAN_POINT('Ctrl Pts',(-1.6065301671167,2.46639746806327,21.1641545174365));
#101588=CARTESIAN_POINT('Ctrl Pts',(-1.52683928116303,2.51478146356648,
21.1591138918373));
#101589=CARTESIAN_POINT('Ctrl Pts',(-1.44709942512561,2.56319519105577,
21.1540701687715));
#101590=CARTESIAN_POINT('Ctrl Pts',(-1.36512905761604,2.60776741632088,
21.1490264457057));
#101591=CARTESIAN_POINT('Ctrl Pts',(-1.28133927752646,2.64830769659947,
21.1439827226398));
#101592=CARTESIAN_POINT('Ctrl Pts',(-1.1974138951143,2.68891358578833,21.1389308369967));
#101593=CARTESIAN_POINT('Ctrl Pts',(-1.111663629993,2.72547432934193,21.1338789513535));
#101594=CARTESIAN_POINT('Ctrl Pts',(-1.02451842458105,2.75784807371508,
21.1288270657103));
#101595=CARTESIAN_POINT('Ctrl Pts',(-0.980532177941858,2.77418861130289,
21.1262771435793));
#101596=CARTESIAN_POINT('Ctrl Pts',(-0.936190770239545,2.78946322732056,
21.1237272214482));
#101597=CARTESIAN_POINT('Ctrl Pts',(-0.891550584329987,2.80365860182385,
21.1211772993172));
#101598=CARTESIAN_POINT('Ctrl Pts',(-0.803101577759515,2.83178498049207,
21.1161249440295));
#101599=CARTESIAN_POINT('Ctrl Pts',(-0.713161579104362,2.85577217652358,
21.1110725887419));
#101600=CARTESIAN_POINT('Ctrl Pts',(-0.622153749527225,2.87546321693553,
21.1060202334542));
#101601=CARTESIAN_POINT('Ctrl Pts',(-0.531271405829407,2.89512710641407,
21.1009748445918));
#101602=CARTESIAN_POINT('Ctrl Pts',(-0.439324587436848,2.91050651838266,
21.0959294557295));
#101603=CARTESIAN_POINT('Ctrl Pts',(-0.346752647075515,2.92149389897465,
21.0908840668671));
#101604=CARTESIAN_POINT('Ctrl Pts',(-0.254279748641262,2.93246952426214,
21.0858440760231));
#101605=CARTESIAN_POINT('Ctrl Pts',(-0.161183496380621,2.9390624060705,
21.0808040851791));
#101606=CARTESIAN_POINT('Ctrl Pts',(-0.0679134145633014,2.9412160356088,
21.0757640943351));
#101607=CARTESIAN_POINT('Ctrl Pts',(0.0252894643036301,2.94336811341415,
21.0707277349049));
#101608=CARTESIAN_POINT('Ctrl Pts',(0.118665480934454,2.94108728633357,
21.0656913754746));
#101609=CARTESIAN_POINT('Ctrl Pts',(0.211761057785966,2.93436897039302,
21.0606550160444));
#101610=CARTESIAN_POINT('Ctrl Pts',(0.304822802940564,2.92765309594363,
21.0556204868684));
#101611=CARTESIAN_POINT('Ctrl Pts',(0.397603868137938,2.91650296822374,
21.0505859576925));
#101612=CARTESIAN_POINT('Ctrl Pts',(0.489652792247862,2.90096607064679,
21.0455514285166));
#101613=CARTESIAN_POINT('Ctrl Pts',(0.581694012986908,2.88543047331844,
21.0405173206694));
#101614=CARTESIAN_POINT('Ctrl Pts',(0.673002776447296,2.86550891017267,
21.0354832128221));
#101615=CARTESIAN_POINT('Ctrl Pts',(0.763135984593806,2.84130031306408,
21.0304491049748));
#101616=CARTESIAN_POINT('Ctrl Pts',(0.853286861478556,2.81708697036422,
21.0254140102955));
#101617=CARTESIAN_POINT('Ctrl Pts',(0.942261296475986,2.78858504027873,
21.0203789156162));
#101618=CARTESIAN_POINT('Ctrl Pts',(1.02963067704451,2.75594351699901,21.0153438209369));
#101619=CARTESIAN_POINT('Ctrl Pts',(1.11709604102944,2.7232661339604,21.0103031947363));
#101620=CARTESIAN_POINT('Ctrl Pts',(1.20295241404228,2.68644023564748,21.0052625685357));
#101621=CARTESIAN_POINT('Ctrl Pts',(1.28679081669276,2.64566312936382,21.0002219423351));
#101622=CARTESIAN_POINT('Ctrl Pts',(1.37068073811,2.60486096551512,20.9951782186656));
#101623=CARTESIAN_POINT('Ctrl Pts',(1.45254983097636,2.56010297292139,20.9901344949961));
#101624=CARTESIAN_POINT('Ctrl Pts',(1.53201532440119,2.51163155056627,20.9850907713266));
#101625=CARTESIAN_POINT('Ctrl Pts',(1.61160942182922,2.46308168386145,20.9800388850821));
#101626=CARTESIAN_POINT('Ctrl Pts',(1.68879178678088,2.41080663864604,20.9749869988375));
#101627=CARTESIAN_POINT('Ctrl Pts',(1.76321028395472,2.35509097373251,20.969935112593));
#101628=CARTESIAN_POINT('Ctrl Pts',(1.80077267675144,2.32696874915272,20.9673851963398));
#101629=CARTESIAN_POINT('Ctrl Pts',(1.83763147156774,2.29797058715442,20.9648352800866));
#101630=CARTESIAN_POINT('Ctrl Pts',(1.87374493010958,2.26813666627226,20.9622853638334));
#101631=CARTESIAN_POINT('Ctrl Pts',(1.9452994429478,2.20902430869222,20.9572330087656));
#101632=CARTESIAN_POINT('Ctrl Pts',(2.01418231319909,2.14641649512292,20.9521806536979));
#101633=CARTESIAN_POINT('Ctrl Pts',(2.08003236992982,2.08058389401728,20.9471282986302));
#101634=CARTESIAN_POINT('Ctrl Pts',(2.14579162946986,2.0148420660337,20.94208290999));
#101635=CARTESIAN_POINT('Ctrl Pts',(2.20852607379946,1.94588459762376,20.9370375213498));
#101636=CARTESIAN_POINT('Ctrl Pts',(2.2679073017104,1.87402253744416,20.9319921327096));
#101637=CARTESIAN_POINT('Ctrl Pts',(2.32722499812845,1.8022373618984,20.9269521420897));
#101638=CARTESIAN_POINT('Ctrl Pts',(2.38319632753376,1.72755411202577,20.9219121514698));
#101639=CARTESIAN_POINT('Ctrl Pts',(2.43553028618555,1.65032003716641,20.9168721608499));
#101640=CARTESIAN_POINT('Ctrl Pts',(2.48782653715735,1.57314161102642,20.9118358016455));
#101641=CARTESIAN_POINT('Ctrl Pts',(2.53649037810421,1.49341637973467,20.9067994424412));
#101642=CARTESIAN_POINT('Ctrl Pts',(2.58127225646249,1.41152312698625,20.9017630832369));
#101643=CARTESIAN_POINT('Ctrl Pts',(2.6260378607082,1.3296596349371,20.896728554288));
#101644=CARTESIAN_POINT('Ctrl Pts',(2.66692409202634,1.24563007601361,20.8916940253391));
#101645=CARTESIAN_POINT('Ctrl Pts',(2.7037263109431,1.15983965939867,20.8866594963902));
#101646=CARTESIAN_POINT('Ctrl Pts',(2.74052544995759,1.07405642240787,20.8816253887707));
#101647=CARTESIAN_POINT('Ctrl Pts',(2.77324108115085,0.986513029051207,
20.8765912811513));
#101648=CARTESIAN_POINT('Ctrl Pts',(2.80171634164585,0.897635527903511,
20.8715571735318));
#101649=CARTESIAN_POINT('Ctrl Pts',(2.83019718411992,0.808740604181175,
20.8665220790808));
#101650=CARTESIAN_POINT('Ctrl Pts',(2.85443586987536,0.718511476424425,
20.8614869846299));
#101651=CARTESIAN_POINT('Ctrl Pts',(2.87432546396001,0.627389135410446,
20.8564518901789));
#101652=CARTESIAN_POINT('Ctrl Pts',(2.8942369086229,0.536166687987395,20.8514112642061));
#101653=CARTESIAN_POINT('Ctrl Pts',(2.90978962952486,0.444049503253866,
20.8463706382332));
#101654=CARTESIAN_POINT('Ctrl Pts',(2.92092793772647,0.351488239645315,
20.8413300122604));
#101655=CARTESIAN_POINT('Ctrl Pts',(2.93207309042788,0.258870097062211,
20.8362862888186));
#101656=CARTESIAN_POINT('Ctrl Pts',(2.9387983980545,0.16580777509446,20.8312425653768));
#101657=CARTESIAN_POINT('Ctrl Pts',(2.94110027163261,0.0727543277242745,
20.826198841935));
#101658=CARTESIAN_POINT('Ctrl Pts',(2.94340587047861,-0.0204497139370955,
20.821146955916));
#101659=CARTESIAN_POINT('Ctrl Pts',(2.94127375394385,-0.113644408764254,
20.8160950698969));
#101660=CARTESIAN_POINT('Ctrl Pts',(2.9347523666932,-0.206379616698647,
20.8110431838779));
#101661=CARTESIAN_POINT('Ctrl Pts',(2.93146072353358,-0.253187328174839,
20.8084932653684));
#101662=CARTESIAN_POINT('Ctrl Pts',(2.92705165208535,-0.29987809960563,
20.8059433468589));
#101663=CARTESIAN_POINT('Ctrl Pts',(2.92153631622689,-0.346395082192867,
20.8033934283495));
#101664=CARTESIAN_POINT('Ctrl Pts',(2.91060834546502,-0.438562855595892,
20.7983410733104));
#101665=CARTESIAN_POINT('Ctrl Pts',(2.89529496721321,-0.530378368764436,
20.7932887182714));
#101666=CARTESIAN_POINT('Ctrl Pts',(2.87562805568234,-0.621391410765094,
20.7882363632323));
#101667=CARTESIAN_POINT('Ctrl Pts',(2.85598826182905,-0.712278959633502,
20.7831909746219));
#101668=CARTESIAN_POINT('Ctrl Pts',(2.83200695617007,-0.802365805612182,
20.7781455860114));
#101669=CARTESIAN_POINT('Ctrl Pts',(2.80376770668779,-0.891207409604904,
20.773100197401));
#101670=CARTESIAN_POINT('Ctrl Pts',(2.77555867015495,-0.979953962668943,
20.7680602068118));
#101671=CARTESIAN_POINT('Ctrl Pts',(2.74310087848207,-1.06745750075294,
20.7630202162227));
#101672=CARTESIAN_POINT('Ctrl Pts',(2.70652858702614,-1.15328531058462,
20.7579802256336));
#101673=CARTESIAN_POINT('Ctrl Pts',(2.6699826466595,-1.23905127971149,20.7529438664615));
#101674=CARTESIAN_POINT('Ctrl Pts',(2.6293282726804,-1.3231435129482,20.7479075072894));
#101675=CARTESIAN_POINT('Ctrl Pts',(2.58474868127479,-1.40514705801502,
20.7428711481173));
#101676=CARTESIAN_POINT('Ctrl Pts',(2.54018529047687,-1.48712080228686,
20.7378366192016));
#101677=CARTESIAN_POINT('Ctrl Pts',(2.49169972802963,-1.56700697641706,
20.7328020902858));
#101678=CARTESIAN_POINT('Ctrl Pts',(2.4395217518428,-1.64441406655557,20.72776756137));
#101679=CARTESIAN_POINT('Ctrl Pts',(2.38734814233266,-1.7218146786403,20.7227334537845));
#101680=CARTESIAN_POINT('Ctrl Pts',(2.33148298192939,-1.79673625097007,
20.717699346199));
#101681=CARTESIAN_POINT('Ctrl Pts',(2.27219942586216,-1.86881614106676,
20.7126652386135));
#101682=CARTESIAN_POINT('Ctrl Pts',(2.21290424850348,-1.94091016090645,
20.7076301441973));
#101683=CARTESIAN_POINT('Ctrl Pts',(2.1501896271088,-2.01016104936067,20.7025950497811));
#101684=CARTESIAN_POINT('Ctrl Pts',(2.08436832254254,-2.07624003814135,
20.6975599553649));
#101685=CARTESIAN_POINT('Ctrl Pts',(2.01847470713354,-2.14239162085491,
20.6925193294279));
#101686=CARTESIAN_POINT('Ctrl Pts',(1.9494679098428,-2.20536403295075,20.6874787034908));
#101687=CARTESIAN_POINT('Ctrl Pts',(1.87769657750741,-2.26486634546433,
20.6824380775537));
#101688=CARTESIAN_POINT('Ctrl Pts',(1.80588114163647,-2.32440522219192,
20.6773943541484));
#101689=CARTESIAN_POINT('Ctrl Pts',(1.73129814356105,-2.38046948745456,
20.6723506307431));
#101690=CARTESIAN_POINT('Ctrl Pts',(1.6543264659011,-2.43281070866995,20.6673069073377));
#101691=CARTESIAN_POINT('Ctrl Pts',(1.57723022010592,-2.48523663699477,
20.6622550213557));
#101692=CARTESIAN_POINT('Ctrl Pts',(1.49773795559287,-2.53392726090745,
20.6572031353737));
#101693=CARTESIAN_POINT('Ctrl Pts',(1.4162542918173,-2.57867946455334,20.6521512493917));
#101694=CARTESIAN_POINT('Ctrl Pts',(1.37512574490992,-2.60126795679305,
20.6496013305497));
#101695=CARTESIAN_POINT('Ctrl Pts',(1.33349019287243,-2.62285381878076,
20.6470514117076));
#101696=CARTESIAN_POINT('Ctrl Pts',(1.2914014689021,-2.6434156400607,20.6445014928655));
#101697=CARTESIAN_POINT('Ctrl Pts',(1.20800776383333,-2.68415639667532,
20.6394491377499));
#101698=CARTESIAN_POINT('Ctrl Pts',(1.12253461990779,-2.72102006398541,
20.6343967826342));
#101699=CARTESIAN_POINT('Ctrl Pts',(1.03537774009605,-2.7537895590102,20.6293444275185));
#101700=CARTESIAN_POINT('Ctrl Pts',(0.948341036332749,-2.78651386989772,
20.6242990388302));
#101701=CARTESIAN_POINT('Ctrl Pts',(0.859625622245854,-2.81515507133425,
20.6192536501419));
#101702=CARTESIAN_POINT('Ctrl Pts',(0.769650435297222,-2.8395426053234,
20.6142082614536));
#101703=CARTESIAN_POINT('Ctrl Pts',(0.679771512067372,-2.86390404728881,
20.6091682707855));
#101704=CARTESIAN_POINT('Ctrl Pts',(0.588635921442568,-2.88402075195228,
20.6041282801174));
#101705=CARTESIAN_POINT('Ctrl Pts',(0.496680117319169,-2.89977117391352,
20.5990882894493));
#101706=CARTESIAN_POINT('Ctrl Pts',(0.404790569221353,-2.91551024737567,
20.5940519301969));
#101707=CARTESIAN_POINT('Ctrl Pts',(0.312082418887491,-2.92688921646361,
20.5890155709445));
#101708=CARTESIAN_POINT('Ctrl Pts',(0.219003712426472,-2.93383731211249,
20.5839792116921));
#101709=CARTESIAN_POINT('Ctrl Pts',(0.125958831554236,-2.94078288276467,
20.5789446826952));
#101710=CARTESIAN_POINT('Ctrl Pts',(0.032544104639384,-2.94330074581374,
20.5739101536984));
#101711=CARTESIAN_POINT('Ctrl Pts',(-0.0607869127297559,-2.94137195050894,
20.5688756247015));
#101712=CARTESIAN_POINT('Ctrl Pts',(-0.154110119414693,-2.93944331662113,
20.5638415170342));
#101713=CARTESIAN_POINT('Ctrl Pts',(-0.247349186341164,-2.93306877362979,
20.5588074093669));
#101714=CARTESIAN_POINT('Ctrl Pts',(-0.340051318546357,-2.92228148896626,
20.5537733016995));
#101715=CARTESIAN_POINT('Ctrl Pts',(-0.432771623061142,-2.91149208968173,
20.548738207201));
#101716=CARTESIAN_POINT('Ctrl Pts',(-0.524954342625254,-2.89628828249211,
20.5437031127024));
#101717=CARTESIAN_POINT('Ctrl Pts',(-0.616153702080383,-2.87675487579541,
20.5386680182038));
#101718=CARTESIAN_POINT('Ctrl Pts',(-0.707453252544559,-2.85720000982817,
20.5336273921839));
#101719=CARTESIAN_POINT('Ctrl Pts',(-0.797766851411304,-2.83330614307377,
20.528586766164));
#101720=CARTESIAN_POINT('Ctrl Pts',(-0.886661091238355,-2.8052087461157,
20.5235461401442));
#101721=CARTESIAN_POINT('Ctrl Pts',(-0.975609956645429,-2.77709408328519,
20.5185024166557));
#101722=CARTESIAN_POINT('Ctrl Pts',(-1.06313731021647,-2.74477090163821,
20.5134586931671));
#101723=CARTESIAN_POINT('Ctrl Pts',(-1.14882908750468,-2.7084231072163,
20.5084149696786));
#101724=CARTESIAN_POINT('Ctrl Pts',(-1.23465954521045,-2.67201648886205,
20.5033630836137));
#101725=CARTESIAN_POINT('Ctrl Pts',(-1.31864809640367,-2.63157244728363,
20.4983111975488));
#101726=CARTESIAN_POINT('Ctrl Pts',(-1.40040482739467,-2.58732107002778,
20.4932593114839));
#101727=CARTESIAN_POINT('Ctrl Pts',(-1.44167119011148,-2.56498537530976,
20.4907093934498));
#101728=CARTESIAN_POINT('Ctrl Pts',(-1.48236940596208,-2.54168038747084,
20.4881594754158));
#101729=CARTESIAN_POINT('Ctrl Pts',(-1.52245231683729,-2.51743975954873,
20.4856095573817));
#101730=CARTESIAN_POINT('Ctrl Pts',(-1.60187177098416,-2.46940987859161,
20.4805572023017));
#101731=CARTESIAN_POINT('Ctrl Pts',(-1.67915864883517,-2.41753188053811,
20.4755048472216));
#101732=CARTESIAN_POINT('Ctrl Pts',(-1.75391612625696,-2.36202079204561,
20.4704524921416));
#101733=CARTESIAN_POINT('Ctrl Pts',(-1.82857052450901,-2.30658624488531,
20.4654071034893));
#101734=CARTESIAN_POINT('Ctrl Pts',(-1.90070209918824,-2.2475288243089,
20.460361714837));
#101735=CARTESIAN_POINT('Ctrl Pts',(-1.96994054805034,-2.18510828956991,
20.4553163261848));
#101736=CARTESIAN_POINT('Ctrl Pts',(-2.03910491925542,-2.1227545380567,
20.450276335553));
#101737=CARTESIAN_POINT('Ctrl Pts',(-2.10538198891141,-2.05704512015461,
20.4452363449213));
#101738=CARTESIAN_POINT('Ctrl Pts',(-2.1684331651186,-1.98828106876612,
20.4401963542896));
#101739=CARTESIAN_POINT('Ctrl Pts',(-2.23143891166714,-1.91956656327938,
20.4351599950739));
#101740=CARTESIAN_POINT('Ctrl Pts',(-2.29122308531933,-1.84780212544846,
20.4301236358583));
#101741=CARTESIAN_POINT('Ctrl Pts',(-2.34748349618322,-1.7733260374639,
20.4250872766426));
#101742=CARTESIAN_POINT('Ctrl Pts',(-2.40372346153572,-1.69887701472258,
20.4200527476827));
#101743=CARTESIAN_POINT('Ctrl Pts',(-2.45644194058178,-1.62171865361694,
20.4150182187228));
#101744=CARTESIAN_POINT('Ctrl Pts',(-2.50537731626918,-1.54222193705181,
20.4099836897629));
#101745=CARTESIAN_POINT('Ctrl Pts',(-2.55430859665226,-1.46273187340888,
20.4049495821327));
#101746=CARTESIAN_POINT('Ctrl Pts',(-2.59945717043663,-1.38090422179658,
20.3999154745025));
#101747=CARTESIAN_POINT('Ctrl Pts',(-2.64060564193848,-1.29713755776428,
20.3948813668723));
#101748=CARTESIAN_POINT('Ctrl Pts',(-2.68176217973455,-1.21335447303556,
20.3898462724109));
#101749=CARTESIAN_POINT('Ctrl Pts',(-2.71891686242717,-1.12763201986958,
20.3848111779496));
#101750=CARTESIAN_POINT('Ctrl Pts',(-2.75189950511258,-1.04039084663465,
20.3797760834882));
#101751=CARTESIAN_POINT('Ctrl Pts',(-2.78491838231024,-0.953053830826071,
20.3747354575055));
#101752=CARTESIAN_POINT('Ctrl Pts',(-2.81375591321227,-0.864195180694685,
20.3696948315229));
#101753=CARTESIAN_POINT('Ctrl Pts',(-2.83829119787571,-0.77425259189832,
20.3646542055402));
#101754=CARTESIAN_POINT('Ctrl Pts',(-2.86284155949075,-0.68425473331088,
20.3596104820889));
#101755=CARTESIAN_POINT('Ctrl Pts',(-2.88308431540144,-0.593172043357264,
20.3545667586376));
#101756=CARTESIAN_POINT('Ctrl Pts',(-2.89894975734376,-0.50145219552474,
20.3495230351863));
#101757=CARTESIAN_POINT('Ctrl Pts',(-2.9148408753344,-0.409583911660327,
20.3444711491583));
#101758=CARTESIAN_POINT('Ctrl Pts',(-2.926340482152,-0.317076851642814,
20.3394192631303));
#101759=CARTESIAN_POINT('Ctrl Pts',(-2.93343077091723,-0.224383404546675,
20.3343673771022));
#101760=CARTESIAN_POINT('Ctrl Pts',(-2.9370095645982,-0.177596773745147,
20.3318174587008));
#101761=CARTESIAN_POINT('Ctrl Pts',(-2.9394658317974,-0.130762655653171,
20.3292675402993));
#101762=CARTESIAN_POINT('Ctrl Pts',(-2.94080231530881,-0.0839389199023072,
20.3267176218979));
#101763=CARTESIAN_POINT('Ctrl Pts',(-2.94159575851465,-0.0561406158553956,
20.3252037869618));
#101764=CARTESIAN_POINT('Ctrl Pts',(-2.94199506204502,-0.0283310083262269,
20.3236899520257));
#101765=CARTESIAN_POINT('Ctrl Pts',(-2.94199995448524,-0.000517502503631551,
20.3221761170896));
#101766=CARTESIAN_POINT('',(-2.94199904186917,-0.0023743716766289,19.3221761171224));
#101767=CARTESIAN_POINT('Ctrl Pts',(-2.94199995448535,-0.000517501908740767,
20.3221761170572));
#101768=CARTESIAN_POINT('Ctrl Pts',(-2.94201620488574,0.0918660746620151,
20.3171478589648));
#101769=CARTESIAN_POINT('Ctrl Pts',(-2.9376766891411,0.184422648897923,
20.3121196008723));
#101770=CARTESIAN_POINT('Ctrl Pts',(-2.92895857371174,0.276705029734675,
20.3070913427799));
#101771=CARTESIAN_POINT('Ctrl Pts',(-2.92025239438784,0.368861065349422,
20.3020699689526));
#101772=CARTESIAN_POINT('Ctrl Pts',(-2.90717956698,0.460743210390338,20.2970485951254));
#101773=CARTESIAN_POINT('Ctrl Pts',(-2.88976926150288,0.551903628610208,
20.2920272212981));
#101774=CARTESIAN_POINT('Ctrl Pts',(-2.87182607555534,0.64585421077106,
20.2868521573446));
#101775=CARTESIAN_POINT('Ctrl Pts',(-2.84927557040695,0.739037686100096,
20.2816770933911));
#101776=CARTESIAN_POINT('Ctrl Pts',(-2.82220749584933,0.830968621773331,
20.2765020294376));
#101777=CARTESIAN_POINT('Ctrl Pts',(-2.79598934880378,0.920012960127909,
20.2714894605748));
#101778=CARTESIAN_POINT('Ctrl Pts',(-2.76553324655604,1.00788178111871,
20.266476891712));
#101779=CARTESIAN_POINT('Ctrl Pts',(-2.7309724190848,1.09414516687601,20.2614643228493));
#101780=CARTESIAN_POINT('Ctrl Pts',(-2.69642279554893,1.18038058775313,
20.256453378962));
#101781=CARTESIAN_POINT('Ctrl Pts',(-2.65777125670995,1.26501119075463,
20.2514424350747));
#101782=CARTESIAN_POINT('Ctrl Pts',(-2.61519994227204,1.34762504501079,
20.2464314911874));
#101783=CARTESIAN_POINT('Ctrl Pts',(-2.57263022705451,1.43023579582132,
20.2414207355396));
#101784=CARTESIAN_POINT('Ctrl Pts',(-2.52614123529246,1.51082954974157,
20.2364099798918));
#101785=CARTESIAN_POINT('Ctrl Pts',(-2.47596147827404,1.58901817425196,
20.231399224244));
#101786=CARTESIAN_POINT('Ctrl Pts',(-2.42576922385174,1.66722627185024,
20.226387220654));
#101787=CARTESIAN_POINT('Ctrl Pts',(-2.37188462195081,1.74302767324794,
20.221375217064));
#101788=CARTESIAN_POINT('Ctrl Pts',(-2.31457931158189,1.81606349294212,
20.216363213474));
#101789=CARTESIAN_POINT('Ctrl Pts',(-2.25720983495547,1.88918109275723,
20.2113455978123));
#101790=CARTESIAN_POINT('Ctrl Pts',(-2.19641228545946,1.95952657909388,
20.2063279821506));
#101791=CARTESIAN_POINT('Ctrl Pts',(-2.13249808730623,2.02677475503206,
20.2013103664888));
#101792=CARTESIAN_POINT('Ctrl Pts',(-2.06854077114854,2.09406829815366,
20.1962893658269));
#101793=CARTESIAN_POINT('Ctrl Pts',(-2.00146294661669,2.15826006370198,
20.1912683651649));
#101794=CARTESIAN_POINT('Ctrl Pts',(-1.9316107009224,2.21906378909712,20.186247364503));
#101795=CARTESIAN_POINT('Ctrl Pts',(-1.86165120023888,2.27996087588454,
20.1812186543198));
#101796=CARTESIAN_POINT('Ctrl Pts',(-1.78890913164896,2.33745926826067,
20.1761899441366));
#101797=CARTESIAN_POINT('Ctrl Pts',(-1.71376084649715,2.39131506937362,
20.1711612339534));
#101798=CARTESIAN_POINT('Ctrl Pts',(-1.6971455403518,2.40322260154667,20.1700493847736));
#101799=CARTESIAN_POINT('Ctrl Pts',(-1.68041270353207,2.41495224119587,
20.1689375355938));
#101800=CARTESIAN_POINT('Ctrl Pts',(-1.66356656305616,2.42650165676463,
20.167825686414));
#101801=CARTESIAN_POINT('Ctrl Pts',(-1.58701599746003,2.47898336884331,
20.1627733313245));
#101802=CARTESIAN_POINT('Ctrl Pts',(-1.50784212642289,2.52793320386305,
20.157720976235));
#101803=CARTESIAN_POINT('Ctrl Pts',(-1.42640471145188,2.57307862280729,
20.1526686211455));
#101804=CARTESIAN_POINT('Ctrl Pts',(-1.3450795862654,2.61816179309878,20.1476232324837));
#101805=CARTESIAN_POINT('Ctrl Pts',(-1.2614975043014,2.6594507577,20.1425778438219));
#101806=CARTESIAN_POINT('Ctrl Pts',(-1.17604800636927,2.69671561101924,
20.1375324551601));
#101807=CARTESIAN_POINT('Ctrl Pts',(-1.09068993016381,2.73394059497333,
20.1324924645189));
#101808=CARTESIAN_POINT('Ctrl Pts',(-1.00346881420423,2.76714984858702,
20.1274524738776));
#101809=CARTESIAN_POINT('Ctrl Pts',(-0.91479868509532,2.79615939562606,
20.1224124832364));
#101810=CARTESIAN_POINT('Ctrl Pts',(-0.826192444622468,2.82514804069493,
20.1173761240111));
#101811=CARTESIAN_POINT('Ctrl Pts',(-0.736139687189324,2.84994285600389,
20.1123397647859));
#101812=CARTESIAN_POINT('Ctrl Pts',(-0.64507332202963,2.87040840460128,
20.1073034055606));
#101813=CARTESIAN_POINT('Ctrl Pts',(-0.554040051160576,2.89086651584447,
20.1022688765911));
#101814=CARTESIAN_POINT('Ctrl Pts',(-0.461994337333051,2.9069983885859,
20.0972343476216));
#101815=CARTESIAN_POINT('Ctrl Pts',(-0.369382107035341,2.91871904420452,
20.0921998186521));
#101816=CARTESIAN_POINT('Ctrl Pts',(-0.276777627271035,2.93043871894477,
20.0871657110123));
#101817=CARTESIAN_POINT('Ctrl Pts',(-0.183607166047962,2.93774785495905,
20.0821316033725));
#101818=CARTESIAN_POINT('Ctrl Pts',(-0.0903235080035432,2.94061314421022,
20.0770974957327));
#101819=CARTESIAN_POINT('Ctrl Pts',(0.00297843634419862,2.94347899514122,
20.0720624012618));
#101820=CARTESIAN_POINT('Ctrl Pts',(0.0963931775675672,2.94189925598673,
20.0670273067909));
#101821=CARTESIAN_POINT('Ctrl Pts',(0.189467334651144,2.93589273119782,
20.0619922123199));
#101822=CARTESIAN_POINT('Ctrl Pts',(0.282643742384046,2.92987960768076,
20.0569515863277));
#101823=CARTESIAN_POINT('Ctrl Pts',(0.375478375100996,2.91943001959899,
20.0519109603355));
#101824=CARTESIAN_POINT('Ctrl Pts',(0.467522688922141,2.90461469653774,
20.0468703343433));
#101825=CARTESIAN_POINT('Ctrl Pts',(0.559623564045482,2.88979026944898,
20.0418266108825));
#101826=CARTESIAN_POINT('Ctrl Pts',(0.650932719021392,2.87059485787772,
20.0367828874217));
#101827=CARTESIAN_POINT('Ctrl Pts',(0.741013672775681,2.84714993225849,
20.031739163961));
#101828=CARTESIAN_POINT('Ctrl Pts',(0.831240410233106,2.82366706423374,
20.0266872779236));
#101829=CARTESIAN_POINT('Ctrl Pts',(0.920234554756113,2.79592108465082,
20.0216353918862));
#101830=CARTESIAN_POINT('Ctrl Pts',(1.00757677343834,2.7640826770608,20.0165835058489));
#101831=CARTESIAN_POINT('Ctrl Pts',(1.05166239229028,2.748012374256,20.0140335875426));
#101832=CARTESIAN_POINT('Ctrl Pts',(1.0953274965222,2.73090020389196,20.0114836692364));
#101833=CARTESIAN_POINT('Ctrl Pts',(1.13852051928327,2.71277257195861,20.0089337509301));
#101834=CARTESIAN_POINT('Ctrl Pts',(1.22410227600109,2.67685485917033,20.0038813958462));
#101835=CARTESIAN_POINT('Ctrl Pts',(1.30813624208454,2.63681886627311,19.9988290407623));
#101836=CARTESIAN_POINT('Ctrl Pts',(1.39019844753919,2.59281936826683,19.9937766856784));
#101837=CARTESIAN_POINT('Ctrl Pts',(1.47214750171708,2.5488805388637,19.9887312970223));
#101838=CARTESIAN_POINT('Ctrl Pts',(1.55212980967024,2.50098927224878,19.9836859083661));
#101839=CARTESIAN_POINT('Ctrl Pts',(1.629741106866,2.44934846940797,19.97864051971));
#101840=CARTESIAN_POINT('Ctrl Pts',(1.70726936836178,2.39776291664501,19.9736005290745));
#101841=CARTESIAN_POINT('Ctrl Pts',(1.78243129336603,2.34243604609097,19.9685605384389));
#101842=CARTESIAN_POINT('Ctrl Pts',(1.85484796074386,2.28361622049861,19.9635205478034));
#101843=CARTESIAN_POINT('Ctrl Pts',(1.92721245043526,2.22483877579073,19.9584841885839));
#101844=CARTESIAN_POINT('Ctrl Pts',(1.99683527024948,2.16257365770787,19.9534478293644));
#101845=CARTESIAN_POINT('Ctrl Pts',(2.06336807148347,2.09711139465279,19.948411470145));
#101846=CARTESIAN_POINT('Ctrl Pts',(2.12987669413183,2.03167292114067,19.9433769411813));
#101847=CARTESIAN_POINT('Ctrl Pts',(2.19329721269772,1.963039922091,19.9383424122176));
#101848=CARTESIAN_POINT('Ctrl Pts',(2.25331664124461,1.89154120079106,19.9333078832539));
#101849=CARTESIAN_POINT('Ctrl Pts',(2.31333104688447,1.82004846307742,19.9282737756199));
#101850=CARTESIAN_POINT('Ctrl Pts',(2.36994464293867,1.74569082031407,19.923239667986));
#101851=CARTESIAN_POINT('Ctrl Pts',(2.4228841615683,1.66883083013871,19.918205560352));
#101852=CARTESIAN_POINT('Ctrl Pts',(2.47583405787918,1.59195577317584,19.9131704658869));
#101853=CARTESIAN_POINT('Ctrl Pts',(2.52510819472144,1.51257776064216,19.9081353714219));
#101854=CARTESIAN_POINT('Ctrl Pts',(2.57047678576047,1.43108808040125,19.9031002769568));
#101855=CARTESIAN_POINT('Ctrl Pts',(2.61589521843168,1.34950887613994,19.8980596509705));
#101856=CARTESIAN_POINT('Ctrl Pts',(2.6573993243255,1.2658137621942,19.8930190249841));
#101857=CARTESIAN_POINT('Ctrl Pts',(2.69480558441763,1.18041808787886,19.8879783989978));
#101858=CARTESIAN_POINT('Ctrl Pts',(2.73223483068551,1.09496993785559,19.8829346755429));
#101859=CARTESIAN_POINT('Ctrl Pts',(2.7655610594934,1.00781956170815,19.877890952088));
#101860=CARTESIAN_POINT('Ctrl Pts',(2.79464993773324,0.919399654952938,
19.872847228633));
#101861=CARTESIAN_POINT('Ctrl Pts',(2.82378589234436,0.830836652670853,
19.8677953426015));
#101862=CARTESIAN_POINT('Ctrl Pts',(2.84867068767718,0.741000445689483,
19.86274345657));
#101863=CARTESIAN_POINT('Ctrl Pts',(2.86922064706356,0.650335973527639,
19.8576915705384));
#101864=CARTESIAN_POINT('Ctrl Pts',(2.8795931531915,0.604573460064577,19.8551416521744));
#101865=CARTESIAN_POINT('Ctrl Pts',(2.88886209993438,0.558600050050892,
19.8525917338103));
#101866=CARTESIAN_POINT('Ctrl Pts',(2.8970217502022,0.512473393314626,19.8500418154463));
#101867=CARTESIAN_POINT('Ctrl Pts',(2.91318911112535,0.421078997334762,
19.844989460362));
#101868=CARTESIAN_POINT('Ctrl Pts',(2.92505631463085,0.328754798638797,
19.8399371052778));
#101869=CARTESIAN_POINT('Ctrl Pts',(2.93252379981452,0.23594101703904,19.8348847501935));
#101870=CARTESIAN_POINT('Ctrl Pts',(2.93998098847401,0.143255211501282,
19.8298393615371));
#101871=CARTESIAN_POINT('Ctrl Pts',(2.94305047849443,0.0500816034598757,
19.8247939728806));
#101872=CARTESIAN_POINT('Ctrl Pts',(2.94168383686064,-0.0431300817628487,
19.8197485842242));
#101873=CARTESIAN_POINT('Ctrl Pts',(2.9403186573857,-0.136242040556156,
19.8147085935883));
#101874=CARTESIAN_POINT('Ctrl Pts',(2.93452678649661,-0.229391553749678,
19.8096686029524));
#101875=CARTESIAN_POINT('Ctrl Pts',(2.92431173361142,-0.322125572816807,
19.8046286123166));
#101876=CARTESIAN_POINT('Ctrl Pts',(2.91410404088029,-0.414792775130863,
19.7995922530968));
#101877=CARTESIAN_POINT('Ctrl Pts',(2.89947954925317,-0.507044638062517,
19.794555893877));
#101878=CARTESIAN_POINT('Ctrl Pts',(2.88049377246798,-0.598430970767051,
19.7895195346573));
#101879=CARTESIAN_POINT('Ctrl Pts',(2.86151489527552,-0.689784092901165,
19.7844850056933));
#101880=CARTESIAN_POINT('Ctrl Pts',(2.83817797182982,-0.780271875163795,
19.7794504767293));
#101881=CARTESIAN_POINT('Ctrl Pts',(2.81058984458734,-0.869453118634081,
19.7744159477653));
#101882=CARTESIAN_POINT('Ctrl Pts',(2.7830040261406,-0.95862689870266,19.769381840131));
#101883=CARTESIAN_POINT('Ctrl Pts',(2.75116784272559,-1.04649393303362,
19.7643477324968));
#101884=CARTESIAN_POINT('Ctrl Pts',(2.71523802490897,-1.13262812435877,
19.7593136248626));
#101885=CARTESIAN_POINT('Ctrl Pts',(2.67930116380589,-1.21877920048377,
19.7542785303972));
#101886=CARTESIAN_POINT('Ctrl Pts',(2.6392692459469,-1.30319634915029,19.7492434359319));
#101887=CARTESIAN_POINT('Ctrl Pts',(2.59534670545318,-1.38547445970445,
19.7442083414665));
#101888=CARTESIAN_POINT('Ctrl Pts',(2.551375911949,-1.46784296044286,19.7391677154799));
#101889=CARTESIAN_POINT('Ctrl Pts',(2.50350617351727,-1.54806733982987,
19.7341270894933));
#101890=CARTESIAN_POINT('Ctrl Pts',(2.45198721241842,-1.62576834454868,
19.7290864635067));
#101891=CARTESIAN_POINT('Ctrl Pts',(2.40043659287825,-1.7035170965948,19.7240427400516));
#101892=CARTESIAN_POINT('Ctrl Pts',(2.34523254902948,-1.77873902912197,
19.7189990165964));
#101893=CARTESIAN_POINT('Ctrl Pts',(2.28666602757342,-1.8510868370613,19.7139552931413));
#101894=CARTESIAN_POINT('Ctrl Pts',(2.22800472421211,-1.92355173003328,
19.7089034071095));
#101895=CARTESIAN_POINT('Ctrl Pts',(2.16597037481727,-1.99313288135999,
19.7038515210777));
#101896=CARTESIAN_POINT('Ctrl Pts',(2.10089165831102,-2.05951893412981,
19.698799635046));
#101897=CARTESIAN_POINT('Ctrl Pts',(2.06804344813789,-2.09302701681822,
19.6962497166848));
#101898=CARTESIAN_POINT('Ctrl Pts',(2.03442017375972,-2.12572171390069,
19.6936997983236));
#101899=CARTESIAN_POINT('Ctrl Pts',(2.00006718655783,-2.15756697445401,
19.6911498799624));
#101900=CARTESIAN_POINT('Ctrl Pts',(1.93200089383406,-2.22066450987208,
19.6860975248768));
#101901=CARTESIAN_POINT('Ctrl Pts',(1.86082366896969,-2.28065109878669,
19.6810451697912));
#101902=CARTESIAN_POINT('Ctrl Pts',(1.78685161924509,-2.33720458899113,
19.6759928147056));
#101903=CARTESIAN_POINT('Ctrl Pts',(1.7129815657048,-2.39368010055051,19.6709474260478));
#101904=CARTESIAN_POINT('Ctrl Pts',(1.63632469483503,-2.44673165243948,
19.66590203739));
#101905=CARTESIAN_POINT('Ctrl Pts',(1.55723279960355,-2.49607492031768,
19.6608566487321));
#101906=CARTESIAN_POINT('Ctrl Pts',(1.47822552415187,-2.54536539623216,
19.6558166580949));
#101907=CARTESIAN_POINT('Ctrl Pts',(1.39678877747987,-2.59095524019785,
19.6507766674576));
#101908=CARTESIAN_POINT('Ctrl Pts',(1.31330528277103,-2.63260198933407,
19.6457366768203));
#101909=CARTESIAN_POINT('Ctrl Pts',(1.22988193962321,-2.67421873113793,
19.6407003175992));
#101910=CARTESIAN_POINT('Ctrl Pts',(1.14441517603931,-2.71189782742285,
19.635663958378));
#101911=CARTESIAN_POINT('Ctrl Pts',(1.05731348343144,-2.74544207692569,
19.6306275991568));
#101912=CARTESIAN_POINT('Ctrl Pts',(0.97024344431919,-2.77897413616308,
19.6255930701913));
#101913=CARTESIAN_POINT('Ctrl Pts',(0.881540070663633,-2.80837417428135,
19.6205585412259));
#101914=CARTESIAN_POINT('Ctrl Pts',(0.791632099835083,-2.83349300661052,
19.6155240122605));
#101915=CARTESIAN_POINT('Ctrl Pts',(0.701731653226236,-2.85860973679444,
19.6104899046248));
#101916=CARTESIAN_POINT('Ctrl Pts',(0.610627237784615,-2.87944585418853,
19.6054557969891));
#101917=CARTESIAN_POINT('Ctrl Pts',(0.518761920775194,-2.89590228936572,
19.6004216893534));
#101918=CARTESIAN_POINT('Ctrl Pts',(0.426878595499444,-2.91236195048146,
19.5953865948866));
#101919=CARTESIAN_POINT('Ctrl Pts',(0.334234509743728,-2.92444014634262,
19.5903515004198));
#101920=CARTESIAN_POINT('Ctrl Pts',(0.241280930547855,-2.93208927431515,
19.5853164059531));
#101921=CARTESIAN_POINT('Ctrl Pts',(0.148225233168343,-2.93974680556879,
19.580275779965));
#101922=CARTESIAN_POINT('Ctrl Pts',(0.0548598070819101,-2.9429655198555,
19.5752351539769));
#101923=CARTESIAN_POINT('Ctrl Pts',(-0.0383612835256337,-2.94174988942403,
19.5701945279889));
#101924=CARTESIAN_POINT('Ctrl Pts',(-0.131639658565474,-2.94053351198671,
19.5651508045322));
#101925=CARTESIAN_POINT('Ctrl Pts',(-0.224773078460283,-2.93487739197961,
19.5601070810756));
#101926=CARTESIAN_POINT('Ctrl Pts',(-0.317312003031018,-2.92483796008128,
19.555063357619));
#101927=CARTESIAN_POINT('Ctrl Pts',(-0.410000689195166,-2.91478228073546,
19.5500114715857));
#101928=CARTESIAN_POINT('Ctrl Pts',(-0.502092520991421,-2.90032919643848,
19.5449595855525));
#101929=CARTESIAN_POINT('Ctrl Pts',(-0.593147736187301,-2.88158632753834,
19.5399076995192));
#101930=CARTESIAN_POINT('Ctrl Pts',(-0.639107475240012,-2.87212594284871,
19.5373577811723));
#101931=CARTESIAN_POINT('Ctrl Pts',(-0.684803347257254,-2.86157345247506,
19.5348078628254));
#101932=CARTESIAN_POINT('Ctrl Pts',(-0.730180482178185,-2.84994744924289,
19.5322579444784));
#101933=CARTESIAN_POINT('Ctrl Pts',(-0.820089791871933,-2.82691192866796,
19.5272055893937));
#101934=CARTESIAN_POINT('Ctrl Pts',(-0.909069278997653,-2.79957625496688,
19.522153234309));
#101935=CARTESIAN_POINT('Ctrl Pts',(-0.996676917005936,-2.76803163332855,
19.5171008792243));
#101936=CARTESIAN_POINT('Ctrl Pts',(-1.08416375743151,-2.73653050691653,
19.5120554905673));
#101937=CARTESIAN_POINT('Ctrl Pts',(-1.17028209318973,-2.70083211405906,
19.5070101019103));
#101938=CARTESIAN_POINT('Ctrl Pts',(-1.25460236430888,-2.66107814756925,
19.5019647132533));
#101939=CARTESIAN_POINT('Ctrl Pts',(-1.33883242185103,-2.62136671352708,
19.4969247226169));
#101940=CARTESIAN_POINT('Ctrl Pts',(-1.42126783880829,-2.57760851875703,
19.4918847319805));
#101941=CARTESIAN_POINT('Ctrl Pts',(-1.5014974883339,-2.52999393132217,
19.4868447413441));
#101942=CARTESIAN_POINT('Ctrl Pts',(-1.58166933075983,-2.48241365116919,
19.4818083821238));
#101943=CARTESIAN_POINT('Ctrl Pts',(-1.65963818378397,-2.43098272730459,
19.4767720229035));
#101944=CARTESIAN_POINT('Ctrl Pts',(-1.7350170079866,-2.37593770583263,
19.4717356636832));
#101945=CARTESIAN_POINT('Ctrl Pts',(-1.81036843888357,-2.32091268818953,
19.4667011347187));
#101946=CARTESIAN_POINT('Ctrl Pts',(-1.88313135242865,-2.26227644386214,
19.4616666057541));
#101947=CARTESIAN_POINT('Ctrl Pts',(-1.95294810376865,-2.20030854745111,
19.4566320767896));
#101948=CARTESIAN_POINT('Ctrl Pts',(-2.02275901228322,-2.13834583701042,
19.4515979691548));
#101949=CARTESIAN_POINT('Ctrl Pts',(-2.0896239166873,-2.07305232387743,
19.44656386152));
#101950=CARTESIAN_POINT('Ctrl Pts',(-2.15321953545585,-2.00474677506444,
19.4415297538852));
#101951=CARTESIAN_POINT('Ctrl Pts',(-2.21682762081048,-1.93642783638246,
19.4364946594193));
#101952=CARTESIAN_POINT('Ctrl Pts',(-2.27716484532294,-1.86509601475816,
19.4314595649534));
#101953=CARTESIAN_POINT('Ctrl Pts',(-2.33394674751587,-1.79110484890195,
19.4264244704875));
#101954=CARTESIAN_POINT('Ctrl Pts',(-2.39079102992836,-1.71703239684375,
19.4213838445003));
#101955=CARTESIAN_POINT('Ctrl Pts',(-2.44407192261281,-1.64029512179496,
19.4163432185131));
#101956=CARTESIAN_POINT('Ctrl Pts',(-2.49354722184721,-1.56127712223617,
19.411302592526));
#101957=CARTESIAN_POINT('Ctrl Pts',(-2.54305292369132,-1.48221056605544,
19.4062588690702));
#101958=CARTESIAN_POINT('Ctrl Pts',(-2.58874815910735,-1.40086088226812,
19.4012151456145));
#101959=CARTESIAN_POINT('Ctrl Pts',(-2.6304368500518,-1.31763651205086,
19.3961714221588));
#101960=CARTESIAN_POINT('Ctrl Pts',(-2.67219300844091,-1.23427745457275,
19.3911195361264));
#101961=CARTESIAN_POINT('Ctrl Pts',(-2.70992949818134,-1.14903805952311,
19.3860676500941));
#101962=CARTESIAN_POINT('Ctrl Pts',(-2.74349856672358,-1.06234627800245,
19.3810157640618));
#101963=CARTESIAN_POINT('Ctrl Pts',(-2.76044241373679,-1.01858896368972,
19.3784658457061));
#101964=CARTESIAN_POINT('Ctrl Pts',(-2.77632532715895,-0.974461864885243,
19.3759159273504));
#101965=CARTESIAN_POINT('Ctrl Pts',(-2.79113321301135,-0.930021175686314,
19.3733660089946));
#101966=CARTESIAN_POINT('Ctrl Pts',(-2.82599674499543,-0.825390480614395,
19.3673625078171));
#101967=CARTESIAN_POINT('Ctrl Pts',(-2.8550003049623,-0.718715539266835,
19.3613590066396));
#101968=CARTESIAN_POINT('Ctrl Pts',(-2.8779384302806,-0.610601663536891,
19.3553555054621));
#101969=CARTESIAN_POINT('Ctrl Pts',(-2.90063211165595,-0.503639921283632,
19.3494159815922));
#101970=CARTESIAN_POINT('Ctrl Pts',(-2.91738889183095,-0.395269828056337,
19.3434764577223));
#101971=CARTESIAN_POINT('Ctrl Pts',(-2.92805595837851,-0.286098417688969,
19.3375369338524));
#101972=CARTESIAN_POINT('Ctrl Pts',(-2.93725169291171,-0.191985260723234,
19.3324166616091));
#101973=CARTESIAN_POINT('Ctrl Pts',(-2.9419224497351,-0.0972769462315368,
19.3272963893658));
#101974=CARTESIAN_POINT('Ctrl Pts',(-2.94199904186917,-0.00237437167659856,
19.3221761171224));
#101975=CARTESIAN_POINT('',(-2.94199948962717,0.00173292627207862,18.3221761170896));
#101976=CARTESIAN_POINT('Ctrl Pts',(-2.94199904186967,-0.00237437106792486,
19.3221761170896));
#101977=CARTESIAN_POINT('Ctrl Pts',(-2.94207416580396,0.0907090335007012,
19.3171539944026));
#101978=CARTESIAN_POINT('Ctrl Pts',(-2.93772732127096,0.183853550265652,
19.3121318717157));
#101979=CARTESIAN_POINT('Ctrl Pts',(-2.92896782757791,0.276607058864309,
19.3071097490287));
#101980=CARTESIAN_POINT('Ctrl Pts',(-2.92021036671541,0.369339041998981,
19.3020887918343));
#101981=CARTESIAN_POINT('Ctrl Pts',(-2.90704233305619,0.461679753029792,
19.2970678346399));
#101982=CARTESIAN_POINT('Ctrl Pts',(-2.88952502403285,0.553180924732574,
19.2920468774454));
#101983=CARTESIAN_POINT('Ctrl Pts',(-2.87200682498055,0.644686745476608,
19.2870256651435));
#101984=CARTESIAN_POINT('Ctrl Pts',(-2.85013899630507,0.735352503844594,
19.2820044528415));
#101985=CARTESIAN_POINT('Ctrl Pts',(-2.82403397171941,0.82474003575351,
19.2769832405396));
#101986=CARTESIAN_POINT('Ctrl Pts',(-2.79695214293673,0.917472292201672,
19.2717741432872));
#101987=CARTESIAN_POINT('Ctrl Pts',(-2.76530992063666,1.00882828203394,
19.2665650460348));
#101988=CARTESIAN_POINT('Ctrl Pts',(-2.72928894331806,1.09833777312891,
19.2613559487824));
#101989=CARTESIAN_POINT('Ctrl Pts',(-2.69451270762369,1.18475417243064,
19.2563268572005));
#101990=CARTESIAN_POINT('Ctrl Pts',(-2.65565561648089,1.26944920412853,
19.2512977656186));
#101991=CARTESIAN_POINT('Ctrl Pts',(-2.61292887903296,1.35202317772869,
19.2462686740367));
#101992=CARTESIAN_POINT('Ctrl Pts',(-2.57017004308213,1.4346591851065,19.2412358043449));
#101993=CARTESIAN_POINT('Ctrl Pts',(-2.5235359999055,1.51517057890675,19.2362029346531));
#101994=CARTESIAN_POINT('Ctrl Pts',(-2.47328191787931,1.59318566234172,
19.2311700649612));
#101995=CARTESIAN_POINT('Ctrl Pts',(-2.4229493979775,1.67132251374389,19.2261293398358));
#101996=CARTESIAN_POINT('Ctrl Pts',(-2.36898582885025,1.74695492290091,
19.2210886147103));
#101997=CARTESIAN_POINT('Ctrl Pts',(-2.3116870171327,1.8197437003106,19.2160478895848));
#101998=CARTESIAN_POINT('Ctrl Pts',(-2.30572373548415,1.82731907521868,
19.2155232842268));
#101999=CARTESIAN_POINT('Ctrl Pts',(-2.29972436162034,1.83486368309387,
19.2149986788688));
#102000=CARTESIAN_POINT('Ctrl Pts',(-2.29368925134959,1.84237716503526,
19.2144740735107));
#102001=CARTESIAN_POINT('Ctrl Pts',(-2.23556647467933,1.91473780358269,
19.2094217184257));
#102002=CARTESIAN_POINT('Ctrl Pts',(-2.17391183306994,1.98447512038605,
19.2043693633407));
#102003=CARTESIAN_POINT('Ctrl Pts',(-2.10899100269114,2.05122425652775,
19.1993170082556));
#102004=CARTESIAN_POINT('Ctrl Pts',(-2.04415968824456,2.11788135578218,
19.1942716195984));
#102005=CARTESIAN_POINT('Ctrl Pts',(-1.9760714412638,2.18155814614139,19.1892262309411));
#102006=CARTESIAN_POINT('Ctrl Pts',(-1.90503276494137,2.24192198002068,
19.1841808422839));
#102007=CARTESIAN_POINT('Ctrl Pts',(-1.83407009232494,2.30222123112167,
19.1791408516472));
#102008=CARTESIAN_POINT('Ctrl Pts',(-1.76016360138424,2.35921428487592,
19.1741008610105));
#102009=CARTESIAN_POINT('Ctrl Pts',(-1.68365650684848,2.41260538981135,
19.1690608703738));
#102010=CARTESIAN_POINT('Ctrl Pts',(-1.60720453723539,2.46595802536628,
19.1640245111532));
#102011=CARTESIAN_POINT('Ctrl Pts',(-1.52815605170076,2.5157136170833,19.1589881519326));
#102012=CARTESIAN_POINT('Ctrl Pts',(-1.44688636636842,2.56161742709898,
19.153951792712));
#102013=CARTESIAN_POINT('Ctrl Pts',(-1.36564621513072,2.60750455527981,
19.1489172637472));
#102014=CARTESIAN_POINT('Ctrl Pts',(-1.28218685410517,2.64954246429721,
19.1438827347823));
#102015=CARTESIAN_POINT('Ctrl Pts',(-1.19691064003318,2.68752096173692,
19.1388482058175));
#102016=CARTESIAN_POINT('Ctrl Pts',(-1.11164156255831,2.72549628083156,
19.1338140981824));
#102017=CARTESIAN_POINT('Ctrl Pts',(-1.0245563402353,2.75941268323711,19.1287799905473));
#102018=CARTESIAN_POINT('Ctrl Pts',(-0.936078824233458,2.7891074620426,
19.1237458829122));
#102019=CARTESIAN_POINT('Ctrl Pts',(-0.84758396407199,2.8188080618861,19.118710788446));
#102020=CARTESIAN_POINT('Ctrl Pts',(-0.757696689436905,2.84428525360216,
19.1136756939798));
#102021=CARTESIAN_POINT('Ctrl Pts',(-0.666856478877766,2.86542604800381,
19.1086405995136));
#102022=CARTESIAN_POINT('Ctrl Pts',(-0.57591647186845,2.88659006754136,
19.1035999735261));
#102023=CARTESIAN_POINT('Ctrl Pts',(-0.484021872569202,2.90340807954448,
19.0985593475386));
#102024=CARTESIAN_POINT('Ctrl Pts',(-0.391622530990364,2.91581820304708,
19.0935187215512));
#102025=CARTESIAN_POINT('Ctrl Pts',(-0.29916640994461,2.92823595258018,
19.0884749980952));
#102026=CARTESIAN_POINT('Ctrl Pts',(-0.206205371415175,2.93624038313473,
19.0834312746391));
#102027=CARTESIAN_POINT('Ctrl Pts',(-0.113192377192708,2.93982167584115,
19.0783875511831));
#102028=CARTESIAN_POINT('Ctrl Pts',(-0.0200288541598324,2.94340876438002,
19.0733356651505));
#102029=CARTESIAN_POINT('Ctrl Pts',(0.0731863487657453,2.94255842859601,
19.0682837791178));
#102030=CARTESIAN_POINT('Ctrl Pts',(0.166002467893603,2.93731291840914,
19.0632318930852));
#102031=CARTESIAN_POINT('Ctrl Pts',(0.212851015954096,2.93466526907409,
19.0606819747324));
#102032=CARTESIAN_POINT('Ctrl Pts',(0.259598001505305,2.93089868913091,
19.0581320563796));
#102033=CARTESIAN_POINT('Ctrl Pts',(0.306186427613535,2.92602355963606,
19.0555821380269));
#102034=CARTESIAN_POINT('Ctrl Pts',(0.398495764220038,2.91636407965072,
19.050529782942));
#102035=CARTESIAN_POINT('Ctrl Pts',(0.490513180381778,2.90231476261001,
19.0454774278571));
#102036=CARTESIAN_POINT('Ctrl Pts',(0.581788069406744,2.88390128858392,
19.0404250727722));
#102037=CARTESIAN_POINT('Ctrl Pts',(0.67293710426812,2.86551320393268,19.0353796841151));
#102038=CARTESIAN_POINT('Ctrl Pts',(0.763345214788649,2.84277300694814,
19.030334295458));
#102039=CARTESIAN_POINT('Ctrl Pts',(0.852566754704504,2.81575814458072,
19.0252889068009));
#102040=CARTESIAN_POINT('Ctrl Pts',(0.941692837215947,2.78877218519619,
19.0202489161644));
#102041=CARTESIAN_POINT('Ctrl Pts',(1.02963444955838,2.7575207788669,19.0152089255278));
#102042=CARTESIAN_POINT('Ctrl Pts',(1.11595707314046,2.72213221774913,19.0101689348913));
#102043=CARTESIAN_POINT('Ctrl Pts',(1.2022174995107,2.6867691548118,19.0051325756708));
#102044=CARTESIAN_POINT('Ctrl Pts',(1.28686084587408,2.64727503007975,19.0000962164504));
#102045=CARTESIAN_POINT('Ctrl Pts',(1.36946967966179,2.60382733615097,18.9950598572299));
#102046=CARTESIAN_POINT('Ctrl Pts',(1.45204849269696,2.56039543148355,18.9900253282652));
#102047=CARTESIAN_POINT('Ctrl Pts',(1.53259386919414,2.51301301848245,18.9849907993005));
#102048=CARTESIAN_POINT('Ctrl Pts',(1.61071117277391,2.46190444938493,18.9799562703358));
#102049=CARTESIAN_POINT('Ctrl Pts',(1.68882193887125,2.41080015746233,18.9749221627009));
#102050=CARTESIAN_POINT('Ctrl Pts',(1.76450466441769,2.35597057281577,18.969888055066));
#102051=CARTESIAN_POINT('Ctrl Pts',(1.83739298489219,2.29768383792657,18.964853947431));
#102052=CARTESIAN_POINT('Ctrl Pts',(1.91029559359169,2.23938567714668,18.959818852965));
#102053=CARTESIAN_POINT('Ctrl Pts',(1.98040236262021,2.17762929792242,18.9547837584989));
#102054=CARTESIAN_POINT('Ctrl Pts',(2.04738025380189,2.11272291045042,18.9497486640329));
#102055=CARTESIAN_POINT('Ctrl Pts',(2.114431726449,2.04774521725319,18.9447080380456));
#102056=CARTESIAN_POINT('Ctrl Pts',(2.17834714035993,1.9796109177247,18.9396674120583));
#102057=CARTESIAN_POINT('Ctrl Pts',(2.23883079961385,1.9086646249932,18.934626786071));
#102058=CARTESIAN_POINT('Ctrl Pts',(2.29935162612304,1.83767473571008,18.9295830626151));
#102059=CARTESIAN_POINT('Ctrl Pts',(2.35643622814713,1.76386976430429,18.9245393391592));
#102060=CARTESIAN_POINT('Ctrl Pts',(2.4098309863379,1.68762514122233,18.9194956157033));
#102061=CARTESIAN_POINT('Ctrl Pts',(2.46331215664244,1.61125712664527,18.9144437296709));
#102062=CARTESIAN_POINT('Ctrl Pts',(2.51309132483308,1.53244195335265,18.9093918436384));
#102063=CARTESIAN_POINT('Ctrl Pts',(2.55895983008073,1.45158140937158,18.9043399576059));
#102064=CARTESIAN_POINT('Ctrl Pts',(2.58211176634023,1.41076738785398,18.9017900392516));
#102065=CARTESIAN_POINT('Ctrl Pts',(2.60426813968415,1.36943262154935,18.8992401208973));
#102066=CARTESIAN_POINT('Ctrl Pts',(2.62540680139961,1.32763064410424,18.896690202543));
#102067=CARTESIAN_POINT('Ctrl Pts',(2.6672905051767,1.24480507717982,18.8916378474581));
#102068=CARTESIAN_POINT('Ctrl Pts',(2.70532608200568,1.15984695171912,18.8865854923732));
#102069=CARTESIAN_POINT('Ctrl Pts',(2.73929102786788,1.07314894802284,18.8815331372883));
#102070=CARTESIAN_POINT('Ctrl Pts',(2.77320914124541,0.986570487662384,
18.8764877486311));
#102071=CARTESIAN_POINT('Ctrl Pts',(2.80306761633522,0.898257326286103,
18.871442359974));
#102072=CARTESIAN_POINT('Ctrl Pts',(2.82869015019114,0.808626016284171,
18.8663969713168));
#102073=CARTESIAN_POINT('Ctrl Pts',(2.85428527070502,0.719090602096955,
18.8613569806803));
#102074=CARTESIAN_POINT('Ctrl Pts',(2.87565333658132,0.628240267261544,
18.8563169900437));
#102075=CARTESIAN_POINT('Ctrl Pts',(2.89266681195559,0.536509752950196,
18.8512769994071));
#102076=CARTESIAN_POINT('Ctrl Pts',(2.90966802877374,0.4448453323459,18.8462406401866));
#102077=CARTESIAN_POINT('Ctrl Pts',(2.9223208106768,0.352302428338124,18.8412042809661));
#102078=CARTESIAN_POINT('Ctrl Pts',(2.93054823392241,0.259328071473634,
18.8361679217457));
#102079=CARTESIAN_POINT('Ctrl Pts',(2.93877266725247,0.166387502280889,
18.8311333927809));
#102080=CARTESIAN_POINT('Ctrl Pts',(2.94257489769723,0.0730162337843075,
18.8260988638162));
#102081=CARTESIAN_POINT('Ctrl Pts',(2.94192973916421,-0.0203324819239022,
18.8210643348515));
#102082=CARTESIAN_POINT('Ctrl Pts',(2.94128463462324,-0.113673385462975,
18.8160302272165));
#102083=CARTESIAN_POINT('Ctrl Pts',(2.93619288436819,-0.206991295738175,
18.8109961195815));
#102084=CARTESIAN_POINT('Ctrl Pts',(2.92668142602032,-0.299833004500295,
18.8059620119466));
#102085=CARTESIAN_POINT('Ctrl Pts',(2.9171681031507,-0.392692912930471,
18.8009269174805));
#102086=CARTESIAN_POINT('Ctrl Pts',(2.90323339717147,-0.485075992593114,
18.7958918230144));
#102087=CARTESIAN_POINT('Ctrl Pts',(2.88495597832126,-0.576535344231749,
18.7908567285483));
#102088=CARTESIAN_POINT('Ctrl Pts',(2.86665848002041,-0.668095172505063,
18.7858161025609));
#102089=CARTESIAN_POINT('Ctrl Pts',(2.84400883282038,-0.758728810793993,
18.7807754765736));
#102090=CARTESIAN_POINT('Ctrl Pts',(2.81713653443116,-0.848001029700555,
18.7757348505862));
#102091=CARTESIAN_POINT('Ctrl Pts',(2.79024772299382,-0.937328106454573,
18.7706911271303));
#102092=CARTESIAN_POINT('Ctrl Pts',(2.75913124262189,-1.0252916798351,18.7656474036744));
#102093=CARTESIAN_POINT('Ctrl Pts',(2.72396528790127,-1.11147519554372,
18.7606036802185));
#102094=CARTESIAN_POINT('Ctrl Pts',(2.6887424218923,-1.19779818748587,18.755551794186));
#102095=CARTESIAN_POINT('Ctrl Pts',(2.64945718524543,-1.28233496828952,
18.7504999081535));
#102096=CARTESIAN_POINT('Ctrl Pts',(2.60633428179739,-1.36469249705847,
18.7454480221209));
#102097=CARTESIAN_POINT('Ctrl Pts',(2.58456817657085,-1.40626211538306,
18.742898103767));
#102098=CARTESIAN_POINT('Ctrl Pts',(2.56182505668172,-1.44727696979346,
18.7403481854131));
#102099=CARTESIAN_POINT('Ctrl Pts',(2.53813792349735,-1.48768944383718,
18.7377982670592));
#102100=CARTESIAN_POINT('Ctrl Pts',(2.49120473145713,-1.56776187769192,
18.7327459119742));
#102101=CARTESIAN_POINT('Ctrl Pts',(2.44039445977421,-1.64575485479938,
18.7276935568893));
#102102=CARTESIAN_POINT('Ctrl Pts',(2.38591665779354,-1.72126863158059,
18.7226412018044));
#102103=CARTESIAN_POINT('Ctrl Pts',(2.33151397240029,-1.79667828637065,
18.7175958131472));
#102104=CARTESIAN_POINT('Ctrl Pts',(2.27345406320861,-1.86961517656822,
18.71255042449));
#102105=CARTESIAN_POINT('Ctrl Pts',(2.21199157264906,-1.93970546282922,
18.7075050358328));
#102106=CARTESIAN_POINT('Ctrl Pts',(2.1505948403116,-2.00972076005923,18.7024650451962));
#102107=CARTESIAN_POINT('Ctrl Pts',(2.08580305376895,-2.07689517465094,
18.6974250545596));
#102108=CARTESIAN_POINT('Ctrl Pts',(2.01791256126694,-2.14088600702632,
18.692385063923));
#102109=CARTESIAN_POINT('Ctrl Pts',(1.9500709852501,-2.20483073270121,18.6873487047025));
#102110=CARTESIAN_POINT('Ctrl Pts',(1.87913546338631,-2.26559613165534,
18.682312345482));
#102111=CARTESIAN_POINT('Ctrl Pts',(1.80544009027429,-2.32287539063772,
18.6772759862615));
#102112=CARTESIAN_POINT('Ctrl Pts',(1.73177149868744,-2.38013383385039,
18.6722414572967));
#102113=CARTESIAN_POINT('Ctrl Pts',(1.65534539872847,-2.43390838156707,
18.667206928332));
#102114=CARTESIAN_POINT('Ctrl Pts',(1.5765291405612,-2.48393233985175,18.6621723993672));
#102115=CARTESIAN_POINT('Ctrl Pts',(1.49771947837047,-2.53395211173043,
18.6571382917322));
#102116=CARTESIAN_POINT('Ctrl Pts',(1.41652043084509,-2.58022168034536,
18.6521041840973));
#102117=CARTESIAN_POINT('Ctrl Pts',(1.33332754630043,-2.62251818950346,
18.6470700764623));
#102118=CARTESIAN_POINT('Ctrl Pts',(1.25011835353707,-2.66482299000431,
18.6420349819961));
#102119=CARTESIAN_POINT('Ctrl Pts',(1.16491494366667,-2.70315298328898,
18.63699988753));
#102120=CARTESIAN_POINT('Ctrl Pts',(1.07813558496178,-2.73733221594295,
18.6319647930639));
#102121=CARTESIAN_POINT('Ctrl Pts',(0.991260891031381,-2.77154899767426,
18.6269241670765));
#102122=CARTESIAN_POINT('Ctrl Pts',(0.902807206311567,-2.80160575344233,
18.6218835410892));
#102123=CARTESIAN_POINT('Ctrl Pts',(0.813210522501238,-2.82737557570501,
18.6168429151018));
#102124=CARTESIAN_POINT('Ctrl Pts',(0.723558781459588,-2.85316123354336,
18.6117991916459));
#102125=CARTESIAN_POINT('Ctrl Pts',(0.632763075009238,-2.87465461119352,
18.6067554681899));
#102126=CARTESIAN_POINT('Ctrl Pts',(0.541270075704358,-2.8917798507402,
18.601711744734));
#102127=CARTESIAN_POINT('Ctrl Pts',(0.449629007492839,-2.908932805145,18.5966598587015));
#102128=CARTESIAN_POINT('Ctrl Pts',(0.357288833070872,-2.9217034478382,
18.5916079726689));
#102129=CARTESIAN_POINT('Ctrl Pts',(0.264701653862861,-2.93006775253445,
18.5865560866364));
#102130=CARTESIAN_POINT('Ctrl Pts',(0.217968662251847,-2.93428960035988,
18.5840061682827));
#102131=CARTESIAN_POINT('Ctrl Pts',(0.17117275126887,-2.93738968091731,
18.581456249929));
#102132=CARTESIAN_POINT('Ctrl Pts',(0.124371822788037,-2.93936994093911,
18.5789063315753));
#102133=CARTESIAN_POINT('Ctrl Pts',(0.031641438442038,-2.94329358687708,
18.5738539764904));
#102134=CARTESIAN_POINT('Ctrl Pts',(-0.061441185936314,-2.94283182361192,
18.5688016214055));
#102135=CARTESIAN_POINT('Ctrl Pts',(-0.154426523870621,-2.93794425555102,
18.5637492663206));
#102136=CARTESIAN_POINT('Ctrl Pts',(-0.247283649193262,-2.9330634267017,
18.5587038776634));
#102137=CARTESIAN_POINT('Ctrl Pts',(-0.340043314851987,-2.92376894264891,
18.5536584890063));
#102138=CARTESIAN_POINT('Ctrl Pts',(-0.432253342304631,-2.91007234412935,
18.5486131003491));
#102139=CARTESIAN_POINT('Ctrl Pts',(-0.524364714993929,-2.89639039948988,
18.5435731097126));
#102140=CARTESIAN_POINT('Ctrl Pts',(-0.615927181263999,-2.87831576672546,
18.538533119076));
#102141=CARTESIAN_POINT('Ctrl Pts',(-0.706492146231467,-2.85591191168657,
18.5334931284394));
#102142=CARTESIAN_POINT('Ctrl Pts',(-0.796991857293626,-2.83352419908241,
18.5284567692189));
#102143=CARTESIAN_POINT('Ctrl Pts',(-0.88649506560938,-2.80681357061309,
18.5234204099985));
#102144=CARTESIAN_POINT('Ctrl Pts',(-0.974562894613587,-2.77589466018478,
18.518384050778));
#102145=CARTESIAN_POINT('Ctrl Pts',(-1.06259871902001,-2.74498698595138,
18.5133495218133));
#102146=CARTESIAN_POINT('Ctrl Pts',(-1.149199781652,-2.70987421494151,18.5083149928485));
#102147=CARTESIAN_POINT('Ctrl Pts',(-1.23394291503919,-2.67072066724032,
18.5032804638838));
#102148=CARTESIAN_POINT('Ctrl Pts',(-1.31867895644151,-2.63157039622194,
18.4982463562488));
#102149=CARTESIAN_POINT('Ctrl Pts',(-1.4015569745436,-2.58838020735632,
18.4932122486139));
#102150=CARTESIAN_POINT('Ctrl Pts',(-1.48217537615585,-2.54136187000538,
18.4881781409789));
#102151=CARTESIAN_POINT('Ctrl Pts',(-1.56280958131321,-2.49433431569653,
18.4831430465128));
#102152=CARTESIAN_POINT('Ctrl Pts',(-1.64118290674502,-2.4434773466619,
18.4781079520467));
#102153=CARTESIAN_POINT('Ctrl Pts',(-1.71692087743556,-2.38904723700179,
18.4730728575807));
#102154=CARTESIAN_POINT('Ctrl Pts',(-1.79274205335657,-2.33455733078551,
18.4680322315933));
#102155=CARTESIAN_POINT('Ctrl Pts',(-1.8659217341141,-2.27648670798884,
18.462991605606));
#102156=CARTESIAN_POINT('Ctrl Pts',(-1.93611707088297,-2.21513310837872,
18.4579509796186));
#102157=CARTESIAN_POINT('Ctrl Pts',(-2.00635554274028,-2.15374180693444,
18.4529072561627));
#102158=CARTESIAN_POINT('Ctrl Pts',(-2.07360569975744,-2.08906382015598,
18.4478635327068));
#102159=CARTESIAN_POINT('Ctrl Pts',(-2.13756181851492,-2.02143351907185,
18.4428198092509));
#102160=CARTESIAN_POINT('Ctrl Pts',(-2.20162144150386,-1.95369376759464,
18.4377679232184));
#102161=CARTESIAN_POINT('Ctrl Pts',(-2.26237609450512,-1.88299249981471,
18.4327160371859));
#102162=CARTESIAN_POINT('Ctrl Pts',(-2.31956068179755,-1.80969672692937,
18.4276641511534));
#102163=CARTESIAN_POINT('Ctrl Pts',(-2.34842436315619,-1.77270099200033,
18.4251142327994));
#102164=CARTESIAN_POINT('Ctrl Pts',(-2.37637919570815,-1.7350447160066,
18.4225643144454));
#102165=CARTESIAN_POINT('Ctrl Pts',(-2.40339545084291,-1.69677762445984,
18.4200143960914));
#102166=CARTESIAN_POINT('Ctrl Pts',(-2.45748613940064,-1.62016103490882,
18.4149090682491));
#102167=CARTESIAN_POINT('Ctrl Pts',(-2.50800397783905,-1.54082190742877,
18.4098037404068));
#102168=CARTESIAN_POINT('Ctrl Pts',(-2.55466696623876,-1.45912326128003,
18.4046984125645));
#102169=CARTESIAN_POINT('Ctrl Pts',(-2.60126251559766,-1.37754268897355,
18.399600463127));
#102170=CARTESIAN_POINT('Ctrl Pts',(-2.64401407535284,-1.29360974706232,
18.3945025136894));
#102171=CARTESIAN_POINT('Ctrl Pts',(-2.68268178742546,-1.20771785919383,
18.3894045642518));
#102172=CARTESIAN_POINT('Ctrl Pts',(-2.72130365097083,-1.12192781382781,
18.384312659482));
#102173=CARTESIAN_POINT('Ctrl Pts',(-2.75585111713689,-1.03418383174471,
18.3792207547122));
#102174=CARTESIAN_POINT('Ctrl Pts',(-2.78612980181422,-0.944904612880396,
18.3741288499424));
#102175=CARTESIAN_POINT('Ctrl Pts',(-2.81637713708088,-0.855717830359562,
18.3690422171392));
#102176=CARTESIAN_POINT('Ctrl Pts',(-2.84236434750889,-0.764999381684115,
18.363955584336));
#102177=CARTESIAN_POINT('Ctrl Pts',(-2.86394525918279,-0.673187605652688,
18.3588689515328));
#102178=CARTESIAN_POINT('Ctrl Pts',(-2.8855131439674,-0.581431249978891,
18.3537853891745));
#102179=CARTESIAN_POINT('Ctrl Pts',(-2.90267992053475,-0.48858329900202,
18.3487018268163));
#102180=CARTESIAN_POINT('Ctrl Pts',(-2.91534955181019,-0.395096179126181,
18.3436182644581));
#102181=CARTESIAN_POINT('Ctrl Pts',(-2.92801563564908,-0.301635235199658,
18.3385361254732));
#102182=CARTESIAN_POINT('Ctrl Pts',(-2.93618701854107,-0.207535905832476,
18.3334539864883));
#102183=CARTESIAN_POINT('Ctrl Pts',(-2.93981911662979,-0.11325882525462,
18.3283718475034));
#102184=CARTESIAN_POINT('Ctrl Pts',(-2.94129510280155,-0.0749471762164033,
18.3263066040321));
#102185=CARTESIAN_POINT('Ctrl Pts',(-2.94202207254817,-0.0366062362852832,
18.3242413605609));
#102186=CARTESIAN_POINT('Ctrl Pts',(-2.94199948962717,0.00173292627207862,
18.3221761170896));
#102187=CARTESIAN_POINT('',(-2.94199959735173,0.00153921481298652,17.3221761170896));
#102188=CARTESIAN_POINT('Ctrl Pts',(-2.93820320684436,0.00175244785142763,
18.3221749435376));
#102189=CARTESIAN_POINT('Ctrl Pts',(-2.94022008061527,0.379058827004991,
18.3018241158943));
#102190=CARTESIAN_POINT('Ctrl Pts',(-2.69739443497224,1.73582009319941,
18.2285093097562));
#102191=CARTESIAN_POINT('Ctrl Pts',(-0.652918847946833,3.41637487504018,
18.1022305251237));
#102192=CARTESIAN_POINT('Ctrl Pts',(2.51804505593664,2.39945189680271,17.9433385896398));
#102193=CARTESIAN_POINT('Ctrl Pts',(3.38092917609235,-0.816846506422659,
17.7844466541558));
#102194=CARTESIAN_POINT('Ctrl Pts',(1.14480032856239,-3.28441052801307,
17.6255547186722));
#102195=CARTESIAN_POINT('Ctrl Pts',(-2.04137315956266,-2.75784263173558,
17.4714650030246));
#102196=CARTESIAN_POINT('Ctrl Pts',(-2.94019247693566,-0.885490005612207,
17.3703392658718));
#102197=CARTESIAN_POINT('Ctrl Pts',(-2.94584118639794,0.00151562255014574,
17.3221775072136));
#102198=CARTESIAN_POINT('',(-2.94199883051083,-0.00262321804808858,16.3221761170896));
#102199=CARTESIAN_POINT('Ctrl Pts',(-2.94199959735173,0.00153921481298652,
17.3221761170896));
#102200=CARTESIAN_POINT('Ctrl Pts',(-2.94195338985515,0.0898585547750324,
17.3173743606278));
#102201=CARTESIAN_POINT('Ctrl Pts',(-2.93793050094627,0.178071157293918,
17.3125726041661));
#102202=CARTESIAN_POINT('Ctrl Pts',(-2.92995744410738,0.265919867102419,
17.3077708477044));
#102203=CARTESIAN_POINT('Ctrl Pts',(-2.92156828181176,0.358353308746736,
17.3027184926196));
#102204=CARTESIAN_POINT('Ctrl Pts',(-2.90878568317249,0.450555224986806,
17.2976661375348));
#102205=CARTESIAN_POINT('Ctrl Pts',(-2.89162912925254,0.542074698596224,
17.29261378245));
#102206=CARTESIAN_POINT('Ctrl Pts',(-2.87449623160611,0.633467980797424,
17.2875683937929));
#102207=CARTESIAN_POINT('Ctrl Pts',(-2.85300144423318,0.724180257378679,
17.2825230051358));
#102208=CARTESIAN_POINT('Ctrl Pts',(-2.82721607839617,0.813764859193481,
17.2774776164788));
#102209=CARTESIAN_POINT('Ctrl Pts',(-2.80145830011376,0.903253615166505,
17.2724376258423));
#102210=CARTESIAN_POINT('Ctrl Pts',(-2.77141918981817,0.991616669841535,
17.2673976352058));
#102211=CARTESIAN_POINT('Ctrl Pts',(-2.7372210521935,1.07841778148763,17.2623576445692));
#102212=CARTESIAN_POINT('Ctrl Pts',(-2.70304755502481,1.16515635116161,
17.2573212853488));
#102213=CARTESIAN_POINT('Ctrl Pts',(-2.66472114919312,1.25033480259103,
17.2522849261284));
#102214=CARTESIAN_POINT('Ctrl Pts',(-2.62241357013272,1.3335333018653,17.2472485669079));
#102215=CARTESIAN_POINT('Ctrl Pts',(-2.58012136600628,1.41670156609753,
17.2422140379432));
#102216=CARTESIAN_POINT('Ctrl Pts',(-2.53385106402202,1.49789091201869,
17.2371795089785));
#102217=CARTESIAN_POINT('Ctrl Pts',(-2.4838215683074,1.57670365535537,17.2321449800138));
#102218=CARTESIAN_POINT('Ctrl Pts',(-2.43379625946213,1.65550980300973,
17.2271108723789));
#102219=CARTESIAN_POINT('Ctrl Pts',(-2.38001262062241,1.73193936857028,
17.2220767647439));
#102220=CARTESIAN_POINT('Ctrl Pts',(-2.32273373080331,1.80562233476121,
17.217042657109));
#102221=CARTESIAN_POINT('Ctrl Pts',(-2.2654436126604,1.87931974495073,17.2120075626429));
#102222=CARTESIAN_POINT('Ctrl Pts',(-2.2046571557093,1.95026913599676,17.2069724681769));
#102223=CARTESIAN_POINT('Ctrl Pts',(-2.14067796118339,2.0181332628208,17.2019373737108));
#102224=CARTESIAN_POINT('Ctrl Pts',(-2.07662847954028,2.0860719447228,17.1968967477235));
#102225=CARTESIAN_POINT('Ctrl Pts',(-2.00937956411379,2.15091827292692,
17.1918561217361));
#102226=CARTESIAN_POINT('Ctrl Pts',(-1.93927172914376,2.21237184047885,
17.1868154957488));
#102227=CARTESIAN_POINT('Ctrl Pts',(-1.86912081285496,2.27386317129553,
17.1817717722929));
#102228=CARTESIAN_POINT('Ctrl Pts',(-1.7961078269276,2.33195731453227,17.176728048837));
#102229=CARTESIAN_POINT('Ctrl Pts',(-1.72060467862743,2.38639551204016,
17.1716843253811));
#102230=CARTESIAN_POINT('Ctrl Pts',(-1.6449793388078,2.44092181032556,17.1666324393486));
#102231=CARTESIAN_POINT('Ctrl Pts',(-1.5668561630896,2.49178010898528,17.1615805533161));
#102232=CARTESIAN_POINT('Ctrl Pts',(-1.48663403208002,2.53875624167849,
17.1565286672836));
#102233=CARTESIAN_POINT('Ctrl Pts',(-1.44614224683807,2.562467248262,17.1539787489291));
#102234=CARTESIAN_POINT('Ctrl Pts',(-1.40511607543183,2.5851899471607,17.1514288305747));
#102235=CARTESIAN_POINT('Ctrl Pts',(-1.36360874186484,2.60690145558089,
17.1488789122202));
#102236=CARTESIAN_POINT('Ctrl Pts',(-1.28136697618504,2.64992018587747,
17.1438265571353));
#102237=CARTESIAN_POINT('Ctrl Pts',(-1.19693993558253,2.68912047926456,
17.1387742020504));
#102238=CARTESIAN_POINT('Ctrl Pts',(-1.11071720343281,2.7242744527669,17.1337218469654));
#102239=CARTESIAN_POINT('Ctrl Pts',(-1.02461335929191,2.75937995429663,
17.1286764583083));
#102240=CARTESIAN_POINT('Ctrl Pts',(-0.936719151501308,2.79045005638599,
17.1236310696511));
#102241=CARTESIAN_POINT('Ctrl Pts',(-0.847448668608993,2.81730274448325,
17.118585680994));
#102242=CARTESIAN_POINT('Ctrl Pts',(-0.75827369548509,2.84412670310647,
17.1135456903574));
#102243=CARTESIAN_POINT('Ctrl Pts',(-0.667725797136911,2.8667420891036,
17.1085056997208));
#102244=CARTESIAN_POINT('Ctrl Pts',(-0.57623791980171,2.88501540026784,
17.1034657090842));
#102245=CARTESIAN_POINT('Ctrl Pts',(-0.484815961348971,2.90327554513851,
17.0984293498637));
#102246=CARTESIAN_POINT('Ctrl Pts',(-0.392455804470684,2.9171997468574,
17.0933929906432));
#102247=CARTESIAN_POINT('Ctrl Pts',(-0.299603379615979,2.92670494155504,
17.0883566314227));
#102248=CARTESIAN_POINT('Ctrl Pts',(-0.206784698121945,2.9362066819841,
17.083322102458));
#102249=CARTESIAN_POINT('Ctrl Pts',(-0.113474545530137,2.94129256050306,
17.0782875734933));
#102250=CARTESIAN_POINT('Ctrl Pts',(-0.0201257847241223,2.94193116044364,
17.0732530445286));
#102251=CARTESIAN_POINT('Ctrl Pts',(0.0732151639092051,2.94256970694105,
17.0682189368936));
#102252=CARTESIAN_POINT('Ctrl Pts',(0.1665942701018,2.93876171199624,17.0631848292586));
#102253=CARTESIAN_POINT('Ctrl Pts',(0.259557998022685,2.93052787832883,
17.0581507216237));
#102254=CARTESIAN_POINT('Ctrl Pts',(0.352539949530698,2.92229243059119,
17.0531156271576));
#102255=CARTESIAN_POINT('Ctrl Pts',(0.44510591860608,2.9096294606468,17.0480805326915));
#102256=CARTESIAN_POINT('Ctrl Pts',(0.536807966405932,2.89261148569993,
17.0430454382254));
#102257=CARTESIAN_POINT('Ctrl Pts',(0.628610757464931,2.87557481491908,
17.0380048122381));
#102258=CARTESIAN_POINT('Ctrl Pts',(0.719547295281639,2.8541736701438,17.0329641862508));
#102259=CARTESIAN_POINT('Ctrl Pts',(0.809180610807341,2.82853155172317,
17.0279235602634));
#102260=CARTESIAN_POINT('Ctrl Pts',(0.898869006074743,2.80287367620094,
17.0228798368075));
#102261=CARTESIAN_POINT('Ctrl Pts',(0.98725216425927,2.77296978110414,17.0178361133516));
#102262=CARTESIAN_POINT('Ctrl Pts',(1.07391111998423,2.73899231586622,17.0127923898957));
#102263=CARTESIAN_POINT('Ctrl Pts',(1.16071032137726,2.7049598627477,17.0077405038632));
#102264=CARTESIAN_POINT('Ctrl Pts',(1.24577934477105,2.66684085979808,17.0026886178307));
#102265=CARTESIAN_POINT('Ctrl Pts',(1.32872209638949,2.62485458465156,16.9976367317981));
#102266=CARTESIAN_POINT('Ctrl Pts',(1.37058710349889,2.60366218780907,16.9950868134443));
#102267=CARTESIAN_POINT('Ctrl Pts',(1.41191083470068,2.58148523977796,16.9925368950905));
#102268=CARTESIAN_POINT('Ctrl Pts',(1.45264522422215,2.55835608400093,16.9899869767367));
#102269=CARTESIAN_POINT('Ctrl Pts',(1.533355494699,2.51252845676519,16.9849346216518));
#102270=CARTESIAN_POINT('Ctrl Pts',(1.61203982124248,2.46279552056619,16.9798822665668));
#102271=CARTESIAN_POINT('Ctrl Pts',(1.68829561642655,2.40936130780647,16.9748299114819));
#102272=CARTESIAN_POINT('Ctrl Pts',(1.76444626648908,2.35600077268372,16.9697845228247));
#102273=CARTESIAN_POINT('Ctrl Pts',(1.83817467858619,2.29894935502687,16.9647391341676));
#102274=CARTESIAN_POINT('Ctrl Pts',(1.90910354697363,2.23845653228574,16.9596937455104));
#102275=CARTESIAN_POINT('Ctrl Pts',(1.9799565291378,2.17802843032696,16.9546537548738));
#102276=CARTESIAN_POINT('Ctrl Pts',(2.04801558483876,2.11416652841203,16.9496137642372));
#102277=CARTESIAN_POINT('Ctrl Pts',(2.11293397163064,2.04716243408509,16.9445737736006));
#102278=CARTESIAN_POINT('Ctrl Pts',(2.17780558340019,1.98020661757531,16.9395374143801));
#102279=CARTESIAN_POINT('Ctrl Pts',(2.23954071589448,1.91011342683583,16.9345010551596));
#102280=CARTESIAN_POINT('Ctrl Pts',(2.29782799052727,1.83721270569017,16.9294646959391));
#102281=CARTESIAN_POINT('Ctrl Pts',(2.3560940830689,1.76433847728639,16.9244301669743));
#102282=CARTESIAN_POINT('Ctrl Pts',(2.41091452979415,1.68865909199619,16.9193956380096));
#102283=CARTESIAN_POINT('Ctrl Pts',(2.46201761031975,1.61053819776975,16.9143611090448));
#102284=CARTESIAN_POINT('Ctrl Pts',(2.51311641412983,1.5324238413261,16.9093270014098));
#102285=CARTESIAN_POINT('Ctrl Pts',(2.56049822724371,1.45186875405722,16.9042928937748));
#102286=CARTESIAN_POINT('Ctrl Pts',(2.6039347751051,1.36926538223909,16.8992587861398));
#102287=CARTESIAN_POINT('Ctrl Pts',(2.64737983778979,1.28664581776409,16.8942236916737));
#102288=CARTESIAN_POINT('Ctrl Pts',(2.68687789285477,1.2019775646535,16.8891885972076));
#102289=CARTESIAN_POINT('Ctrl Pts',(2.72224725165072,1.11567643198202,16.8841535027415));
#102290=CARTESIAN_POINT('Ctrl Pts',(2.75765546698875,1.02928048946079,16.8791128767541));
#102291=CARTESIAN_POINT('Ctrl Pts',(2.78892576343315,0.94124849829791,16.8740722507667));
#102292=CARTESIAN_POINT('Ctrl Pts',(2.81592524984324,0.8520146637795,16.8690316247793));
#102293=CARTESIAN_POINT('Ctrl Pts',(2.8429413274586,0.762725995000777,16.8639879013234));
#102294=CARTESIAN_POINT('Ctrl Pts',(2.86568126215085,0.672234443114071,
16.8589441778675));
#102295=CARTESIAN_POINT('Ctrl Pts',(2.88406306069973,0.580985595266636,
16.8539004544115));
#102296=CARTESIAN_POINT('Ctrl Pts',(2.90247460767559,0.489589073638481,
16.848848568379));
#102297=CARTESIAN_POINT('Ctrl Pts',(2.91651387117682,0.397433247954863,
16.8437966823464));
#102298=CARTESIAN_POINT('Ctrl Pts',(2.92615061005617,0.304969846489582,
16.8387447963138));
#102299=CARTESIAN_POINT('Ctrl Pts',(2.93101471371576,0.258299331175658,
16.8361948779601));
#102300=CARTESIAN_POINT('Ctrl Pts',(2.93475802142384,0.211550476305253,
16.8336449596063));
#102301=CARTESIAN_POINT('Ctrl Pts',(2.93738168348325,0.164781205048134,
16.8310950412526));
#102302=CARTESIAN_POINT('Ctrl Pts',(2.94258015280972,0.0721135456674554,
16.8260426861677));
#102303=CARTESIAN_POINT('Ctrl Pts',(2.94339847148584,-0.020966626985196,
16.8209903310827));
#102304=CARTESIAN_POINT('Ctrl Pts',(2.93979006601469,-0.114010384445283,
16.8159379759978));
#102305=CARTESIAN_POINT('Ctrl Pts',(2.93618663598482,-0.206925848742052,
16.8108925873407));
#102306=CARTESIAN_POINT('Ctrl Pts',(2.92816862786905,-0.299804557566006,
16.8058471986835));
#102307=CARTESIAN_POINT('Ctrl Pts',(2.91574136311853,-0.392194216428167,
16.8008018100264));
#102308=CARTESIAN_POINT('Ctrl Pts',(2.90332739419818,-0.484485028340664,
16.7957618193898));
#102309=CARTESIAN_POINT('Ctrl Pts',(2.88651360415682,-0.576287392381419,
16.7907218287532));
#102310=CARTESIAN_POINT('Ctrl Pts',(2.86535728393064,-0.667151883326165,
16.7856818381167));
#102311=CARTESIAN_POINT('Ctrl Pts',(2.84421620726486,-0.757950904551132,
16.7806454788962));
#102312=CARTESIAN_POINT('Ctrl Pts',(2.818738919959,-0.847812964418424,16.7756091196757));
#102313=CARTESIAN_POINT('Ctrl Pts',(2.78903400980932,-0.936297651458644,
16.7705727604552));
#102314=CARTESIAN_POINT('Ctrl Pts',(2.75933989467654,-1.02475018241126,
16.7655382314905));
#102315=CARTESIAN_POINT('Ctrl Pts',(2.72542135007341,-1.11182591421406,
16.7605037025258));
#102316=CARTESIAN_POINT('Ctrl Pts',(2.68743686130267,-1.19709945974078,
16.7554691735611));
#102317=CARTESIAN_POINT('Ctrl Pts',(2.6494555513785,-1.2823658688935,16.7504350659261));
#102318=CARTESIAN_POINT('Ctrl Pts',(2.60740915475619,-1.3658299859131,16.7454009582911));
#102319=CARTESIAN_POINT('Ctrl Pts',(2.56150389821012,-1.44708734340894,
16.7403668506562));
#102320=CARTESIAN_POINT('Ctrl Pts',(2.51558964290223,-1.52836062970383,
16.7353317561901));
#102321=CARTESIAN_POINT('Ctrl Pts',(2.4658152441783,-1.60742591077158,16.730296661724));
#102322=CARTESIAN_POINT('Ctrl Pts',(2.41243180226208,-1.68390522281823,
16.7252615672579));
#102323=CARTESIAN_POINT('Ctrl Pts',(2.35898971365203,-1.76046855452786,
16.7202209412706));
#102324=CARTESIAN_POINT('Ctrl Pts',(2.3019309221703,-1.8344398815566,16.7151803152832));
#102325=CARTESIAN_POINT('Ctrl Pts',(2.2415484246982,-1.90547229308983,16.7101396892959));
#102326=CARTESIAN_POINT('Ctrl Pts',(2.18112882213468,-1.97654835409491,
16.70509596584));
#102327=CARTESIAN_POINT('Ctrl Pts',(2.117381750805,-2.04468158012666,16.7000522423841));
#102328=CARTESIAN_POINT('Ctrl Pts',(2.05063734592326,-2.10956167852585,
16.6950085189282));
#102329=CARTESIAN_POINT('Ctrl Pts',(1.98378492435044,-2.17454677649105,
16.6899566328956));
#102330=CARTESIAN_POINT('Ctrl Pts',(1.9139258177695,-2.2362679426719,16.6849047468631));
#102331=CARTESIAN_POINT('Ctrl Pts',(1.84142335717426,-2.2944550594102,16.6798528608306));
#102332=CARTESIAN_POINT('Ctrl Pts',(1.80482804330819,-2.32382476331429,
16.6773029424767));
#102333=CARTESIAN_POINT('Ctrl Pts',(1.76755975267996,-2.35229478787051,
16.6747530241228));
#102334=CARTESIAN_POINT('Ctrl Pts',(1.72966779728228,-2.37983472347234,
16.6722031057688));
#102335=CARTESIAN_POINT('Ctrl Pts',(1.65458946654393,-2.43440177792827,
16.6671507506839));
#102336=CARTESIAN_POINT('Ctrl Pts',(1.57679169355735,-2.48551043379844,
16.662098395599));
#102337=CARTESIAN_POINT('Ctrl Pts',(1.49662660875606,-2.53287836146218,
16.6570460405141));
#102338=CARTESIAN_POINT('Ctrl Pts',(1.41657205939096,-2.58018097597171,
16.6520006518569));
#102339=CARTESIAN_POINT('Ctrl Pts',(1.33415706366861,-2.6237528876472,16.6469552631998));
#102340=CARTESIAN_POINT('Ctrl Pts',(1.24976469250958,-2.66335356521744,
16.6419098745426));
#102341=CARTESIAN_POINT('Ctrl Pts',(1.16546261206667,-2.70291187434267,
16.6368698839061));
#102342=CARTESIAN_POINT('Ctrl Pts',(1.07918776122747,-2.73850720678566,
16.6318298932695));
#102343=CARTESIAN_POINT('Ctrl Pts',(0.991348950535218,-2.76994426988572,
16.6267899026329));
#102344=CARTESIAN_POINT('Ctrl Pts',(0.903573429498407,-2.80135868194034,
16.6217535434124));
#102345=CARTESIAN_POINT('Ctrl Pts',(0.81423660546987,-2.82862063059728,
16.6167171841919));
#102346=CARTESIAN_POINT('Ctrl Pts',(0.72376749934292,-2.85158282483516,
16.6116808249714));
#102347=CARTESIAN_POINT('Ctrl Pts',(0.633331270458338,-2.87453667441643,
16.6066462960067));
#102348=CARTESIAN_POINT('Ctrl Pts',(0.541764007080707,-2.89319376461131,
16.601611767042));
#102349=CARTESIAN_POINT('Ctrl Pts',(0.44950913007251,-2.90745688566167,
16.5965772380772));
#102350=CARTESIAN_POINT('Ctrl Pts',(0.357261973692089,-2.92171881305971,
16.5915431304423));
#102351=CARTESIAN_POINT('Ctrl Pts',(0.264327757146549,-2.93158743474038,
16.5865090228073));
#102352=CARTESIAN_POINT('Ctrl Pts',(0.171158177829341,-2.93701700338322,
16.5814749151723));
#102353=CARTESIAN_POINT('Ctrl Pts',(0.0779703345721042,-2.942447636379,
16.5764398207062));
#102354=CARTESIAN_POINT('Ctrl Pts',(-0.0154525196048733,-2.9434374626752,
16.5714047262401));
#102355=CARTESIAN_POINT('Ctrl Pts',(-0.108656658027342,-2.93999281132902,
16.566369631774));
#102356=CARTESIAN_POINT('Ctrl Pts',(-0.201963189895715,-2.93654437571181,
16.5613290057867));
#102357=CARTESIAN_POINT('Ctrl Pts',(-0.295050081760897,-2.92865175443276,
16.5562883797993));
#102358=CARTESIAN_POINT('Ctrl Pts',(-0.387467014278742,-2.91637331506889,
16.551247753812));
#102359=CARTESIAN_POINT('Ctrl Pts',(-0.479940737073067,-2.90408733059454,
16.5462040303561));
#102360=CARTESIAN_POINT('Ctrl Pts',(-0.571743244163261,-2.88741024198242,
16.5411603069001));
#102361=CARTESIAN_POINT('Ctrl Pts',(-0.662434879041171,-2.86645147020313,
16.5361165834442));
#102362=CARTESIAN_POINT('Ctrl Pts',(-0.753273285926816,-2.84545877951812,
16.5310646974117));
#102363=CARTESIAN_POINT('Ctrl Pts',(-0.84299680448902,-2.82017069252342,
16.5260128113792));
#102364=CARTESIAN_POINT('Ctrl Pts',(-0.931181566508105,-2.7907462962791,
16.5209609253466));
#102365=CARTESIAN_POINT('Ctrl Pts',(-0.975692456452476,-2.77589445529293,
16.5184110069927));
#102366=CARTESIAN_POINT('Ctrl Pts',(-1.01981164286292,-2.75998957632416,
16.5158610886389));
#102367=CARTESIAN_POINT('Ctrl Pts',(-1.06348685220657,-2.7430566372541,
16.513311170285));
#102368=CARTESIAN_POINT('Ctrl Pts',(-1.15002400178893,-2.70950606467081,
16.5082588152));
#102369=CARTESIAN_POINT('Ctrl Pts',(-1.23512720159307,-2.67179620429352,
16.5032064601151));
#102370=CARTESIAN_POINT('Ctrl Pts',(-1.31836838556014,-2.63007011312542,
16.4981541050302));
#102371=CARTESIAN_POINT('Ctrl Pts',(-1.40149479261909,-2.58840155587867,
16.493108716373));
#102372=CARTESIAN_POINT('Ctrl Pts',(-1.48276389197391,-2.54272796945177,
16.4880633277158));
#102373=CARTESIAN_POINT('Ctrl Pts',(-1.56176599207779,-2.49324106054535,
16.4830179390587));
#102374=CARTESIAN_POINT('Ctrl Pts',(-1.64068356847286,-2.44380709728306,
16.4779779484221));
#102375=CARTESIAN_POINT('Ctrl Pts',(-1.71733859210254,-2.39056815541317,
16.4729379577855));
#102376=CARTESIAN_POINT('Ctrl Pts',(-1.7913454550035,-2.33376208316922,
16.4678979671489));
#102377=CARTESIAN_POINT('Ctrl Pts',(-1.86529899444966,-2.27699694085942,
16.4628616079283));
#102378=CARTESIAN_POINT('Ctrl Pts',(-1.93660781431016,-2.21667004650681,
16.4578252487078));
#102379=CARTESIAN_POINT('Ctrl Pts',(-2.00491570790697,-2.15306223880963,
16.4527888894873));
#102380=CARTESIAN_POINT('Ctrl Pts',(-2.07319877783451,-2.08947754673053,
16.4477543605226));
#102381=CARTESIAN_POINT('Ctrl Pts',(-2.13848276323585,-2.02261461240077,
16.4427198315578));
#102382=CARTESIAN_POINT('Ctrl Pts',(-2.20044575423982,-1.95279350742672,
16.4376853025931));
#102383=CARTESIAN_POINT('Ctrl Pts',(-2.26240355968384,-1.88297824564261,
16.4326511949581));
#102384=CARTESIAN_POINT('Ctrl Pts',(-2.3210406285842,-1.81020563781778,
16.4276170873231));
#102385=CARTESIAN_POINT('Ctrl Pts',(-2.37607382587819,-1.73483058941689,
16.4225829796881));
#102386=CARTESIAN_POINT('Ctrl Pts',(-2.43111781127525,-1.65944076532005,
16.417547885222));
#102387=CARTESIAN_POINT('Ctrl Pts',(-2.48255626038281,-1.58144784646101,
16.4125127907559));
#102388=CARTESIAN_POINT('Ctrl Pts',(-2.53014871309665,-1.50123665343455,
16.4074776962898));
#102389=CARTESIAN_POINT('Ctrl Pts',(-2.5777934505621,-1.4209373409256,16.4024370703024));
#102390=CARTESIAN_POINT('Ctrl Pts',(-2.621583530638,-1.33841527239376,16.397396444315));
#102391=CARTESIAN_POINT('Ctrl Pts',(-2.66132408132544,-1.25408059316669,
16.3923558183277));
#102392=CARTESIAN_POINT('Ctrl Pts',(-2.701089052612,-1.16969409021402,16.3873120948717));
#102393=CARTESIAN_POINT('Ctrl Pts',(-2.73679937061715,-1.08349316921749,
16.3822683714158));
#102394=CARTESIAN_POINT('Ctrl Pts',(-2.76830885362323,-0.995906667791344,
16.3772246479598));
#102395=CARTESIAN_POINT('Ctrl Pts',(-2.79986933041819,-0.908178419591311,
16.3721727619273));
#102396=CARTESIAN_POINT('Ctrl Pts',(-2.8272152697665,-0.819060538510984,
16.3671208758947));
#102397=CARTESIAN_POINT('Ctrl Pts',(-2.8502507905131,-0.72899549462217,
16.3620689898622));
#102398=CARTESIAN_POINT('Ctrl Pts',(-2.86187787330175,-0.68353554026831,
16.3595190715085));
#102399=CARTESIAN_POINT('Ctrl Pts',(-2.87240761389315,-0.637834420508285,
16.3569691531547));
#102400=CARTESIAN_POINT('Ctrl Pts',(-2.88183269195836,-0.591949605591588,
16.354419234801));
#102401=CARTESIAN_POINT('Ctrl Pts',(-2.90840445752944,-0.462588284995289,
16.3472303465763));
#102402=CARTESIAN_POINT('Ctrl Pts',(-2.92627321214746,-0.331383124856715,
16.3400414583515));
#102403=CARTESIAN_POINT('Ctrl Pts',(-2.9352414658756,-0.199302626687303,
16.3328525701267));
#102404=CARTESIAN_POINT('Ctrl Pts',(-2.93968114819087,-0.133916937378105,
16.3292937524477));
#102405=CARTESIAN_POINT('Ctrl Pts',(-2.94194025492879,-0.0683170683806231,
16.3257349347686));
#102406=CARTESIAN_POINT('Ctrl Pts',(-2.94199883051083,-0.00262321804808858,
16.3221761170896));
#102407=CARTESIAN_POINT('',(-2.93715977492128,-5.64784450823863E-5,15.3221761170896));
#102408=CARTESIAN_POINT('Ctrl Pts',(-2.94289363775603,-0.00261552165817143,
16.3221756570734));
#102409=CARTESIAN_POINT('Ctrl Pts',(-2.93569250517499,0.776915332964193,
16.2799595378213));
#102410=CARTESIAN_POINT('Ctrl Pts',(-2.21711677136678,2.54616453756175,
16.1847794400746));
#102411=CARTESIAN_POINT('Ctrl Pts',(0.770275962800985,3.39184245653139,
16.0366353638335));
#102412=CARTESIAN_POINT('Ctrl Pts',(3.26835708375775,1.18985809316026,15.8777434283494));
#102413=CARTESIAN_POINT('Ctrl Pts',(2.77061059104582,-2.1027689510703,15.7188514928656));
#102414=CARTESIAN_POINT('Ctrl Pts',(-0.266721235415331,-3.46796483421923,
15.5599595573817));
#102415=CARTESIAN_POINT('Ctrl Pts',(-2.59084841052653,-1.95874493369377,
15.4277344321231));
#102416=CARTESIAN_POINT('Ctrl Pts',(-2.93724320497234,-0.488041625186228,
15.348473285359));
#102417=CARTESIAN_POINT('Ctrl Pts',(-2.93715977492128,-5.64784450823863E-5,
15.3221761170896));
#102418=CARTESIAN_POINT('',(-2.94199880731857,0.0026491010035377,14.3221761170896));
#102419=CARTESIAN_POINT('Ctrl Pts',(-2.93715977492128,-5.64784450823863E-5,
15.3221761170896));
#102420=CARTESIAN_POINT('Ctrl Pts',(-2.937075172149,0.494787953759478,15.2955093068644));
#102421=CARTESIAN_POINT('Ctrl Pts',(-2.58366435956491,1.97257547511542,
15.2158785181446));
#102422=CARTESIAN_POINT('Ctrl Pts',(-0.242551610946432,3.46973904275675,
15.08328375093));
#102423=CARTESIAN_POINT('Ctrl Pts',(2.78519444500115,2.08341359608163,14.9243918154463));
#102424=CARTESIAN_POINT('Ctrl Pts',(3.25998737681471,-1.212601588244,14.7654998799623));
#102425=CARTESIAN_POINT('Ctrl Pts',(0.746624500255915,-3.39712704566971,
14.6066079444785));
#102426=CARTESIAN_POINT('Ctrl Pts',(-2.22736502755342,-2.53281667794069,
14.4588334749138));
#102427=CARTESIAN_POINT('Ctrl Pts',(-2.93553126956538,-0.770202959613324,
14.3640229838439));
#102428=CARTESIAN_POINT('Ctrl Pts',(-2.94268592639251,0.00264317858251727,
14.3221764712686));
#102429=CARTESIAN_POINT('',(-2.94204920351317,-0.00143517523068308,13.3221761001659));
#102430=CARTESIAN_POINT('Ctrl Pts',(-2.94199880731857,0.0026491010035377,
14.3221761170896));
#102431=CARTESIAN_POINT('Ctrl Pts',(-2.94188124569359,0.13320892489109,
14.3151051111609));
#102432=CARTESIAN_POINT('Ctrl Pts',(-2.93306924346563,0.263391909828143,
14.3080341052323));
#102433=CARTESIAN_POINT('Ctrl Pts',(-2.91573305821569,0.392255953719244,
14.3009630993036));
#102434=CARTESIAN_POINT('Ctrl Pts',(-2.90581252724635,0.465997651781654,
14.2969167573727));
#102435=CARTESIAN_POINT('Ctrl Pts',(-2.89310147223706,0.539308078417644,
14.2928704154417));
#102436=CARTESIAN_POINT('Ctrl Pts',(-2.87763831285705,0.612014493600619,
14.2888240735108));
#102437=CARTESIAN_POINT('Ctrl Pts',(-2.85833065837412,0.702797386575274,
14.2837717184259));
#102438=CARTESIAN_POINT('Ctrl Pts',(-2.83468815976649,0.792828605861353,
14.278719363341));
#102439=CARTESIAN_POINT('Ctrl Pts',(-2.80678371344977,0.881662739324452,
14.273667008256));
#102440=CARTESIAN_POINT('Ctrl Pts',(-2.77891774311241,0.970374384054174,
14.2686216195989));
#102441=CARTESIAN_POINT('Ctrl Pts',(-2.746801634558,1.05789180276783,14.2635762309417));
#102442=CARTESIAN_POINT('Ctrl Pts',(-2.71055924304341,1.14377995696373,
14.2585308422846));
#102443=CARTESIAN_POINT('Ctrl Pts',(-2.67435562697068,1.22957622011739,
14.253490851648));
#102444=CARTESIAN_POINT('Ctrl Pts',(-2.63403467456658,1.31374627641001,
14.2484508610114));
#102445=CARTESIAN_POINT('Ctrl Pts',(-2.58976963518443,1.39587149719331,
14.2434108703748));
#102446=CARTESIAN_POINT('Ctrl Pts',(-2.54553648966638,1.47793754507929,
14.2383745111543));
#102447=CARTESIAN_POINT('Ctrl Pts',(-2.49736511581005,1.55796129600922,
14.2333381519338));
#102448=CARTESIAN_POINT('Ctrl Pts',(-2.44547589519023,1.63554628367513,
14.2283017927133));
#102449=CARTESIAN_POINT('Ctrl Pts',(-2.3936055315544,1.71310307629683,14.2232672637486));
#102450=CARTESIAN_POINT('Ctrl Pts',(-2.33802025197507,1.78822249742819,
14.2182327347838));
#102451=CARTESIAN_POINT('Ctrl Pts',(-2.27898464227407,1.8605356756265,14.2131982058191));
#102452=CARTESIAN_POINT('Ctrl Pts',(-2.21995397314617,1.93284280207831,
14.2081640981841));
#102453=CARTESIAN_POINT('Ctrl Pts',(-2.15747382908572,2.0023438085244,14.2031299905491));
#102454=CARTESIAN_POINT('Ctrl Pts',(-2.0918493722751,2.06870254113835,14.1980958829141));
#102455=CARTESIAN_POINT('Ctrl Pts',(-2.02621205116752,2.13507428198861,
14.193060788448));
#102456=CARTESIAN_POINT('Ctrl Pts',(-1.95742950579981,2.19830221008539,
14.1880256939819));
#102457=CARTESIAN_POINT('Ctrl Pts',(-1.88584324157823,2.25808752447591,
14.1829905995158));
#102458=CARTESIAN_POINT('Ctrl Pts',(-1.81417833316336,2.31793851861479,
14.1779499735285));
#102459=CARTESIAN_POINT('Ctrl Pts',(-1.73970389906165,2.37433906447225,
14.1729093475411));
#102460=CARTESIAN_POINT('Ctrl Pts',(-1.66279372134582,2.4270313224705,14.1678687215537));
#102461=CARTESIAN_POINT('Ctrl Pts',(-1.58583628226625,2.47975595990209,
14.1628249980978));
#102462=CARTESIAN_POINT('Ctrl Pts',(-1.50644049753725,2.52876753975748,
14.1577812746419));
#102463=CARTESIAN_POINT('Ctrl Pts',(-1.42500637364472,2.57385330488587,
14.1527375511859));
#102464=CARTESIAN_POINT('Ctrl Pts',(-1.34344045975996,2.619012035159,14.1476856651534));
#102465=CARTESIAN_POINT('Ctrl Pts',(-1.25983001907856,2.66023207077413,
14.1426337791208));
#102466=CARTESIAN_POINT('Ctrl Pts',(-1.17459654456991,2.69734813427641,
14.1375818930883));
#102467=CARTESIAN_POINT('Ctrl Pts',(-1.13157530465883,2.71608231215302,
14.1350319747345));
#102468=CARTESIAN_POINT('Ctrl Pts',(-1.08814083723376,2.73377171078363,
14.1324820563807));
#102469=CARTESIAN_POINT('Ctrl Pts',(-1.04434870727625,2.75039993048473,
14.1299321380268));
#102470=CARTESIAN_POINT('Ctrl Pts',(-0.957579893624153,2.78334673846167,
14.1248797829419));
#102471=CARTESIAN_POINT('Ctrl Pts',(-0.869094768662942,2.81224260057255,
14.119827427857));
#102472=CARTESIAN_POINT('Ctrl Pts',(-0.779307222990149,2.83690751562249,
14.1147750727721));
#102473=CARTESIAN_POINT('Ctrl Pts',(-0.689643480660821,2.86153842151307,
14.1097296841149));
#102474=CARTESIAN_POINT('Ctrl Pts',(-0.598681310840846,2.88194985626464,
14.1046842954578));
#102475=CARTESIAN_POINT('Ctrl Pts',(-0.5068534882937,2.89801027282591,14.0996389068006));
#102476=CARTESIAN_POINT('Ctrl Pts',(-0.415123911592111,2.91405350647724,
14.094598916164));
#102477=CARTESIAN_POINT('Ctrl Pts',(-0.322530958285855,2.92575489857701,
14.0895589255274));
#102478=CARTESIAN_POINT('Ctrl Pts',(-0.229520365786315,2.9330333107023,
14.0845189348909));
#102479=CARTESIAN_POINT('Ctrl Pts',(-0.13657678931646,2.94030647858315,
14.0794825756704));
#102480=CARTESIAN_POINT('Ctrl Pts',(-0.0432166133828939,2.94316296624148,
14.0744462164499));
#102481=CARTESIAN_POINT('Ctrl Pts',(0.0501075226029547,2.94157325867954,
14.0694098572294));
#102482=CARTESIAN_POINT('Ctrl Pts',(0.143397743804282,2.93998412883085,
14.0643753282647));
#102483=CARTESIAN_POINT('Ctrl Pts',(0.236651507348711,2.93395202125452,
14.0593407992999));
#102484=CARTESIAN_POINT('Ctrl Pts',(0.329415424340849,2.92349952594597,
14.0543062703352));
#102485=CARTESIAN_POINT('Ctrl Pts',(0.422171578104676,2.91304790538604,
14.0492721627002));
#102486=CARTESIAN_POINT('Ctrl Pts',(0.514437525396893,2.89817668253496,
14.0442380550652));
#102487=CARTESIAN_POINT('Ctrl Pts',(0.605765399102198,2.87896027781742,
14.0392039474303));
#102488=CARTESIAN_POINT('Ctrl Pts',(0.697111175719796,2.85974010612717,
14.0341688529642));
#102489=CARTESIAN_POINT('Ctrl Pts',(0.787518078926407,2.83617315275461,
14.0291337584981));
#102490=CARTESIAN_POINT('Ctrl Pts',(0.87654995273421,2.80838462115887,14.024098664032));
#102491=CARTESIAN_POINT('Ctrl Pts',(0.965679636365806,2.78056556126733,
14.0190580380446));
#102492=CARTESIAN_POINT('Ctrl Pts',(1.05343085055078,2.74851579813489,14.0140174120573));
#102493=CARTESIAN_POINT('Ctrl Pts',(1.13938438647404,2.71240985469733,14.0089767860699));
#102494=CARTESIAN_POINT('Ctrl Pts',(1.2253907409116,2.6762817241296,14.003933062614));
#102495=CARTESIAN_POINT('Ctrl Pts',(1.30959681727519,2.63609264232766,13.9988893391581));
#102496=CARTESIAN_POINT('Ctrl Pts',(1.39160709644178,2.59206359666056,13.9938456157022));
#102497=CARTESIAN_POINT('Ctrl Pts',(1.47375009802917,2.54796329600462,13.9887937296696));
#102498=CARTESIAN_POINT('Ctrl Pts',(1.55368982763823,2.50001085334448,13.9837418436371));
#102499=CARTESIAN_POINT('Ctrl Pts',(1.6310590374262,2.44847103646956,13.9786899576046));
#102500=CARTESIAN_POINT('Ctrl Pts',(1.67011082259928,2.42245652938108,13.9761400392507));
#102501=CARTESIAN_POINT('Ctrl Pts',(1.7085082324844,2.39552872407528,13.9735901208969));
#102502=CARTESIAN_POINT('Ctrl Pts',(1.7462073827726,2.36772544361682,13.971040202543));
#102503=CARTESIAN_POINT('Ctrl Pts',(1.82090369348704,2.31263660314882,13.9659878474581));
#102504=CARTESIAN_POINT('Ctrl Pts',(1.89312458469929,2.25391070546273,13.9609354923732));
#102505=CARTESIAN_POINT('Ctrl Pts',(1.96249455027468,2.19179815223532,13.9558831372882));
#102506=CARTESIAN_POINT('Ctrl Pts',(2.03176886523832,2.12977124275394,13.9508377486311));
#102507=CARTESIAN_POINT('Ctrl Pts',(2.09819973786452,2.06436725075727,13.9457923599739));
#102508=CARTESIAN_POINT('Ctrl Pts',(2.16144216205209,1.99587869874489,13.9407469713168));
#102509=CARTESIAN_POINT('Ctrl Pts',(2.22461692368092,1.92746342208102,13.9357069806802));
#102510=CARTESIAN_POINT('Ctrl Pts',(2.2846097175847,1.8559704695705,13.9306669900436));
#102511=CARTESIAN_POINT('Ctrl Pts',(2.34111088823028,1.78173056577295,13.9256269994071));
#102512=CARTESIAN_POINT('Ctrl Pts',(2.39757134862952,1.70754415334095,13.9205906401866));
#102513=CARTESIAN_POINT('Ctrl Pts',(2.45054491798368,1.63061507612066,13.9155542809661));
#102514=CARTESIAN_POINT('Ctrl Pts',(2.49976159546301,1.55130782433668,13.9105179217456));
#102515=CARTESIAN_POINT('Ctrl Pts',(2.54896038718329,1.4720293934823,13.9054833927809));
#102516=CARTESIAN_POINT('Ctrl Pts',(2.59440476530919,1.39037488207133,13.9004488638161));
#102517=CARTESIAN_POINT('Ctrl Pts',(2.63586812127884,1.30673763519153,13.8954143348514));
#102518=CARTESIAN_POINT('Ctrl Pts',(2.67732800726243,1.22310738774712,13.8903802272164));
#102519=CARTESIAN_POINT('Ctrl Pts',(2.71480733634799,1.137495132841,13.8853461195814));
#102520=CARTESIAN_POINT('Ctrl Pts',(2.74812605854376,1.05031765021481,13.8803120119465));
#102521=CARTESIAN_POINT('Ctrl Pts',(2.78145131217553,0.963123078273342,
13.8752769174804));
#102522=CARTESIAN_POINT('Ctrl Pts',(2.81061418089074,0.874363084317866,
13.8702418230143));
#102523=CARTESIAN_POINT('Ctrl Pts',(2.83548364557246,0.784472112755514,
13.8652067285482));
#102524=CARTESIAN_POINT('Ctrl Pts',(2.8603804316825,0.694482387570324,13.8601661025608));
#102525=CARTESIAN_POINT('Ctrl Pts',(2.88097428003247,0.603359633453046,
13.8551254765735));
#102526=CARTESIAN_POINT('Ctrl Pts',(2.89718480847178,0.51155076537951,13.8500848505861));
#102527=CARTESIAN_POINT('Ctrl Pts',(2.91340529829334,0.41968548068555,13.8450411271302));
#102528=CARTESIAN_POINT('Ctrl Pts',(2.92523704957329,0.327133683002962,
13.8399974036743));
#102529=CARTESIAN_POINT('Ctrl Pts',(2.93265156961317,0.234347543715293,
13.8349536802183));
#102530=CARTESIAN_POINT('Ctrl Pts',(2.94007808903971,0.14141124275094,13.8299017941858));
#102531=CARTESIAN_POINT('Ctrl Pts',(2.94307309153277,0.0482402865086057,
13.8248499081533));
#102532=CARTESIAN_POINT('Ctrl Pts',(2.9416601995369,-0.0447132023066298,
13.8197980221207));
#102533=CARTESIAN_POINT('Ctrl Pts',(2.94094704820904,-0.0916310871635579,
13.8172481037669));
#102534=CARTESIAN_POINT('Ctrl Pts',(2.93911172949345,-0.138493645669141,
13.814698185413));
#102535=CARTESIAN_POINT('Ctrl Pts',(2.93616226480297,-0.185243501227722,
13.8121482670592));
#102536=CARTESIAN_POINT('Ctrl Pts',(2.93031825693337,-0.277872690744211,
13.8070959119743));
#102537=CARTESIAN_POINT('Ctrl Pts',(2.92007610727964,-0.370391264863159,
13.8020435568893));
#102538=CARTESIAN_POINT('Ctrl Pts',(2.90544288901117,-0.46234794115951,
13.7969912018044));
#102539=CARTESIAN_POINT('Ctrl Pts',(2.89082984772084,-0.55417782321183,
13.7919458131473));
#102540=CARTESIAN_POINT('Ctrl Pts',(2.87183783832533,-0.645446912097945,
13.7869004244901));
#102541=CARTESIAN_POINT('Ctrl Pts',(2.84852586141555,-0.735706746500822,
13.7818550358329));
#102542=CARTESIAN_POINT('Ctrl Pts',(2.82523882580154,-0.825870012636004,
13.7768150451964));
#102543=CARTESIAN_POINT('Ctrl Pts',(2.79764111989872,-0.915025742726424,
13.7717750545598));
#102544=CARTESIAN_POINT('Ctrl Pts',(2.76584300519413,-1.00273449657359,
13.7667350639232));
#102545=CARTESIAN_POINT('Ctrl Pts',(2.73406780168002,-1.09038005447396,
13.7616987047027));
#102546=CARTESIAN_POINT('Ctrl Pts',(2.69809835589883,-1.17658029195788,
13.7566623454822));
#102547=CARTESIAN_POINT('Ctrl Pts',(2.65809479261838,-1.26091081106279,
13.7516259862617));
#102548=CARTESIAN_POINT('Ctrl Pts',(2.61810576697296,-1.34521068374006,
13.746591457297));
#102549=CARTESIAN_POINT('Ctrl Pts',(2.57408572646743,-1.42764178691665,
13.7415569283322));
#102550=CARTESIAN_POINT('Ctrl Pts',(2.52624255585271,-1.50780056671921,
13.7365223993675));
#102551=CARTESIAN_POINT('Ctrl Pts',(2.4784033891381,-1.58795263819239,13.7314882917325));
#102552=CARTESIAN_POINT('Ctrl Pts',(2.42674195628704,-1.66583238302116,
13.7264541840975));
#102553=CARTESIAN_POINT('Ctrl Pts',(2.37151106109142,-1.74106268902674,
13.7214200764626));
#102554=CARTESIAN_POINT('Ctrl Pts',(2.31626933903834,-1.8163077423544,13.7163849819965));
#102555=CARTESIAN_POINT('Ctrl Pts',(2.25745702817861,-1.88890196753801,
13.7113498875304));
#102556=CARTESIAN_POINT('Ctrl Pts',(2.19536834045367,-1.95849989781305,
13.7063147930643));
#102557=CARTESIAN_POINT('Ctrl Pts',(2.13321144250977,-2.02817428791091,
13.7012741670769));
#102558=CARTESIAN_POINT('Ctrl Pts',(2.06777127905937,-2.09484548045587,
13.6962335410895));
#102559=CARTESIAN_POINT('Ctrl Pts',(1.99937997416244,-2.15820381774247,
13.6911929151022));
#102560=CARTESIAN_POINT('Ctrl Pts',(1.93094664275576,-2.22160108877634,
13.6861491916463));
#102561=CARTESIAN_POINT('Ctrl Pts',(1.85955889925544,-2.28168116592815,
13.6811054681903));
#102562=CARTESIAN_POINT('Ctrl Pts',(1.78558139424408,-2.33817516121641,
13.6760617447344));
#102563=CARTESIAN_POINT('Ctrl Pts',(1.71148416675828,-2.39476058430973,
13.6710098587019));
#102564=CARTESIAN_POINT('Ctrl Pts',(1.63478917564768,-2.44774808722873,
13.6659579726693));
#102565=CARTESIAN_POINT('Ctrl Pts',(1.55588926093913,-2.49691261514981,
13.6609060866368));
#102566=CARTESIAN_POINT('Ctrl Pts',(1.51606485885711,-2.52172820506945,
13.658356168283));
#102567=CARTESIAN_POINT('Ctrl Pts',(1.47567909360101,-2.5455705570747,13.6558062499291));
#102568=CARTESIAN_POINT('Ctrl Pts',(1.43478453975205,-2.56841533333075,
13.6532563315753));
#102569=CARTESIAN_POINT('Ctrl Pts',(1.35375692301572,-2.61367949690957,
13.6482039764903));
#102570=CARTESIAN_POINT('Ctrl Pts',(1.27043984828923,-2.65518676429196,
13.6431516214054));
#102571=CARTESIAN_POINT('Ctrl Pts',(1.18521648466747,-2.69269862488777,
13.6380992663205));
#102572=CARTESIAN_POINT('Ctrl Pts',(1.10011063107759,-2.73015876234397,
13.6330538776633));
#102573=CARTESIAN_POINT('Ctrl Pts',(1.01310411479439,-2.76363426280696,
13.6280084890062));
#102574=CARTESIAN_POINT('Ctrl Pts',(0.924605862229365,-2.79293179285336,
13.622963100349));
#102575=CARTESIAN_POINT('Ctrl Pts',(0.836202293229886,-2.82219797770903,
13.6179231097124));
#102576=CARTESIAN_POINT('Ctrl Pts',(0.746310579702538,-2.84729493804633,
13.6128831190759));
#102577=CARTESIAN_POINT('Ctrl Pts',(0.655359832737792,-2.86807731583964,
13.6078431284393));
#102578=CARTESIAN_POINT('Ctrl Pts',(0.564474617642048,-2.88884471950569,
13.6028067692188));
#102579=CARTESIAN_POINT('Ctrl Pts',(0.472532317622279,-2.90530362102314,
13.5977704099983));
#102580=CARTESIAN_POINT('Ctrl Pts',(0.379976410158043,-2.91735872455264,
13.5927340507778));
#102581=CARTESIAN_POINT('Ctrl Pts',(0.287454138297511,-2.92940944715503,
13.5876995218131));
#102582=CARTESIAN_POINT('Ctrl Pts',(0.19431914206243,-2.93705949377639,
13.5826649928483));
#102583=CARTESIAN_POINT('Ctrl Pts',(0.101023249077452,-2.94026500559828,
13.5776304638836));
#102584=CARTESIAN_POINT('Ctrl Pts',(0.0077351638408286,-2.94347024915723,
13.5725963562486));
#102585=CARTESIAN_POINT('Ctrl Pts',(-0.085713347389459,-2.94223168238076,
13.5675622486136));
#102586=CARTESIAN_POINT('Ctrl Pts',(-0.178868350977806,-2.93655752761945,
13.5625281409787));
#102587=CARTESIAN_POINT('Ctrl Pts',(-0.272041615648986,-2.93088226055923,
13.5574930465125));
#102588=CARTESIAN_POINT('Ctrl Pts',(-0.364920815042746,-2.9207697060519,
13.5524579520464));
#102589=CARTESIAN_POINT('Ctrl Pts',(-0.45705618546169,-2.90628003525662,
13.5474228575803));
#102590=CARTESIAN_POINT('Ctrl Pts',(-0.549292775185043,-2.89177444620548,
13.542382231593));
#102591=CARTESIAN_POINT('Ctrl Pts',(-0.64078346525242,-2.87288221132512,
13.5373416056056));
#102592=CARTESIAN_POINT('Ctrl Pts',(-0.731088055541054,-2.8497147673136,
13.5323009796183));
#102593=CARTESIAN_POINT('Ctrl Pts',(-0.82144813807025,-2.82653308688982,
13.5272572561624));
#102594=CARTESIAN_POINT('Ctrl Pts',(-0.91062024555729,-2.79907109790597,
13.5222135327065));
#102595=CARTESIAN_POINT('Ctrl Pts',(-0.998180828609589,-2.76748966274425,
13.5171698092505));
#102596=CARTESIAN_POINT('Ctrl Pts',(-1.0858831164905,-2.7358571173489,13.512117923218));
#102597=CARTESIAN_POINT('Ctrl Pts',(-1.17196826360719,-2.70009198666347,
13.5070660371855));
#102598=CARTESIAN_POINT('Ctrl Pts',(-1.25603429571042,-2.66040257254409,
13.5020141511529));
#102599=CARTESIAN_POINT('Ctrl Pts',(-1.2984662739487,-2.64036950670205,
13.4994642327991));
#102600=CARTESIAN_POINT('Ctrl Pts',(-1.34038425681472,-2.61933737659354,
13.4969143144452));
#102601=CARTESIAN_POINT('Ctrl Pts',(-1.38173930724864,-2.59733719158758,
13.4943643960914));
#102602=CARTESIAN_POINT('Ctrl Pts',(-1.46367934232157,-2.55374648350997,
13.4893120410065));
#102603=CARTESIAN_POINT('Ctrl Pts',(-1.54370159831407,-2.50619622870097,
13.4842596859216));
#102604=CARTESIAN_POINT('Ctrl Pts',(-1.62139802903702,-2.45487931097129,
13.4792073308366));
#102605=CARTESIAN_POINT('Ctrl Pts',(-1.69898732822169,-2.40363315145129,
13.4741619421795));
#102606=CARTESIAN_POINT('Ctrl Pts',(-1.77425680730785,-2.3486308921786,
13.4691165535223));
#102607=CARTESIAN_POINT('Ctrl Pts',(-1.84682244245705,-2.29011154008641,
13.4640711648652));
#102608=CARTESIAN_POINT('Ctrl Pts',(-1.91931044021938,-2.23165479737632,
13.4590311742286));
#102609=CARTESIAN_POINT('Ctrl Pts',(-1.98910000002059,-2.16968871857654,
13.453991183592));
#102610=CARTESIAN_POINT('Ctrl Pts',(-2.05583649115529,-2.10449526529149,
13.4489511929554));
#102611=CARTESIAN_POINT('Ctrl Pts',(-2.12252489728635,-2.03934878521983,
13.4439148337349));
#102612=CARTESIAN_POINT('Ctrl Pts',(-2.18616429029692,-1.97097986224065,
13.4388784745144));
#102613=CARTESIAN_POINT('Ctrl Pts',(-2.24643433844286,-1.89970965230606,
13.4338421152939));
#102614=CARTESIAN_POINT('Ctrl Pts',(-2.30668248394084,-1.82846534257174,
13.4288075863292));
#102615=CARTESIAN_POINT('Ctrl Pts',(-2.36356343050931,-1.75432217933678,
13.4237730573645));
#102616=CARTESIAN_POINT('Ctrl Pts',(-2.41679555997163,-1.67763620052185,
13.4187385283997));
#102617=CARTESIAN_POINT('Ctrl Pts',(-2.47002323454262,-1.6009566394044,
13.4137044207648));
#102618=CARTESIAN_POINT('Ctrl Pts',(-2.5196024459703,-1.52173505085027,
13.4086703131298));
#102619=CARTESIAN_POINT('Ctrl Pts',(-2.56529421349996,-1.44035745500332,
13.4036362054948));
#102620=CARTESIAN_POINT('Ctrl Pts',(-2.61099493794135,-1.3589639067872,
13.3986011110287));
#102621=CARTESIAN_POINT('Ctrl Pts',(-2.65280648788912,-1.27541389942849,
13.3935660165626));
#102622=CARTESIAN_POINT('Ctrl Pts',(-2.69053580838343,-1.19011808817719,
13.3885309220965));
#102623=CARTESIAN_POINT('Ctrl Pts',(-2.72830657805803,-1.10472857151557,
13.3834902961092));
#102624=CARTESIAN_POINT('Ctrl Pts',(-2.76198598629454,-1.01758982945085,
13.3784496701218));
#102625=CARTESIAN_POINT('Ctrl Pts',(-2.79142925127766,-0.929132248450908,
13.3734090441344));
#102626=CARTESIAN_POINT('Ctrl Pts',(-2.8208906091699,-0.840620310198972,
13.3683653206785));
#102627=CARTESIAN_POINT('Ctrl Pts',(-2.84611052153083,-0.750788346994598,
13.3633215972226));
#102628=CARTESIAN_POINT('Ctrl Pts',(-2.8669947722064,-0.660079522588877,
13.3582778737667));
#102629=CARTESIAN_POINT('Ctrl Pts',(-2.88791282118546,-0.569223898356644,
13.3532259877341));
#102630=CARTESIAN_POINT('Ctrl Pts',(-2.90448112172261,-0.477489016526742,
13.3481741017016));
#102631=CARTESIAN_POINT('Ctrl Pts',(-2.91665702127834,-0.385325602870807,
13.3431222156691));
#102632=CARTESIAN_POINT('Ctrl Pts',(-2.92280275567371,-0.33880650514767,
13.3405722973152));
#102633=CARTESIAN_POINT('Ctrl Pts',(-2.9278302724095,-0.292178274858314,
13.3380223789614));
#102634=CARTESIAN_POINT('Ctrl Pts',(-2.93173912842756,-0.2454988448992,
13.3354724606075));
#102635=CARTESIAN_POINT('Ctrl Pts',(-2.93853326653527,-0.164363471156356,
13.3310403461016));
#102636=CARTESIAN_POINT('Ctrl Pts',(-2.94195988097664,-0.082942196459933,
13.3266082315956));
#102637=CARTESIAN_POINT('Ctrl Pts',(-2.941999649804,-0.00143546270055514,
13.3221761170896));
#102638=CARTESIAN_POINT('',(-2.94199943776035,-0.00181885067937308,12.3221761170896));
#102639=CARTESIAN_POINT('Ctrl Pts',(-2.94597788009644,-0.00141238427974306,
13.3221747584359));
#102640=CARTESIAN_POINT('Ctrl Pts',(-2.94060189892318,0.892291696921148,
13.2736433473318));
#102641=CARTESIAN_POINT('Ctrl Pts',(-2.0297603205157,2.77078909882355,13.172147957733));
#102642=CARTESIAN_POINT('Ctrl Pts',(1.16765677021709,3.2763543727395,13.0176885896398));
#102643=CARTESIAN_POINT('Ctrl Pts',(3.38653851180909,0.793269952057298,
12.8587966541559));
#102644=CARTESIAN_POINT('Ctrl Pts',(2.50126568019329,-2.41693820895166,
12.6999047186721));
#102645=CARTESIAN_POINT('Ctrl Pts',(-0.676706694895887,-3.41174271566395,
12.5410127831881));
#102646=CARTESIAN_POINT('Ctrl Pts',(-2.70347308096043,-1.72194475430307,
12.4151036473877));
#102647=CARTESIAN_POINT('Ctrl Pts',(-2.9404125071609,-0.372252179371909,
12.3421584900819));
#102648=CARTESIAN_POINT('Ctrl Pts',(-2.93832851344324,-0.00183871897317971,
12.3221773112706));
#102649=CARTESIAN_POINT('',(-2.94199908735515,0.00231732635699392,11.3221761170896));
#102650=CARTESIAN_POINT('Ctrl Pts',(-2.94199943776035,-0.00181885067937308,
12.3221761170896));
#102651=CARTESIAN_POINT('Ctrl Pts',(-2.94205766824479,0.0923692288830542,
12.317101658888));
#102652=CARTESIAN_POINT('Ctrl Pts',(-2.93758841679311,0.186573850448379,
12.3120272006865));
#102653=CARTESIAN_POINT('Ctrl Pts',(-2.92861347223371,0.280333962001044,
12.3069527424849));
#102654=CARTESIAN_POINT('Ctrl Pts',(-2.9196373468526,0.374106409448843,
12.3018776166435));
#102655=CARTESIAN_POINT('Ctrl Pts',(-2.90615439122099,0.467433798315638,
12.2968024908021));
#102656=CARTESIAN_POINT('Ctrl Pts',(-2.88823823698857,0.559860595503181,
12.2917273649607));
#102657=CARTESIAN_POINT('Ctrl Pts',(-2.87031501762493,0.65232384066058,
12.286650237773));
#102658=CARTESIAN_POINT('Ctrl Pts',(-2.84795520670616,0.743885361994522,
12.2815731105852));
#102659=CARTESIAN_POINT('Ctrl Pts',(-2.82128325111986,0.834101203062655,
12.2764959833975));
#102660=CARTESIAN_POINT('Ctrl Pts',(-2.79457535859223,0.924438598074477,
12.2714120154507));
#102661=CARTESIAN_POINT('Ctrl Pts',(-2.76354384624255,1.01342627637935,
12.2663280475039));
#102662=CARTESIAN_POINT('Ctrl Pts',(-2.72836260045467,1.10063687038016,
12.2612440795571));
#102663=CARTESIAN_POINT('Ctrl Pts',(-2.69315476612227,1.18791337457571,
12.2561562693556));
#102664=CARTESIAN_POINT('Ctrl Pts',(-2.65379113463881,1.27340972623707,
12.251068459154));
#102665=CARTESIAN_POINT('Ctrl Pts',(-2.61049222133598,1.35672191783886,
12.2459806489525));
#102666=CARTESIAN_POINT('Ctrl Pts',(-2.56711616167106,1.4401825480967,12.2408837737187));
#102667=CARTESIAN_POINT('Ctrl Pts',(-2.51979103835353,1.52145087340081,
12.2357868984848));
#102668=CARTESIAN_POINT('Ctrl Pts',(-2.46878144487779,1.60015067335146,
12.230690023251));
#102669=CARTESIAN_POINT('Ctrl Pts',(-2.44389114620892,1.63855249921357,
12.2282029862408));
#102670=CARTESIAN_POINT('Ctrl Pts',(-2.41812420531121,1.67634324929415,
12.2257159492306));
#102671=CARTESIAN_POINT('Ctrl Pts',(-2.39151476236182,1.71348216839438,
12.2232289122205));
#102672=CARTESIAN_POINT('Ctrl Pts',(-2.33745832739843,1.78892897758803,
12.2181765571355));
#102673=CARTESIAN_POINT('Ctrl Pts',(-2.27973113806503,1.86195061683415,
12.2131242020506));
#102674=CARTESIAN_POINT('Ctrl Pts',(-2.21857840853751,1.9321681720728,12.2080718469657));
#102675=CARTESIAN_POINT('Ctrl Pts',(-2.15750999930541,2.00228890800271,
12.2030264583086));
#102676=CARTESIAN_POINT('Ctrl Pts',(-2.09302572490762,2.06961291087218,
12.1979810696514));
#102677=CARTESIAN_POINT('Ctrl Pts',(-2.02541333578534,2.13379118454053,
12.1929356809943));
#102678=CARTESIAN_POINT('Ctrl Pts',(-1.95787328461187,2.19790079439246,
12.1878956903577));
#102679=CARTESIAN_POINT('Ctrl Pts',(-1.8872120913524,2.25887106047546,12.1828556997211));
#102680=CARTESIAN_POINT('Ctrl Pts',(-1.81375619102398,2.3163878085334,12.1778157090845));
#102681=CARTESIAN_POINT('Ctrl Pts',(-1.74035321717071,2.37386311460067,
12.172779349864));
#102682=CARTESIAN_POINT('Ctrl Pts',(-1.66415988741759,2.42788957546218,
12.1677429906435));
#102683=CARTESIAN_POINT('Ctrl Pts',(-1.58553694457079,2.47819220348244,
12.162706631423));
#102684=CARTESIAN_POINT('Ctrl Pts',(-1.5069425739699,2.52847655109998,12.1576721024583));
#102685=CARTESIAN_POINT('Ctrl Pts',(-1.42592071816484,2.57503951512635,
12.1526375734935));
#102686=CARTESIAN_POINT('Ctrl Pts',(-1.34286156881112,2.61764909928931,
12.1476030445288));
#102687=CARTESIAN_POINT('Ctrl Pts',(-1.25980937051293,2.66025511754065,
12.1425689368938));
#102688=CARTESIAN_POINT('Ctrl Pts',(-1.17472061300241,2.6989082111315,12.1375348292588));
#102689=CARTESIAN_POINT('Ctrl Pts',(-1.08800956062951,2.73342261569242,
12.1325007216238));
#102690=CARTESIAN_POINT('Ctrl Pts',(-1.00128151037501,2.76794378607783,
12.1274656271577));
#102691=CARTESIAN_POINT('Ctrl Pts',(-0.91293094653178,2.7983244922465,12.1224305326916));
#102692=CARTESIAN_POINT('Ctrl Pts',(-0.82339047069958,2.8244277531495,12.1173954382255));
#102693=CARTESIAN_POINT('Ctrl Pts',(-0.73375162629706,2.85055969092105,
12.1123548122381));
#102694=CARTESIAN_POINT('Ctrl Pts',(-0.642920687670014,2.87240467881097,
12.1073141862508));
#102695=CARTESIAN_POINT('Ctrl Pts',(-0.551343422148798,2.88987619645777,
12.1022735602634));
#102696=CARTESIAN_POINT('Ctrl Pts',(-0.459709882327092,2.90735845036569,
12.0972298368075));
#102697=CARTESIAN_POINT('Ctrl Pts',(-0.367329542101543,2.92046182139928,
12.0921861133516));
#102698=CARTESIAN_POINT('Ctrl Pts',(-0.274654138277992,2.92915160145848,
12.0871423898957));
#102699=CARTESIAN_POINT('Ctrl Pts',(-0.18182875198803,2.93785544473825,
12.0820905038631));
#102700=CARTESIAN_POINT('Ctrl Pts',(-0.0887077920051848,2.94213141701459,
12.0770386178306));
#102701=CARTESIAN_POINT('Ctrl Pts',(0.00425633687013605,2.94199692107188,
12.071986731798));
#102702=CARTESIAN_POINT('Ctrl Pts',(0.0511795922524226,2.94192903480711,
12.0694368134442));
#102703=CARTESIAN_POINT('Ctrl Pts',(0.0980629581512809,2.94073832643697,
12.0668868950904));
#102704=CARTESIAN_POINT('Ctrl Pts',(0.14484895308894,2.9384320275938,12.0643369767366));
#102705=CARTESIAN_POINT('Ctrl Pts',(0.237549748419017,2.93386237513018,
12.0592846216516));
#102706=CARTESIAN_POINT('Ctrl Pts',(0.330200420451757,2.92489347562024,
12.0542322665667));
#102707=CARTESIAN_POINT('Ctrl Pts',(0.42234963216692,2.91152619569333,12.0491799114818));
#102708=CARTESIAN_POINT('Ctrl Pts',(0.514371784161062,2.8981773472085,12.0441345228246));
#102709=CARTESIAN_POINT('Ctrl Pts',(0.605893413987775,2.88044223286289,
12.0390891341675));
#102710=CARTESIAN_POINT('Ctrl Pts',(0.69646529138112,2.85837368059206,12.0340437455103));
#102711=CARTESIAN_POINT('Ctrl Pts',(0.78694026665451,2.83632873928704,12.0290037548737));
#102712=CARTESIAN_POINT('Ctrl Pts',(0.876467079918468,2.80995968003446,
12.0239637642371));
#102713=CARTESIAN_POINT('Ctrl Pts',(0.964604816251452,2.77937071087405,
12.0189237736005));
#102714=CARTESIAN_POINT('Ctrl Pts',(1.05267904754699,2.74880378169006,12.0138874143801));
#102715=CARTESIAN_POINT('Ctrl Pts',(1.13936577278185,2.71402313132016,12.0088510551596));
#102716=CARTESIAN_POINT('Ctrl Pts',(1.22423843214642,2.67518303322514,12.0038146959391));
#102717=CARTESIAN_POINT('Ctrl Pts',(1.30908024806488,2.63635704995205,11.9987801669743));
#102718=CARTESIAN_POINT('Ctrl Pts',(1.39210890423529,2.59347473434825,11.9937456380096));
#102719=CARTESIAN_POINT('Ctrl Pts',(1.47291802618841,2.54673840198188,11.9887111090449));
#102720=CARTESIAN_POINT('Ctrl Pts',(1.55372038538624,2.50000598088657,11.9836770014099));
#102721=CARTESIAN_POINT('Ctrl Pts',(1.63230319521567,2.44942040687475,11.9786428937749));
#102722=CARTESIAN_POINT('Ctrl Pts',(1.70828590269151,2.39522927392462,11.9736087861399));
#102723=CARTESIAN_POINT('Ctrl Pts',(1.78428350498215,2.34102751794043,11.9685736916738));
#102724=CARTESIAN_POINT('Ctrl Pts',(1.85767963122038,2.28321905755688,11.9635385972077));
#102725=CARTESIAN_POINT('Ctrl Pts',(1.92812480141315,2.22209332616241,11.9585035027416));
#102726=CARTESIAN_POINT('Ctrl Pts',(1.99864736220074,2.16090044244651,11.9534628767543));
#102727=CARTESIAN_POINT('Ctrl Pts',(2.06621215968135,2.09638330480715,11.9484222507669));
#102728=CARTESIAN_POINT('Ctrl Pts',(2.13050499818133,2.02886974759948,11.9433816247796));
#102729=CARTESIAN_POINT('Ctrl Pts',(2.19483734468032,1.96131470325866,11.9383379013237));
#102730=CARTESIAN_POINT('Ctrl Pts',(2.25589343896197,1.89075990934853,11.9332941778677));
#102731=CARTESIAN_POINT('Ctrl Pts',(2.31339940392865,1.81756628432158,11.9282504544118));
#102732=CARTESIAN_POINT('Ctrl Pts',(2.37099843443491,1.74425420542274,11.9231985683793));
#102733=CARTESIAN_POINT('Ctrl Pts',(2.42503560847699,1.66829513125387,11.9181466823467));
#102734=CARTESIAN_POINT('Ctrl Pts',(2.47528049031936,1.59007876982379,11.9130947963142));
#102735=CARTESIAN_POINT('Ctrl Pts',(2.500641384364,1.55059938840126,11.9105448779604));
#102736=CARTESIAN_POINT('Ctrl Pts',(2.52503685218335,1.51054531327355,11.9079949596065));
#102737=CARTESIAN_POINT('Ctrl Pts',(2.54844183525752,1.4699687793655,11.9054450412527));
#102738=CARTESIAN_POINT('Ctrl Pts',(2.59481598095077,1.38957128071249,11.9003926861678));
#102739=CARTESIAN_POINT('Ctrl Pts',(2.63746506948364,1.30683287709102,11.8953403310828));
#102740=CARTESIAN_POINT('Ctrl Pts',(2.67614534361757,1.22213342145365,11.8902879759979));
#102741=CARTESIAN_POINT('Ctrl Pts',(2.71477228354784,1.1375507534585,11.8852425873407));
#102742=CARTESIAN_POINT('Ctrl Pts',(2.74944110048464,1.05101280721965,11.8801971986836));
#102743=CARTESIAN_POINT('Ctrl Pts',(2.77995285587913,0.962925811830535,
11.8751518100264));
#102744=CARTESIAN_POINT('Ctrl Pts',(2.81043196699289,0.874933060006497,
11.8701118193898));
#102745=CARTESIAN_POINT('Ctrl Pts',(2.83676271224308,0.78539497071694,11.8650718287532));
#102746=CARTESIAN_POINT('Ctrl Pts',(2.85879384636977,0.69473861556585,11.8600318381167));
#102747=CARTESIAN_POINT('Ctrl Pts',(2.88080910661477,0.604147580168466,
11.8549954788962));
#102748=CARTESIAN_POINT('Ctrl Pts',(2.89853080876147,0.512440310854052,
11.8499591196757));
#102749=CARTESIAN_POINT('Ctrl Pts',(2.91185756744108,0.420058932694123,
11.8449227604552));
#102750=CARTESIAN_POINT('Ctrl Pts',(2.92517948306328,0.32771112671245,11.8398882314904));
#102751=CARTESIAN_POINT('Ctrl Pts',(2.93410956478644,0.234690137804377,
11.8348537025257));
#102752=CARTESIAN_POINT('Ctrl Pts',(2.93859774457073,0.141447147740094,
11.829819173561));
#102753=CARTESIAN_POINT('Ctrl Pts',(2.94308554874817,0.0482119609966004,
11.824785065926));
#102754=CARTESIAN_POINT('Ctrl Pts',(2.94313216890858,-0.0452447462288223,
11.819750958291));
#102755=CARTESIAN_POINT('Ctrl Pts',(2.93873958429541,-0.138468970152959,
11.814716850656));
#102756=CARTESIAN_POINT('Ctrl Pts',(2.93434613860826,-0.231711468728897,
11.8096817561899));
#102757=CARTESIAN_POINT('Ctrl Pts',(2.92551178117756,-0.324720949791183,
11.8046466617238));
#102758=CARTESIAN_POINT('Ctrl Pts',(2.91229049248657,-0.417046864719446,
11.7996115672577));
#102759=CARTESIAN_POINT('Ctrl Pts',(2.89905467897586,-0.509474208283074,
11.7945709412703));
#102760=CARTESIAN_POINT('Ctrl Pts',(2.88142237708944,-0.601216046274095,
11.789530315283));
#102761=CARTESIAN_POINT('Ctrl Pts',(2.85949895951669,-0.691830687757469,
11.7844896892956));
#102762=CARTESIAN_POINT('Ctrl Pts',(2.83756206998686,-0.782501012008185,
11.7794459658397));
#102763=CARTESIAN_POINT('Ctrl Pts',(2.81132894003605,-0.872042334790647,
11.7744022423838));
#102764=CARTESIAN_POINT('Ctrl Pts',(2.78095459233893,-0.960028934641571,
11.7693585189279));
#102765=CARTESIAN_POINT('Ctrl Pts',(2.75053108791417,-1.04815792877096,
11.7643066328953));
#102766=CARTESIAN_POINT('Ctrl Pts',(2.71595315063959,-1.13472676485469,
11.7592547468628));
#102767=CARTESIAN_POINT('Ctrl Pts',(2.67742353487152,-1.21933064216237,
11.7542028608302));
#102768=CARTESIAN_POINT('Ctrl Pts',(2.65797587239862,-1.26203409551843,
11.7516529424764));
#102769=CARTESIAN_POINT('Ctrl Pts',(2.63752217185223,-1.30423734087188,
11.7491030241226));
#102770=CARTESIAN_POINT('Ctrl Pts',(2.61609276670458,-1.34589101936076,
11.7465531057688));
#102771=CARTESIAN_POINT('Ctrl Pts',(2.57363298994241,-1.42842274983934,
11.7415007506839));
#102772=CARTESIAN_POINT('Ctrl Pts',(2.52718766825847,-1.50909133282075,
11.7364483955989));
#102773=CARTESIAN_POINT('Ctrl Pts',(2.47694405592248,-1.58748610823222,
11.731396040514));
#102774=CARTESIAN_POINT('Ctrl Pts',(2.42676972187185,-1.6657727891941,11.7263506518569));
#102775=CARTESIAN_POINT('Ctrl Pts',(2.37280774191927,-1.74179152192844,
11.7213052631997));
#102776=CARTESIAN_POINT('Ctrl Pts',(2.31529181944221,-1.81515503217328,
11.7162598745426));
#102777=CARTESIAN_POINT('Ctrl Pts',(2.25783743278584,-1.88844005139133,
11.711219883906));
#102778=CARTESIAN_POINT('Ctrl Pts',(2.19683693394232,-1.95907514691681,
11.7061798932694));
#102779=CARTESIAN_POINT('Ctrl Pts',(2.13256738110225,-2.02670184414449,
11.7011399026328));
#102780=CARTESIAN_POINT('Ctrl Pts',(2.06834413578643,-2.0942798149569,11.6961035434124));
#102781=CARTESIAN_POINT('Ctrl Pts',(2.00085682335587,-2.1588533748168,11.6910671841919));
#102782=CARTESIAN_POINT('Ctrl Pts',(1.93042216430952,-2.22009780585058,
11.6860308249714));
#102783=CARTESIAN_POINT('Ctrl Pts',(1.86001310181708,-2.28131998013744,
11.6809962960067));
#102784=CARTESIAN_POINT('Ctrl Pts',(1.78665915544363,-2.33921513786641,
11.6759617670419));
#102785=CARTESIAN_POINT('Ctrl Pts',(1.71071245673316,-2.39349679138661,
11.6709272380772));
#102786=CARTESIAN_POINT('Ctrl Pts',(1.63477211385139,-2.4477739021828,11.6658931304422));
#102787=CARTESIAN_POINT('Ctrl Pts',(1.55623981156895,-2.49843785186136,
11.6608590228072));
#102788=CARTESIAN_POINT('Ctrl Pts',(1.4754982471522,-2.54524437385702,11.6558249151723));
#102789=CARTESIAN_POINT('Ctrl Pts',(1.3947408550467,-2.59206007128872,11.6507898207062));
#102790=CARTESIAN_POINT('Ctrl Pts',(1.3117737252013,-2.63501661681924,11.6457547262401));
#102791=CARTESIAN_POINT('Ctrl Pts',(1.22700481921386,-2.67391532656252,
11.640719631774));
#102792=CARTESIAN_POINT('Ctrl Pts',(1.14214278667079,-2.7128567701693,11.6356790057866));
#102793=CARTESIAN_POINT('Ctrl Pts',(1.05547543121897,-2.7477312939191,11.6306383797993));
#102794=CARTESIAN_POINT('Ctrl Pts',(0.967431107643021,-2.77838821116931,
11.6255977538119));
#102795=CARTESIAN_POINT('Ctrl Pts',(0.879332680762282,-2.80906396711883,
11.620554030356));
#102796=CARTESIAN_POINT('Ctrl Pts',(0.789856026937357,-2.83551683110188,
11.6155103069001));
#102797=CARTESIAN_POINT('Ctrl Pts',(0.699442972388415,-2.8576465016472,
11.6104665834442));
#102798=CARTESIAN_POINT('Ctrl Pts',(0.608883596675779,-2.87981198603779,
11.6054146974116));
#102799=CARTESIAN_POINT('Ctrl Pts',(0.51738523035346,-2.89764022452043,
11.6003628113791));
#102800=CARTESIAN_POINT('Ctrl Pts',(0.425397970031113,-2.91108237037247,
11.5953109253466));
#102801=CARTESIAN_POINT('Ctrl Pts',(0.378967784966315,-2.91786723729199,
11.5927610069927));
#102802=CARTESIAN_POINT('Ctrl Pts',(0.332413100333541,-2.92353549303978,
11.5902110886388));
#102803=CARTESIAN_POINT('Ctrl Pts',(0.285791837458446,-2.92808589792754,
11.587661170285));
#102804=CARTESIAN_POINT('Ctrl Pts',(0.19341743880498,-2.93710197533974,
11.5826088152));
#102805=CARTESIAN_POINT('Ctrl Pts',(0.100450220757555,-2.94175864314905,
11.5775564601151));
#102806=CARTESIAN_POINT('Ctrl Pts',(0.00733680887932632,-2.94199085165734,
11.5725041050302));
#102807=CARTESIAN_POINT('Ctrl Pts',(-0.085648213792534,-2.94222273998547,
11.567458716373));
#102808=CARTESIAN_POINT('Ctrl Pts',(-0.17877858934624,-2.938042290704,11.5624133277159));
#102809=CARTESIAN_POINT('Ctrl Pts',(-0.271602188677053,-2.9294361660746,
11.5573679390587));
#102810=CARTESIAN_POINT('Ctrl Pts',(-0.364326476789299,-2.92083924906836,
11.5523279484221));
#102811=CARTESIAN_POINT('Ctrl Pts',(-0.456744201093304,-2.90782610903195,
11.5472879577855));
#102812=CARTESIAN_POINT('Ctrl Pts',(-0.548403955851965,-2.89043545183177,
11.5422479671489));
#102813=CARTESIAN_POINT('Ctrl Pts',(-0.63999766788659,-2.87305732495503,
11.5372116079284));
#102814=CARTESIAN_POINT('Ctrl Pts',(-0.730834060691916,-2.85130803268609,
11.5321752487079));
#102815=CARTESIAN_POINT('Ctrl Pts',(-0.820468618902273,-2.8252779058699,
11.5271388894874));
#102816=CARTESIAN_POINT('Ctrl Pts',(-0.910070603152004,-2.79925723862313,
11.5221043605227));
#102817=CARTESIAN_POINT('Ctrl Pts',(-0.998471194286752,-2.76895895114635,
11.517069831558));
#102818=CARTESIAN_POINT('Ctrl Pts',(-1.08523883050169,-2.73452384900394,
11.5120353025932));
#102819=CARTESIAN_POINT('Ctrl Pts',(-1.17199920530529,-2.70009162866692,
11.5070011949583));
#102820=CARTESIAN_POINT('Ctrl Pts',(-1.2571264840562,-2.66152344603806,
11.5019670873233));
#102821=CARTESIAN_POINT('Ctrl Pts',(-1.34020803781096,-2.61900867035352,
11.4969329796883));
#102822=CARTESIAN_POINT('Ctrl Pts',(-1.4233058779603,-2.57648556053966,
11.4918978852222));
#102823=CARTESIAN_POINT('Ctrl Pts',(-1.50435680140709,-2.53001452389156,
11.4868627907561));
#102824=CARTESIAN_POINT('Ctrl Pts',(-1.58297280946911,-2.47983085803881,
11.4818276962899));
#102825=CARTESIAN_POINT('Ctrl Pts',(-1.66167518455394,-2.429592060745,11.4767870703026));
#102826=CARTESIAN_POINT('Ctrl Pts',(-1.73793692964973,-2.37563273214714,
11.4717464443152));
#102827=CARTESIAN_POINT('Ctrl Pts',(-1.81139934462327,-2.31823131164653,
11.4667058183279));
#102828=CARTESIAN_POINT('Ctrl Pts',(-1.88490690230741,-2.2607946179288,
11.461662094872));
#102829=CARTESIAN_POINT('Ctrl Pts',(-1.95561136892047,-2.19991191107742,
11.4566183714161));
#102830=CARTESIAN_POINT('Ctrl Pts',(-2.02318909957356,-2.13590024752251,
11.4515746479602));
#102831=CARTESIAN_POINT('Ctrl Pts',(-2.09087619554172,-2.07178498984443,
11.4465227619276));
#102832=CARTESIAN_POINT('Ctrl Pts',(-2.1554261462877,-2.00453098635218,
11.4414708758951));
#102833=CARTESIAN_POINT('Ctrl Pts',(-2.21655407859464,-1.93449011800667,
11.4364189898625));
#102834=CARTESIAN_POINT('Ctrl Pts',(-2.24740814686075,-1.89913728253861,
11.4338690715087));
#102835=CARTESIAN_POINT('Ctrl Pts',(-2.27739105792315,-1.86307493612799,
11.4313191531549));
#102836=CARTESIAN_POINT('Ctrl Pts',(-2.30647039420271,-1.82635109457803,
11.4287692348011));
#102837=CARTESIAN_POINT('Ctrl Pts',(-2.36400612788006,-1.75369011130406,
11.4237240225619));
#102838=CARTESIAN_POINT('Ctrl Pts',(-2.41821268241222,-1.67817153783343,
11.4186788103228));
#102839=CARTESIAN_POINT('Ctrl Pts',(-2.46879265417749,-1.6001333790279,
11.4136335980836));
#102840=CARTESIAN_POINT('Ctrl Pts',(-2.51930480111526,-1.52219986489644,
11.4085951511833));
#102841=CARTESIAN_POINT('Ctrl Pts',(-2.56619978421412,-1.44175384536167,
11.4035567042831));
#102842=CARTESIAN_POINT('Ctrl Pts',(-2.60922039845594,-1.3591662563062,
11.3985182573828));
#102843=CARTESIAN_POINT('Ctrl Pts',(-2.65219541974529,-1.27666619301227,
11.393485150194));
#102844=CARTESIAN_POINT('Ctrl Pts',(-2.69130402539409,-1.19202946153317,
11.3884520430053));
#102845=CARTESIAN_POINT('Ctrl Pts',(-2.72633294005123,-1.10565487381534,
11.3834189358166));
#102846=CARTESIAN_POINT('Ctrl Pts',(-2.76185224237784,-1.01807108412288,
11.3783153675893));
#102847=CARTESIAN_POINT('Ctrl Pts',(-2.79317649350139,-0.928700795946386,
11.3732117993621));
#102848=CARTESIAN_POINT('Ctrl Pts',(-2.82013231123186,-0.8379843358596,
11.3681082311348));
#102849=CARTESIAN_POINT('Ctrl Pts',(-2.84668412971332,-0.748627485119997,
11.363081152434));
#102850=CARTESIAN_POINT('Ctrl Pts',(-2.86899744628251,-0.657964982397529,
11.3580540737331));
#102851=CARTESIAN_POINT('Ctrl Pts',(-2.88695609225618,-0.56643492246236,
11.3530269950322));
#102852=CARTESIAN_POINT('Ctrl Pts',(-2.90532461295226,-0.47281584880292,
11.3478851820418));
#102853=CARTESIAN_POINT('Ctrl Pts',(-2.91913711330609,-0.378289593421233,
11.3427433690513));
#102854=CARTESIAN_POINT('Ctrl Pts',(-2.92832451093351,-0.283336476059814,
11.3376015560609));
#102855=CARTESIAN_POINT('Ctrl Pts',(-2.93751190856094,-0.188383358698396,
11.3324597430705));
#102856=CARTESIAN_POINT('Ctrl Pts',(-2.94207416906968,-0.0930038764377092,
11.32731793008));
#102857=CARTESIAN_POINT('Ctrl Pts',(-2.94199908735515,0.00231732635699392,
11.3221761170896));
#102858=CARTESIAN_POINT('',(-2.94239657372082,0.000640158651710834,10.3221761814368));
#102859=CARTESIAN_POINT('Ctrl Pts',(-2.93935298557806,0.00233601540201734,
11.3221749955287));
#102860=CARTESIAN_POINT('Ctrl Pts',(-2.94172337671491,0.325219974538946,
11.3047424301248));
#102861=CARTESIAN_POINT('Ctrl Pts',(-2.74371032010323,1.6262663578991,11.2343458862266));
#102862=CARTESIAN_POINT('Ctrl Pts',(-0.839765383495511,3.3753095279522,
11.1109853638332));
#102863=CARTESIAN_POINT('Ctrl Pts',(2.38231317487652,2.53426601713663,10.9520934283495));
#102864=CARTESIAN_POINT('Ctrl Pts',(3.42072593089031,-0.62972566609421,
10.7932014928655));
#102865=CARTESIAN_POINT('Ctrl Pts',(1.32364738655828,-3.21650087903925,
10.6343095573817));
#102866=CARTESIAN_POINT('Ctrl Pts',(-1.94746159165213,-2.85926666405493,
10.4773013514598));
#102867=CARTESIAN_POINT('Ctrl Pts',(-2.94388221610062,-0.939423273160714,
10.3732571240324));
#102868=CARTESIAN_POINT('Ctrl Pts',(-2.94667239079342,0.000628324869612199,
10.3221768750997));
#102869=CARTESIAN_POINT('',(-2.94199877210839,-0.00268791977826042,9.32217614139002));
#102870=CARTESIAN_POINT('Ctrl Pts',(-2.94199993011391,0.000641256405411553,
10.3221761170896));
#102871=CARTESIAN_POINT('Ctrl Pts',(-2.94199238686346,0.0352486959386637,
10.3202926401977));
#102872=CARTESIAN_POINT('Ctrl Pts',(-2.94137422245853,0.0698487503835785,
10.3184091633059));
#102873=CARTESIAN_POINT('Ctrl Pts',(-2.94014608467686,0.104427011636639,
10.3165256864141));
#102874=CARTESIAN_POINT('Ctrl Pts',(-2.93685165181546,0.19718188153905,
10.3114733313293));
#102875=CARTESIAN_POINT('Ctrl Pts',(-2.92915769861534,0.289947129723463,
10.3064209762446));
#102876=CARTESIAN_POINT('Ctrl Pts',(-2.91705888500192,0.382271449929681,
10.3013686211598));
#102877=CARTESIAN_POINT('Ctrl Pts',(-2.90497675380882,0.474468468966993,
10.2963232325027));
#102878=CARTESIAN_POINT('Ctrl Pts',(-2.88850188851419,0.566225331492591,
10.2912778438456));
#102879=CARTESIAN_POINT('Ctrl Pts',(-2.8676809344076,0.65709212324846,10.2862324551885));
#102880=CARTESIAN_POINT('Ctrl Pts',(-2.84688225647159,0.747861697357949,
10.281192464552));
#102881=CARTESIAN_POINT('Ctrl Pts',(-2.82174683069095,0.837742662806323,
10.2761524739154));
#102882=CARTESIAN_POINT('Ctrl Pts',(-2.79237279195056,0.926292713333228,
10.2711124832788));
#102883=CARTESIAN_POINT('Ctrl Pts',(-2.76301991780447,1.01477896174185,
10.2660761240583));
#102884=CARTESIAN_POINT('Ctrl Pts',(-2.7294346404374,1.1019357808457,10.2610397648378));
#102885=CARTESIAN_POINT('Ctrl Pts',(-2.69176535282754,1.18733452965761,
10.2560034056173));
#102886=CARTESIAN_POINT('Ctrl Pts',(-2.65410975455708,1.27270224383808,
10.2509688766525));
#102887=CARTESIAN_POINT('Ctrl Pts',(-2.6123732736043,1.35631275092138,10.2459343476877));
#102888=CARTESIAN_POINT('Ctrl Pts',(-2.56675261809335,1.43775693269445,
10.2408998187229));
#102889=CARTESIAN_POINT('Ctrl Pts',(-2.52113578048464,1.51919429856537,
10.2358657110879));
#102890=CARTESIAN_POINT('Ctrl Pts',(-2.4716356318738,1.59846531209709,10.2308316034528));
#102891=CARTESIAN_POINT('Ctrl Pts',(-2.4184945096012,1.67518605146678,10.2257974958177));
#102892=CARTESIAN_POINT('Ctrl Pts',(-2.36534297012712,1.75192183032689,
10.2207624013516));
#102893=CARTESIAN_POINT('Ctrl Pts',(-2.30854929274796,1.82610597720804,
10.2157273068854));
#102894=CARTESIAN_POINT('Ctrl Pts',(-2.24839807756254,1.89738506498103,
10.2106922124192));
#102895=CARTESIAN_POINT('Ctrl Pts',(-2.1881807806527,1.96874245948516,10.2056515864317));
#102896=CARTESIAN_POINT('Ctrl Pts',(-2.12459887007337,2.03718808428977,
10.2006109604442));
#102897=CARTESIAN_POINT('Ctrl Pts',(-2.05797582847605,2.10240326517258,
10.1955703344568));
#102898=CARTESIAN_POINT('Ctrl Pts',(-1.99131184696814,2.16765852083448,
10.1905266110008));
#102899=CARTESIAN_POINT('Ctrl Pts',(-1.92160334571709,2.22967908553681,
10.1854828875448));
#102900=CARTESIAN_POINT('Ctrl Pts',(-1.84920744278971,2.28818614486041,
10.1804391640887));
#102901=CARTESIAN_POINT('Ctrl Pts',(-1.77669437699459,2.34678788985787,
10.1753872780561));
#102902=CARTESIAN_POINT('Ctrl Pts',(-1.70148558487444,2.40186451570675,
10.1703353920235));
#102903=CARTESIAN_POINT('Ctrl Pts',(-1.62396756871984,2.45318024933884,
10.1652835059909));
#102904=CARTESIAN_POINT('Ctrl Pts',(-1.58484067415706,2.47908165134621,
10.1627335876371));
#102905=CARTESIAN_POINT('Ctrl Pts',(-1.54512586404205,2.50402562139544,
10.1601836692833));
#102906=CARTESIAN_POINT('Ctrl Pts',(-1.50487502376479,2.52798638502048,
10.1576337509296));
#102907=CARTESIAN_POINT('Ctrl Pts',(-1.42512284768101,2.57546174271645,
10.1525813958446));
#102908=CARTESIAN_POINT('Ctrl Pts',(-1.34297876235402,2.61924458675749,
10.1475290407596));
#102909=CARTESIAN_POINT('Ctrl Pts',(-1.25881923275757,2.65908595935514,
10.1424766856747));
#102910=CARTESIAN_POINT('Ctrl Pts',(-1.17477574632801,2.69887239677109,
10.1374312970175));
#102911=CARTESIAN_POINT('Ctrl Pts',(-1.08872273587955,2.7347279737394,10.1323859083604));
#102912=CARTESIAN_POINT('Ctrl Pts',(-1.00106365636304,2.76644818420824,
10.1273405197032));
#102913=CARTESIAN_POINT('Ctrl Pts',(-0.913498362587476,2.79813445748017,
10.1223005290666));
#102914=CARTESIAN_POINT('Ctrl Pts',(-0.824330830657412,2.82569400806737,
10.1172605384301));
#102915=CARTESIAN_POINT('Ctrl Pts',(-0.733986011924087,2.84896973207856,
10.1122205477935));
#102916=CARTESIAN_POINT('Ctrl Pts',(-0.643706288476191,2.87222868545564,
10.107184188573));
#102917=CARTESIAN_POINT('Ctrl Pts',(-0.552251393216398,2.89120983676699,
10.1021478293526));
#102918=CARTESIAN_POINT('Ctrl Pts',(-0.460062015195089,2.90580573028801,
10.0971114701321));
#102919=CARTESIAN_POINT('Ctrl Pts',(-0.367906139577596,2.92039631953723,
10.0920769411674));
#102920=CARTESIAN_POINT('Ctrl Pts',(-0.275016749791795,2.93060474753725,
10.0870424122027));
#102921=CARTESIAN_POINT('Ctrl Pts',(-0.181844296427517,2.93637474649555,
10.082007883238));
#102922=CARTESIAN_POINT('Ctrl Pts',(-0.0886796404811632,2.94214426257407,
10.0769737756031));
#102923=CARTESIAN_POINT('Ctrl Pts',(0.00476758854223665,2.9434760608548,
10.0719396679682));
#102924=CARTESIAN_POINT('Ctrl Pts',(0.0980434025714094,2.94036587709969,
10.0669055603332));
#102925=CARTESIAN_POINT('Ctrl Pts',(0.191337501365793,2.93725508365834,
10.0618704658672));
#102926=CARTESIAN_POINT('Ctrl Pts',(0.284459674477728,2.92970059402629,
10.0568353714011));
#102927=CARTESIAN_POINT('Ctrl Pts',(0.376958673570008,2.9177501878023,10.0518002769351));
#102928=CARTESIAN_POINT('Ctrl Pts',(0.469559291446737,2.9057866529416,10.0467596509478));
#102929=CARTESIAN_POINT('Ctrl Pts',(0.561534927474578,2.88941761860679,
10.0417190249605));
#102930=CARTESIAN_POINT('Ctrl Pts',(0.652442483437231,2.86874237355087,
10.0366783989732));
#102931=CARTESIAN_POINT('Ctrl Pts',(0.743405902163319,2.84805442354087,
10.0316346755173));
#102932=CARTESIAN_POINT('Ctrl Pts',(0.833299506507768,2.82305511373853,
10.0265909520614));
#102933=CARTESIAN_POINT('Ctrl Pts',(0.921695483447506,2.79389359779367,
10.0215472286055));
#102934=CARTESIAN_POINT('Ctrl Pts',(1.01023451718657,2.7646848879235,10.016495342573));
#102935=CARTESIAN_POINT('Ctrl Pts',(1.09727067065002,2.73130068331518,10.0114434565406));
#102936=CARTESIAN_POINT('Ctrl Pts',(1.18239639318077,2.69393815248107,10.006391570508));
#102937=CARTESIAN_POINT('Ctrl Pts',(1.2253632457321,2.67507957124889,10.0038416521542));
#102938=CARTESIAN_POINT('Ctrl Pts',(1.26784377224799,2.65520816839446,10.0012917338004));
#102939=CARTESIAN_POINT('Ctrl Pts',(1.30978820139893,2.63435359575668,9.99874181544654));
#102940=CARTESIAN_POINT('Ctrl Pts',(1.39289601917855,2.59303278015049,9.99368946036164));
#102941=CARTESIAN_POINT('Ctrl Pts',(1.47419567339604,2.54770117516414,9.98863710527674));
#102942=CARTESIAN_POINT('Ctrl Pts',(1.55327396775754,2.49854037011347,9.98358475019183));
#102943=CARTESIAN_POINT('Ctrl Pts',(1.63224322520128,2.44944735032171,9.97853936153469));
#102944=CARTESIAN_POINT('Ctrl Pts',(1.70899683519463,2.3965358547847,9.97349397287754));
#102945=CARTESIAN_POINT('Ctrl Pts',(1.78314434629204,2.34003423912701,9.96844858422039));
#102946=CARTESIAN_POINT('Ctrl Pts',(1.85721252756636,2.28359307409144,9.9634085935838));
#102947=CARTESIAN_POINT('Ctrl Pts',(1.9286798005607,2.22356969139925,9.95836860294721));
#102948=CARTESIAN_POINT('Ctrl Pts',(1.99718391456342,2.16023619343097,9.95332861231061));
#102949=CARTESIAN_POINT('Ctrl Pts',(2.06563866995415,2.09694832854032,9.94829225309011));
#102950=CARTESIAN_POINT('Ctrl Pts',(2.13113418474373,2.03035538961638,9.94325589386961));
#102951=CARTESIAN_POINT('Ctrl Pts',(2.1933414163386,1.96076960180787,9.9382195346491));
#102952=CARTESIAN_POINT('Ctrl Pts',(2.25552604129659,1.89120910206629,9.93318500568435));
#102953=CARTESIAN_POINT('Ctrl Pts',(2.31442446126173,1.81865824498921,9.9281504767196));
#102954=CARTESIAN_POINT('Ctrl Pts',(2.36974537328843,1.74346518915006,9.92311594775485));
#102955=CARTESIAN_POINT('Ctrl Pts',(2.42506165561767,1.6682784260687,9.91808184011985));
#102956=CARTESIAN_POINT('Ctrl Pts',(2.47680076216299,1.5904502618047,9.91304773248484));
#102957=CARTESIAN_POINT('Ctrl Pts',(2.52471318674338,1.51035999837261,9.90801362484984));
#102958=CARTESIAN_POINT('Ctrl Pts',(2.57263500354874,1.43025403492578,9.90297853038372));
#102959=CARTESIAN_POINT('Ctrl Pts',(2.61672842087429,1.34788547303943,9.8979434359176));
#102960=CARTESIAN_POINT('Ctrl Pts',(2.65678916348219,1.26365950350701,9.89290834145147));
#102961=CARTESIAN_POINT('Ctrl Pts',(2.6968939165552,1.17934100388526,9.88786771546409));
#102962=CARTESIAN_POINT('Ctrl Pts',(2.73295696047361,1.09316142526529,9.88282708947671));
#102963=CARTESIAN_POINT('Ctrl Pts',(2.76482173226482,1.00554700973956,9.87778646348933));
#102964=CARTESIAN_POINT('Ctrl Pts',(2.79670608498293,0.917878755087725,
9.87274274003339));
#102965=CARTESIAN_POINT('Ctrl Pts',(2.82438689791758,0.828774332145286,
9.86769901657745));
#102966=CARTESIAN_POINT('Ctrl Pts',(2.84775780324887,0.738674146044887,
9.8626552931215));
#102967=CARTESIAN_POINT('Ctrl Pts',(2.87116653119416,0.648428145115718,
9.85760340708895));
#102968=CARTESIAN_POINT('Ctrl Pts',(2.89025133600985,0.557183598143385,
9.85255152105639));
#102969=CARTESIAN_POINT('Ctrl Pts',(2.90495718602783,0.465389887454911,
9.84749963502384));
#102970=CARTESIAN_POINT('Ctrl Pts',(2.91237990234179,0.419057395758485,
9.84494971666997));
#102971=CARTESIAN_POINT('Ctrl Pts',(2.91868782514139,0.372585061037236,
9.8423997983161));
#102972=CARTESIAN_POINT('Ctrl Pts',(2.92387891834262,0.326030782092145,
9.83984987996223));
#102973=CARTESIAN_POINT('Ctrl Pts',(2.93416444222685,0.233789104001969,
9.83479752487729));
#102974=CARTESIAN_POINT('Ctrl Pts',(2.9400991209621,0.140894713563981,9.82974516979236));
#102975=CARTESIAN_POINT('Ctrl Pts',(2.94161176916946,0.0477932995695164,
9.82469281470743));
#102976=CARTESIAN_POINT('Ctrl Pts',(2.94312233166544,-0.0451797417620558,
9.81964742605027));
#102977=CARTESIAN_POINT('Ctrl Pts',(2.94022297261431,-0.138358799087583,
9.81460203739312));
#102978=CARTESIAN_POINT('Ctrl Pts',(2.93289413802449,-0.231291969470567,
9.80955664873596));
#102979=CARTESIAN_POINT('Ctrl Pts',(2.9255731444956,-0.324125711405322,
9.80451665809938));
#102980=CARTESIAN_POINT('Ctrl Pts',(2.91383212977308,-0.416713648807271,
9.79947666746279));
#102981=CARTESIAN_POINT('Ctrl Pts',(2.89770358849643,-0.508603886354484,
9.79443667682621));
#102982=CARTESIAN_POINT('Ctrl Pts',(2.88158666816288,-0.60042791511054,
9.78940031760572));
#102983=CARTESIAN_POINT('Ctrl Pts',(2.86108858138902,-0.691554806919165,
9.78436395838523));
#102984=CARTESIAN_POINT('Ctrl Pts',(2.83629353766523,-0.781538846250444,
9.77932759916474));
#102985=CARTESIAN_POINT('Ctrl Pts',(2.81150750467114,-0.871490184616759,
9.77429307020002));
#102986=CARTESIAN_POINT('Ctrl Pts',(2.78242773481146,-0.960299067741857,
9.7692585412353));
#102987=CARTESIAN_POINT('Ctrl Pts',(2.74918908565584,-1.04753203832188,
9.76422401227058));
#102988=CARTESIAN_POINT('Ctrl Pts',(2.71595321817689,-1.13475770854751,
9.75918990463561));
#102989=CARTESIAN_POINT('Ctrl Pts',(2.67855932175438,-1.22040731338701,
9.75415579700064));
#102990=CARTESIAN_POINT('Ctrl Pts',(2.63719107339544,-1.30406565877774,
9.74912168936567));
#102991=CARTESIAN_POINT('Ctrl Pts',(2.59581471565988,-1.38774040363078,
9.74408659489958));
#102992=CARTESIAN_POINT('Ctrl Pts',(2.55046265594753,-1.46942271578298,
9.7390515004335));
#102993=CARTESIAN_POINT('Ctrl Pts',(2.50136483402241,-1.54872139751347,
9.73401640596741));
#102994=CARTESIAN_POINT('Ctrl Pts',(2.45221307355703,-1.62810719624769,
9.72897577998007));
#102995=CARTESIAN_POINT('Ctrl Pts',(2.3993075709415,-1.70510375916307,9.72393515399273));
#102996=CARTESIAN_POINT('Ctrl Pts',(2.34292180653509,-1.7793485910474,9.71889452800539));
#102997=CARTESIAN_POINT('Ctrl Pts',(2.28650139303285,-1.85363904643832,
9.71385080454948));
#102998=CARTESIAN_POINT('Ctrl Pts',(2.22659674516041,-1.92517406412833,
9.70880708109357));
#102999=CARTESIAN_POINT('Ctrl Pts',(2.16352043872119,-1.9936256697875,9.70376335763766));
#103000=CARTESIAN_POINT('Ctrl Pts',(2.10034205190652,-2.06218805500877,
9.69871147160514));
#103001=CARTESIAN_POINT('Ctrl Pts',(2.03398207519571,-2.12765675453755,
9.69365958557261));
#103002=CARTESIAN_POINT('Ctrl Pts',(1.96478843880395,-2.18974208315554,
9.68860769954008));
#103003=CARTESIAN_POINT('Ctrl Pts',(1.92986324012209,-2.22107939320721,
9.68605778118624));
#103004=CARTESIAN_POINT('Ctrl Pts',(1.89421661775184,-2.25155538536574,
9.6835078628324));
#103005=CARTESIAN_POINT('Ctrl Pts',(1.85789613716139,-2.28113698482156,
9.68095794447856));
#103006=CARTESIAN_POINT('Ctrl Pts',(1.78593149385365,-2.33974934949027,
9.67590558939365));
#103007=CARTESIAN_POINT('Ctrl Pts',(1.71106137704479,-2.3950580630494,9.67085323430873));
#103008=CARTESIAN_POINT('Ctrl Pts',(1.6336218619111,-2.44676186260251,9.6658008792238));
#103009=CARTESIAN_POINT('Ctrl Pts',(1.55628912406838,-2.49839437049478,
9.66075549056665));
#103010=CARTESIAN_POINT('Ctrl Pts',(1.47639439417413,-2.54643159712274,
9.6557101019095));
#103011=CARTESIAN_POINT('Ctrl Pts',(1.39430693918763,-2.59061231359176,
9.65066471325235));
#103012=CARTESIAN_POINT('Ctrl Pts',(1.31230730890611,-2.63474576146911,
9.64562472261577));
#103013=CARTESIAN_POINT('Ctrl Pts',(1.22812000560482,-2.67503069093299,
9.64058473197918));
#103014=CARTESIAN_POINT('Ctrl Pts',(1.14214248417568,-2.71124962809421,
9.6355447413426));
#103015=CARTESIAN_POINT('Ctrl Pts',(1.05622691130505,-2.74744246877219,
9.6305083821221));
#103016=CARTESIAN_POINT('Ctrl Pts',(0.968524092363189,-2.7795749682352,
9.6254720229016));
#103017=CARTESIAN_POINT('Ctrl Pts',(0.879454301178353,-2.80747647045151,
9.6204356636811));
#103018=CARTESIAN_POINT('Ctrl Pts',(0.790416878712944,-2.8353678330247,
9.61540113471637));
#103019=CARTESIAN_POINT('Ctrl Pts',(0.700013894391332,-2.85903112025962,
9.61036660575163));
#103020=CARTESIAN_POINT('Ctrl Pts',(0.608682753724642,-2.8783448899182,
9.6053320767869));
#103021=CARTESIAN_POINT('Ctrl Pts',(0.517359256380052,-2.89765704324568,
9.60029796915191));
#103022=CARTESIAN_POINT('Ctrl Pts',(0.425108191794256,-2.91262031099064,
9.59526386151691));
#103023=CARTESIAN_POINT('Ctrl Pts',(0.332378058922914,-2.92316418046381,
9.59022975388192));
#103024=CARTESIAN_POINT('Ctrl Pts',(0.239629748255843,-2.93371011684122,
9.58519465941582));
#103025=CARTESIAN_POINT('Ctrl Pts',(0.14640262420569,-2.93983488459261,
9.58015956494972));
#103026=CARTESIAN_POINT('Ctrl Pts',(0.0531500751266599,-2.94151985706608,
9.57512447048362));
#103027=CARTESIAN_POINT('Ctrl Pts',(-0.040204920581921,-2.94320668063908,
9.57008384449625));
#103028=CARTESIAN_POINT('Ctrl Pts',(-0.13358495222081,-2.94044396478311,
9.5650432185089));
#103029=CARTESIAN_POINT('Ctrl Pts',(-0.226537172506329,-2.93326522999078,
9.56000259252154));
#103030=CARTESIAN_POINT('Ctrl Pts',(-0.319546512003089,-2.92608208386036,
9.55495886906561));
#103031=CARTESIAN_POINT('Ctrl Pts',(-0.412127076320044,-2.91447757166104,
9.54991514560968));
#103032=CARTESIAN_POINT('Ctrl Pts',(-0.503833857938221,-2.89853677630543,
9.54487142215376));
#103033=CARTESIAN_POINT('Ctrl Pts',(-0.595689054440318,-2.88257018295266,
9.53981953612121));
#103034=CARTESIAN_POINT('Ctrl Pts',(-0.686667212163074,-2.86225339323529,
9.53476765008867));
#103035=CARTESIAN_POINT('Ctrl Pts',(-0.776336357326798,-2.83772194908038,
9.52971576405613));
#103036=CARTESIAN_POINT('Ctrl Pts',(-0.821596483456769,-2.82533980520498,
9.52716584570228));
#103037=CARTESIAN_POINT('Ctrl Pts',(-0.866523395126456,-2.81188468007406,
9.52461592734843));
#103038=CARTESIAN_POINT('Ctrl Pts',(-0.911063524573254,-2.79737863976119,
9.52206600899458));
#103039=CARTESIAN_POINT('Ctrl Pts',(-0.999314408823774,-2.76863667379735,
9.51701365390965));
#103040=CARTESIAN_POINT('Ctrl Pts',(-1.08636219212492,-2.73566287194053,
9.51196129882473));
#103041=CARTESIAN_POINT('Ctrl Pts',(-1.17177159054851,-2.69857653950808,
9.5069089437398));
#103042=CARTESIAN_POINT('Ctrl Pts',(-1.25706322242659,-2.66154134347674,
9.50186355508265));
#103043=CARTESIAN_POINT('Ctrl Pts',(-1.34072055456809,-2.62040506039286,
9.49681816642549));
#103044=CARTESIAN_POINT('Ctrl Pts',(-1.42232397497759,-2.57533658192555,
9.49177277776833));
#103045=CARTESIAN_POINT('Ctrl Pts',(-1.50384008854676,-2.53031632185929,
9.48673278713175));
#103046=CARTESIAN_POINT('Ctrl Pts',(-1.58330627139328,-2.48137244213095,
9.48169279649516));
#103047=CARTESIAN_POINT('Ctrl Pts',(-1.66032442179078,-2.42872123027842,
9.47665280585858));
#103048=CARTESIAN_POINT('Ctrl Pts',(-1.73728707903936,-2.37610795469838,
9.47161644663809));
#103049=CARTESIAN_POINT('Ctrl Pts',(-1.81180484407345,-2.31979290638618,
9.4665800874176));
#103050=CARTESIAN_POINT('Ctrl Pts',(-1.88350660834158,-2.26003691481657,
9.46154372819711));
#103051=CARTESIAN_POINT('Ctrl Pts',(-1.95518231557898,-2.20030263908234,
9.45650919923238));
#103052=CARTESIAN_POINT('Ctrl Pts',(-2.02404371414397,-2.13713018840411,
9.45147467026765));
#103053=CARTESIAN_POINT('Ctrl Pts',(-2.08975178336914,-2.07082145147898,
9.44644014130293));
#103054=CARTESIAN_POINT('Ctrl Pts',(-2.15545435361622,-2.00451826380062,
9.44140603366795));
#103055=CARTESIAN_POINT('Ctrl Pts',(-2.21800380665003,-1.93507962740859,
9.43637192603297));
#103056=CARTESIAN_POINT('Ctrl Pts',(-2.27709792277764,-1.86284434402924,
9.43133781839799));
#103057=CARTESIAN_POINT('Ctrl Pts',(-2.3362036230661,-1.7905949004391,9.4263027239319));
#103058=CARTESIAN_POINT('Ctrl Pts',(-2.39185236025071,-1.71554806513985,
9.4212676294658));
#103059=CARTESIAN_POINT('Ctrl Pts',(-2.44378288029811,-1.63807485603127,
9.41623253499971));
#103060=CARTESIAN_POINT('Ctrl Pts',(-2.49577045086908,-1.56051653537099,
9.41119190901236));
#103061=CARTESIAN_POINT('Ctrl Pts',(-2.54403140282222,-1.48052688963884,
9.40615128302501));
#103062=CARTESIAN_POINT('Ctrl Pts',(-2.58834860890672,-1.39850472962041,
9.40111065703766));
#103063=CARTESIAN_POINT('Ctrl Pts',(-2.63269304794863,-1.31643216692123,
9.39606693358174));
#103064=CARTESIAN_POINT('Ctrl Pts',(-2.67308872434821,-1.23232500360651,
9.39102321012582));
#103065=CARTESIAN_POINT('Ctrl Pts',(-2.70936609977634,-1.14660339149277,
9.38597948666991));
#103066=CARTESIAN_POINT('Ctrl Pts',(-2.7457021851752,-1.06074305067338,
9.38092760063737));
#103067=CARTESIAN_POINT('Ctrl Pts',(-2.77790651068688,-0.973263461366016,
9.37587571460483));
#103068=CARTESIAN_POINT('Ctrl Pts',(-2.80585901294174,-0.884601152776558,
9.3708238285723));
#103069=CARTESIAN_POINT('Ctrl Pts',(-2.81996792159021,-0.839849223198082,
9.36827391021845));
#103070=CARTESIAN_POINT('Ctrl Pts',(-2.83299440725562,-0.794796160531161,
9.36572399186461));
#103071=CARTESIAN_POINT('Ctrl Pts',(-2.8449280009364,-0.749498945621697,
9.36317407351076));
#103072=CARTESIAN_POINT('Ctrl Pts',(-2.8769063231013,-0.628116487805915,
9.35634108482397));
#103073=CARTESIAN_POINT('Ctrl Pts',(-2.90113079108199,-0.504612143223255,
9.34950809613718));
#103074=CARTESIAN_POINT('Ctrl Pts',(-2.91737508842437,-0.379850751533926,
9.34267510745039));
#103075=CARTESIAN_POINT('Ctrl Pts',(-2.93256699151605,-0.263172083803379,
9.33628479706833));
#103076=CARTESIAN_POINT('Ctrl Pts',(-2.94077959844473,-0.14539389336001,
9.32989448668627));
#103077=CARTESIAN_POINT('Ctrl Pts',(-2.9418738304784,-0.0272463859323058,
9.32350417630422));
#103078=CARTESIAN_POINT('Ctrl Pts',(-2.94194963161366,-0.0190619105047869,
9.32306149799949));
#103079=CARTESIAN_POINT('Ctrl Pts',(-2.94199129147202,-0.010875672699581,
9.32261881969475));
#103080=CARTESIAN_POINT('Ctrl Pts',(-2.94199877210839,-0.00268791977826042,
9.32217614139002));
#103081=CARTESIAN_POINT('',(-2.93737145535825,0.000822519638358221,8.3221761170896));
#103082=CARTESIAN_POINT('Ctrl Pts',(-2.94126103584025,-0.00268679640793773,
9.3221761170896));
#103083=CARTESIAN_POINT('Ctrl Pts',(-2.934746619203,0.723990958988464,9.28287812406869));
#103084=CARTESIAN_POINT('Ctrl Pts',(-2.2959122451109,2.44028323228705,9.19061615255315));
#103085=CARTESIAN_POINT('Ctrl Pts',(0.582625545836898,3.42906223071866,
9.04539020254303));
#103086=CARTESIAN_POINT('Ctrl Pts',(3.19799441672963,1.36775437099239,8.88649826705913));
#103087=CARTESIAN_POINT('Ctrl Pts',(2.88203120349949,-1.94725870157488,
8.72760633157527));
#103088=CARTESIAN_POINT('Ctrl Pts',(-0.0756472328928887,-3.47738375865513,
8.56871439609139));
#103089=CARTESIAN_POINT('Ctrl Pts',(-2.53228522578548,-2.06778972386557,
8.43357099126284));
#103090=CARTESIAN_POINT('Ctrl Pts',(-2.93601614403195,-0.541218415403109,
8.35139156492891));
#103091=CARTESIAN_POINT('Ctrl Pts',(-2.93737145535825,0.000822519638358221,
8.3221761170896));
#103092=CARTESIAN_POINT('',(-2.94199909588776,0.00230646821441294,7.3221761170896));
#103093=CARTESIAN_POINT('Ctrl Pts',(-2.93737145535825,0.000822519638358221,
8.3221761170896));
#103094=CARTESIAN_POINT('Ctrl Pts',(-2.93847315514246,0.441434480580057,
8.29842758643428));
#103095=CARTESIAN_POINT('Ctrl Pts',(-2.63857366541807,1.86327470776546,
8.22171507728432));
#103096=CARTESIAN_POINT('Ctrl Pts',(-0.432952847726418,3.45115518927333,
8.09203858963981));
#103097=CARTESIAN_POINT('Ctrl Pts',(2.66643443613374,2.2333937643423,7.9331466541559));
#103098=CARTESIAN_POINT('Ctrl Pts',(3.32172589169603,-1.03153158421828,
7.77425471867204));
#103099=CARTESIAN_POINT('Ctrl Pts',(0.932271043120299,-3.35093882530888,
7.61536278318816));
#103100=CARTESIAN_POINT('Ctrl Pts',(-2.1443156395293,-2.63763485171723,
7.46467029144031));
#103101=CARTESIAN_POINT('Ctrl Pts',(-2.93716327839541,-0.823293308472798,
7.36694177818707));
#103102=CARTESIAN_POINT('Ctrl Pts',(-2.94428241720801,0.00228748565644199,
7.32217724342845));
#103103=CARTESIAN_POINT('',(-2.9419992148765,-0.00214934084322361,6.3221761170896));
#103104=CARTESIAN_POINT('Ctrl Pts',(-2.94199909588776,0.00230646821441294,
7.3221761170896));
#103105=CARTESIAN_POINT('Ctrl Pts',(-2.94188064052067,0.1534013676358,7.31397704879987));
#103106=CARTESIAN_POINT('Ctrl Pts',(-2.93012005936685,0.304050427900592,
7.30577798051015));
#103107=CARTESIAN_POINT('Ctrl Pts',(-2.90693455819628,0.452874678431272,
7.29757891222043));
#103108=CARTESIAN_POINT('Ctrl Pts',(-2.89264740011975,0.544581800796651,
7.29252655713551));
#103109=CARTESIAN_POINT('Ctrl Pts',(-2.87399062726682,0.635776718490721,
7.2874742020506));
#103110=CARTESIAN_POINT('Ctrl Pts',(-2.85101253679382,0.72601068521369,
7.28242184696568));
#103111=CARTESIAN_POINT('Ctrl Pts',(-2.82806612960614,0.816120233046577,
7.27737645830853));
#103112=CARTESIAN_POINT('Ctrl Pts',(-2.80081035366142,0.9052710360974,7.27233106965139));
#103113=CARTESIAN_POINT('Ctrl Pts',(-2.76934495822611,0.993021904263771,
7.26728568099424));
#103114=CARTESIAN_POINT('Ctrl Pts',(-2.73791322736321,1.08067888848511,
7.26224569035767));
#103115=CARTESIAN_POINT('Ctrl Pts',(-2.70228097821773,1.16693849896334,
7.2572056997211));
#103116=CARTESIAN_POINT('Ctrl Pts',(-2.66259818166292,1.25137321491445,
7.25216570908452));
#103117=CARTESIAN_POINT('Ctrl Pts',(-2.62294397737271,1.33574709392993,
7.24712934986403));
#103118=CARTESIAN_POINT('Ctrl Pts',(-2.57924521502232,1.41829829102065,
7.24209299064354));
#103119=CARTESIAN_POINT('Ctrl Pts',(-2.5317001449129,1.49861882286591,7.23705663142306));
#103120=CARTESIAN_POINT('Ctrl Pts',(-2.48417235308614,1.57891016554709,
7.23202210245833));
#103121=CARTESIAN_POINT('Ctrl Pts',(-2.43280125640771,1.65697207151327,
7.2269875734936));
#103122=CARTESIAN_POINT('Ctrl Pts',(-2.37783075974406,1.73242168019653,
7.22195304452886));
#103123=CARTESIAN_POINT('Ctrl Pts',(-2.32286486345237,1.80786497465153,
7.21691893689389));
#103124=CARTESIAN_POINT('Ctrl Pts',(-2.26430042782968,1.88069604754626,
7.21188482925891));
#103125=CARTESIAN_POINT('Ctrl Pts',(-2.20242367156039,1.95056247553121,
7.20685072162393));
#103126=CARTESIAN_POINT('Ctrl Pts',(-2.14053478565207,2.0204425993626,7.20181562715784));
#103127=CARTESIAN_POINT('Ctrl Pts',(-2.07533258435519,2.08735659180591,
7.19678053269174));
#103128=CARTESIAN_POINT('Ctrl Pts',(-2.00714162828726,2.15098732771636,
7.19174543822565));
#103129=CARTESIAN_POINT('Ctrl Pts',(-1.93887575808903,2.21468796792961,
7.1867048122383));
#103130=CARTESIAN_POINT('Ctrl Pts',(-1.86761490432089,2.27509784814801,
7.18166418625095));
#103131=CARTESIAN_POINT('Ctrl Pts',(-1.79371810752436,2.33193896805625,
7.1766235602636));
#103132=CARTESIAN_POINT('Ctrl Pts',(-1.71977590108904,2.38881501687664,
7.17157983680768));
#103133=CARTESIAN_POINT('Ctrl Pts',(-1.64319489128419,2.44211768594572,
7.16653611335176));
#103134=CARTESIAN_POINT('Ctrl Pts',(-1.56436278205414,2.49161254735238,
7.16149238989584));
#103135=CARTESIAN_POINT('Ctrl Pts',(-1.48540309383668,2.54118750942313,
7.15644050386331));
#103136=CARTESIAN_POINT('Ctrl Pts',(-1.40418541977465,2.58694214358168,
7.15138861783078));
#103137=CARTESIAN_POINT('Ctrl Pts',(-1.32112152825515,2.62868824845792,
7.14633673179825));
#103138=CARTESIAN_POINT('Ctrl Pts',(-1.2791953762858,2.64975942036129,7.14378681344435));
#103139=CARTESIAN_POINT('Ctrl Pts',(-1.23679917931604,2.66981011279453,
7.14123689509045));
#103140=CARTESIAN_POINT('Ctrl Pts',(-1.1939875166179,2.68882089588738,7.13868697673655));
#103141=CARTESIAN_POINT('Ctrl Pts',(-1.10916138036285,2.72648846531395,
7.13363462165162));
#103142=CARTESIAN_POINT('Ctrl Pts',(-1.02239880566903,2.76020557994489,
7.1285822665667));
#103143=CARTESIAN_POINT('Ctrl Pts',(-0.934103160531709,2.78976975492328,
7.12352991148177));
#103144=CARTESIAN_POINT('Ctrl Pts',(-0.845929261634393,2.8192931654094,
7.11848452282463));
#103145=CARTESIAN_POINT('Ctrl Pts',(-0.756226910426811,2.84467487525731,
7.11343913416748));
#103146=CARTESIAN_POINT('Ctrl Pts',(-0.665420994541296,2.86575974220165,
7.10839374551033));
#103147=CARTESIAN_POINT('Ctrl Pts',(-0.574712231171534,2.8868220506172,
7.10335375487374));
#103148=CARTESIAN_POINT('Ctrl Pts',(-0.482902680340056,2.90359655374513,
7.09831376423715));
#103149=CARTESIAN_POINT('Ctrl Pts',(-0.390432944213572,2.91597772900835,
7.09327377360056));
#103150=CARTESIAN_POINT('Ctrl Pts',(-0.298029834418809,2.92834998338217,
7.08823741438007));
#103151=CARTESIAN_POINT('Ctrl Pts',(-0.204967923849687,2.93633514294952,
7.08320105515958));
#103152=CARTESIAN_POINT('Ctrl Pts',(-0.111697544516788,2.93987885099861,
7.07816469593908));
#103153=CARTESIAN_POINT('Ctrl Pts',(-0.0184610604327648,2.94342127123407,
7.07313016697435));
#103154=CARTESIAN_POINT('Ctrl Pts',(0.0749832984381998,2.94252542961131,
7.06809563800962));
#103155=CARTESIAN_POINT('Ctrl Pts',(0.168181586974739,2.93718895439205,
7.06306110904489));
#103156=CARTESIAN_POINT('Ctrl Pts',(0.261372075931218,2.93185292577182,
7.05802700140991));
#103157=CARTESIAN_POINT('Ctrl Pts',(0.354316091994384,2.92207702801956,
7.05299289377493));
#103158=CARTESIAN_POINT('Ctrl Pts',(0.446562353806051,2.90791094501933,
7.04795878613995));
#103159=CARTESIAN_POINT('Ctrl Pts',(0.538826698560719,2.89374208505593,
7.04292369167385));
#103160=CARTESIAN_POINT('Ctrl Pts',(0.630392578408343,2.87518139847378,
7.03788859720775));
#103161=CARTESIAN_POINT('Ctrl Pts',(0.720817613325796,2.85232991926237,
7.03285350274166));
#103162=CARTESIAN_POINT('Ctrl Pts',(0.811341988584582,2.82945333556804,
7.02781287675431));
#103163=CARTESIAN_POINT('Ctrl Pts',(0.900722585767078,2.80227665889332,
7.02277225076695));
#103164=CARTESIAN_POINT('Ctrl Pts',(0.988531234777763,2.77095109986964,
7.0177316247796));
#103165=CARTESIAN_POINT('Ctrl Pts',(1.07639384227117,2.73960629126571,7.01268790132368));
#103166=CARTESIAN_POINT('Ctrl Pts',(1.16268216802116,2.70410769366106,7.00764417786776));
#103167=CARTESIAN_POINT('Ctrl Pts',(1.24698914115239,2.6646542143115,7.00260045441184));
#103168=CARTESIAN_POINT('Ctrl Pts',(1.33143255358951,2.6251368849014,6.9975485683793));
#103169=CARTESIAN_POINT('Ctrl Pts',(1.41388781949333,2.58165210306019,6.99249668234676));
#103170=CARTESIAN_POINT('Ctrl Pts',(1.49397368943538,2.5344440446131,6.98744479631423));
#103171=CARTESIAN_POINT('Ctrl Pts',(1.53439669746323,2.5106159744808,6.98489487796038));
#103172=CARTESIAN_POINT('Ctrl Pts',(1.57421653361987,2.48584000965761,6.98234495960653));
#103173=CARTESIAN_POINT('Ctrl Pts',(1.61338730044221,2.46015150321516,6.97979504125269));
#103174=CARTESIAN_POINT('Ctrl Pts',(1.69099944148848,2.40925283190953,6.97474268616776));
#103175=CARTESIAN_POINT('Ctrl Pts',(1.76633987464382,2.35458650481048,6.96969033108284));
#103176=CARTESIAN_POINT('Ctrl Pts',(1.83901989453574,2.29638189931504,6.96463797599791));
#103177=CARTESIAN_POINT('Ctrl Pts',(1.91159969975537,2.23825754910124,6.95959258734076));
#103178=CARTESIAN_POINT('Ctrl Pts',(1.98152603736183,2.176604890473,6.95454719868361));
#103179=CARTESIAN_POINT('Ctrl Pts',(2.04843834005712,2.11169703484757,6.94950181002646));
#103180=CARTESIAN_POINT('Ctrl Pts',(2.11527905382032,2.0468586236125,6.94446181938987));
#103181=CARTESIAN_POINT('Ctrl Pts',(2.17911182508806,1.97877224544958,6.93942182875328));
#103182=CARTESIAN_POINT('Ctrl Pts',(2.23960928329026,1.90775109964588,6.93438183811669));
#103183=CARTESIAN_POINT('Ctrl Pts',(2.30006315183939,1.83678112602691,6.9293454788962));
#103184=CARTESIAN_POINT('Ctrl Pts',(2.35718619670429,1.76288092496186,6.9243091196757));
#103185=CARTESIAN_POINT('Ctrl Pts',(2.41068878558327,1.68639959056655,6.91927276045521));
#103186=CARTESIAN_POINT('Ctrl Pts',(2.46417193116656,1.60994605013843,6.91423823149048));
#103187=CARTESIAN_POINT('Ctrl Pts',(2.51403698016615,1.53091360347701,6.90920370252574));
#103188=CARTESIAN_POINT('Ctrl Pts',(2.56003604045838,1.44968254164633,6.90416917356101));
#103189=CARTESIAN_POINT('Ctrl Pts',(2.60603125118043,1.3684582778822,6.89913506592603));
#103190=CARTESIAN_POINT('Ctrl Pts',(2.64816089772338,1.28503615143493,6.89410095829104));
#103191=CARTESIAN_POINT('Ctrl Pts',(2.68622228766056,1.19982241239096,6.88906685065606));
#103192=CARTESIAN_POINT('Ctrl Pts',(2.72429113873418,1.11459196898242,6.88403175618996));
#103193=CARTESIAN_POINT('Ctrl Pts',(2.75828996854704,1.02756962122026,6.87899666172386));
#103194=CARTESIAN_POINT('Ctrl Pts',(2.7880640701717,0.939181952881126,6.87396156725776));
#103195=CARTESIAN_POINT('Ctrl Pts',(2.81787088142616,0.850697182438061,
6.8689209412704));
#103196=CARTESIAN_POINT('Ctrl Pts',(2.84344355796929,0.76084451902619,6.86388031528305));
#103197=CARTESIAN_POINT('Ctrl Pts',(2.86467726760925,0.67006578217577,6.8588396892957));
#103198=CARTESIAN_POINT('Ctrl Pts',(2.8859240253802,0.579231261721361,6.85379596583977));
#103199=CARTESIAN_POINT('Ctrl Pts',(2.90282642775214,0.487469971480362,
6.84875224238385));
#103200=CARTESIAN_POINT('Ctrl Pts',(2.91533116449869,0.395231832349964,
6.84370851892793));
#103201=CARTESIAN_POINT('Ctrl Pts',(2.92785613845147,0.302844418406204,
6.83865663289539));
#103202=CARTESIAN_POINT('Ctrl Pts',(2.93596919993952,0.20997905693951,6.83360474686285));
#103203=CARTESIAN_POINT('Ctrl Pts',(2.93966907772781,0.117088485560753,
6.82855286083031));
#103204=CARTESIAN_POINT('Ctrl Pts',(2.94153657557289,0.0702023580171901,
6.82600294247648));
#103205=CARTESIAN_POINT('Ctrl Pts',(2.94228056151857,0.0233097757748152,
6.82345302412264));
#103206=CARTESIAN_POINT('Ctrl Pts',(2.94190589024871,-0.0235315303354603,
6.8209031057688));
#103207=CARTESIAN_POINT('Ctrl Pts',(2.94116352440293,-0.116341918069838,
6.81585075068388));
#103208=CARTESIAN_POINT('Ctrl Pts',(2.93602358759243,-0.209283669915334,
6.81079839559896));
#103209=CARTESIAN_POINT('Ctrl Pts',(2.92646833053807,-0.301905797158144,
6.80574604051404));
#103210=CARTESIAN_POINT('Ctrl Pts',(2.91692624872714,-0.39440021260147,
6.80070065185689));
#103211=CARTESIAN_POINT('Ctrl Pts',(2.90298098961361,-0.48657544113512,
6.79565526319974));
#103212=CARTESIAN_POINT('Ctrl Pts',(2.88466680790186,-0.577980455888684,
6.79060987454259));
#103213=CARTESIAN_POINT('Ctrl Pts',(2.86637222038517,-0.669287677155403,
6.785569883906));
#103214=CARTESIAN_POINT('Ctrl Pts',(2.84371808791363,-0.759825889314803,
6.78052989326942));
#103215=CARTESIAN_POINT('Ctrl Pts',(2.81679034453784,-0.849150254618343,
6.77548990263283));
#103216=CARTESIAN_POINT('Ctrl Pts',(2.78988200315061,-0.938410259894014,
6.77045354341234));
#103217=CARTESIAN_POINT('Ctrl Pts',(2.75870629910473,-1.02645773259668,
6.76541718419185));
#103218=CARTESIAN_POINT('Ctrl Pts',(2.72339978133985,-1.11286011295133,
6.76038082497136));
#103219=CARTESIAN_POINT('Ctrl Pts',(2.68810609426371,-1.19923109394634,
6.75534629600663));
#103220=CARTESIAN_POINT('Ctrl Pts',(2.6486847435846,-1.28395775945165,6.7503117670419));
#103221=CARTESIAN_POINT('Ctrl Pts',(2.60532111200398,-1.36662573638372,
6.74527723807717));
#103222=CARTESIAN_POINT('Ctrl Pts',(2.56196110943974,-1.44928679499666,
6.74024313044219));
#103223=CARTESIAN_POINT('Ctrl Pts',(2.5146596884601,-1.52988911426925,6.73520902280721));
#103224=CARTESIAN_POINT('Ctrl Pts',(2.46364853664272,-1.60804225314454,
6.73017491517223));
#103225=CARTESIAN_POINT('Ctrl Pts',(2.41262738515996,-1.68621071230196,
6.72513982070614));
#103226=CARTESIAN_POINT('Ctrl Pts',(2.35789530169561,-1.76192866577616,
6.72010472624004));
#103227=CARTESIAN_POINT('Ctrl Pts',(2.29972705922584,-1.83483499341615,
6.71506963177394));
#103228=CARTESIAN_POINT('Ctrl Pts',(2.24149491351219,-1.90782141546228,
6.71002900578659));
#103229=CARTESIAN_POINT('Ctrl Pts',(2.17981935106033,-1.97798969821184,
6.70498837979924));
#103230=CARTESIAN_POINT('Ctrl Pts',(2.11501496842135,-2.04501239198046,
6.69994775381189));
#103231=CARTESIAN_POINT('Ctrl Pts',(2.05017076343912,-2.11207627124624,
6.69490403035597));
#103232=CARTESIAN_POINT('Ctrl Pts',(1.98219423402991,-2.1759904092918,6.68986030690005));
#103233=CARTESIAN_POINT('Ctrl Pts',(1.91143469560998,-2.23646627616389,
6.68481658344413));
#103234=CARTESIAN_POINT('Ctrl Pts',(1.84056064255445,-2.29704001495561,
6.6797646974116));
#103235=CARTESIAN_POINT('Ctrl Pts',(1.76689493960156,-2.3541641021299,6.67471281137906));
#103236=CARTESIAN_POINT('Ctrl Pts',(1.69081745894377,-2.40759222471974,
6.66966092534653));
#103237=CARTESIAN_POINT('Ctrl Pts',(1.65241766864856,-2.4345598462232,6.66711100699267));
#103238=CARTESIAN_POINT('Ctrl Pts',(1.61340385513976,-2.46058656595473,
6.66456108863881));
#103239=CARTESIAN_POINT('Ctrl Pts',(1.57382717536845,-2.48564519231361,
6.66201117028495));
#103240=CARTESIAN_POINT('Ctrl Pts',(1.49541076686486,-2.53529583234839,
6.65695881520003));
#103241=CARTESIAN_POINT('Ctrl Pts',(1.4145018071766,-2.58132113439736,6.6519064601151));
#103242=CARTESIAN_POINT('Ctrl Pts',(1.3314697723869,-2.62346188179283,6.64685410503018));
#103243=CARTESIAN_POINT('Ctrl Pts',(1.24855222612056,-2.66554452351914,
6.64180871637303));
#103244=CARTESIAN_POINT('Ctrl Pts',(1.1635178145737,-2.7037530547636,6.63676332771588));
#103245=CARTESIAN_POINT('Ctrl Pts',(1.07676421605117,-2.73787195154042,
6.63171793905872));
#103246=CARTESIAN_POINT('Ctrl Pts',(0.990103434502904,-2.77195434478517,
6.62667794842214));
#103247=CARTESIAN_POINT('Ctrl Pts',(0.901727533154306,-2.80195563875512,
6.62163795778556));
#103248=CARTESIAN_POINT('Ctrl Pts',(0.81205698217149,-2.8277071025314,6.61659796714897));
#103249=CARTESIAN_POINT('Ctrl Pts',(0.722451040650323,-2.85344001185259,
6.61156160792848));
#103250=CARTESIAN_POINT('Ctrl Pts',(0.631552729364438,-2.87492905504814,
6.60652524870799));
#103251=CARTESIAN_POINT('Ctrl Pts',(0.539799615584686,-2.89205469779094,
6.6014888894875));
#103252=CARTESIAN_POINT('Ctrl Pts',(0.448079845666546,-2.90917411692957,
6.59645436052277));
#103253=CARTESIAN_POINT('Ctrl Pts',(0.355506326638361,-2.92193320434845,
6.59141983155803));
#103254=CARTESIAN_POINT('Ctrl Pts',(0.262527791320864,-2.93026332584363,
6.5863853025933));
#103255=CARTESIAN_POINT('Ctrl Pts',(0.169557037192701,-2.93859275020746,
6.58135119495831));
#103256=CARTESIAN_POINT('Ctrl Pts',(0.0761817766508294,-2.94249390613339,
6.57631708732333));
#103257=CARTESIAN_POINT('Ctrl Pts',(-0.0171442912079515,-2.94195004602032,
6.57128297968835));
#103258=CARTESIAN_POINT('Ctrl Pts',(-0.110488653683019,-2.9414060792949,
6.56624788522225));
#103259=CARTESIAN_POINT('Ctrl Pts',(-0.203783360120329,-2.93641536897968,
6.56121279075615));
#103260=CARTESIAN_POINT('Ctrl Pts',(-0.296576018880584,-2.92701326697112,
6.55617769629006));
#103261=CARTESIAN_POINT('Ctrl Pts',(-0.389470619037941,-2.91760083587589,
6.5511370703027));
#103262=CARTESIAN_POINT('Ctrl Pts',(-0.481861627908431,-2.90376738411304,
6.54609644431535));
#103263=CARTESIAN_POINT('Ctrl Pts',(-0.573303384354947,-2.88559997738549,
6.54105581832799));
#103264=CARTESIAN_POINT('Ctrl Pts',(-0.664801331831481,-2.86742140677248,
6.53601209487207));
#103265=CARTESIAN_POINT('Ctrl Pts',(-0.755348434826439,-2.84490368637615,
6.53096837141616));
#103266=CARTESIAN_POINT('Ctrl Pts',(-0.844512940296811,-2.81818414828968,
6.52592464796024));
#103267=CARTESIAN_POINT('Ctrl Pts',(-0.933821746324855,-2.79142136828508,
6.5208727619277));
#103268=CARTESIAN_POINT('Ctrl Pts',(-1.02174306938939,-2.76044334256319,
6.51582087589516));
#103269=CARTESIAN_POINT('Ctrl Pts',(-1.10786409070903,-2.72543595714841,
6.51076898986263));
#103270=CARTESIAN_POINT('Ctrl Pts',(-1.15133331616283,-2.70776612572019,
6.50821907150878));
#103271=CARTESIAN_POINT('Ctrl Pts',(-1.19434425278957,-2.68907048144247,
6.50566915315492));
#103272=CARTESIAN_POINT('Ctrl Pts',(-1.23684633263854,-2.66937729619449,
6.50311923480107));
#103273=CARTESIAN_POINT('Ctrl Pts',(-1.32105906788969,-2.63035762935858,
6.49806687971615));
#103274=CARTESIAN_POINT('Ctrl Pts',(-1.40357462284592,-2.5872789643746,
6.49301452463123));
#103275=CARTESIAN_POINT('Ctrl Pts',(-1.48397496366263,-2.54031145870393,
6.4879621695463));
#103276=CARTESIAN_POINT('Ctrl Pts',(-1.56426444466102,-2.49340871406652,
6.48291678088914));
#103277=CARTESIAN_POINT('Ctrl Pts',(-1.64244412683902,-2.44262800610038,
6.47787139223199));
#103278=CARTESIAN_POINT('Ctrl Pts',(-1.71811742649312,-2.38818686638643,
6.47282600357483));
#103279=CARTESIAN_POINT('Ctrl Pts',(-1.79370976389519,-2.33380397280811,
6.46778601293824));
#103280=CARTESIAN_POINT('Ctrl Pts',(-1.86680069010308,-2.27576868970264,
6.46274602230166));
#103281=CARTESIAN_POINT('Ctrl Pts',(-1.9370206084162,-2.21434305440032,
6.45770603166507));
#103282=CARTESIAN_POINT('Ctrl Pts',(-2.00718993184539,-2.15296167752158,
6.45266967244457));
#103283=CARTESIAN_POINT('Ctrl Pts',(-2.07449202565071,-2.08819509554047,
6.44763331322408));
#103284=CARTESIAN_POINT('Ctrl Pts',(-2.13858938528684,-2.0203463666259,
6.44259695400358));
#103285=CARTESIAN_POINT('Ctrl Pts',(-2.20266345139744,-1.95252229451635,
6.43756242503885));
#103286=CARTESIAN_POINT('Ctrl Pts',(-2.26353479223544,-1.88161862323202,
6.43252789607412));
#103287=CARTESIAN_POINT('Ctrl Pts',(-2.32090264043655,-1.80797536864158,
6.42749336710939));
#103288=CARTESIAN_POINT('Ctrl Pts',(-2.37826568763615,-1.73433827710915,
6.42245925947441));
#103289=CARTESIAN_POINT('Ctrl Pts',(-2.43212555229379,-1.65796240868285,
6.41742515183943));
#103290=CARTESIAN_POINT('Ctrl Pts',(-2.48222239153612,-1.57922006033254,
6.41239104420445));
#103291=CARTESIAN_POINT('Ctrl Pts',(-2.53232905121202,-1.500462276198,6.40735594973836));
#103292=CARTESIAN_POINT('Ctrl Pts',(-2.57867098233763,-1.41933746582406,
6.40232085527227));
#103293=CARTESIAN_POINT('Ctrl Pts',(-2.62103284391699,-1.33624504904917,
6.39728576080618));
#103294=CARTESIAN_POINT('Ctrl Pts',(-2.6634412439555,-1.25306134749833,
6.39224513481882));
#103295=CARTESIAN_POINT('Ctrl Pts',(-2.70186064439241,-1.1679061211299,
6.38720450883146));
#103296=CARTESIAN_POINT('Ctrl Pts',(-2.73612281952669,-1.08120114523864,
6.38216388284411));
#103297=CARTESIAN_POINT('Ctrl Pts',(-2.77040604879409,-0.994442889072623,
6.37712015938818));
#103298=CARTESIAN_POINT('Ctrl Pts',(-2.80052682370888,-0.906133407638423,
6.37207643593226));
#103299=CARTESIAN_POINT('Ctrl Pts',(-2.82636670524513,-0.816710014314636,
6.36703271247633));
#103300=CARTESIAN_POINT('Ctrl Pts',(-2.85224840509566,-0.727141901458713,
6.3619808264438));
#103301=CARTESIAN_POINT('Ctrl Pts',(-2.87383527787349,-0.636456709444174,
6.35692894041126));
#103302=CARTESIAN_POINT('Ctrl Pts',(-2.89105995440951,-0.545102137227228,
6.35187705437872));
#103303=CARTESIAN_POINT('Ctrl Pts',(-2.89975403787761,-0.49899129883871,
6.34932713602488));
#103304=CARTESIAN_POINT('Ctrl Pts',(-2.90733759523971,-0.452710012748207,
6.34677721767104));
#103305=CARTESIAN_POINT('Ctrl Pts',(-2.91380699892608,-0.40631609986484,
6.3442272993172));
#103306=CARTESIAN_POINT('Ctrl Pts',(-2.93245570054395,-0.27258101697472,
6.33687690524133));
#103307=CARTESIAN_POINT('Ctrl Pts',(-2.9419003072094,-0.137533302805858,
6.32952651116546));
#103308=CARTESIAN_POINT('Ctrl Pts',(-2.9419992148765,-0.00214934084322361,
6.3221761170896));
#103309=CARTESIAN_POINT('',(-2.94170074019424,-0.00106841483045282,5.32217617144154));
#103310=CARTESIAN_POINT('Ctrl Pts',(-2.94471353758293,-0.00212782599804863,
6.32217484249879));
#103311=CARTESIAN_POINT('Ctrl Pts',(-2.93780032435234,0.838783439956008,
6.27656168294363));
#103312=CARTESIAN_POINT('Ctrl Pts',(-2.11923631689247,2.66785949385505,
6.17798454489385));
#103313=CARTESIAN_POINT('Ctrl Pts',(0.985754882321845,3.33559704112804,
6.02644342834946));
#103314=CARTESIAN_POINT('Ctrl Pts',(3.33780171542183,0.978263776969118,
5.86755149286558));
#103315=CARTESIAN_POINT('Ctrl Pts',(2.63036689099525,-2.27576148301134,
5.70865955738172));
#103316=CARTESIAN_POINT('Ctrl Pts',(-0.488103681415864,-3.44378790069809,
5.54976762189784));
#103317=CARTESIAN_POINT('Ctrl Pts',(-2.65377056339368,-1.83145342118466,
5.42094007970052));
#103318=CARTESIAN_POINT('Ctrl Pts',(-2.93890109085433,-0.425887727767073,
5.34507651599781));
#103319=CARTESIAN_POINT('Ctrl Pts',(-2.93752250330966,-0.0010809852794131,
5.32217693078973));
#103320=CARTESIAN_POINT('',(-2.94199880936505,0.00264682727074493,4.32217611708959));
#103321=CARTESIAN_POINT('Ctrl Pts',(-2.94199980632419,-0.00106751507401821,
5.32217611708959));
#103322=CARTESIAN_POINT('Ctrl Pts',(-2.9420345110113,0.0945762704193298,
5.31702819360726));
#103323=CARTESIAN_POINT('Ctrl Pts',(-2.93740083055662,0.190188226245283,
5.31188027012492));
#103324=CARTESIAN_POINT('Ctrl Pts',(-2.92813433093512,0.285295180469558,
5.30673234664258));
#103325=CARTESIAN_POINT('Ctrl Pts',(-2.91886212799877,0.380460670810617,
5.30158125473316));
#103326=CARTESIAN_POINT('Ctrl Pts',(-2.90495147051173,0.475120127456848,
5.29643016282373));
#103327=CARTESIAN_POINT('Ctrl Pts',(-2.88648955217386,0.568807581868541,
5.2912790709143));
#103328=CARTESIAN_POINT('Ctrl Pts',(-2.86799656128149,0.662652718081264,
5.28611930939746));
#103329=CARTESIAN_POINT('Ctrl Pts',(-2.84493708928312,0.755522175674526,
5.28095954788062));
#103330=CARTESIAN_POINT('Ctrl Pts',(-2.81744913705144,0.84696184101061,
5.27579978636378));
#103331=CARTESIAN_POINT('Ctrl Pts',(-2.78993722170672,0.938481220507241,
5.27063552673272));
#103332=CARTESIAN_POINT('Ctrl Pts',(-2.7579892716372,1.02856793235365,5.26547126710167));
#103333=CARTESIAN_POINT('Ctrl Pts',(-2.72179192390167,1.11678678492525,
5.26030700747062));
#103334=CARTESIAN_POINT('Ctrl Pts',(-2.68551790829933,1.20519248961893,
5.25513180966884));
#103335=CARTESIAN_POINT('Ctrl Pts',(-2.64497668398172,1.29172205155361,
5.24995661186705));
#103336=CARTESIAN_POINT('Ctrl Pts',(-2.60040169900902,1.37596330030674,
5.24478141406527));
#103337=CARTESIAN_POINT('Ctrl Pts',(-2.56365877865534,1.44540290853826,
5.24051552635355));
#103338=CARTESIAN_POINT('Ctrl Pts',(-2.52417597520646,1.51328808545775,
5.23624963864182));
#103339=CARTESIAN_POINT('Ctrl Pts',(-2.48210558902173,1.57940363585344,
5.23198375093009));
#103340=CARTESIAN_POINT('Ctrl Pts',(-2.43227902444048,1.6577083779861,5.22693139584518));
#103341=CARTESIAN_POINT('Ctrl Pts',(-2.37865392063076,1.73379343846384,
5.22187904076027));
#103342=CARTESIAN_POINT('Ctrl Pts',(-2.32145428796571,1.80726699435518,
5.21682668567535));
#103343=CARTESIAN_POINT('Ctrl Pts',(-2.26433352487776,1.8806392414092,5.2117812970182));
#103344=CARTESIAN_POINT('Ctrl Pts',(-2.20364829748771,1.95140679176675,
5.20673590836105));
#103345=CARTESIAN_POINT('Ctrl Pts',(-2.13966673299798,2.0192053564959,5.2016905197039));
#103346=CARTESIAN_POINT('Ctrl Pts',(-2.07575362186734,2.08693138408824,
5.19665052906732));
#103347=CARTESIAN_POINT('Ctrl Pts',(-2.00855148680339,2.15169441846654,
5.19161053843074));
#103348=CARTESIAN_POINT('Ctrl Pts',(-1.93836899559704,2.21316281301402,
5.18657054779416));
#103349=CARTESIAN_POINT('Ctrl Pts',(-1.86823707230764,2.27458691832899,
5.18153418857367));
#103350=CARTESIAN_POINT('Ctrl Pts',(-1.79512939437758,2.33272081033483,
5.17649782935319));
#103351=CARTESIAN_POINT('Ctrl Pts',(-1.71939103999525,2.38727008350209,
5.1714614701327));
#103352=CARTESIAN_POINT('Ctrl Pts',(-1.64368020957482,2.4417995329997,5.16642694116798));
#103353=CARTESIAN_POINT('Ctrl Pts',(-1.56534096203413,2.49274669221162,
5.16139241220325));
#103354=CARTESIAN_POINT('Ctrl Pts',(-1.48475014355556,2.53985846283051,
5.15635788323852));
#103355=CARTESIAN_POINT('Ctrl Pts',(-1.40416606956303,2.58696629075859,
5.15132377560356));
#103356=CARTESIAN_POINT('Ctrl Pts',(-1.32133118288554,2.63023914423385,
5.14628966796859));
#103357=CARTESIAN_POINT('Ctrl Pts',(-1.23664890784301,2.66946876339295,
5.14125556033363));
#103358=CARTESIAN_POINT('Ctrl Pts',(-1.15195003261822,2.70870607269532,
5.13622046586754));
#103359=CARTESIAN_POINT('Ctrl Pts',(-1.06540345303215,2.74389838720553,
5.13118537140146));
#103360=CARTESIAN_POINT('Ctrl Pts',(-0.977433585051243,2.77488514840054,
5.12615027693538));
#103361=CARTESIAN_POINT('Ctrl Pts',(-0.889367073959015,2.80590595144511,
5.12110965094803));
#103362=CARTESIAN_POINT('Ctrl Pts',(-0.799874572968278,2.83271183091539,
5.11606902496069));
#103363=CARTESIAN_POINT('Ctrl Pts',(-0.709396418217592,2.85519188879137,
5.11102839897334));
#103364=CARTESIAN_POINT('Ctrl Pts',(-0.61886266457064,2.87768576068036,
5.10598467551742));
#103365=CARTESIAN_POINT('Ctrl Pts',(-0.527342486780911,2.89584843256464,
5.1009409520615));
#103366=CARTESIAN_POINT('Ctrl Pts',(-0.435285030099101,2.90962041211077,
5.09589722860558));
#103367=CARTESIAN_POINT('Ctrl Pts',(-0.343078591013989,2.92341467972225,
5.09084534257305));
#103368=CARTESIAN_POINT('Ctrl Pts',(-0.250333578589815,2.93280402461145,
5.08579345654052));
#103369=CARTESIAN_POINT('Ctrl Pts',(-0.157502670145837,2.93778094978113,
5.080741570508));
#103370=CARTESIAN_POINT('Ctrl Pts',(-0.110646657217539,2.94029303195293,
5.07819165215408));
#103371=CARTESIAN_POINT('Ctrl Pts',(-0.0637687400751823,2.94168179722519,
5.07564173380016));
#103372=CARTESIAN_POINT('Ctrl Pts',(-0.016926710850602,2.94195130592941,
5.07309181544624));
#103373=CARTESIAN_POINT('Ctrl Pts',(0.075885109643817,2.94248530485926,
5.06803946036135));
#103374=CARTESIAN_POINT('Ctrl Pts',(0.168888755618728,2.93862395512216,
5.06298710527645));
#103375=CARTESIAN_POINT('Ctrl Pts',(0.261633525086621,2.93034330728513,
5.05793475019156));
#103376=CARTESIAN_POINT('Ctrl Pts',(0.354250413650165,2.92207407719963,
5.05288936153444));
#103377=CARTESIAN_POINT('Ctrl Pts',(0.446608696373017,2.90939769682623,
5.04784397287732));
#103378=CARTESIAN_POINT('Ctrl Pts',(0.538256917974871,2.89234221527332,
5.04279858422019));
#103379=CARTESIAN_POINT('Ctrl Pts',(0.629807085884844,2.87530498124234,
5.03775859358363));
#103380=CARTESIAN_POINT('Ctrl Pts',(0.720648268274743,2.85389803935472,
5.03271860294707));
#103381=CARTESIAN_POINT('Ctrl Pts',(0.810334487725388,2.82820119828891,
5.02767861231051));
#103382=CARTESIAN_POINT('Ctrl Pts',(0.899956086424732,2.80252287232147,
5.02264225309005));
#103383=CARTESIAN_POINT('Ctrl Pts',(0.988423950419802,2.77256091290418,
5.01760589386959));
#103384=CARTESIAN_POINT('Ctrl Pts',(1.0753036830665,2.7384459076607,5.01256953464914));
#103385=CARTESIAN_POINT('Ctrl Pts',(1.16215184287962,2.7043433001002,5.00753500568444));
#103386=CARTESIAN_POINT('Ctrl Pts',(1.24741260480997,2.66609080721475,5.00250047671975));
#103387=CARTESIAN_POINT('Ctrl Pts',(1.33066908564115,2.62386809586895,4.99746594775506));
#103388=CARTESIAN_POINT('Ctrl Pts',(1.41391859890251,2.58164891805815,4.99243184012011));
#103389=CARTESIAN_POINT('Ctrl Pts',(1.49516376844178,2.53546038349343,4.98739773248516));
#103390=CARTESIAN_POINT('Ctrl Pts',(1.57401100403843,2.48552878864155,4.98236362485022));
#103391=CARTESIAN_POINT('Ctrl Pts',(1.65287369598042,2.43558740574869,4.97732853038415));
#103392=CARTESIAN_POINT('Ctrl Pts',(1.72933714533686,2.38190174331353,4.97229343591808));
#103393=CARTESIAN_POINT('Ctrl Pts',(1.80303648752597,2.32474158233771,4.96725834145201));
#103394=CARTESIAN_POINT('Ctrl Pts',(1.87681679532157,2.26751862558971,4.96221771546469));
#103395=CARTESIAN_POINT('Ctrl Pts',(1.94782658290908,2.20681382368379,4.95717708947737));
#103396=CARTESIAN_POINT('Ctrl Pts',(2.01573410535022,2.14293724045478,4.95213646349006));
#103397=CARTESIAN_POINT('Ctrl Pts',(2.08368335701646,2.07902140501595,4.94709274003417));
#103398=CARTESIAN_POINT('Ctrl Pts',(2.14852623987871,2.01193022724544,4.94204901657828));
#103399=CARTESIAN_POINT('Ctrl Pts',(2.20996944760846,1.94200902177028,4.93700529312239));
#103400=CARTESIAN_POINT('Ctrl Pts',(2.27151209276674,1.87197465838672,4.93195340708989));
#103401=CARTESIAN_POINT('Ctrl Pts',(2.32964380225102,1.79910147072921,4.92690152105739));
#103402=CARTESIAN_POINT('Ctrl Pts',(2.38411306252143,1.72376590786415,4.92184963502488));
#103403=CARTESIAN_POINT('Ctrl Pts',(2.41160619391993,1.68574059746802,4.91929971667071));
#103404=CARTESIAN_POINT('Ctrl Pts',(2.43816695633939,1.64708838298131,4.91674979831653));
#103405=CARTESIAN_POINT('Ctrl Pts',(2.46376745725854,1.60786004258885,4.91419987996235));
#103406=CARTESIAN_POINT('Ctrl Pts',(2.51449175624882,1.53013382647908,4.90914752487733));
#103407=CARTESIAN_POINT('Ctrl Pts',(2.56162533671277,1.44986544055092,4.9040951697923));
#103408=CARTESIAN_POINT('Ctrl Pts',(2.60490392559348,1.36742076129759,4.89904281470728));
#103409=CARTESIAN_POINT('Ctrl Pts',(2.64812283989505,1.28508976069378,4.89399742605002));
#103410=CARTESIAN_POINT('Ctrl Pts',(2.68749712040228,1.20058881962297,4.88895203739277));
#103411=CARTESIAN_POINT('Ctrl Pts',(2.722805794782,1.1143126149791,4.88390664873551));
#103412=CARTESIAN_POINT('Ctrl Pts',(2.75807669269622,1.02812871654966,4.87886665809883));
#103413=CARTESIAN_POINT('Ctrl Pts',(2.7892904629384,0.940173738710766,4.87382666746214));
#103414=CARTESIAN_POINT('Ctrl Pts',(2.81627260839231,0.850865791543631,
4.86878667682545));
#103415=CARTESIAN_POINT('Ctrl Pts',(2.84323531265985,0.761622192574762,
4.86375031760486));
#103416=CARTESIAN_POINT('Ctrl Pts',(2.86597232429127,0.671027985947263,
4.85871395838427));
#103417=CARTESIAN_POINT('Ctrl Pts',(2.88435810299701,0.579519053763985,
4.85367759916368));
#103418=CARTESIAN_POINT('Ctrl Pts',(2.90273720015446,0.488043376704628,
4.84864307019884));
#103419=CARTESIAN_POINT('Ctrl Pts',(2.9167681183433,0.395654069573802,4.84360854123401));
#103420=CARTESIAN_POINT('Ctrl Pts',(2.92637605903953,0.302798878928364,
4.83857401226918));
#103421=CARTESIAN_POINT('Ctrl Pts',(2.93598319566624,0.209951459149804,
4.8335399046341));
#103422=CARTESIAN_POINT('Ctrl Pts',(2.94116804520858,0.116638675275587,
4.82850579699901));
#103423=CARTESIAN_POINT('Ctrl Pts',(2.94190762254467,0.023313953194666,
4.82347168936393));
#103424=CARTESIAN_POINT('Ctrl Pts',(2.94264734485937,-0.0700290632391486,
4.81843659489771));
#103425=CARTESIAN_POINT('Ctrl Pts',(2.93894006120845,-0.16338357832546,
4.81340150043149));
#103426=CARTESIAN_POINT('Ctrl Pts',(2.93081489902085,-0.256296757055925,
4.80836640596527));
#103427=CARTESIAN_POINT('Ctrl Pts',(2.92268081058422,-0.349312009585432,
4.80332577997782));
#103428=CARTESIAN_POINT('Ctrl Pts',(2.91011919431999,-0.441884514709381,
4.79828515399038));
#103429=CARTESIAN_POINT('Ctrl Pts',(2.89321097912903,-0.533567456135797,
4.79324452800293));
#103430=CARTESIAN_POINT('Ctrl Pts',(2.87629237382679,-0.625306736800511,
4.78820080454692));
#103431=CARTESIAN_POINT('Ctrl Pts',(2.85502195337702,-0.71615493329788,
4.7831570810909));
#103432=CARTESIAN_POINT('Ctrl Pts',(2.82953109957676,-0.805678444869855,
4.77811335763489));
#103433=CARTESIAN_POINT('Ctrl Pts',(2.80399899231585,-0.895346838001744,
4.77306147160227));
#103434=CARTESIAN_POINT('Ctrl Pts',(2.77423295776426,-0.983685845888612,
4.76800958556964));
#103435=CARTESIAN_POINT('Ctrl Pts',(2.74041318743611,-1.07028013254767,
4.76295769953702));
#103436=CARTESIAN_POINT('Ctrl Pts',(2.72334279976471,-1.11398823668486,
4.76040778118417));
#103437=CARTESIAN_POINT('Ctrl Pts',(2.70524039402295,-1.15725220193419,
4.75785786283133));
#103438=CARTESIAN_POINT('Ctrl Pts',(2.68613354402471,-1.2000210763421,4.75530794447849));
#103439=CARTESIAN_POINT('Ctrl Pts',(2.64827562961882,-1.28476243280432,
4.75025558939365));
#103440=CARTESIAN_POINT('Ctrl Pts',(2.60633576187254,-1.36786258731512,
4.74520323430881));
#103441=CARTESIAN_POINT('Ctrl Pts',(2.56047833350861,-1.44890120561512,
4.74015087922396));
#103442=CARTESIAN_POINT('Ctrl Pts',(2.51468413555046,-1.52982808400947,
4.73510549056689));
#103443=CARTESIAN_POINT('Ctrl Pts',(2.46498332777356,-1.60869869141865,
4.73006010190981));
#103444=CARTESIAN_POINT('Ctrl Pts',(2.41158796751508,-1.68511349022447,
4.72501471325273));
#103445=CARTESIAN_POINT('Ctrl Pts',(2.35824973452142,-1.76144653345404,
4.71997472261624));
#103446=CARTESIAN_POINT('Ctrl Pts',(2.3012250588703,-1.83532862834624,4.71493473197975));
#103447=CARTESIAN_POINT('Ctrl Pts',(2.24077087055533,-1.90638660970714,
4.70989474134326));
#103448=CARTESIAN_POINT('Ctrl Pts',(2.18036024071641,-1.97739339234278,
4.70485838212285));
#103449=CARTESIAN_POINT('Ctrl Pts',(2.11652529677877,-2.04557976857979,
4.69982202290243));
#103450=CARTESIAN_POINT('Ctrl Pts',(2.04956442701537,-2.11060409824134,
4.69478566368202));
#103451=CARTESIAN_POINT('Ctrl Pts',(1.98262789140132,-2.17560479750869,
4.68975113471736));
#103452=CARTESIAN_POINT('Ctrl Pts',(1.91256800510489,-2.23744542387134,
4.68471660575271));
#103453=CARTESIAN_POINT('Ctrl Pts',(1.8397206158004,-2.29582056263093,4.67968207678805));
#103454=CARTESIAN_POINT('Ctrl Pts',(1.76687932294954,-2.35419081609086,
4.67464796915315));
#103455=CARTESIAN_POINT('Ctrl Pts',(1.69125133769096,-2.40909588092382,
4.66961386151824));
#103456=CARTESIAN_POINT('Ctrl Pts',(1.61320534852639,-2.46027081913472,
4.66457975388334));
#103457=CARTESIAN_POINT('Ctrl Pts',(1.53514406008434,-2.51145578911777,
4.65954465941733));
#103458=CARTESIAN_POINT('Ctrl Pts',(1.4546641980517,-2.55890893701755,4.65450956495132));
#103459=CARTESIAN_POINT('Ctrl Pts',(1.37216218320771,-2.60240944952455,
4.64947447048531));
#103460=CARTESIAN_POINT('Ctrl Pts',(1.28956953219932,-2.64595775140506,
4.64443384449803));
#103461=CARTESIAN_POINT('Ctrl Pts',(1.20495068753058,-2.68554454256647,
4.63939321851076));
#103462=CARTESIAN_POINT('Ctrl Pts',(1.1187250712355,-2.72099581311496,4.63435259252348));
#103463=CARTESIAN_POINT('Ctrl Pts',(1.03244646923242,-2.75646886849666,
4.62930886906763));
#103464=CARTESIAN_POINT('Ctrl Pts',(0.944559548089188,-2.7878011950038,
4.62426514561178));
#103465=CARTESIAN_POINT('Ctrl Pts',(0.855499951102573,-2.81486835103589,
4.61922142215593));
#103466=CARTESIAN_POINT('Ctrl Pts',(0.766296223338374,-2.8419793115582,
4.61416953612346));
#103467=CARTESIAN_POINT('Ctrl Pts',(0.675916461150174,-2.86481121278395,
4.609117650091));
#103468=CARTESIAN_POINT('Ctrl Pts',(0.584807394724338,-2.88329053532171,
4.60406576405853));
#103469=CARTESIAN_POINT('Ctrl Pts',(0.538820474342438,-2.89261789611677,
4.60151584570389));
#103470=CARTESIAN_POINT('Ctrl Pts',(0.492647850825972,-2.90083717974908,
4.59896592734925));
#103471=CARTESIAN_POINT('Ctrl Pts',(0.446347289731649,-2.9079439638599,
4.59641600899461));
#103472=CARTESIAN_POINT('Ctrl Pts',(0.35460832293488,-2.92202519778373,
4.59136365390988));
#103473=CARTESIAN_POINT('Ctrl Pts',(0.26203775074848,-2.93178620956139,
4.58631129882515));
#103474=CARTESIAN_POINT('Ctrl Pts',(0.16907794671422,-2.93713749217412,
4.58125894374042));
#103475=CARTESIAN_POINT('Ctrl Pts',(0.0762463200841915,-2.94248139618358,
4.57621355508346));
#103476=CARTESIAN_POINT('Ctrl Pts',(-0.0169730322596317,-2.94342762814871,
4.57116816642649));
#103477=CARTESIAN_POINT('Ctrl Pts',(-0.11012939840714,-2.93993801220476,
4.56612277776953));
#103478=CARTESIAN_POINT('Ctrl Pts',(-0.203186097311192,-2.93645212977271,
4.56108278713312));
#103479=CARTESIAN_POINT('Ctrl Pts',(-0.296179502418778,-2.92853984913072,
4.55604279649672));
#103480=CARTESIAN_POINT('Ctrl Pts',(-0.388656762707934,-2.91621499907009,
4.55100280586031));
#103481=CARTESIAN_POINT('Ctrl Pts',(-0.481067391243812,-2.90389902931546,
4.54596644664001));
#103482=CARTESIAN_POINT('Ctrl Pts',(-0.57296217506985,-2.88717686806095,
4.54093008741971));
#103483=CARTESIAN_POINT('Ctrl Pts',(-0.663892304744306,-2.86611426982619,
4.53589372819941));
#103484=CARTESIAN_POINT('Ctrl Pts',(-0.754789389636509,-2.8450593259187,
4.53085919923488));
#103485=CARTESIAN_POINT('Ctrl Pts',(-0.844722084464464,-2.8196671787591,
4.52582467027034));
#103486=CARTESIAN_POINT('Ctrl Pts',(-0.933251738626908,-2.79005469343342,
4.5207901413058));
#103487=CARTESIAN_POINT('Ctrl Pts',(-1.02177398391817,-2.76044468631791,
4.51575603367101));
#103488=CARTESIAN_POINT('Ctrl Pts',(-1.10889300076054,-2.72661518436128,
4.51072192603622));
#103489=CARTESIAN_POINT('Ctrl Pts',(-1.19418637272005,-2.68873258380407,
4.50568781840143));
#103490=CARTESIAN_POINT('Ctrl Pts',(-1.27949646465428,-2.65084255715843,
4.50065272393553));
#103491=CARTESIAN_POINT('Ctrl Pts',(-1.36297979513366,-2.60889803463047,
4.49561762946964));
#103492=CARTESIAN_POINT('Ctrl Pts',(-1.44423601556269,-2.56311262556907,
4.49058253500374));
#103493=CARTESIAN_POINT('Ctrl Pts',(-1.52558150353447,-2.51727691696213,
4.48554190901659));
#103494=CARTESIAN_POINT('Ctrl Pts',(-1.60469460995704,-2.46759211748283,
4.48050128302944));
#103495=CARTESIAN_POINT('Ctrl Pts',(-1.68120186850992,-2.41431652384661,
4.47546065704229));
#103496=CARTESIAN_POINT('Ctrl Pts',(-1.75775614083244,-2.36100819231683,
4.47041693358656));
#103497=CARTESIAN_POINT('Ctrl Pts',(-1.83170102561651,-2.30410494455138,
4.46537321013084));
#103498=CARTESIAN_POINT('Ctrl Pts',(-1.90269593557739,-2.24390556323952,
4.46032948667512));
#103499=CARTESIAN_POINT('Ctrl Pts',(-1.97380574109052,-2.1836087574621,
4.45527760064277));
#103500=CARTESIAN_POINT('Ctrl Pts',(-2.04195571647358,-2.12000547152758,
4.45022571461044));
#103501=CARTESIAN_POINT('Ctrl Pts',(-2.10684207279745,-2.05343139166872,
4.44517382857809));
#103502=CARTESIAN_POINT('Ctrl Pts',(-2.13959318989923,-2.01982840316806,
4.44262391022231));
#103503=CARTESIAN_POINT('Ctrl Pts',(-2.17151347677769,-1.98546908022081,
4.44007399186653));
#103504=CARTESIAN_POINT('Ctrl Pts',(-2.202567924953,-1.95039958366696,4.43752407351075));
#103505=CARTESIAN_POINT('Ctrl Pts',(-2.26351815036058,-1.88156906676898,
4.43251937667381));
#103506=CARTESIAN_POINT('Ctrl Pts',(-2.32135890021934,-1.80974292607652,
4.42751467983687));
#103507=CARTESIAN_POINT('Ctrl Pts',(-2.37577747337919,-1.73523640953732,
4.42250998299993));
#103508=CARTESIAN_POINT('Ctrl Pts',(-2.43012647817473,-1.66082514166389,
4.41751168413619));
#103509=CARTESIAN_POINT('Ctrl Pts',(-2.48106172605355,-1.58374066173396,
4.41251338527245));
#103510=CARTESIAN_POINT('Ctrl Pts',(-2.52830867149839,-1.50433349415149,
4.40751508640872));
#103511=CARTESIAN_POINT('Ctrl Pts',(-2.57550903848734,-1.42500461021716,
4.4025217151237));
#103512=CARTESIAN_POINT('Ctrl Pts',(-2.6190280927908,-1.34335797234546,
4.39752834383869));
#103513=CARTESIAN_POINT('Ctrl Pts',(-2.65863353621515,-1.2597744719243,
4.39253497255368));
#103514=CARTESIAN_POINT('Ctrl Pts',(-2.69821151611528,-1.17624893064434,
4.38754506381223));
#103515=CARTESIAN_POINT('Ctrl Pts',(-2.73388108272753,-1.09078960304317,
4.38255515507078));
#103516=CARTESIAN_POINT('Ctrl Pts',(-2.76545562710603,-1.00380235828952,
4.37756524632933));
#103517=CARTESIAN_POINT('Ctrl Pts',(-2.79702472347893,-0.916830122683444,
4.37257619856787));
#103518=CARTESIAN_POINT('Ctrl Pts',(-2.82450003557403,-0.828330915147752,
4.3675871508064));
#103519=CARTESIAN_POINT('Ctrl Pts',(-2.8477432903,-0.738730094521212,4.36259810304494));
#103520=CARTESIAN_POINT('Ctrl Pts',(-2.87098353801618,-0.649140865668232,
4.35760970072301));
#103521=CARTESIAN_POINT('Ctrl Pts',(-2.88999270855973,-0.558450747278933,
4.35262129840107));
#103522=CARTESIAN_POINT('Ctrl Pts',(-2.90468299020389,-0.467098197834468,
4.34763289607914));
#103523=CARTESIAN_POINT('Ctrl Pts',(-2.91938238808987,-0.375688958399173,
4.34264139814047));
#103524=CARTESIAN_POINT('Ctrl Pts',(-2.92975747686044,-0.283616915626116,
4.33764990020179));
#103525=CARTESIAN_POINT('Ctrl Pts',(-2.9357720645064,-0.191327952123688,
4.33265840226312));
#103526=CARTESIAN_POINT('Ctrl Pts',(-2.93998233189044,-0.126724817908505,
4.32916430720527));
#103527=CARTESIAN_POINT('Ctrl Pts',(-2.9420569841351,-0.0620155351335664,
4.32567021214743));
#103528=CARTESIAN_POINT('Ctrl Pts',(-2.94199880936505,0.00264682727074493,
4.32217611708959));
#103529=CARTESIAN_POINT('',(-2.94245552567036,-0.000355218061749572,3.3221761170896));
#103530=CARTESIAN_POINT('Ctrl Pts',(-2.94080193791859,0.00265685637863251,
4.32217551672762));
#103531=CARTESIAN_POINT('Ctrl Pts',(-2.9431405362452,0.271157122569686,
4.3076610571607));
#103532=CARTESIAN_POINT('Ctrl Pts',(-2.78627811663743,1.51674327414858,
4.24018261909918));
#103533=CARTESIAN_POINT('Ctrl Pts',(-1.02407150506552,3.32403337258514,
4.119740202543));
#103534=CARTESIAN_POINT('Ctrl Pts',(2.23937444558007,2.66141360932405,3.96084826705914));
#103535=CARTESIAN_POINT('Ctrl Pts',(3.45017448606169,-0.440699812455072,
3.80195633157526));
#103536=CARTESIAN_POINT('Ctrl Pts',(1.49849021612704,-3.13886084204111,
3.6430643960914));
#103537=CARTESIAN_POINT('Ctrl Pts',(-1.82673380221927,-2.95989255113387,
3.48417246060752));
#103538=CARTESIAN_POINT('Ctrl Pts',(-2.93802558998807,-1.01302275008816,
3.37720970094026));
#103539=CARTESIAN_POINT('Ctrl Pts',(-2.94682272625454,-0.0193976123279483,
3.32321091976762));
#103540=CARTESIAN_POINT('Ctrl Pts',(-2.9467902630953,-0.000355741358367689,
3.3221761170896));
#103541=CARTESIAN_POINT('',(-2.94199898604255,-0.00244256517021028,2.32217614961572));
#103542=CARTESIAN_POINT('Ctrl Pts',(-2.94199997856207,-0.000355163067354804,
3.3221761170896));
#103543=CARTESIAN_POINT('Ctrl Pts',(-2.94201114633791,0.0921533191625664,
3.3171406920142));
#103544=CARTESIAN_POINT('Ctrl Pts',(-2.93765476336845,0.184833200119386,
3.3121052669388));
#103545=CARTESIAN_POINT('Ctrl Pts',(-2.928908341081,0.277236234186919,3.30706984186339));
#103546=CARTESIAN_POINT('Ctrl Pts',(-2.92017394505773,0.369512214784784,
3.30204134045921));
#103547=CARTESIAN_POINT('Ctrl Pts',(-2.90706154442541,0.461511663166572,
3.29701283905502));
#103548=CARTESIAN_POINT('Ctrl Pts',(-2.88960065316893,0.552785731731266,
3.29198433765083));
#103549=CARTESIAN_POINT('Ctrl Pts',(-2.87142912184824,0.647774559697056,
3.2867511814837));
#103550=CARTESIAN_POINT('Ctrl Pts',(-2.84854757434183,0.741977213308869,
3.28151802531657));
#103551=CARTESIAN_POINT('Ctrl Pts',(-2.82104910386007,0.83489277970905,
3.27628486914945));
#103552=CARTESIAN_POINT('Ctrl Pts',(-2.79467306622296,0.924015717585553,
3.27126532000337));
#103553=CARTESIAN_POINT('Ctrl Pts',(-2.76404977901021,1.01195410927705,
3.2662457708573));
#103554=CARTESIAN_POINT('Ctrl Pts',(-2.72931331381235,1.09827721229507,
3.26122622171123));
#103555=CARTESIAN_POINT('Ctrl Pts',(-2.69458840529123,1.18457159597764,
3.25620834254817));
#103556=CARTESIAN_POINT('Ctrl Pts',(-2.65575320396844,1.26925134360697,
3.25119046338511));
#103557=CARTESIAN_POINT('Ctrl Pts',(-2.6129906737564,1.35190374615284,3.24617258422205));
#103558=CARTESIAN_POINT('Ctrl Pts',(-2.57023019747324,1.4345521788177,3.24115494607295));
#103559=CARTESIAN_POINT('Ctrl Pts',(-2.5235429735275,1.51517306272391,3.23613730792386));
#103560=CARTESIAN_POINT('Ctrl Pts',(-2.47315832393181,1.59337751483031,
3.23111966977476));
#103561=CARTESIAN_POINT('Ctrl Pts',(-2.42276175155821,1.67160047285709,
3.22610084427623));
#103562=CARTESIAN_POINT('Ctrl Pts',(-2.36866625893787,1.7474054877297,3.2210820187777));
#103563=CARTESIAN_POINT('Ctrl Pts',(-2.31114429061703,1.82043293420777,
3.21606319327917));
#103564=CARTESIAN_POINT('Ctrl Pts',(-2.25355816621311,1.89354183052248,
3.21103877012474));
#103565=CARTESIAN_POINT('Ctrl Pts',(-2.19253821770682,1.96386662495742,
3.2060143469703));
#103566=CARTESIAN_POINT('Ctrl Pts',(-2.12839669278391,2.03108136669768,
3.20098992381587));
#103567=CARTESIAN_POINT('Ctrl Pts',(-2.06421283811086,2.09834046633599,
3.19596218482856));
#103568=CARTESIAN_POINT('Ctrl Pts',(-1.99690363100382,2.16248512071508,
3.19093444584125));
#103569=CARTESIAN_POINT('Ctrl Pts',(-1.92681600729287,2.22322830002678,
3.18590670685395));
#103570=CARTESIAN_POINT('Ctrl Pts',(-1.85661932603274,2.28406599677129,
3.18087114461821));
#103571=CARTESIAN_POINT('Ctrl Pts',(-1.78363595308645,2.3414913825842,3.17583558238248));
#103572=CARTESIAN_POINT('Ctrl Pts',(-1.70824317556668,2.39525974648468,
3.17080002014675));
#103573=CARTESIAN_POINT('Ctrl Pts',(-1.68622709717687,2.41096109817205,
3.16932954331109));
#103574=CARTESIAN_POINT('Ctrl Pts',(-1.66400572326432,2.42635089419769,
3.16785906647543));
#103575=CARTESIAN_POINT('Ctrl Pts',(-1.64158883621474,2.44142378394558,
3.16638858963977));
#103576=CARTESIAN_POINT('Ctrl Pts',(-1.56456751209218,2.4932121488585,3.1613362345682));
#103577=CARTESIAN_POINT('Ctrl Pts',(-1.48495488029135,2.54144509380551,
3.15628387949662));
#103578=CARTESIAN_POINT('Ctrl Pts',(-1.40311314851733,2.58585333931717,
3.15123152442505));
#103579=CARTESIAN_POINT('Ctrl Pts',(-1.32138426402925,2.6302003526204,3.14618613578179));
#103580=CARTESIAN_POINT('Ctrl Pts',(-1.23743277426245,2.6707329359363,3.14114074713852));
#103581=CARTESIAN_POINT('Ctrl Pts',(-1.1516502800556,2.70722471037183,3.13609535849526));
#103582=CARTESIAN_POINT('Ctrl Pts',(-1.06595956385464,2.74367744254915,
3.13105536787304));
#103583=CARTESIAN_POINT('Ctrl Pts',(-0.978442143574573,2.77609778596146,
3.12601537725082));
#103584=CARTESIAN_POINT('Ctrl Pts',(-0.889513690136257,2.80430551029309,
3.1209753866286));
#103585=CARTESIAN_POINT('Ctrl Pts',(-0.800649311475535,2.83249291037986,
3.11593902742316));
#103586=CARTESIAN_POINT('Ctrl Pts',(-0.710376342680051,2.85647359050147,
3.11090266821772));
#103587=CARTESIAN_POINT('Ctrl Pts',(-0.619128898248618,2.87611602814515,
3.10586630901228));
#103588=CARTESIAN_POINT('Ctrl Pts',(-0.527914613921933,2.89575132755835,
3.10083178006301));
#103589=CARTESIAN_POINT('Ctrl Pts',(-0.435726991337099,2.91105142309791,
3.09579725111375));
#103590=CARTESIAN_POINT('Ctrl Pts',(-0.343012706107742,2.92193536606282,
3.09076272216449));
#103591=CARTESIAN_POINT('Ctrl Pts',(-0.250306179960344,2.93281839817126,
3.08572861454536));
#103592=CARTESIAN_POINT('Ctrl Pts',(-0.157073520032592,2.93928596090582,
3.08069450692624));
#103593=CARTESIAN_POINT('Ctrl Pts',(-0.0637677932525789,2.94130883596805,
3.07566039930712));
#103594=CARTESIAN_POINT('Ctrl Pts',(0.0295562241494228,2.94333210757231,
3.07062530485725));
#103595=CARTESIAN_POINT('Ctrl Pts',(0.122952892733062,2.94090895186493,
3.06559021040739));
#103596=CARTESIAN_POINT('Ctrl Pts',(0.215969019761832,2.93406226629619,
3.06055511595753));
#103597=CARTESIAN_POINT('Ctrl Pts',(0.309087333680491,2.92720805900485,
3.05551448998685));
#103598=CARTESIAN_POINT('Ctrl Pts',(0.401823827821623,2.91592065407017,
3.05047386401618));
#103599=CARTESIAN_POINT('Ctrl Pts',(0.493730615240738,2.90027482828335,
3.04543323804551));
#103600=CARTESIAN_POINT('Ctrl Pts',(0.585693879446819,2.88461938812532,
3.04038951460655));
#103601=CARTESIAN_POINT('Ctrl Pts',(0.67682598833652,2.86460029047912,3.0353457911676));
#103602=CARTESIAN_POINT('Ctrl Pts',(0.766691575439549,2.84034294199662,
3.03030206772864));
#103603=CARTESIAN_POINT('Ctrl Pts',(0.856702597700644,2.81604633631429,
3.02525018171334));
#103604=CARTESIAN_POINT('Ctrl Pts',(0.94544258386381,2.78749792249483,3.02019829569804));
#103605=CARTESIAN_POINT('Ctrl Pts',(1.03249375929331,2.75487216346247,3.01514640968273));
#103606=CARTESIAN_POINT('Ctrl Pts',(1.07643247896761,2.73840444693582,3.01259649117379));
#103607=CARTESIAN_POINT('Ctrl Pts',(1.11994129363676,2.72089870215936,3.01004657266485));
#103608=CARTESIAN_POINT('Ctrl Pts',(1.16296887697036,2.70238179967197,3.00749665415591));
#103609=CARTESIAN_POINT('Ctrl Pts',(1.24822283225128,2.66569279568209,3.00244429885987));
#103610=CARTESIAN_POINT('Ctrl Pts',(1.33189187407922,2.62489965481643,2.99739194356383));
#103611=CARTESIAN_POINT('Ctrl Pts',(1.41355344725012,2.58016097400285,2.99233958826779));
#103612=CARTESIAN_POINT('Ctrl Pts',(1.49510242157254,2.53548398100332,2.98729419939875));
#103613=CARTESIAN_POINT('Ctrl Pts',(1.57464904137417,2.48687247022385,2.98224881052971));
#103614=CARTESIAN_POINT('Ctrl Pts',(1.65179089066202,2.43453298468638,2.97720342166067));
#103615=CARTESIAN_POINT('Ctrl Pts',(1.72885020651887,2.38224949673463,2.97216343081175));
#103616=CARTESIAN_POINT('Ctrl Pts',(1.80350950014496,2.32624620991823,2.96712343996282));
#103617=CARTESIAN_POINT('Ctrl Pts',(1.87539210840759,2.2667748983352,2.9620834491139));
#103618=CARTESIAN_POINT('Ctrl Pts',(1.94722292378378,2.20734643704602,2.95704708968125));
#103619=CARTESIAN_POINT('Ctrl Pts',(2.01628068909037,2.14445520004328,2.9520107302486));
#103620=CARTESIAN_POINT('Ctrl Pts',(2.08221969311326,2.0783948493035,2.94697437081595));
#103621=CARTESIAN_POINT('Ctrl Pts',(2.14813473434,2.01235850545831,2.94193984163925));
#103622=CARTESIAN_POINT('Ctrl Pts',(2.21093295235516,1.94315564991739,2.93690531246256));
#103623=CARTESIAN_POINT('Ctrl Pts',(2.27030434287066,1.87111789867517,2.93187078328586));
#103624=CARTESIAN_POINT('Ctrl Pts',(2.32967076470694,1.79908617613592,2.92683667543937));
#103625=CARTESIAN_POINT('Ctrl Pts',(2.38561064684502,1.72422037253094,2.92180256759289));
#103626=CARTESIAN_POINT('Ctrl Pts',(2.43785400625811,1.6468854981969,2.9167684597464));
#103627=CARTESIAN_POINT('Ctrl Pts',(2.49010760687746,1.56953546399552,2.91173336506948));
#103628=CARTESIAN_POINT('Ctrl Pts',(2.538662997306,1.4897157661196,2.90669827039257));
#103629=CARTESIAN_POINT('Ctrl Pts',(2.58329393366614,1.40781975134736,2.90166317571565));
#103630=CARTESIAN_POINT('Ctrl Pts',(2.62797390125282,1.32583376620074,2.89662254951984));
#103631=CARTESIAN_POINT('Ctrl Pts',(2.66872059585565,1.24176730164257,2.89158192332404));
#103632=CARTESIAN_POINT('Ctrl Pts',(2.70535425628224,1.15603734715431,2.88654129712823));
#103633=CARTESIAN_POINT('Ctrl Pts',(2.74201042811318,1.07025471156216,2.88149757346486));
#103634=CARTESIAN_POINT('Ctrl Pts',(2.77454837928104,0.982806967050958,
2.8764538498015));
#103635=CARTESIAN_POINT('Ctrl Pts',(2.8028376891304,0.894128004477065,2.87141012613814));
#103636=CARTESIAN_POINT('Ctrl Pts',(2.83117278133661,0.805305527199894,
2.86635823990179));
#103637=CARTESIAN_POINT('Ctrl Pts',(2.85524539090762,0.715248282604754,
2.86130635366543));
#103638=CARTESIAN_POINT('Ctrl Pts',(2.87497586211889,0.624401947653728,
2.85625446742907));
#103639=CARTESIAN_POINT('Ctrl Pts',(2.88493472636369,0.578547679540833,
2.85370455117673));
#103640=CARTESIAN_POINT('Ctrl Pts',(2.89378817376357,0.532492488326335,
2.85115463492438));
#103641=CARTESIAN_POINT('Ctrl Pts',(2.9015309880173,0.486294073144374,2.84860471867204));
#103642=CARTESIAN_POINT('Ctrl Pts',(2.91687245028162,0.394757427687029,
2.84355236397507));
#103643=CARTESIAN_POINT('Ctrl Pts',(2.92790553549581,0.302329845343127,
2.83850000927811));
#103644=CARTESIAN_POINT('Ctrl Pts',(2.93453466172541,0.209452426894869,
2.83344765458114));
#103645=CARTESIAN_POINT('Ctrl Pts',(2.94115464739987,0.116703072257054,
2.82840226631159));
#103646=CARTESIAN_POINT('Ctrl Pts',(2.94338270935698,0.0235055533119512,
2.82335687804205));
#103647=CARTESIAN_POINT('Ctrl Pts',(2.94117447729558,-0.0696899856870516,
2.8183114897725));
#103648=CARTESIAN_POINT('Ctrl Pts',(2.93896860780362,-0.162785815540424,
2.81327149952263));
#103649=CARTESIAN_POINT('Ctrl Pts',(2.93233588886659,-0.25587922792747,
2.80823150927276));
#103650=CARTESIAN_POINT('Ctrl Pts',(2.92128392050546,-0.348517224533101,
2.8031915190229));
#103651=CARTESIAN_POINT('Ctrl Pts',(2.91023991530746,-0.441088473618765,
2.7981551601863));
#103652=CARTESIAN_POINT('Ctrl Pts',(2.89478304212267,-0.533204519295604,
2.79311880134969));
#103653=CARTESIAN_POINT('Ctrl Pts',(2.87497287736889,-0.624415690380407,
2.78808244251309));
#103654=CARTESIAN_POINT('Ctrl Pts',(2.85516991179049,-0.715593714582038,
2.78304791393035));
#103655=CARTESIAN_POINT('Ctrl Pts',(2.83101689169364,-0.805867083784066,
2.77801338534761));
#103656=CARTESIAN_POINT('Ctrl Pts',(2.80262463893058,-0.89479558182817,
2.77297885676487));
#103657=CARTESIAN_POINT('Ctrl Pts',(2.77423476224573,-0.983716637663765,
2.76794474950951));
#103658=CARTESIAN_POINT('Ctrl Pts',(2.74160649355356,-1.07129262297736,
2.76291064225416));
#103659=CARTESIAN_POINT('Ctrl Pts',(2.70490040442368,-1.15709887310835,
2.7578765349988));
#103660=CARTESIAN_POINT('Ctrl Pts',(2.66818711981468,-1.24292194380224,
2.75284144090953));
#103661=CARTESIAN_POINT('Ctrl Pts',(2.62739460225923,-1.32697418206009,
2.74780634682026));
#103662=CARTESIAN_POINT('Ctrl Pts',(2.5827309354394,-1.40885233971639,2.74277125273098));
#103663=CARTESIAN_POINT('Ctrl Pts',(2.53801820135102,-1.49082044828437,
2.73773062711393));
#103664=CARTESIAN_POINT('Ctrl Pts',(2.48942604193384,-1.57060931806829,
2.73269000149688));
#103665=CARTESIAN_POINT('Ctrl Pts',(2.43720759368571,-1.64784196611226,
2.72764937587983));
#103666=CARTESIAN_POINT('Ctrl Pts',(2.38495705712568,-1.72512207373004,
2.72260565279105));
#103667=CARTESIAN_POINT('Ctrl Pts',(2.32907606136527,-1.79984247695622,
2.71756192970227));
#103668=CARTESIAN_POINT('Ctrl Pts',(2.26985867718656,-1.87165851201571,
2.71251820661349));
#103669=CARTESIAN_POINT('Ctrl Pts',(2.21054545766423,-1.94359077163483,
2.70746632093965));
#103670=CARTESIAN_POINT('Ctrl Pts',(2.14788536855418,-2.01260895098623,
2.70241443526581));
#103671=CARTESIAN_POINT('Ctrl Pts',(2.08220988672817,-2.07840467368881,
2.69736254959197));
#103672=CARTESIAN_POINT('Ctrl Pts',(2.04906041035026,-2.11161484124075,
2.69481262745737));
#103673=CARTESIAN_POINT('Ctrl Pts',(2.01514324348483,-2.14400465555415,
2.69226270532277));
#103674=CARTESIAN_POINT('Ctrl Pts',(1.98050406139377,-2.17553847651628,
2.68971278318817));
#103675=CARTESIAN_POINT('Ctrl Pts',(1.91187080920727,-2.23801883996161,
2.68466042807019));
#103676=CARTESIAN_POINT('Ctrl Pts',(1.84015484173131,-2.29736029386187,
2.67960807295222));
#103677=CARTESIAN_POINT('Ctrl Pts',(1.76567516219451,-2.35324355339803,
2.67455571783425));
#103678=CARTESIAN_POINT('Ctrl Pts',(1.6912981788371,-2.40904975839687,2.66951032914753));
#103679=CARTESIAN_POINT('Ctrl Pts',(1.61416540810677,-2.46140698000676,
2.66446494046082));
#103680=CARTESIAN_POINT('Ctrl Pts',(1.53463119590279,-2.51003408195227,
2.6594195517741));
#103681=CARTESIAN_POINT('Ctrl Pts',(1.45518207676411,-2.55860915812111,
2.65437956111142));
#103682=CARTESIAN_POINT('Ctrl Pts',(1.37333699997642,-2.60346181652224,
2.64933957044874));
#103683=CARTESIAN_POINT('Ctrl Pts',(1.28948086241099,-2.64435305991386,
2.64429957978605));
#103684=CARTESIAN_POINT('Ctrl Pts',(1.20568514499045,-2.68521484028797,
2.63926322054469));
#103685=CARTESIAN_POINT('Ctrl Pts',(1.11988164505737,-2.72212068479541,
2.63422686130334));
#103686=CARTESIAN_POINT('Ctrl Pts',(1.03248061797671,-2.75487708863797,
2.62919050206198));
#103687=CARTESIAN_POINT('Ctrl Pts',(0.945111353228246,-2.78762158850394,
2.62415597307961));
#103688=CARTESIAN_POINT('Ctrl Pts',(0.856146130235803,-2.81621948765529,
2.61912144409723));
#103689=CARTESIAN_POINT('Ctrl Pts',(0.766015015937392,-2.84052547873777,
2.61408691511486));
#103690=CARTESIAN_POINT('Ctrl Pts',(0.67589144459097,-2.86482943568448,
2.60905280746546));
#103691=CARTESIAN_POINT('Ctrl Pts',(0.584602604900241,-2.88484208321642,
2.60401869981607));
#103692=CARTESIAN_POINT('Ctrl Pts',(0.4925924406045,-2.90046835656921,2.59898459216667));
#103693=CARTESIAN_POINT('Ctrl Pts',(0.400564239707177,-2.91609769311473,
2.59394949768941));
#103694=CARTESIAN_POINT('Ctrl Pts',(0.307814871387626,-2.92733887379562,
2.58891440321214));
#103695=CARTESIAN_POINT('Ctrl Pts',(0.214796014112857,-2.93414837258126,
2.58387930873488));
#103696=CARTESIAN_POINT('Ctrl Pts',(0.121674967031744,-2.94096535223026,
2.57883868274127));
#103697=CARTESIAN_POINT('Ctrl Pts',(0.0282842837671854,-2.94334089918746,
2.57379805674766));
#103698=CARTESIAN_POINT('Ctrl Pts',(-0.0649220303857701,-2.94128358543861,
2.56875743075405));
#103699=CARTESIAN_POINT('Ctrl Pts',(-0.158185619839219,-2.93922500747001,
2.56371370729466));
#103700=CARTESIAN_POINT('Ctrl Pts',(-0.251264171800973,-2.93272817676389,
2.55866998383527));
#103701=CARTESIAN_POINT('Ctrl Pts',(-0.343708673950207,-2.92185358076879,
2.55362626037589));
#103702=CARTESIAN_POINT('Ctrl Pts',(-0.436302784803891,-2.91096138573664,
2.5485743743442));
#103703=CARTESIAN_POINT('Ctrl Pts',(-0.528260359646463,-2.89567735423824,
2.54352248831251));
#103704=CARTESIAN_POINT('Ctrl Pts',(-0.619142625915856,-2.87611307301608,
2.53847060228083));
#103705=CARTESIAN_POINT('Ctrl Pts',(-0.665015066951347,-2.86623808448856,
2.53592068408865));
#103706=CARTESIAN_POINT('Ctrl Pts',(-0.710613790669298,-2.85527341748435,
2.53337076589647));
#103707=CARTESIAN_POINT('Ctrl Pts',(-0.755884097136884,-2.84323815951031,
2.5308208477043));
#103708=CARTESIAN_POINT('Ctrl Pts',(-0.845581768488794,-2.81939174231928,
2.52576849127415));
#103709=CARTESIAN_POINT('Ctrl Pts',(-0.934310826130412,-2.79125374089853,
2.52071613484401));
#103710=CARTESIAN_POINT('Ctrl Pts',(-1.02163008489205,-2.75891934815852,
2.51566377841386));
#103711=CARTESIAN_POINT('Ctrl Pts',(-1.1088289438365,-2.72662953956903,
2.51061838840555));
#103712=CARTESIAN_POINT('Ctrl Pts',(-1.19462145369141,-2.69015499047006,
2.50557299839724));
#103713=CARTESIAN_POINT('Ctrl Pts',(-1.27857935125012,-2.64964126676741,
2.50052760838893));
#103714=CARTESIAN_POINT('Ctrl Pts',(-1.36244742302372,-2.60917088832644,
2.49548761639714));
#103715=CARTESIAN_POINT('Ctrl Pts',(-1.44448438599058,-2.56467011690487,
2.49044762440536));
#103716=CARTESIAN_POINT('Ctrl Pts',(-1.52428084884236,-2.51633302522787,
2.48540763241357));
#103717=CARTESIAN_POINT('Ctrl Pts',(-1.60401981673635,-2.46803076139844,
2.48037127183748));
#103718=CARTESIAN_POINT('Ctrl Pts',(-1.68152111434295,-2.41589790094858,
2.47533491126138));
#103719=CARTESIAN_POINT('Ctrl Pts',(-1.7563998537718,-2.36017447526034,
2.47029855068528));
#103720=CARTESIAN_POINT('Ctrl Pts',(-1.83125138163373,-2.30447129993607,
2.46526402036519));
#103721=CARTESIAN_POINT('Ctrl Pts',(-1.90348188864995,-2.24518041653238,
2.4602294900451));
#103722=CARTESIAN_POINT('Ctrl Pts',(-1.97273626882861,-2.18258461775212,
2.45519495972501));
#103723=CARTESIAN_POINT('Ctrl Pts',(-2.04198485322095,-2.11999405751236,
2.45016085073657));
#103724=CARTESIAN_POINT('Ctrl Pts',(-2.10825747653603,-2.05409942982767,
2.44512674174813));
#103725=CARTESIAN_POINT('Ctrl Pts',(-2.17123374859856,-1.98522240792982,
2.44009263275968));
#103726=CARTESIAN_POINT('Ctrl Pts',(-2.23422236578921,-1.91633188419021,
2.43505753694369));
#103727=CARTESIAN_POINT('Ctrl Pts',(-2.29391304893903,-1.84445813323679,
2.43002244112769));
#103728=CARTESIAN_POINT('Ctrl Pts',(-2.35002454030773,-1.76995724805754,
2.4249873453117));
#103729=CARTESIAN_POINT('Ctrl Pts',(-2.40619767521922,-1.69537451692497,
2.41994671798804));
#103730=CARTESIAN_POINT('Ctrl Pts',(-2.45878350181698,-1.61815924588878,
2.41490609066438));
#103731=CARTESIAN_POINT('Ctrl Pts',(-2.50754329433084,-1.53869770489738,
2.40986546334073));
#103732=CARTESIAN_POINT('Ctrl Pts',(-2.55633304971164,-1.45918733483068,
2.40482173855422));
#103733=CARTESIAN_POINT('Ctrl Pts',(-2.60129187653794,-1.37742833581499,
2.39977801376772));
#103734=CARTESIAN_POINT('Ctrl Pts',(-2.64222739263561,-1.29383090301864,
2.39473428898121));
#103735=CARTESIAN_POINT('Ctrl Pts',(-2.68322915707253,-1.21009817960876,
2.38968240163997));
#103736=CARTESIAN_POINT('Ctrl Pts',(-2.72019443614329,-1.12452149002621,
2.38463051429873));
#103737=CARTESIAN_POINT('Ctrl Pts',(-2.75297934735898,-1.03753010222109,
2.3795786269575));
#103738=CARTESIAN_POINT('Ctrl Pts',(-2.76952730270978,-0.993621805754092,
2.37702872204514));
#103739=CARTESIAN_POINT('Ctrl Pts',(-2.78501103996012,-0.949353323379518,
2.37447881713278));
#103740=CARTESIAN_POINT('Ctrl Pts',(-2.79941697330728,-0.904780973252142,
2.37192891222043));
#103741=CARTESIAN_POINT('Ctrl Pts',(-2.83367003860432,-0.798801056327432,
2.36586598957881));
#103742=CARTESIAN_POINT('Ctrl Pts',(-2.86192675554772,-0.690794327218017,
2.35980306693719));
#103743=CARTESIAN_POINT('Ctrl Pts',(-2.88398318981509,-0.581381940607001,
2.35374014429557));
#103744=CARTESIAN_POINT('Ctrl Pts',(-2.90578467662655,-0.473234237546983,
2.34774730218846));
#103745=CARTESIAN_POINT('Ctrl Pts',(-2.92152834520193,-0.363713232418249,
2.34175446008135));
#103746=CARTESIAN_POINT('Ctrl Pts',(-2.93106335006533,-0.253439613919819,
2.33576161797424));
#103747=CARTESIAN_POINT('Ctrl Pts',(-2.93826847380877,-0.170111385114324,
2.3312331285214));
#103748=CARTESIAN_POINT('Ctrl Pts',(-2.94192931955188,-0.0863538349346285,
2.32670463906856));
#103749=CARTESIAN_POINT('Ctrl Pts',(-2.94199898604255,-0.00244256517021028,
2.32217614961572));
#103750=CARTESIAN_POINT('',(-2.93804968218247,0.00161843370594106,1.3221761170896));
#103751=CARTESIAN_POINT('Ctrl Pts',(-2.93974867080922,-0.00244009463185479,
2.3221761170896));
#103752=CARTESIAN_POINT('Ctrl Pts',(-2.93448192828745,0.671152046916237,
2.28579640363858));
#103753=CARTESIAN_POINT('Ctrl Pts',(-2.36994396481666,2.3333813133397,2.19645271169295));
#103754=CARTESIAN_POINT('Ctrl Pts',(0.393212503661621,3.45590805701087,
2.05414504125267));
#103755=CARTESIAN_POINT('Ctrl Pts',(3.11795753103548,1.54151400144106,1.89525310576881));
#103756=CARTESIAN_POINT('Ctrl Pts',(2.98473289321859,-1.78585963759114,
1.73636117028493));
#103757=CARTESIAN_POINT('Ctrl Pts',(0.115656289204281,-3.47627940135573,
1.57746923480107));
#103758=CARTESIAN_POINT('Ctrl Pts',(-2.46940960925412,-2.17641804373625,
1.43940755040262));
#103759=CARTESIAN_POINT('Ctrl Pts',(-2.93508362518438,-0.594223152876953,
1.3543098444988));
#103760=CARTESIAN_POINT('Ctrl Pts',(-2.93804968218247,0.00161843370594106,
1.3221761170896));
#103761=CARTESIAN_POINT('Ctrl Pts',(-2.93804968218247,0.00161843370594106,
1.3221761170896));
#103762=CARTESIAN_POINT('Ctrl Pts',(-2.93997238822952,0.387864625988779,
1.30134586600417));
#103763=CARTESIAN_POINT('Ctrl Pts',(-2.68942924946335,1.75380081078585,
1.22755163642413));
#103764=CARTESIAN_POINT('Ctrl Pts',(-0.62204903688223,3.42210546244733,
1.10079342834945));
#103765=CARTESIAN_POINT('Ctrl Pts',(2.53961703903404,2.37666649300172,0.941901492865588));
#103766=CARTESIAN_POINT('Ctrl Pts',(3.37339857704762,-0.847434397963935,
0.783009557381711));
#103767=CARTESIAN_POINT('Ctrl Pts',(1.11513000686983,-3.29443532088267,
0.624117621897844));
#103768=CARTESIAN_POINT('Ctrl Pts',(-2.05637049788623,-2.7413454552293,
0.470506475133804));
#103769=CARTESIAN_POINT('Ctrl Pts',(-2.93964728609037,-0.876412749831535,
0.369859306864387));
#103770=CARTESIAN_POINT('Ctrl Pts',(-2.94561598299575,0.00187102060485729,
0.322176117089595));
#103771=CARTESIAN_POINT('Origin',(0.,0.,-1.84858989190503));
#103772=CARTESIAN_POINT('',(-2.37174933328259,-0.00177836262041549,23.651410108095));
#103773=CARTESIAN_POINT('Ctrl Pts',(-2.36542649498009,0.173076744094118,
23.6397760267629));
#103774=CARTESIAN_POINT('Ctrl Pts',(-2.36967824820991,0.114968361061076,
23.6440297226054));
#103775=CARTESIAN_POINT('Ctrl Pts',(-2.37179115015004,0.0566713851742079,
23.6482936118239));
#103776=CARTESIAN_POINT('Ctrl Pts',(-2.37174939305784,-0.00169677038972837,
23.6525333695376));
#103777=CARTESIAN_POINT('',(-2.34668236863856,0.3439184833953,24.62825));
#103778=CARTESIAN_POINT('Ctrl Pts',(-2.37174933328259,-0.0017783626204155,
23.651410108095));
#103779=CARTESIAN_POINT('Ctrl Pts',(-2.37166213645339,-0.118070180242878,
23.6592395344289));
#103780=CARTESIAN_POINT('Ctrl Pts',(-2.3630207288615,-0.234043937961113,
23.6670689607629));
#103781=CARTESIAN_POINT('Ctrl Pts',(-2.34597095750765,-0.348738195543054,
23.6748983870969));
#103782=CARTESIAN_POINT('Ctrl Pts',(-2.33435655987608,-0.426868552013454,
23.6802318351991));
#103783=CARTESIAN_POINT('Ctrl Pts',(-2.3188129279233,-0.504565287258719,
23.6855652833013));
#103784=CARTESIAN_POINT('Ctrl Pts',(-2.29938446161523,-0.581402752128369,
23.6908987314035));
#103785=CARTESIAN_POINT('Ctrl Pts',(-2.27998401512876,-0.658129401660169,
23.6962244875828));
#103786=CARTESIAN_POINT('Ctrl Pts',(-2.2567099746355,-0.733998791410123,
23.7015502437621));
#103787=CARTESIAN_POINT('Ctrl Pts',(-2.22965819359468,-0.808592853193823,
23.7068759999414));
#103788=CARTESIAN_POINT('Ctrl Pts',(-2.20263780793542,-0.883100343633887,
23.7121955752284));
#103789=CARTESIAN_POINT('Ctrl Pts',(-2.17184855336974,-0.956335009257643,
23.7175151505153));
#103790=CARTESIAN_POINT('Ctrl Pts',(-2.13743638304207,-1.02789287912119,
23.7228347258023));
#103791=CARTESIAN_POINT('Ctrl Pts',(-2.10304607897219,-1.09940527952392,
23.7281509209128));
#103792=CARTESIAN_POINT('Ctrl Pts',(-2.06503763097987,-1.16924257789309,
23.7334671160234));
#103793=CARTESIAN_POINT('Ctrl Pts',(-2.02360503864635,-1.23702090122403,
23.738783311134));
#103794=CARTESIAN_POINT('Ctrl Pts',(-1.98218588602492,-1.30477723893687,
23.7440977818019));
#103795=CARTESIAN_POINT('Ctrl Pts',(-1.9373450388303,-1.37047552841582,
23.7494122524697));
#103796=CARTESIAN_POINT('Ctrl Pts',(-1.88932163343825,-1.43375793909649,
23.7547267231376));
#103797=CARTESIAN_POINT('Ctrl Pts',(-1.84129886847173,-1.49703950586218,
23.7600411229333));
#103798=CARTESIAN_POINT('Ctrl Pts',(-1.79009391396709,-1.5579048854719,
23.765355522729));
#103799=CARTESIAN_POINT('Ctrl Pts',(-1.7359873831785,-1.61602780543685,
23.7706699225247));
#103800=CARTESIAN_POINT('Ctrl Pts',(-1.68182686780958,-1.6742087173188,
23.7759896247421));
#103801=CARTESIAN_POINT('Ctrl Pts',(-1.62475931293704,-1.72964135975047,
23.7813093269595));
#103802=CARTESIAN_POINT('Ctrl Pts',(-1.56510314122222,-1.78203541486591,
23.7866290291769));
#103803=CARTESIAN_POINT('Ctrl Pts',(-1.50541836579805,-1.83445459167927,
23.7919512820645));
#103804=CARTESIAN_POINT('Ctrl Pts',(-1.44314286848062,-1.88383198720657,
23.797273534952));
#103805=CARTESIAN_POINT('Ctrl Pts',(-1.37862719154216,-1.92991842554047,
23.8025957878396));
#103806=CARTESIAN_POINT('Ctrl Pts',(-1.3139940832985,-1.97608875031657,
23.8079277282811));
#103807=CARTESIAN_POINT('Ctrl Pts',(-1.24711304291611,-2.01895589452395,
23.8132596687226));
#103808=CARTESIAN_POINT('Ctrl Pts',(-1.17836238220007,-2.05831488327607,
23.8185916091642));
#103809=CARTESIAN_POINT('Ctrl Pts',(-1.11303772220215,-2.09571252471422,
23.8236578469697));
#103810=CARTESIAN_POINT('Ctrl Pts',(-1.04602564777549,-2.12994316111438,
23.8287240847752));
#103811=CARTESIAN_POINT('Ctrl Pts',(-0.977666994686801,-2.1608714237548,
23.8337903225807));
#103812=CARTESIAN_POINT('Ctrl Pts',(-0.905825097966649,-2.19337564889603,
23.839114712643));
#103813=CARTESIAN_POINT('Ctrl Pts',(-0.832222031729365,-2.22235580829395,
23.8444391027054));
#103814=CARTESIAN_POINT('Ctrl Pts',(-0.757238117187071,-2.24761840541916,
23.8497634927677));
#103815=CARTESIAN_POINT('Ctrl Pts',(-0.682363045020286,-2.27284433279861,
23.855080154249));
#103816=CARTESIAN_POINT('Ctrl Pts',(-0.606111546422999,-2.29436326425291,
23.8603968157303));
#103817=CARTESIAN_POINT('Ctrl Pts',(-0.528885553033947,-2.31202900809916,
23.8657134772116));
#103818=CARTESIAN_POINT('Ctrl Pts',(-0.451749529117852,-2.32967417108145,
23.8710239447003));
#103819=CARTESIAN_POINT('Ctrl Pts',(-0.373641722320833,-2.34347496198871,
23.876334412189));
#103820=CARTESIAN_POINT('Ctrl Pts',(-0.294979449900713,-2.35333490745288,
23.8816448796777));
#103821=CARTESIAN_POINT('Ctrl Pts',(-0.216367310215482,-2.36318856901479,
23.8869519627198));
#103822=CARTESIAN_POINT('Ctrl Pts',(-0.137201871580469,-2.36910631132213,
23.8922590457619));
#103823=CARTESIAN_POINT('Ctrl Pts',(-0.0579096591383827,-2.37104292113797,
23.897566128804));
#103824=CARTESIAN_POINT('Ctrl Pts',(0.021356906466357,-2.37297890456295,
23.9028714952855));
#103825=CARTESIAN_POINT('Ctrl Pts',(0.100749694667562,-2.37093630073283,
23.9081768617669));
#103826=CARTESIAN_POINT('Ctrl Pts',(0.179839568219446,-2.36492194209505,
23.9134822282483));
#103827=CARTESIAN_POINT('Ctrl Pts',(0.258928683893683,-2.35890764108979,
23.9187875438911));
#103828=CARTESIAN_POINT('Ctrl Pts',(0.337714421852944,-2.34892169793918,
23.9240928595339));
#103829=CARTESIAN_POINT('Ctrl Pts',(0.415771675756215,-2.33502290698376,
23.9293981751768));
#103830=CARTESIAN_POINT('Ctrl Pts',(0.493908338240533,-2.32110997662152,
23.9347088879808));
#103831=CARTESIAN_POINT('Ctrl Pts',(0.571314572142124,-2.30327632954018,
23.9400196007849));
#103832=CARTESIAN_POINT('Ctrl Pts',(0.64757499476761,-2.28163202305975,
23.945330313589));
#103833=CARTESIAN_POINT('Ctrl Pts',(0.723872570910351,-2.25997717163232,
23.9506436137333));
#103834=CARTESIAN_POINT('Ctrl Pts',(0.799022777893084,-2.23450811410081,
23.9559569138776));
#103835=CARTESIAN_POINT('Ctrl Pts',(0.872627438099414,-2.20538418802168,
23.9612702140219));
#103836=CARTESIAN_POINT('Ctrl Pts',(0.946368638599109,-2.17620623561596,
23.9665933706014));
#103837=CARTESIAN_POINT('Ctrl Pts',(1.01855813423093,-2.14336006233295,
23.9719165271809));
#103838=CARTESIAN_POINT('Ctrl Pts',(1.08881987715376,-2.10705228639796,
23.9772396837603));
#103839=CARTESIAN_POINT('Ctrl Pts',(1.15676340963184,-2.0719424463794,23.9823872085284));
#103840=CARTESIAN_POINT('Ctrl Pts',(1.22290412114906,-2.03359613277576,
23.9875347332965));
#103841=CARTESIAN_POINT('Ctrl Pts',(1.28692882879557,-1.9922380008711,23.9926822580646));
#103842=CARTESIAN_POINT('Ctrl Pts',(1.35337617358078,-1.94931491459144,
23.9980245605229));
#103843=CARTESIAN_POINT('Ctrl Pts',(1.41779753409028,-1.90298390981766,
24.0033668629812));
#103844=CARTESIAN_POINT('Ctrl Pts',(1.47982291798039,-1.85346221809887,
24.0087091654396));
#103845=CARTESIAN_POINT('Ctrl Pts',(1.54175842012147,-1.80401228887453,
24.0140437263015));
#103846=CARTESIAN_POINT('Ctrl Pts',(1.60130447951582,-1.75138114452795,
24.0193782871635));
#103847=CARTESIAN_POINT('Ctrl Pts',(1.65811931244879,-1.69582971084492,
24.0247128480254));
#103848=CARTESIAN_POINT('Ctrl Pts',(1.71486708816156,-1.64034384322146,
24.0300411126298));
#103849=CARTESIAN_POINT('Ctrl Pts',(1.76888971219997,-1.58194486139646,
24.0353693772341));
#103850=CARTESIAN_POINT('Ctrl Pts',(1.81987897285177,-1.52093345898891,
24.0406976418385));
#103851=CARTESIAN_POINT('Ctrl Pts',(1.87083517715617,-1.45996161028518,
24.0460224521279));
#103852=CARTESIAN_POINT('Ctrl Pts',(1.9187616232362,-1.39638106028224,24.0513472624173));
#103853=CARTESIAN_POINT('Ctrl Pts',(1.9633882594744,-1.33052794223123,24.0566720727067));
#103854=CARTESIAN_POINT('Ctrl Pts',(2.00799972638391,-1.2646972087397,24.0619950730054));
#103855=CARTESIAN_POINT('Ctrl Pts',(2.04931334932713,-1.19659582750647,
24.067318073304));
#103856=CARTESIAN_POINT('Ctrl Pts',(2.08710143426901,-1.1265902829211,24.0726410736027));
#103857=CARTESIAN_POINT('Ctrl Pts',(2.12488832724072,-1.0565869465588,24.0779639059951));
#103858=CARTESIAN_POINT('Ctrl Pts',(2.15914968262113,-0.984679977673584,
24.0832867383875));
#103859=CARTESIAN_POINT('Ctrl Pts',(2.18970366579744,-0.911260620510532,
24.0886095707798));
#103860=CARTESIAN_POINT('Ctrl Pts',(2.22028687598047,-0.837771032633785,
24.093937494831));
#103861=CARTESIAN_POINT('Ctrl Pts',(2.24715544940571,-0.762766598356138,
24.0992654188823));
#103862=CARTESIAN_POINT('Ctrl Pts',(2.2701759021778,-0.68665816508012,24.1045933429335));
#103863=CARTESIAN_POINT('Ctrl Pts',(2.29320693481568,-0.61051475347345,
24.1099237156212));
#103864=CARTESIAN_POINT('Ctrl Pts',(2.31238620985614,-0.533266785567809,
24.1152540883089));
#103865=CARTESIAN_POINT('Ctrl Pts',(2.32763095878448,-0.455337437740462,
24.1205844609966));
#103866=CARTESIAN_POINT('Ctrl Pts',(2.34290264706581,-0.377270379136774,
24.1259242531108));
#103867=CARTESIAN_POINT('Ctrl Pts',(2.35422584846339,-0.298519997801786,
24.131264045225));
#103868=CARTESIAN_POINT('Ctrl Pts',(2.36156950805721,-0.219516562278207,
24.1366038373392));
#103869=CARTESIAN_POINT('Ctrl Pts',(2.36843227210291,-0.145686623693552,
24.1415939560756));
#103870=CARTESIAN_POINT('Ctrl Pts',(2.37182013699591,-0.071636038038402,
24.146584074812));
#103871=CARTESIAN_POINT('Ctrl Pts',(2.37174889865758,0.00228565451689994,
24.1515741935483));
#103872=CARTESIAN_POINT('Ctrl Pts',(2.37167267487504,0.0813805793809012,
24.1569135337727));
#103873=CARTESIAN_POINT('Ctrl Pts',(2.36763542177374,0.160617032165804,
24.1622528739972));
#103874=CARTESIAN_POINT('Ctrl Pts',(2.35961988042824,0.239566446706986,
24.1675922142216));
#103875=CARTESIAN_POINT('Ctrl Pts',(2.35161572251256,0.318403739673224,
24.1729239716762));
#103876=CARTESIAN_POINT('Ctrl Pts',(2.33964454414398,0.396954342918136,
24.1782557291308));
#103877=CARTESIAN_POINT('Ctrl Pts',(2.32374109811239,0.474789818175803,
24.1835874865854));
#103878=CARTESIAN_POINT('Ctrl Pts',(2.3078556896909,0.552537012821109,24.188913196787));
#103879=CARTESIAN_POINT('Ctrl Pts',(2.2880469701543,0.629570235907194,24.1942389069886));
#103880=CARTESIAN_POINT('Ctrl Pts',(2.26440130128787,0.705467794605676,
24.1995646171902));
#103881=CARTESIAN_POINT('Ctrl Pts',(2.24077029356514,0.781318294156822,
24.2048870252648));
#103882=CARTESIAN_POINT('Ctrl Pts',(2.21330719763369,0.856034082161029,
24.2102094333393));
#103883=CARTESIAN_POINT('Ctrl Pts',(2.18214881653151,0.929206438317201,
24.2155318414139));
#103884=CARTESIAN_POINT('Ctrl Pts',(2.15100012968629,1.00235602847599,24.2208525935362));
#103885=CARTESIAN_POINT('Ctrl Pts',(2.11615862383116,1.07396271088252,24.2261733456585));
#103886=CARTESIAN_POINT('Ctrl Pts',(2.07780952519887,1.14363702261376,24.2314940977808));
#103887=CARTESIAN_POINT('Ctrl Pts',(2.03946051212473,1.21331117889921,24.2368148380323));
#103888=CARTESIAN_POINT('Ctrl Pts',(1.99760414835687,1.2810525644594,24.2421355782838));
#103889=CARTESIAN_POINT('Ctrl Pts',(1.95247126540384,1.34649694402635,24.2474563185353));
#103890=CARTESIAN_POINT('Ctrl Pts',(1.90729301366787,1.41200711003676,24.2527824073375));
#103891=CARTESIAN_POINT('Ctrl Pts',(1.85883192928299,1.47521527208597,24.2581084961396));
#103892=CARTESIAN_POINT('Ctrl Pts',(1.80736146548855,1.53578728851592,24.2634345849418));
#103893=CARTESIAN_POINT('Ctrl Pts',(1.75586601055456,1.59638871528344,24.2687632597907));
#103894=CARTESIAN_POINT('Ctrl Pts',(1.70135858561781,1.65435110556944,24.2740919346397));
#103895=CARTESIAN_POINT('Ctrl Pts',(1.64415039897993,1.70937635646283,24.2794206094887));
#103896=CARTESIAN_POINT('Ctrl Pts',(1.58683840100284,1.76450145748819,24.284758953878));
#103897=CARTESIAN_POINT('Ctrl Pts',(1.52681620164722,1.81667846148374,24.2900972982674));
#103898=CARTESIAN_POINT('Ctrl Pts',(1.46442891020077,1.86564895665508,24.2954356426568));
#103899=CARTESIAN_POINT('Ctrl Pts',(1.40587696564674,1.91160892144241,24.3004458047819));
#103900=CARTESIAN_POINT('Ctrl Pts',(1.34524234866685,1.95474472685475,24.3054559669071));
#103901=CARTESIAN_POINT('Ctrl Pts',(1.28283147795962,1.99487880876406,24.3104661290322));
#103902=CARTESIAN_POINT('Ctrl Pts',(1.21713308801171,2.03712697056025,24.3157402035848));
#103903=CARTESIAN_POINT('Ctrl Pts',(1.14920531743009,2.07621601382973,24.3210142781374));
#103904=CARTESIAN_POINT('Ctrl Pts',(1.07938820249835,2.1118994225122,24.32628835269));
#103905=CARTESIAN_POINT('Ctrl Pts',(1.00967364853039,2.14753041246055,24.3315546796556));
#103906=CARTESIAN_POINT('Ctrl Pts',(0.938075681216748,2.17976548001854,
24.3368210066212));
#103907=CARTESIAN_POINT('Ctrl Pts',(0.864963090391752,2.20840143876967,
24.3420873335868));
#103908=CARTESIAN_POINT('Ctrl Pts',(0.791342100728035,2.23723652174838,
24.3473902807089));
#103909=CARTESIAN_POINT('Ctrl Pts',(0.716185750227005,2.26242197002789,
24.3526932278309));
#103910=CARTESIAN_POINT('Ctrl Pts',(0.639895415943316,2.28379769663487,
24.357996174953));
#103911=CARTESIAN_POINT('Ctrl Pts',(0.564265586288636,2.30498835698798,
24.3632532103465));
#103912=CARTESIAN_POINT('Ctrl Pts',(0.48752180228139,2.32243487533405,24.3685102457399));
#103913=CARTESIAN_POINT('Ctrl Pts',(0.410072754950791,2.33603047885662,
24.3737672811334));
#103914=CARTESIAN_POINT('Ctrl Pts',(0.332646181205444,2.34962213730865,
24.3790227910797));
#103915=CARTESIAN_POINT('Ctrl Pts',(0.254515222474931,2.35936501513378,
24.3842783010259));
#103916=CARTESIAN_POINT('Ctrl Pts',(0.176098874936079,2.365203426504,24.3895338109722));
#103917=CARTESIAN_POINT('Ctrl Pts',(0.0976795929290665,2.37104205635714,
24.3947895175882));
#103918=CARTESIAN_POINT('Ctrl Pts',(0.0189753795552956,2.37297589548929,
24.4000452242043));
#103919=CARTESIAN_POINT('Ctrl Pts',(-0.0595911775780031,2.3710012555996,
24.4053009308204));
#103920=CARTESIAN_POINT('Ctrl Pts',(-0.139389335116919,2.36899566147979,
24.410639025295));
#103921=CARTESIAN_POINT('Ctrl Pts',(-0.21904497246151,2.36295799177357,
24.4159771197697));
#103922=CARTESIAN_POINT('Ctrl Pts',(-0.298119195240333,2.35293922741945,
24.4213152142443));
#103923=CARTESIAN_POINT('Ctrl Pts',(-0.376107035853347,2.34305810851458,
24.4265799698933));
#103924=CARTESIAN_POINT('Ctrl Pts',(-0.453528874794992,2.32930476836392,
24.4318447255424));
#103925=CARTESIAN_POINT('Ctrl Pts',(-0.529974611026111,2.31177961193703,
24.4371094811914));
#103926=CARTESIAN_POINT('Ctrl Pts',(-0.608017697892443,2.29388826347471,
24.4424842450788));
#103927=CARTESIAN_POINT('Ctrl Pts',(-0.685042921119731,2.27206584119297,
24.4478590089663));
#103928=CARTESIAN_POINT('Ctrl Pts',(-0.760633074143077,2.24647176457209,
24.4532337728538));
#103929=CARTESIAN_POINT('Ctrl Pts',(-0.836223227166402,2.22087768795122,
24.4586085367413));
#103930=CARTESIAN_POINT('Ctrl Pts',(-0.910377856403356,2.19151222800949,
24.4639833006288));
#103931=CARTESIAN_POINT('Ctrl Pts',(-0.982706159455222,2.15858441268086,
24.4693580645162));
#103932=CARTESIAN_POINT('Ctrl Pts',(-1.05647039700162,2.12500288111855,
24.4748395336427));
#103933=CARTESIAN_POINT('Ctrl Pts',(-1.12862529498818,2.08758455147576,
24.4803210027692));
#103934=CARTESIAN_POINT('Ctrl Pts',(-1.19875810291352,2.04650362159444,
24.4858024718957));
#103935=CARTESIAN_POINT('Ctrl Pts',(-1.26877844878286,2.00548856738492,
24.4912751511662));
#103936=CARTESIAN_POINT('Ctrl Pts',(-1.33678277824863,1.96082281185819,
24.4967478304366));
#103937=CARTESIAN_POINT('Ctrl Pts',(-1.40238062809185,1.91272753847815,
24.502220509707));
#103938=CARTESIAN_POINT('Ctrl Pts',(-1.46787345789692,1.86470926407687,
24.5076844273948));
#103939=CARTESIAN_POINT('Ctrl Pts',(-1.53096712723125,1.81327265922936,
24.5131483450825));
#103940=CARTESIAN_POINT('Ctrl Pts',(-1.59129919398357,1.75868272798912,
24.5186122627702));
#103941=CARTESIAN_POINT('Ctrl Pts',(-1.65157432175483,1.7041443165331,24.5240710238319));
#103942=CARTESIAN_POINT('Ctrl Pts',(-1.70909270619569,1.64645878773391,
24.5295297848937));
#103943=CARTESIAN_POINT('Ctrl Pts',(-1.76352453575373,1.58593167390484,
24.5349885459554));
#103944=CARTESIAN_POINT('Ctrl Pts',(-1.81791838836082,1.52544678969126,
24.5404434984532));
#103945=CARTESIAN_POINT('Ctrl Pts',(-1.86922967744731,1.46212458763374,
24.545898450951));
#103946=CARTESIAN_POINT('Ctrl Pts',(-1.91716584794229,1.39630697698741,
24.5513534034488));
#103947=CARTESIAN_POINT('Ctrl Pts',(-1.96508035726408,1.33051910769606,
24.5568058909881));
#103948=CARTESIAN_POINT('Ctrl Pts',(-2.00962252561581,1.26223842631984,
24.5622583785274));
#103949=CARTESIAN_POINT('Ctrl Pts',(-2.05054114082474,1.19183853448577,
24.5677108660667));
#103950=CARTESIAN_POINT('Ctrl Pts',(-2.09146309494411,1.12143289810406,
24.5731637985225));
#103951=CARTESIAN_POINT('Ctrl Pts',(-2.12876067700963,1.0489080787843,24.5786167309784));
#103952=CARTESIAN_POINT('Ctrl Pts',(-2.16222733168544,0.97466457235936,
24.5840696634342));
#103953=CARTESIAN_POINT('Ctrl Pts',(-2.19569368267863,0.900421739633752,
24.5895225464091));
#103954=CARTESIAN_POINT('Ctrl Pts',(-2.22532900145471,0.824460652069974,
24.594975429384));
#103955=CARTESIAN_POINT('Ctrl Pts',(-2.25097447102949,0.747202779219605,
24.6004283123589));
#103956=CARTESIAN_POINT('Ctrl Pts',(-2.27663814439174,0.669890066823669,
24.6058850659247));
#103957=CARTESIAN_POINT('Ctrl Pts',(-2.29830617760441,0.591279147240244,
24.6113418194906));
#103958=CARTESIAN_POINT('Ctrl Pts',(-2.31586947221595,0.511807239259295,
24.6167985730565));
#103959=CARTESIAN_POINT('Ctrl Pts',(-2.32815545768968,0.456214554138488,
24.620615715371));
#103960=CARTESIAN_POINT('Ctrl Pts',(-2.33843389221547,0.4002008733358,24.6244328576855));
#103961=CARTESIAN_POINT('Ctrl Pts',(-2.34668236863855,0.343918483395331,
24.62825));
#103962=CARTESIAN_POINT('',(-0.439445221994668,2.33068358199179,24.62825));
#103963=CARTESIAN_POINT('Origin',(0.,0.,24.62825));
#103964=CARTESIAN_POINT('',(-2.37174962922866,0.00132618012251302,23.848589891949));
#103965=CARTESIAN_POINT('Ctrl Pts',(-2.37174962922866,0.00132618012251301,
23.848589891949));
#103966=CARTESIAN_POINT('Ctrl Pts',(-2.37179321578096,-0.0766243090381988,
23.8538460302553));
#103967=CARTESIAN_POINT('Ctrl Pts',(-2.36798967073156,-0.154732553614779,
23.8591021685616));
#103968=CARTESIAN_POINT('Ctrl Pts',(-2.36031867986084,-0.232580721471071,
23.8643583068678));
#103969=CARTESIAN_POINT('Ctrl Pts',(-2.35253306808389,-0.311592106400268,
23.8696929830509));
#103970=CARTESIAN_POINT('Ctrl Pts',(-2.34076339777506,-0.390335080010402,
23.8750276592339));
#103971=CARTESIAN_POINT('Ctrl Pts',(-2.32504340342227,-0.468370830328489,
23.880362335417));
#103972=CARTESIAN_POINT('Ctrl Pts',(-2.30959037090728,-0.545081353241827,
23.8856064164684));
#103973=CARTESIAN_POINT('Ctrl Pts',(-2.29032023401202,-0.621107992227486,
23.8908504975198));
#103974=CARTESIAN_POINT('Ctrl Pts',(-2.26731719654381,-0.69603936149957,
23.8960945785712));
#103975=CARTESIAN_POINT('Ctrl Pts',(-2.2443252230489,-0.770934690371743,
23.9013361373308));
#103976=CARTESIAN_POINT('Ctrl Pts',(-2.21760405191751,-0.844735333714892,
23.9065776960904));
#103977=CARTESIAN_POINT('Ctrl Pts',(-2.18728829509854,-0.917043061488905,
23.91181925485));
#103978=CARTESIAN_POINT('Ctrl Pts',(-2.15697706859641,-0.989339983762697,
23.9170600303231));
#103979=CARTESIAN_POINT('Ctrl Pts',(-2.1230725101674,-1.0601439884811,23.9223008057963));
#103980=CARTESIAN_POINT('Ctrl Pts',(-2.08575750639758,-1.12907647526912,
23.9275415812694));
#103981=CARTESIAN_POINT('Ctrl Pts',(-2.04727975669769,-1.2001569175808,
23.9329456607687));
#103982=CARTESIAN_POINT('Ctrl Pts',(-2.00517572827963,-1.26924678139352,
23.938349740268));
#103983=CARTESIAN_POINT('Ctrl Pts',(-1.95969619098761,-1.33595991763549,
23.9437538197673));
#103984=CARTESIAN_POINT('Ctrl Pts',(-1.91553321992236,-1.40074180595176,
23.9490014590524));
#103985=CARTESIAN_POINT('Ctrl Pts',(-1.86818787072067,-1.46328234982385,
23.9542490983375));
#103986=CARTESIAN_POINT('Ctrl Pts',(-1.81793154408544,-1.5232606354525,
23.9594967376227));
#103987=CARTESIAN_POINT('Ctrl Pts',(-1.76542788963009,-1.58592098877134,
23.964979037229));
#103988=CARTESIAN_POINT('Ctrl Pts',(-1.70974721301348,-1.64578411662999,
23.9704613368355));
#103989=CARTESIAN_POINT('Ctrl Pts',(-1.65124101992624,-1.70252787249224,
23.9759436364419));
#103990=CARTESIAN_POINT('Ctrl Pts',(-1.59273482683902,-1.75927162835447,
23.9814259360483));
#103991=CARTESIAN_POINT('Ctrl Pts',(-1.53140361733028,-1.81289568600277,
23.9869082356546));
#103992=CARTESIAN_POINT('Ctrl Pts',(-1.46763483942312,-1.86312802582417,
23.992390535261));
#103993=CARTESIAN_POINT('Ctrl Pts',(-1.40549780860171,-1.91207499564471,
23.9977325510687));
#103994=CARTESIAN_POINT('Ctrl Pts',(-1.34079355743106,-1.95800139835332,
24.0030745668764));
#103995=CARTESIAN_POINT('Ctrl Pts',(-1.27384742898195,-2.00062759907387,
24.008416582684));
#103996=CARTESIAN_POINT('Ctrl Pts',(-1.20699840183584,-2.04319197307303,
24.0137508502214));
#103997=CARTESIAN_POINT('Ctrl Pts',(-1.1379143461198,-2.08246540313572,
24.0190851177588));
#103998=CARTESIAN_POINT('Ctrl Pts',(-1.06695280520039,-2.11820909590508,
24.0244193852962));
#103999=CARTESIAN_POINT('Ctrl Pts',(-0.9960751231509,-2.15391054853079,
24.0297473490578));
#104000=CARTESIAN_POINT('Ctrl Pts',(-0.923324780467033,-2.186090345244,
24.0350753128194));
#104001=CARTESIAN_POINT('Ctrl Pts',(-0.849086067784299,-2.21455433710591,
24.0404032765809));
#104002=CARTESIAN_POINT('Ctrl Pts',(-0.774895554277249,-2.2429998488394,
24.0457277811842));
#104003=CARTESIAN_POINT('Ctrl Pts',(-0.699219023791896,-2.26773417796237,
24.0510522857874));
#104004=CARTESIAN_POINT('Ctrl Pts',(-0.622461932851828,-2.28861075865914,
24.0563767903906));
#104005=CARTESIAN_POINT('Ctrl Pts',(-0.545730997554536,-2.30948022548043,
24.0616994806228));
#104006=CARTESIAN_POINT('Ctrl Pts',(-0.467920683258017,-2.32649443208219,
24.0670221708551));
#104007=CARTESIAN_POINT('Ctrl Pts',(-0.389451437705792,-2.33955671873304,
24.0723448610873));
#104008=CARTESIAN_POINT('Ctrl Pts',(-0.310984725306586,-2.35261858370567,
24.0776673794919));
#104009=CARTESIAN_POINT('Ctrl Pts',(-0.231859584730243,-2.36172870688726,
24.0829898978964));
#104010=CARTESIAN_POINT('Ctrl Pts',(-0.152505029891621,-2.36684183636291,
24.0883124163009));
#104011=CARTESIAN_POINT('Ctrl Pts',(-0.0730745180504347,-2.37195986005023,
24.0936400293411));
#104012=CARTESIAN_POINT('Ctrl Pts',(0.00658537969246999,-2.37307321674422,
24.0989676423813));
#104013=CARTESIAN_POINT('Ctrl Pts',(0.0860427682642641,-2.37018874871379,
24.1042952554215));
#104014=CARTESIAN_POINT('Ctrl Pts',(0.165536632852462,-2.36730295652829,
24.1096253141764));
#104015=CARTESIAN_POINT('Ctrl Pts',(0.244827337132171,-2.36041572285409,
24.1149553729312));
#104016=CARTESIAN_POINT('Ctrl Pts',(0.323487755211197,-2.34958586451494,
24.1202854316861));
#104017=CARTESIAN_POINT('Ctrl Pts',(0.402287444608774,-2.33873683149191,
24.1256249275166));
#104018=CARTESIAN_POINT('Ctrl Pts',(0.480454157696104,-2.32393131117814,
24.130964423347));
#104019=CARTESIAN_POINT('Ctrl Pts',(0.557570811734681,-2.30527934368083,
24.1363039191774));
#104020=CARTESIAN_POINT('Ctrl Pts',(0.630032081969307,-2.28775335951983,
24.1413210799336));
#104021=CARTESIAN_POINT('Ctrl Pts',(0.701566063359796,-2.26683188662173,
24.1463382406897));
#104022=CARTESIAN_POINT('Ctrl Pts',(0.771841893365145,-2.24264534738476,
24.1513554014458));
#104023=CARTESIAN_POINT('Ctrl Pts',(0.846625670762385,-2.21690732670013,
24.1566943954232));
#104024=CARTESIAN_POINT('Ctrl Pts',(0.920258278935062,-2.18737722550626,
24.1620333894005));
#104025=CARTESIAN_POINT('Ctrl Pts',(0.992328779471983,-2.15417772152895,
24.1673723833779));
#104026=CARTESIAN_POINT('Ctrl Pts',(1.06429683066958,-2.12102541116376,
24.1727037878921));
#104027=CARTESIAN_POINT('Ctrl Pts',(1.13470676339634,-2.08421425145252,
24.1780351924064));
#104028=CARTESIAN_POINT('Ctrl Pts',(1.20316463057147,-2.04391607808193,
24.1833665969206));
#104029=CARTESIAN_POINT('Ctrl Pts',(1.27154475530295,-2.00366366831167,
24.1886919469603));
#104030=CARTESIAN_POINT('Ctrl Pts',(1.3379768193361,-1.9599323504935,24.194017297));
#104031=CARTESIAN_POINT('Ctrl Pts',(1.40208999717757,-1.91294059037771,
24.1993426470397));
#104032=CARTESIAN_POINT('Ctrl Pts',(1.46616336362737,-1.86597801002542,
24.2046646902772));
#104033=CARTESIAN_POINT('Ctrl Pts',(1.52792032624963,-1.81575928178115,
24.2099867335147));
#104034=CARTESIAN_POINT('Ctrl Pts',(1.58701869317772,-1.76254637669609,
24.2153087767522));
#104035=CARTESIAN_POINT('Ctrl Pts',(1.64609862573789,-1.70935007014531,
24.2206291599015));
#104036=CARTESIAN_POINT('Ctrl Pts',(1.70252126248582,-1.653161753986,24.2259495430508));
#104037=CARTESIAN_POINT('Ctrl Pts',(1.75597833633348,-1.59428295632473,
24.2312699262001));
#104038=CARTESIAN_POINT('Ctrl Pts',(1.80943525472935,-1.53540432988147,
24.2365902938778));
#104039=CARTESIAN_POINT('Ctrl Pts',(1.85992631430492,-1.47383558439784,
24.2419106615556));
#104040=CARTESIAN_POINT('Ctrl Pts',(1.90718190670332,-1.40991320202468,
24.2472310292333));
#104041=CARTESIAN_POINT('Ctrl Pts',(1.95448504064441,-1.34592651046575,
24.252556749473));
#104042=CARTESIAN_POINT('Ctrl Pts',(1.99854592669908,-1.27958182858898,
24.2578824697128));
#104043=CARTESIAN_POINT('Ctrl Pts',(2.03913724985554,-1.21124619246113,
24.2632081899525));
#104044=CARTESIAN_POINT('Ctrl Pts',(2.07974826398607,-1.14287740650878,
24.2685364937153));
#104045=CARTESIAN_POINT('Ctrl Pts',(2.1168861436007,-1.07251615593724,24.2738647974781));
#104046=CARTESIAN_POINT('Ctrl Pts',(2.15036991320664,-1.00055349625878,
24.2791931012408));
#104047=CARTESIAN_POINT('Ctrl Pts',(2.18391456865124,-0.928459981932298,
24.2845310938244));
#104048=CARTESIAN_POINT('Ctrl Pts',(2.21379166050636,-0.85475967381021,
24.289869086408));
#104049=CARTESIAN_POINT('Ctrl Pts',(2.23986875603263,-0.779862820147777,
24.2952070789915));
#104050=CARTESIAN_POINT('Ctrl Pts',(2.26447901027324,-0.709178927894634,
24.3002448085379));
#104051=CARTESIAN_POINT('Ctrl Pts',(2.28570510192159,-0.637429778567851,
24.3052825380843));
#104052=CARTESIAN_POINT('Ctrl Pts',(2.30347747792983,-0.564968646183165,
24.3103202676306));
#104053=CARTESIAN_POINT('Ctrl Pts',(2.32208249405447,-0.489112692212707,
24.3155940160252));
#104054=CARTESIAN_POINT('Ctrl Pts',(2.33697600536397,-0.412174836926209,
24.3208677644198));
#104055=CARTESIAN_POINT('Ctrl Pts',(2.34803532246676,-0.334556702142403,
24.3261415128144));
#104056=CARTESIAN_POINT('Ctrl Pts',(2.35907837887199,-0.257052690590922,
24.3314075071292));
#104057=CARTESIAN_POINT('Ctrl Pts',(2.36629836182808,-0.178870854899216,
24.336673501444));
#104058=CARTESIAN_POINT('Ctrl Pts',(2.36962290107848,-0.10042593880272,
24.3419394957588));
#104059=CARTESIAN_POINT('Ctrl Pts',(2.37297273989634,-0.0213840610531468,
24.3472455640111));
#104060=CARTESIAN_POINT('Ctrl Pts',(2.37236746320867,0.0579244408043494,
24.3525516322635));
#104061=CARTESIAN_POINT('Ctrl Pts',(2.36778602442185,0.137067155265542,
24.3578577005158));
#104062=CARTESIAN_POINT('Ctrl Pts',(2.36324722143088,0.215473351620838,
24.363114389424));
#104063=CARTESIAN_POINT('Ctrl Pts',(2.35480598256657,0.293716345200748,
24.3683710783321));
#104064=CARTESIAN_POINT('Ctrl Pts',(2.34249411781659,0.371374972897555,
24.3736277672403));
#104065=CARTESIAN_POINT('Ctrl Pts',(2.33018583400637,0.449011013368738,
24.378882927226));
#104066=CARTESIAN_POINT('Ctrl Pts',(2.31400923306241,0.526062551519991,
24.3841380872117));
#104067=CARTESIAN_POINT('Ctrl Pts',(2.29404778847505,0.602115276913609,
24.3893932471974));
#104068=CARTESIAN_POINT('Ctrl Pts',(2.27408560879438,0.678170802998758,
24.3946486007078));
#104069=CARTESIAN_POINT('Ctrl Pts',(2.25033843198666,0.753226979464458,
24.3999039542182));
#104070=CARTESIAN_POINT('Ctrl Pts',(2.22294007465867,0.826882994731737,
24.4051593077287));
#104071=CARTESIAN_POINT('Ctrl Pts',(2.19508051054008,0.901778889237123,
24.4105031265692));
#104072=CARTESIAN_POINT('Ctrl Pts',(2.16344587286729,0.975226562332597,
24.4158469454098));
#104073=CARTESIAN_POINT('Ctrl Pts',(2.12822766055512,1.04682619729737,24.4211907642503));
#104074=CARTESIAN_POINT('Ctrl Pts',(2.0935328011096,1.11736184088527,24.4264551723904));
#104075=CARTESIAN_POINT('Ctrl Pts',(2.05536045962072,1.18610361502611,24.4317195805305));
#104076=CARTESIAN_POINT('Ctrl Pts',(2.01393889054517,1.25269637488486,24.4369839886706));
#104077=CARTESIAN_POINT('Ctrl Pts',(1.97158008909876,1.32079590746127,24.4423675128613));
#104078=CARTESIAN_POINT('Ctrl Pts',(1.92582353812938,1.38664755401379,24.4477510370521));
#104079=CARTESIAN_POINT('Ctrl Pts',(1.87695710355523,1.44990692594854,24.4531345612429));
#104080=CARTESIAN_POINT('Ctrl Pts',(1.82809066898111,1.51316629788328,24.4585180854337));
#104081=CARTESIAN_POINT('Ctrl Pts',(1.77611475814255,1.57383305154166,24.4639016096245));
#104082=CARTESIAN_POINT('Ctrl Pts',(1.72135581562934,1.63160418560969,24.4692851338153));
#104083=CARTESIAN_POINT('Ctrl Pts',(1.66560241229698,1.69042448400909,24.4747664265829));
#104084=CARTESIAN_POINT('Ctrl Pts',(1.60674482849547,1.74647496705611,24.4802477193504));
#104085=CARTESIAN_POINT('Ctrl Pts',(1.54508202303006,1.79942201959667,24.485729012118));
#104086=CARTESIAN_POINT('Ctrl Pts',(1.48351820138346,1.85228407922429,24.4912015060759));
#104087=CARTESIAN_POINT('Ctrl Pts',(1.41915844225612,1.90205233235669,24.4966740000338));
#104088=CARTESIAN_POINT('Ctrl Pts',(1.35233888606395,1.94842952136825,24.5021464939917));
#104089=CARTESIAN_POINT('Ctrl Pts',(1.28562644926117,1.9947323624426,24.507610214916));
#104090=CARTESIAN_POINT('Ctrl Pts',(1.21646242279782,2.03765471372029,24.5130739358403));
#104091=CARTESIAN_POINT('Ctrl Pts',(1.1452152697361,2.07694006857764,24.5185376567646));
#104092=CARTESIAN_POINT('Ctrl Pts',(1.07403544407832,2.11618829941189,24.5239962145613));
#104093=CARTESIAN_POINT('Ctrl Pts',(1.0007767869189,2.15180615708435,24.529454772358));
#104094=CARTESIAN_POINT('Ctrl Pts',(0.925835471708704,2.18358117362875,
24.5349133301546));
#104095=CARTESIAN_POINT('Ctrl Pts',(0.850946524880646,2.21533398604978,
24.5403680735554));
#104096=CARTESIAN_POINT('Ctrl Pts',(0.774377659975556,2.24324912780332,
24.5458228169563));
#104097=CARTESIAN_POINT('Ctrl Pts',(0.696547330083548,2.26716119397221,
24.5512775603571));
#104098=CARTESIAN_POINT('Ctrl Pts',(0.618752244884669,2.29106243179904,
24.5567298336314));
#104099=CARTESIAN_POINT('Ctrl Pts',(0.539697248628001,2.31096407270931,
24.5621821069058));
#104100=CARTESIAN_POINT('Ctrl Pts',(0.459817314452615,2.32675011546784,
24.5676343801802));
#104101=CARTESIAN_POINT('Ctrl Pts',(0.3799308894113,2.34253744096511,24.5730870964941));
#104102=CARTESIAN_POINT('Ctrl Pts',(0.299219819518825,2.35420840571182,
24.5785398128081));
#104103=CARTESIAN_POINT('Ctrl Pts',(0.218129982814233,2.3616979851576,24.5839925291221));
#104104=CARTESIAN_POINT('Ctrl Pts',(0.137040934973298,2.36918749174275,
24.5894451923906));
#104105=CARTESIAN_POINT('Ctrl Pts',(0.0555735637191289,2.37249565997143,
24.594897855659));
#104106=CARTESIAN_POINT('Ctrl Pts',(-0.0258219500668697,2.37160943019603,
24.6003505189275));
#104107=CARTESIAN_POINT('Ctrl Pts',(-0.107275365906951,2.37072256998633,
24.6058070610388));
#104108=CARTESIAN_POINT('Ctrl Pts',(-0.188656384466935,2.36563536069865,
24.6112636031501));
#104109=CARTESIAN_POINT('Ctrl Pts',(-0.269516104398332,2.35638688079228,
24.6167201452614));
#104110=CARTESIAN_POINT('Ctrl Pts',(-0.326469195812739,2.34987276570507,
24.6205634301743));
#104111=CARTESIAN_POINT('Ctrl Pts',(-0.383163708688597,2.34129533654314,
24.6244067150871));
#104112=CARTESIAN_POINT('Ctrl Pts',(-0.439445221994602,2.3306835819918,
24.62825));
#104113=CARTESIAN_POINT('Ctrl Pts',(-2.3717496963229,0.00120020508255365,
23.846830862774));
#104114=CARTESIAN_POINT('Ctrl Pts',(-2.37172951172941,0.0410873911748103,
23.8439742920646));
#104115=CARTESIAN_POINT('Ctrl Pts',(-2.3707031149012,0.0809706682818765,
23.8411464421663));
#104116=CARTESIAN_POINT('Ctrl Pts',(-2.3677819269107,0.138244320542981,
23.8371431007408));
#104117=CARTESIAN_POINT('Ctrl Pts',(-2.36670035225053,0.155667035764427,
23.8359329655335));
#104118=CARTESIAN_POINT('Ctrl Pts',(-2.36542649454004,0.173076750108263,
23.8347324553251));
#104119=CARTESIAN_POINT('Origin',(0.,0.,24.5));
#104120=CARTESIAN_POINT('',(-2.86732885971112,2.07314048065506E-11,24.1326711402889));
#104121=CARTESIAN_POINT('Ctrl Pts',(-0.439445221994083,2.33068358199193,
24.62825));
#104122=CARTESIAN_POINT('Ctrl Pts',(-0.252498301061248,2.37423453518697,
24.6200912309808));
#104123=CARTESIAN_POINT('Ctrl Pts',(-0.0607381560960383,2.39429049548881,
24.6126350903112));
#104124=CARTESIAN_POINT('Ctrl Pts',(0.331258812598871,2.3882268490475,24.5972095049321));
#104125=CARTESIAN_POINT('Ctrl Pts',(0.530411343122747,2.3601563111261,24.5892481862326));
#104126=CARTESIAN_POINT('Ctrl Pts',(1.0261899805794,2.22744702151644,24.5675775528286));
#104127=CARTESIAN_POINT('Ctrl Pts',(1.31173953974594,2.08916181590285,24.5530814337998));
#104128=CARTESIAN_POINT('Ctrl Pts',(1.86756500186408,1.67230844586517,24.5222920288584));
#104129=CARTESIAN_POINT('Ctrl Pts',(2.06239788769764,1.41434287106475,24.5109590645687));
#104130=CARTESIAN_POINT('Ctrl Pts',(2.33502645953121,0.960352452908593,
24.4915954879617));
#104131=CARTESIAN_POINT('Ctrl Pts',(2.44004047150229,0.689439917790241,
24.4807543798427));
#104132=CARTESIAN_POINT('Ctrl Pts',(2.56661735298791,0.0761676158146572,
24.4546463607253));
#104133=CARTESIAN_POINT('Ctrl Pts',(2.56936506573517,-0.267196718376941,
24.4390319275492));
#104134=CARTESIAN_POINT('Ctrl Pts',(2.43860393076487,-0.928950669615914,
24.4121318022675));
#104135=CARTESIAN_POINT('Ctrl Pts',(2.30709388532842,-1.24234973758447,
24.4012358857251));
#104136=CARTESIAN_POINT('Ctrl Pts',(2.03281881994024,-1.65534374027188,
24.3833376745132));
#104137=CARTESIAN_POINT('Ctrl Pts',(1.93226128984899,-1.78052177711593,
24.377347194124));
#104138=CARTESIAN_POINT('Ctrl Pts',(1.57667382943023,-2.14998763016186,
24.3572490357678));
#104139=CARTESIAN_POINT('Ctrl Pts',(1.28320635471831,-2.354434589116,24.3418379695899));
#104140=CARTESIAN_POINT('Ctrl Pts',(0.690934627167233,-2.60924580390895,
24.3166545770257));
#104141=CARTESIAN_POINT('Ctrl Pts',(0.405746860161139,-2.67782592413793,
24.3071921961513));
#104142=CARTESIAN_POINT('Ctrl Pts',(-0.238690314097037,-2.72752391529108,
24.2852767058604));
#104143=CARTESIAN_POINT('Ctrl Pts',(-0.597229103766921,-2.68511165509286,
24.2723822195236));
#104144=CARTESIAN_POINT('Ctrl Pts',(-1.18860058374266,-2.49648698036282,
24.2476728398377));
#104145=CARTESIAN_POINT('Ctrl Pts',(-1.51651301242023,-2.35274314730956,
24.2325132567834));
#104146=CARTESIAN_POINT('Ctrl Pts',(-2.1008881867237,-1.87203354808299,
24.2062476358257));
#104147=CARTESIAN_POINT('Ctrl Pts',(-2.3194136975749,-1.61103995421478,
24.1961087219178));
#104148=CARTESIAN_POINT('Ctrl Pts',(-2.59356453211614,-1.13401729928166,
24.1773943967977));
#104149=CARTESIAN_POINT('Ctrl Pts',(-2.67903863724766,-0.937448621830812,
24.1696977612319));
#104150=CARTESIAN_POINT('Ctrl Pts',(-2.81541952069172,-0.495679813412592,
24.1521284724464));
#104151=CARTESIAN_POINT('Ctrl Pts',(-2.85786427493396,-0.248796193213268,
24.1421357250696));
#104152=CARTESIAN_POINT('Ctrl Pts',(-2.86732885971112,4.1433870223706E-11,
24.1326711402889));
#104153=CARTESIAN_POINT('Ctrl Pts',(0.261019001493371,2.92766592745733,
24.0607213977006));
#104154=CARTESIAN_POINT('Ctrl Pts',(0.163059463857162,2.92391694727034,
24.0731547417967));
#104155=CARTESIAN_POINT('Ctrl Pts',(0.065549179711928,2.91537842014871,
24.085491147687));
#104156=CARTESIAN_POINT('Ctrl Pts',(-0.0310928127263946,2.90207104271783,
24.0977623977378));
#104157=CARTESIAN_POINT('Ctrl Pts',(-0.129744753844374,2.88848690003178,
24.1102888637896));
#104158=CARTESIAN_POINT('Ctrl Pts',(-0.227491648374659,2.86993346603253,
24.1227473148004));
#104159=CARTESIAN_POINT('Ctrl Pts',(-0.323877162841241,2.84642522927533,
24.135208035046));
#104160=CARTESIAN_POINT('Ctrl Pts',(-0.414180307230089,2.82440047057626,
24.1468824264289));
#104161=CARTESIAN_POINT('Ctrl Pts',(-0.503288202647077,2.79802678119133,
24.1585592114491));
#104162=CARTESIAN_POINT('Ctrl Pts',(-0.59082047893217,2.76730769459531,
24.1703249806927));
#104163=CARTESIAN_POINT('Ctrl Pts',(-0.619499004310833,2.75724308595102,
24.1741798434492));
#104164=CARTESIAN_POINT('Ctrl Pts',(-0.648008369034724,2.74671193578173,
24.1780444749336));
#104165=CARTESIAN_POINT('Ctrl Pts',(-0.67633512265761,2.73571405062978,
24.1819225409948));
#104166=CARTESIAN_POINT('Ctrl Pts',(-0.698212434468718,2.72722016651107,
24.1849176480788));
#104167=CARTESIAN_POINT('Ctrl Pts',(-0.719980822195904,2.71844788221606,
24.1879207747589));
#104168=CARTESIAN_POINT('Ctrl Pts',(-0.741634076278984,2.70939702033487,
24.1909337286391));
#104169=CARTESIAN_POINT('Ctrl Pts',(-0.754534483051411,2.70400476846083,
24.1927287627938));
#104170=CARTESIAN_POINT('Ctrl Pts',(-0.767392655677935,2.69851414135042,
24.1945271022539));
#104171=CARTESIAN_POINT('Ctrl Pts',(-0.780196516280907,2.69293005235174,
24.1963276099237));
#104172=CARTESIAN_POINT('Ctrl Pts',(-0.863568168703393,2.65656955597254,
24.2080515191642));
#104173=CARTESIAN_POINT('Ctrl Pts',(-0.944764154889942,2.61619706804206,
24.2198839165918));
#104174=CARTESIAN_POINT('Ctrl Pts',(-1.02351699322116,2.57187520645671,
24.2319448862063));
#104175=CARTESIAN_POINT('Ctrl Pts',(-1.06274981800173,2.54979509015393,
24.2379533795839));
#104176=CARTESIAN_POINT('Ctrl Pts',(-1.10137646364671,2.52673412661812,
24.2440188319126));
#104177=CARTESIAN_POINT('Ctrl Pts',(-1.13936436506882,2.50269537352569,
24.2501572246662));
#104178=CARTESIAN_POINT('Ctrl Pts',(-1.21752318249746,2.45323645519046,
24.2627867593489));
#104179=CARTESIAN_POINT('Ctrl Pts',(-1.29298521017775,2.39963837998968,
24.2757248979837));
#104180=CARTESIAN_POINT('Ctrl Pts',(-1.36553505111976,2.34210598208496,
24.288884656243));
#104181=CARTESIAN_POINT('Ctrl Pts',(-1.4404209245149,2.28272109840127,24.302468145581));
#104182=CARTESIAN_POINT('Ctrl Pts',(-1.51220416706068,2.21914223789968,
24.3162871082082));
#104183=CARTESIAN_POINT('Ctrl Pts',(-1.58055507906647,2.15159877555774,
24.3302562578134));
#104184=CARTESIAN_POINT('Ctrl Pts',(-1.59151079358875,2.14077248415138,
24.3324953210637));
#104185=CARTESIAN_POINT('Ctrl Pts',(-1.60237813755092,2.12984438461238,
24.3347382762028));
#104186=CARTESIAN_POINT('Ctrl Pts',(-1.61315554165587,2.1188154898271,24.3369848138799));
#104187=CARTESIAN_POINT('Ctrl Pts',(-1.62162021392896,2.11015329446144,
24.3387492652264));
#104188=CARTESIAN_POINT('Ctrl Pts',(-1.63002854377014,2.1014297392921,24.3405157547639));
#104189=CARTESIAN_POINT('Ctrl Pts',(-1.63837321661078,2.09265245906859,
24.3422827254666));
#104190=CARTESIAN_POINT('Ctrl Pts',(-1.70020980675046,2.02761011527781,
24.3553765213791));
#104191=CARTESIAN_POINT('Ctrl Pts',(-1.75865725508163,1.9595127394449,24.3685160721984));
#104192=CARTESIAN_POINT('Ctrl Pts',(-1.81349417189549,1.88863596512469,
24.3816595102506));
#104193=CARTESIAN_POINT('Ctrl Pts',(-1.86812219692787,1.81802918365808,
24.3947528806412));
#104194=CARTESIAN_POINT('Ctrl Pts',(-1.9191664041851,1.74466328829154,24.4078498587507));
#104195=CARTESIAN_POINT('Ctrl Pts',(-1.96636441994797,1.66882873674077,
24.4209345908626));
#104196=CARTESIAN_POINT('Ctrl Pts',(-2.01275888332875,1.5942852783336,24.4337965537015));
#104197=CARTESIAN_POINT('Ctrl Pts',(-2.05543625621973,1.51735616516087,
24.44664654175));
#104198=CARTESIAN_POINT('Ctrl Pts',(-2.09411646704632,1.43834332346446,
24.4594970392244));
#104199=CARTESIAN_POINT('Ctrl Pts',(-2.11496000855021,1.39576580358944,
24.4664217656344));
#104200=CARTESIAN_POINT('Ctrl Pts',(-2.13464239483683,1.35258370172021,
24.4733471300791));
#104201=CARTESIAN_POINT('Ctrl Pts',(-2.15311705514232,1.30884776401137,
24.4802786815796));
#104202=CARTESIAN_POINT('Ctrl Pts',(-2.15871542149974,1.29559448637429,
24.4823791458958));
#104203=CARTESIAN_POINT('Ctrl Pts',(-2.16420353529864,1.28228872410263,
24.4844804552686));
#104204=CARTESIAN_POINT('Ctrl Pts',(-2.16957799719695,1.26893709952057,
24.4865819988588));
#104205=CARTESIAN_POINT('Ctrl Pts',(-2.20143397005055,1.18979820184384,
24.4990384487929));
#104206=CARTESIAN_POINT('Ctrl Pts',(-2.22918818249487,1.10932539194073,
24.511457595635));
#104207=CARTESIAN_POINT('Ctrl Pts',(-2.25269334859829,1.02782771604728,
24.5239028418307));
#104208=CARTESIAN_POINT('Ctrl Pts',(-2.27585078395726,0.947535700534353,
24.5361639755337));
#104209=CARTESIAN_POINT('Ctrl Pts',(-2.29488421224564,0.866249028053862,
24.5484506467591));
#104210=CARTESIAN_POINT('Ctrl Pts',(-2.30963484158374,0.784256574631775,
24.5608461556698));
#104211=CARTESIAN_POINT('Ctrl Pts',(-2.32395200420878,0.704673577678735,
24.5728774061898));
#104212=CARTESIAN_POINT('Ctrl Pts',(-2.33423483748586,0.62442576084056,
24.5850115045248));
#104213=CARTESIAN_POINT('Ctrl Pts',(-2.34031596902869,0.54376943844709,
24.5973422971468));
#104214=CARTESIAN_POINT('Ctrl Pts',(-2.34532119633868,0.477383236352302,
24.607491464214));
#104215=CARTESIAN_POINT('Ctrl Pts',(-2.34747983552917,0.410720154511199,
24.6177743044544));
#104216=CARTESIAN_POINT('Ctrl Pts',(-2.34668236863854,0.343918483395396,
24.62825));
#104217=CARTESIAN_POINT('',(-2.86788692854124,0.00160361121558927,24.1321126231202));
#104218=CARTESIAN_POINT('Ctrl Pts',(-2.86788692854124,0.00160361121558927,
24.1321126231202));
#104219=CARTESIAN_POINT('Ctrl Pts',(-2.87138354375354,0.0925483242271544,
24.1285651557038));
#104220=CARTESIAN_POINT('Ctrl Pts',(-2.87043240913469,0.183377764669063,
24.1251424880545));
#104221=CARTESIAN_POINT('Ctrl Pts',(-2.86500154312585,0.273846896636642,
24.121940590448));
#104222=CARTESIAN_POINT('Ctrl Pts',(-2.8596177192724,0.363532385082704,
24.118766427675));
#104223=CARTESIAN_POINT('Ctrl Pts',(-2.84983102614631,0.45287124908063,
24.1158088702711));
#104224=CARTESIAN_POINT('Ctrl Pts',(-2.83576722797345,0.541646561528832,
24.112967480463));
#104225=CARTESIAN_POINT('Ctrl Pts',(-2.83488131448154,0.547238738413019,
24.112788494279));
#104226=CARTESIAN_POINT('Ctrl Pts',(-2.83397841666917,0.552828690663718,
24.1126099690542));
#104227=CARTESIAN_POINT('Ctrl Pts',(-2.83305856079414,0.558416368474958,
24.1124318796832));
#104228=CARTESIAN_POINT('Ctrl Pts',(-2.81723894257586,0.654512868045957,
24.1093691109023));
#104229=CARTESIAN_POINT('Ctrl Pts',(-2.79640642791614,0.749933056172748,
24.1064347116094));
#104230=CARTESIAN_POINT('Ctrl Pts',(-2.77068225948842,0.844353392490152,
24.1035171613742));
#104231=CARTESIAN_POINT('Ctrl Pts',(-2.75536245067389,0.90058461740422,
24.1017796392485));
#104232=CARTESIAN_POINT('Ctrl Pts',(-2.7383071381334,0.95646026262038,24.1000484439012));
#104233=CARTESIAN_POINT('Ctrl Pts',(-2.71953884864361,1.01190378419375,
24.0983038033337));
#104234=CARTESIAN_POINT('Ctrl Pts',(-2.71440485874386,1.02707013592327,
24.0978265639424));
#104235=CARTESIAN_POINT('Ctrl Pts',(-2.70914211347083,1.0422054863952,24.0973482919757));
#104236=CARTESIAN_POINT('Ctrl Pts',(-2.70375754058507,1.05729073335641,
24.0968691842923));
#104237=CARTESIAN_POINT('Ctrl Pts',(-2.67057083570499,1.15026554297752,
24.0939163028599));
#104238=CARTESIAN_POINT('Ctrl Pts',(-2.63270767785936,1.24148802007126,
24.0909242366852));
#104239=CARTESIAN_POINT('Ctrl Pts',(-2.59041302986795,1.33060124549307,
24.0878291018868));
#104240=CARTESIAN_POINT('Ctrl Pts',(-2.54756420783155,1.42088209469093,
24.0846934124686));
#104241=CARTESIAN_POINT('Ctrl Pts',(-2.5001667870123,1.50899753746854,24.0814517729648));
#104242=CARTESIAN_POINT('Ctrl Pts',(-2.44846895759319,1.59456926778762,
24.078074027962));
#104243=CARTESIAN_POINT('Ctrl Pts',(-2.39685116861105,1.68000851287929,
24.0747015125054));
#104244=CARTESIAN_POINT('Ctrl Pts',(-2.34094650304388,1.76291158751629,
24.0711933279152));
#104245=CARTESIAN_POINT('Ctrl Pts',(-2.28099543401435,1.84290139915102,
24.0675563539964));
#104246=CARTESIAN_POINT('Ctrl Pts',(-2.23753645918706,1.9008866071973,24.0649198846132));
#104247=CARTESIAN_POINT('Ctrl Pts',(-2.19195107688015,1.95734095850997,
24.0622165183716));
#104248=CARTESIAN_POINT('Ctrl Pts',(-2.14432694750403,2.01212145383533,
24.0594607972727));
#104249=CARTESIAN_POINT('Ctrl Pts',(-2.86732885971111,4.14306955368129E-11,
24.1326711402889));
#104250=CARTESIAN_POINT('Ctrl Pts',(-2.86734966299874,0.000546857498953776,
24.1326503370013));
#104251=CARTESIAN_POINT('Ctrl Pts',(-2.8673703069382,0.00109372421048583,
24.1326295366167));
#104252=CARTESIAN_POINT('Ctrl Pts',(-2.86739079150826,0.00164060010131629,
24.1326087391507));
#104253=CARTESIAN_POINT('',(-2.,-2.44929359829471E-16,25.));
#104254=CARTESIAN_POINT('',(-2.5,3.06161699786838E-16,24.5));
#104255=CARTESIAN_POINT('Origin',(0.,0.,25.));
#104256=CARTESIAN_POINT('Ctrl Pts',(1.70915978346929,-2.39931405854793,
-0.331525224265037));
#104257=CARTESIAN_POINT('Ctrl Pts',(2.50802990535057,-1.83028257961684,
-0.278535267625054));
#104258=CARTESIAN_POINT('Ctrl Pts',(3.47835091600118,0.158233065351694,
-0.172581332490446));
#104259=CARTESIAN_POINT('Ctrl Pts',(1.74735082995237,3.01534926870841,-0.0136634188612144));
#104260=CARTESIAN_POINT('Ctrl Pts',(-1.58653605777943,3.09925236818656,
0.145228516622657));
#104261=CARTESIAN_POINT('Ctrl Pts',(-3.46537971655703,0.346752180227429,
0.304120452106527));
#104262=CARTESIAN_POINT('Ctrl Pts',(-2.16822080433006,-2.72587883991964,
0.463012387590399));
#104263=CARTESIAN_POINT('Ctrl Pts',(1.11658306675895,-3.29872810449766,
0.621904323074271));
#104264=CARTESIAN_POINT('Ctrl Pts',(3.37779425300656,-0.848538639554367,
0.780796258558139));
#104265=CARTESIAN_POINT('Ctrl Pts',(2.54292626363602,2.37976338639486,0.939688194042012));
#104266=CARTESIAN_POINT('Ctrl Pts',(-0.622859592152919,3.42656460546492,
1.09858012952589));
#104267=CARTESIAN_POINT('Ctrl Pts',(-3.21770598735519,1.33261290508638,
1.25747206500976));
#104268=CARTESIAN_POINT('Ctrl Pts',(-2.86316102813789,-1.98288004182896,
1.41636400049363));
#104269=CARTESIAN_POINT('Ctrl Pts',(0.115806994067153,-3.48080913522564,
1.5752559359775));
#104270=CARTESIAN_POINT('Ctrl Pts',(2.98862212193643,-1.78818668555055,
1.73414787146137));
#104271=CARTESIAN_POINT('Ctrl Pts',(3.12202035689114,1.54352265706882,1.89303980694524));
#104272=CARTESIAN_POINT('Ctrl Pts',(0.393724875594412,3.4604112461881,2.05193174242911));
#104273=CARTESIAN_POINT('Ctrl Pts',(-2.69546468997399,2.20543421423937,
2.21082367791299));
#104274=CARTESIAN_POINT('Ctrl Pts',(-3.31394901819685,-1.07107955396263,
2.36971561339685));
#104275=CARTESIAN_POINT('Ctrl Pts',(-0.894815353243767,-3.36582441055242,
2.52860754888072));
#104276=CARTESIAN_POINT('Ctrl Pts',(2.34452011799349,-2.57540183372274,
2.6874994843646));
#104277=CARTESIAN_POINT('Ctrl Pts',(3.43483152420483,0.575674793782504,
2.84639141984846));
#104278=CARTESIAN_POINT('Ctrl Pts',(1.37672220743361,3.19907875884332,3.00528335533234));
#104279=CARTESIAN_POINT('Ctrl Pts',(-1.94331237532776,2.89015675325956,
3.1641752908162));
#104280=CARTESIAN_POINT('Ctrl Pts',(-3.48207621113987,-0.0679285026538166,
3.32306722630008));
#104281=CARTESIAN_POINT('Ctrl Pts',(-1.8291141108827,-2.96374941187267,
3.48195916178395));
#104282=CARTESIAN_POINT('Ctrl Pts',(1.50044281000745,-3.14295090576371,
3.64085109726782));
#104283=CARTESIAN_POINT('Ctrl Pts',(3.45467020416205,-0.441274062288436,
3.79974303275169));
#104284=CARTESIAN_POINT('Ctrl Pts',(2.24229244183481,2.66488153982562,3.95863496823556));
#104285=CARTESIAN_POINT('Ctrl Pts',(-1.02540591201219,3.3283647236689,4.11752690371944));
#104286=CARTESIAN_POINT('Ctrl Pts',(-3.35320104615321,0.941016344939749,
4.2764188392033));
#104287=CARTESIAN_POINT('Ctrl Pts',(-2.6073992534791,-2.30888244615925,
4.43531077468718));
#104288=CARTESIAN_POINT('Ctrl Pts',(0.528385788631286,-3.44242319825643,
4.59420271017105));
#104289=CARTESIAN_POINT('Ctrl Pts',(3.17984408930906,-1.42058459272181,
4.75309464565492));
#104290=CARTESIAN_POINT('Ctrl Pts',(2.91660718202859,1.90338423948601,4.91198658113878));
#104291=CARTESIAN_POINT('Ctrl Pts',(-0.0200378352627403,3.48268107965435,
5.07087851662267));
#104292=CARTESIAN_POINT('Ctrl Pts',(-2.93831585694904,1.86969755367164,
5.22977045210653));
#104293=CARTESIAN_POINT('Ctrl Pts',(-3.16328725505062,-1.45708021722857,
5.3886623875904));
#104294=CARTESIAN_POINT('Ctrl Pts',(-0.488739700424178,-3.44827529681711,
5.54755432307427));
#104295=CARTESIAN_POINT('Ctrl Pts',(2.63379436635632,-2.27872689306034,
5.70644625855815));
#104296=CARTESIAN_POINT('Ctrl Pts',(3.34215100721795,0.979538494577416,
5.86533819404202));
#104297=CARTESIAN_POINT('Ctrl Pts',(0.987039361146014,3.33994346014362,
6.02423012952589));
#104298=CARTESIAN_POINT('Ctrl Pts',(-2.27280811951147,2.63890361121622,
6.18312206500976));
#104299=CARTESIAN_POINT('Ctrl Pts',(-3.44936385740458,-0.480996877992278,
6.34201400049363));
#104300=CARTESIAN_POINT('Ctrl Pts',(-1.46417832016298,-3.16000804811825,
6.5009059359775));
#104301=CARTESIAN_POINT('Ctrl Pts',(1.86309614141146,-2.94250603827164,
6.65979787146138));
#104302=CARTESIAN_POINT('Ctrl Pts',(3.48262731658261,-0.0278566186018233,
6.81868980694524));
#104303=CARTESIAN_POINT('Ctrl Pts',(1.90992740569023,2.91232661671056,6.97758174242912));
#104304=CARTESIAN_POINT('Ctrl Pts',(-1.41344206652397,3.18302537564308,
7.13647367791298));
#104305=CARTESIAN_POINT('Ctrl Pts',(-3.4412282641157,0.536112909430946,
7.29536561339686));
#104306=CARTESIAN_POINT('Ctrl Pts',(-2.31473039960172,-2.60220909893247,
7.45425754888073));
#104307=CARTESIAN_POINT('Ctrl Pts',(0.933485830320249,-3.35530523529509,
7.6131494843646));
#104308=CARTESIAN_POINT('Ctrl Pts',(3.32605423603801,-1.03287571195233,
7.77204141984847));
#104309=CARTESIAN_POINT('Ctrl Pts',(2.66990890897756,2.23630396752532,7.93093335533233));
#104310=CARTESIAN_POINT('Ctrl Pts',(-0.433517002948718,3.45565218527005,
8.08982529081622));
#104311=CARTESIAN_POINT('Ctrl Pts',(-3.13957439756035,1.50749514745186,
8.24871722630007));
#104312=CARTESIAN_POINT('Ctrl Pts',(-2.96784841834379,-1.82245570128375,
8.40760916178396));
#104313=CARTESIAN_POINT('Ctrl Pts',(-0.0757458043231992,-3.48191493154769,
8.56650109726781));
#104314=CARTESIAN_POINT('Ctrl Pts',(2.88578660772602,-1.94979605909861,
8.72539303275171));
#104315=CARTESIAN_POINT('Ctrl Pts',(3.20216153391245,1.36953661073329,8.88428496823555));
#104316=CARTESIAN_POINT('Ctrl Pts',(0.58338473069051,3.4335304386891,9.04317690371945));
#104317=CARTESIAN_POINT('Ctrl Pts',(-2.57013171107317,2.35029615264616,
9.2020688392033));
#104318=CARTESIAN_POINT('Ctrl Pts',(-3.36782492010113,-0.887256628576624,
9.36096077468718));
#104319=CARTESIAN_POINT('Ctrl Pts',(-1.07851672901495,-3.31153600050524,
9.51985271017105));
#104320=CARTESIAN_POINT('Ctrl Pts',(2.19937689376752,-2.70040928315855,
9.67874464565492));
#104321=CARTESIAN_POINT('Ctrl Pts',(3.4612869926098,0.385955142727138,9.8376365811388));
#104322=CARTESIAN_POINT('Ctrl Pts',(1.55052688267461,3.11854700197234,9.99652851662266));
#104323=CARTESIAN_POINT('Ctrl Pts',(-1.78147060488158,2.99262952958601,
10.1554204521065));
#104324=CARTESIAN_POINT('Ctrl Pts',(-3.48054405927083,0.12362066527021,
10.3143123875904));
#104325=CARTESIAN_POINT('Ctrl Pts',(-1.98929597408154,-2.85870084914638,
10.4732043230742));
#104326=CARTESIAN_POINT('Ctrl Pts',(1.32537215309932,-3.22069211089731,
10.6320962585581));
#104327=CARTESIAN_POINT('Ctrl Pts',(3.42518327632198,-0.630546224325814,
10.790988194042));
#104328=CARTESIAN_POINT('Ctrl Pts',(2.38541742612644,2.53756826913872,10.9498801295259));
#104329=CARTESIAN_POINT('Ctrl Pts',(-0.840859632047186,3.37970769395828,
11.1087720650097));
#104330=CARTESIAN_POINT('Ctrl Pts',(-3.29639149918183,1.12395378086871,
11.2676640004936));
#104331=CARTESIAN_POINT('Ctrl Pts',(-2.73039896563801,-2.16203388175354,
11.4265559359775));
#104332=CARTESIAN_POINT('Ctrl Pts',(0.338320292055619,-3.46626721378932,
11.5854478714614));
#104333=CARTESIAN_POINT('Ctrl Pts',(3.09692983797972,-1.59326538782405,
11.7443398069452));
#104334=CARTESIAN_POINT('Ctrl Pts',(3.0168446854836,1.74014860315912,11.9032317424291));
#104335=CARTESIAN_POINT('Ctrl Pts',(0.171472147521156,3.47851495900647,
12.062123677913));
#104336=CARTESIAN_POINT('Ctrl Pts',(-2.83107446333298,2.02841968055707,
12.2210156133968));
#104337=CARTESIAN_POINT('Ctrl Pts',(-3.23861360216155,-1.28095704584561,
12.3799075488807));
#104338=CARTESIAN_POINT('Ctrl Pts',(-0.677588471324607,-3.41618835559974,
12.5387994843646));
#104339=CARTESIAN_POINT('Ctrl Pts',(2.50452493141022,-2.42008757803348,
12.6976914198484));
#104340=CARTESIAN_POINT('Ctrl Pts',(3.39095130963907,0.794303615165157,
12.8565833553323));
#104341=CARTESIAN_POINT('Ctrl Pts',(1.16917827462158,3.28062359614148,13.0154752908162));
#104342=CARTESIAN_POINT('Ctrl Pts',(-2.12428199365964,2.75987228487492,
13.1743672263));
#104343=CARTESIAN_POINT('Ctrl Pts',(-3.47059190696705,-0.290621459465966,
13.3332591617839));
#104344=CARTESIAN_POINT('Ctrl Pts',(-1.63570258034773,-3.07472699374288,
13.4921510972678));
#104345=CARTESIAN_POINT('Ctrl Pts',(1.6984975107849,-3.04048930655329,13.6510430327517));
#104346=CARTESIAN_POINT('Ctrl Pts',(3.47582801449077,-0.219291201575626,
13.8099349682355));
#104347=CARTESIAN_POINT('Ctrl Pts',(2.06715977959038,2.80291267488859,13.9688269037194));
#104348=CARTESIAN_POINT('Ctrl Pts',(-1.23629968859761,3.25592261845714,
14.1277188392033));
#104349=CARTESIAN_POINT('Ctrl Pts',(-3.40654737760948,0.724502575226165,
14.2866107746872));
#104350=CARTESIAN_POINT('Ctrl Pts',(-2.45430005167269,-2.47100794692505,
14.445502710171));
#104351=CARTESIAN_POINT('Ctrl Pts',(0.747597382437242,-3.40155364079126,
14.6043946456549));
#104352=CARTESIAN_POINT('Ctrl Pts',(3.26423527335331,-1.21418165757984,
14.7632865811388));
#104353=CARTESIAN_POINT('Ctrl Pts',(2.7888236669811,2.08612836898727,14.9221785166226));
#104354=CARTESIAN_POINT('Ctrl Pts',(-0.242867665590079,3.47426025427258,
15.0810704521065));
#104355=CARTESIAN_POINT('Ctrl Pts',(-3.05194266818393,1.67783043467617,
15.2399623875904));
#104356=CARTESIAN_POINT('Ctrl Pts',(-3.06355892120926,-1.65652520466382,
15.3988543230742));
#104357=CARTESIAN_POINT('Ctrl Pts',(-0.267068784065951,-3.47248373386902,
15.5577462585581));
#104358=CARTESIAN_POINT('Ctrl Pts',(2.77422080966953,-2.10550894479311,
15.716638194042));
#104359=CARTESIAN_POINT('Ctrl Pts',(3.27261588636508,1.19140852679432,15.8755301295258));
#104360=CARTESIAN_POINT('Ctrl Pts',(0.771279663803726,3.39626216561827,
16.0344220650098));
#104361=CARTESIAN_POINT('Ctrl Pts',(-2.43702365429483,2.48804837690404,
16.1933140004936));
#104362=CARTESIAN_POINT('Ctrl Pts',(-3.41151268234012,-0.70074976677835,
16.3522059359775));
#104363=CARTESIAN_POINT('Ctrl Pts',(-1.25895541886534,-3.2472296301181,
16.5110978714614));
#104364=CARTESIAN_POINT('Ctrl Pts',(2.04758022321287,-2.81724763677509,
16.6699898069452));
#104365=CARTESIAN_POINT('Ctrl Pts',(3.47727156196124,0.195067941453848,
16.8288817424291));
#104366=CARTESIAN_POINT('Ctrl Pts',(1.71964098374098,3.0285811701927,16.9877736779129));
#104367=CARTESIAN_POINT('Ctrl Pts',(-1.61423962244767,3.08604916660887,
17.1466656133968));
#104368=CARTESIAN_POINT('Ctrl Pts',(-3.46848274959953,0.31479585946735,
17.3055575488807));
#104369=CARTESIAN_POINT('Ctrl Pts',(-2.14345992370895,-2.74500429377823,
17.4644494843646));
#104370=CARTESIAN_POINT('Ctrl Pts',(1.14629205009097,-3.28869024891454,
17.6233414198484));
#104371=CARTESIAN_POINT('Ctrl Pts',(3.38533466472848,-0.817910890742338,
17.7822333553323));
#104372=CARTESIAN_POINT('Ctrl Pts',(2.52132617136549,2.40257848050695,17.9411252908162));
#104373=CARTESIAN_POINT('Ctrl Pts',(-0.653769627841278,3.42082655086738,
18.1000172263));
#104374=CARTESIAN_POINT('Ctrl Pts',(-3.2296098824818,1.30349109102539,18.2589091617839));
#104375=CARTESIAN_POINT('Ctrl Pts',(-2.84513881881822,-2.00864484642347,
18.4178010972678));
#104376=CARTESIAN_POINT('Ctrl Pts',(0.147231326769927,-3.4796252605449,
18.5766930327517));
#104377=CARTESIAN_POINT('Ctrl Pts',(3.00464691781065,-1.7611263204821,18.7355849682355));
#104378=CARTESIAN_POINT('Ctrl Pts',(3.10795578947974,1.57164876103529,18.8944769037194));
#104379=CARTESIAN_POINT('Ctrl Pts',(0.362463401803061,3.4638258183312,19.0533688392033));
#104380=CARTESIAN_POINT('Ctrl Pts',(-2.71526865252999,2.18100553919064,
19.2122607746872));
#104381=CARTESIAN_POINT('Ctrl Pts',(-3.30414266619359,-1.10095879076405,
19.371152710171));
#104382=CARTESIAN_POINT('Ctrl Pts',(-0.864387437285646,-3.37376694148966,
19.5300446456549));
#104383=CARTESIAN_POINT('Ctrl Pts',(2.3676789396587,-2.55412714171859,19.6889365811388));
#104384=CARTESIAN_POINT('Ctrl Pts',(3.42949348506363,0.606665850414551,
19.8478285166226));
#104385=CARTESIAN_POINT('Ctrl Pts',(1.34778025145053,3.21137936248784,20.0067204521065));
#104386=CARTESIAN_POINT('Ctrl Pts',(-1.96932960158824,2.87249193869747,
20.1656123875904));
#104387=CARTESIAN_POINT('Ctrl Pts',(-3.48132090556751,-0.0993668687370002,
20.3245043230742));
#104388=CARTESIAN_POINT('Ctrl Pts',(-1.80227859806866,-2.98014443642408,
20.4833962585581));
#104389=CARTESIAN_POINT('Ctrl Pts',(1.52876067262735,-3.12927464877839,
20.642288194042));
#104390=CARTESIAN_POINT('Ctrl Pts',(3.45851382540476,-0.410062392811356,
20.8011801295258));
#104391=CARTESIAN_POINT('Ctrl Pts',(2.21813868189191,2.68501950265137,20.9600720650098));
#104392=CARTESIAN_POINT('Ctrl Pts',(-1.05541730517558,3.31897022882153,
21.1189640004936));
#104393=CARTESIAN_POINT('Ctrl Pts',(-3.36156121580965,0.910700489284517,
21.2778559359775));
#104394=CARTESIAN_POINT('Ctrl Pts',(-2.58644502317988,-2.33233158473218,
21.4367478714614));
#104395=CARTESIAN_POINT('Ctrl Pts',(0.559447225046381,-3.43751193576291,
21.5956398069452));
#104396=CARTESIAN_POINT('Ctrl Pts',(3.19254174220684,-1.39181435274289,
21.7545317424291));
#104397=CARTESIAN_POINT('Ctrl Pts',(2.89930139518638,1.9296415963275,21.913423677913));
#104398=CARTESIAN_POINT('Ctrl Pts',(-0.0514828017540393,3.48235880156699,
22.0723156133968));
#104399=CARTESIAN_POINT('Ctrl Pts',(-2.95507992042546,1.84308884050832,
22.2312075488807));
#104400=CARTESIAN_POINT('Ctrl Pts',(-3.14999873389981,-1.48558119003127,
22.3900994843646));
#104401=CARTESIAN_POINT('Ctrl Pts',(-0.457589516865705,-3.45255212377537,
22.5489914198484));
#104402=CARTESIAN_POINT('Ctrl Pts',(2.65427341857437,-2.25484402904363,
22.7078833553323));
#104403=CARTESIAN_POINT('Ctrl Pts',(3.33314941459721,1.00966036216743,22.8667752908162));
#104404=CARTESIAN_POINT('Ctrl Pts',(0.956880835440033,3.34875003908667,
23.0256672263001));
#104405=CARTESIAN_POINT('Ctrl Pts',(-2.29661858999409,2.61821597477262,
23.1845591617839));
#104406=CARTESIAN_POINT('Ctrl Pts',(-3.4447362843645,-0.512012483791419,
23.3434510972678));
#104407=CARTESIAN_POINT('Ctrl Pts',(-1.43586018489416,-3.17331095792505,
23.5023430327517));
#104408=CARTESIAN_POINT('Ctrl Pts',(1.89011394218839,-2.92516032722353,
23.6612349682356));
#104409=CARTESIAN_POINT('Ctrl Pts',(3.48173145950731,0.00281925901121507,
23.8201269037194));
#104410=CARTESIAN_POINT('Ctrl Pts',(1.88550732670284,2.93094323660242,23.9790188392033));
#104411=CARTESIAN_POINT('Ctrl Pts',(-1.44671136682348,3.16717464109652,
24.1379368411285));
#104412=CARTESIAN_POINT('Ctrl Pts',(-2.77319825394964,1.39625348399268,
24.243890864559));
#104413=CARTESIAN_POINT('Ctrl Pts',(-2.91490778362121,0.425731991800965,
24.2968809094949));
#104414=CARTESIAN_POINT('Ctrl Pts',(1.5973099225308,-2.24229951468148,-0.220223892917422));
#104415=CARTESIAN_POINT('Ctrl Pts',(2.3439008409669,-1.71050626964966,-0.167233936277439));
#104416=CARTESIAN_POINT('Ctrl Pts',(3.25072265677533,0.147878067225332,
-0.0612800011428309));
#104417=CARTESIAN_POINT('Ctrl Pts',(1.63300169230522,2.81802049953892,0.0976379124864005));
#104418=CARTESIAN_POINT('Ctrl Pts',(-1.48271086884576,2.89643286017587,
0.256529847970272));
#104419=CARTESIAN_POINT('Ctrl Pts',(-3.23860031117624,0.324060221574034,
0.415421783454143));
#104420=CARTESIAN_POINT('Ctrl Pts',(-2.02632933356543,-2.54749342965608,
0.574313718938014));
#104421=CARTESIAN_POINT('Ctrl Pts',(1.04351227375809,-3.0828546189813,0.733205654421883));
#104422=CARTESIAN_POINT('Ctrl Pts',(3.15674656563897,-0.793009057268962,
0.892097589905756));
#104423=CARTESIAN_POINT('Ctrl Pts',(2.37651353165193,2.22402826647853,1.05098952538963));
#104424=CARTESIAN_POINT('Ctrl Pts',(-0.582098769530993,3.20232531647345,
1.2098814608735));
#104425=CARTESIAN_POINT('Ctrl Pts',(-3.00713470507515,1.24540481046566,
1.36877339635737));
#104426=CARTESIAN_POINT('Ctrl Pts',(-2.67579167511483,-1.85311753566579,
1.52766533184124));
#104427=CARTESIAN_POINT('Ctrl Pts',(0.108228418730068,-3.2530200066176,
1.68655726732511));
#104428=CARTESIAN_POINT('Ctrl Pts',(2.79304241548106,-1.67116519110322,
1.84544920280898));
#104429=CARTESIAN_POINT('Ctrl Pts',(2.91771087913327,1.44251232660216,2.00434113829285));
#104430=CARTESIAN_POINT('Ctrl Pts',(0.36795895656849,3.23395698461494,2.16323307377672));
#104431=CARTESIAN_POINT('Ctrl Pts',(-2.51906962518594,2.06110744470182,
2.32212500926059));
#104432=CARTESIAN_POINT('Ctrl Pts',(-3.09707945431668,-1.00098657592543,
2.48101694474447));
#104433=CARTESIAN_POINT('Ctrl Pts',(-0.836257356622319,-3.14556004679618,
2.63990888022834));
#104434=CARTESIAN_POINT('Ctrl Pts',(2.1910913679718,-2.40686385398051,2.79880081571221));
#104435=CARTESIAN_POINT('Ctrl Pts',(3.21005123622639,0.538001811857031,
2.95769275119608));
#104436=CARTESIAN_POINT('Ctrl Pts',(1.28662753697526,2.98972646904068,3.11658468667995));
#104437=CARTESIAN_POINT('Ctrl Pts',(-1.81613923385632,2.70102076137102,
3.27547662216383));
#104438=CARTESIAN_POINT('Ctrl Pts',(-3.25420416327164,-0.063483164278144,
3.43436855764768));
#104439=CARTESIAN_POINT('Ctrl Pts',(-1.70941426718082,-2.76979741114071,
3.59326049313157));
#104440=CARTESIAN_POINT('Ctrl Pts',(1.40225168635204,-2.93727170294948,
3.75215242861543));
#104441=CARTESIAN_POINT('Ctrl Pts',(3.22859164459082,-0.412396456472955,
3.91104436409931));
#104442=CARTESIAN_POINT('Ctrl Pts',(2.095553617163,2.49048788012811,4.06993629958317));
#104443=CARTESIAN_POINT('Ctrl Pts',(-0.958301882433825,3.11055177540303,
4.22882823506705));
#104444=CARTESIAN_POINT('Ctrl Pts',(-3.13376277341917,0.879434889337815,
4.38772017055092));
#104445=CARTESIAN_POINT('Ctrl Pts',(-2.43676731682029,-2.15778587635696,
4.54661210603478));
#104446=CARTESIAN_POINT('Ctrl Pts',(0.493807466843058,-3.21714610026924,
4.70550404151867));
#104447=CARTESIAN_POINT('Ctrl Pts',(2.97175054379318,-1.32761950503133,
4.86439597700252));
#104448=CARTESIAN_POINT('Ctrl Pts',(2.72574023624785,1.77882405233552,5.0232879124864));
#104449=CARTESIAN_POINT('Ctrl Pts',(-0.0187265306618801,3.25476944832535,
5.18217984797027));
#104450=CARTESIAN_POINT('Ctrl Pts',(-2.74602826443034,1.74734187142485,
5.34107178345415));
#104451=CARTESIAN_POINT('Ctrl Pts',(-2.95627721245081,-1.36172680366859,
5.49996371893801));
#104452=CARTESIAN_POINT('Ctrl Pts',(-0.456755875356298,-3.22261522912952,
5.65885565442189));
#104453=CARTESIAN_POINT('Ctrl Pts',(2.46143509575639,-2.12960374578606,
5.81774758990576));
#104454=CARTESIAN_POINT('Ctrl Pts',(3.12343586483733,0.915436094402749,
5.97663952538962));
#104455=CARTESIAN_POINT('Ctrl Pts',(0.922446093534211,3.12137278280112,
6.13553146087351));
#104456=CARTESIAN_POINT('Ctrl Pts',(-2.12407230524417,2.46620998432462,
6.29442339635736));
#104457=CARTESIAN_POINT('Ctrl Pts',(-3.22363255275512,-0.449519754299316,
6.45331533184125));
#104458=CARTESIAN_POINT('Ctrl Pts',(-1.36836039659416,-2.95321260151052,
6.6122072673251));
#104459=CARTESIAN_POINT('Ctrl Pts',(1.74117246502532,-2.74994423429374,
6.77109920280899));
#104460=CARTESIAN_POINT('Ctrl Pts',(3.25471920358593,-0.0260336416356283,
6.92999113829285));
#104461=CARTESIAN_POINT('Ctrl Pts',(1.78493902438429,2.72173979724695,7.08888307377672));
#104462=CARTESIAN_POINT('Ctrl Pts',(-1.32094439596421,2.97472364219914,
7.2477750092606));
#104463=CARTESIAN_POINT('Ctrl Pts',(-3.21602936432787,0.501028913805074,
7.40666694474447));
#104464=CARTESIAN_POINT('Ctrl Pts',(-2.16325113136153,-2.43191681341095,
7.56555888022833));
#104465=CARTESIAN_POINT('Ctrl Pts',(0.872397182366315,-3.13572926141387,
7.72445081571221));
#104466=CARTESIAN_POINT('Ctrl Pts',(3.10839248938752,-0.965282847981423,
7.88334275119608));
#104467=CARTESIAN_POINT('Ctrl Pts',(2.49518625105183,2.08995703717797,8.04223468667995));
#104468=CARTESIAN_POINT('Ctrl Pts',(-0.405147030191767,3.22950936345052,
8.20112662216383));
#104469=CARTESIAN_POINT('Ctrl Pts',(-2.93411615827254,1.40884250874675,
8.36001855764769));
#104470=CARTESIAN_POINT('Ctrl Pts',(-2.77362817276533,-1.70319159342991,
8.51891049313157));
#104471=CARTESIAN_POINT('Ctrl Pts',(-0.0707888905447793,-3.25405343804665,
8.67780242861544));
#104472=CARTESIAN_POINT('Ctrl Pts',(2.69693660441204,-1.82219861608723,
8.8366943640993));
#104473=CARTESIAN_POINT('Ctrl Pts',(2.99260750289983,1.27991217600095,8.99558629958318));
#104474=CARTESIAN_POINT('Ctrl Pts',(0.545207199465845,3.20883529560781,
9.15447823506705));
#104475=CARTESIAN_POINT('Ctrl Pts',(-2.40193861569527,2.19648941065502,
9.31337017055092));
#104476=CARTESIAN_POINT('Ctrl Pts',(-3.14742964013857,-0.829193285709043,
9.47226210603479));
#104477=CARTESIAN_POINT('Ctrl Pts',(-1.00793705160453,-3.09482434795427,
9.63115404151866));
#104478=CARTESIAN_POINT('Ctrl Pts',(2.05544652394575,-2.52369063712,9.79004597700253));
#104479=CARTESIAN_POINT('Ctrl Pts',(3.23477542093817,0.360697686133515,
9.94893791248641));
#104480=CARTESIAN_POINT('Ctrl Pts',(1.44905818566578,2.91446482552848,10.1078298479703));
#104481=CARTESIAN_POINT('Ctrl Pts',(-1.66488862035959,2.79678757264204,
10.2667217834542));
#104482=CARTESIAN_POINT('Ctrl Pts',(-3.25277227761243,0.115530752113285,
10.425613718938));
#104483=CARTESIAN_POINT('Ctrl Pts',(-1.85911360013471,-2.67162337661616,
10.5845056544219));
#104484=CARTESIAN_POINT('Ctrl Pts',(1.23863790364548,-3.00992541242147,
10.7433975899058));
#104485=CARTESIAN_POINT('Ctrl Pts',(3.20103438348542,-0.589282377499889,
10.9022895253897));
#104486=CARTESIAN_POINT('Ctrl Pts',(2.2293122977628,2.37150617197835,11.0611814608735));
#104487=CARTESIAN_POINT('Ctrl Pts',(-0.78583257499675,3.15853478827791,
11.2200733963574));
#104488=CARTESIAN_POINT('Ctrl Pts',(-3.08067092445951,1.05040063779377,
11.3789653318413));
#104489=CARTESIAN_POINT('Ctrl Pts',(-2.55171775188206,-2.02054729205179,
11.5378572673251));
#104490=CARTESIAN_POINT('Ctrl Pts',(0.316180128224772,-3.23942972932021,
11.696749202809));
#104491=CARTESIAN_POINT('Ctrl Pts',(2.89426231966781,-1.48899982190694,
11.8556411382929));
#104492=CARTESIAN_POINT('Ctrl Pts',(2.81941805410138,1.62627078953506,12.0145330737768));
#104493=CARTESIAN_POINT('Ctrl Pts',(0.160250764921038,3.25087596457171,
12.1734250092606));
#104494=CARTESIAN_POINT('Ctrl Pts',(-2.64580490100596,1.89567699529763,
12.3323169447445));
#104495=CARTESIAN_POINT('Ctrl Pts',(-3.02667409566324,-1.19712938453989,
12.4912088802284));
#104496=CARTESIAN_POINT('Ctrl Pts',(-0.633246112567888,-3.19262810324119,
12.6501008157122));
#104497=CARTESIAN_POINT('Ctrl Pts',(2.34062523753456,-2.26171358533835,
12.8089927511961));
#104498=CARTESIAN_POINT('Ctrl Pts',(3.16904260566617,0.74232325045119,12.96788468668));
#104499=CARTESIAN_POINT('Ctrl Pts',(1.09266557598831,3.06593489554784,13.1267766221638));
#104500=CARTESIAN_POINT('Ctrl Pts',(-1.98526594151343,2.57926229495074,
13.2856685576477));
#104501=CARTESIAN_POINT('Ctrl Pts',(-3.24347140839053,-0.27160277546613,
13.4445604931316));
#104502=CARTESIAN_POINT('Ctrl Pts',(-1.52865986385155,-2.87351246131581,
13.6034524286155));
#104503=CARTESIAN_POINT('Ctrl Pts',(1.58734540422173,-2.84151533734801,
13.7623443640993));
#104504=CARTESIAN_POINT('Ctrl Pts',(3.24836485754839,-0.204940471679879,
13.9212362995832));
#104505=CARTESIAN_POINT('Ctrl Pts',(1.93188188683804,2.61948606027878,14.0801282350671));
#104506=CARTESIAN_POINT('Ctrl Pts',(-1.15539446862615,3.04285038517439,
14.2390201705509));
#104507=CARTESIAN_POINT('Ctrl Pts',(-3.18361804464065,0.677090090406219,
14.3979121060348));
#104508=CARTESIAN_POINT('Ctrl Pts',(-2.29368714576657,-2.30930165245534,
14.5568040415187));
#104509=CARTESIAN_POINT('Ctrl Pts',(0.698673540399568,-3.17895110510264,
14.7156959770026));
#104510=CARTESIAN_POINT('Ctrl Pts',(3.05061904804408,-1.13472387319489,
14.8745879124864));
#104511=CARTESIAN_POINT('Ctrl Pts',(2.60631905720107,1.94960914461292,15.0334798479703));
#104512=CARTESIAN_POINT('Ctrl Pts',(-0.226974058166443,3.24689969380135,
15.1923717834542));
#104513=CARTESIAN_POINT('Ctrl Pts',(-2.85221917461115,1.56803081113487,
15.351263718938));
#104514=CARTESIAN_POINT('Ctrl Pts',(-2.86307524342312,-1.54811982584858,
15.5101556544219));
#104515=CARTESIAN_POINT('Ctrl Pts',(-0.249591420833051,-3.24523943143405,
15.6690475899058));
#104516=CARTESIAN_POINT('Ctrl Pts',(2.59267183175928,-1.96772142781691,
15.8279395253897));
#104517=CARTESIAN_POINT('Ctrl Pts',(3.0584512217531,1.11344104866165,15.9868314608735));
#104518=CARTESIAN_POINT('Ctrl Pts',(0.720806019399342,3.17400591163366,
16.1457233963574));
#104519=CARTESIAN_POINT('Ctrl Pts',(-2.27754134054451,2.32522693232264,
16.3046153318412));
#104520=CARTESIAN_POINT('Ctrl Pts',(-3.18825841272756,-0.654891699718197,
16.4635072673252));
#104521=CARTESIAN_POINT('Ctrl Pts',(-1.1765675754994,-3.03472627842632,
16.622399202809));
#104522=CARTESIAN_POINT('Ctrl Pts',(1.9135836446356,-2.63288292175533,16.7812911382929));
#104523=CARTESIAN_POINT('Ctrl Pts',(3.24971393720761,0.182302416348347,
16.9401830737767));
#104524=CARTESIAN_POINT('Ctrl Pts',(1.60710521806487,2.83038648646373,17.0990750092606));
#104525=CARTESIAN_POINT('Ctrl Pts',(-1.50860147261613,2.88409369499471,
17.2579669447445));
#104526=CARTESIAN_POINT('Ctrl Pts',(-3.24150027729799,0.294195168153433,
17.4168588802284));
#104527=CARTESIAN_POINT('Ctrl Pts',(-2.00318884038906,-2.56536728645793,
17.5757508157122));
#104528=CARTESIAN_POINT('Ctrl Pts',(1.07127705872643,-3.07347365502525,
17.7346427511961));
#104529=CARTESIAN_POINT('Ctrl Pts',(3.16379352203233,-0.764385632147803,
17.89353468668));
#104530=CARTESIAN_POINT('Ctrl Pts',(2.35632698031541,2.2453503081982,18.0524266221638));
#104531=CARTESIAN_POINT('Ctrl Pts',(-0.610986008271525,3.19696276837624,
18.2113185576477));
#104532=CARTESIAN_POINT('Ctrl Pts',(-3.01825959227787,1.21818876957141,
18.3702104931316));
#104533=CARTESIAN_POINT('Ctrl Pts',(-2.65894886495122,-1.87719625459478,
18.5291024286155));
#104534=CARTESIAN_POINT('Ctrl Pts',(0.137596298152765,-3.25191360638933,
18.6879943640993));
#104535=CARTESIAN_POINT('Ctrl Pts',(2.80801852579208,-1.64587569503084,
18.8468862995832));
#104536=CARTESIAN_POINT('Ctrl Pts',(2.90456671713063,1.4687978180947,19.0057782350671));
#104537=CARTESIAN_POINT('Ctrl Pts',(0.338743278337104,3.23714810227294,
19.164670170551));
#104538=CARTESIAN_POINT('Ctrl Pts',(-2.53757758810555,2.03827741709,19.3235621060348));
#104539=CARTESIAN_POINT('Ctrl Pts',(-3.0879148440151,-1.02891047273259,
19.4824540415187));
#104540=CARTESIAN_POINT('Ctrl Pts',(-0.80782068700727,-3.15298280714823,
19.6413459770026));
#104541=CARTESIAN_POINT('Ctrl Pts',(2.21273464322184,-2.38698140825151,
19.8002379124864));
#104542=CARTESIAN_POINT('Ctrl Pts',(3.20506252600188,0.566964769414809,
19.9591298479703));
#104543=CARTESIAN_POINT('Ctrl Pts',(1.25957958398902,3.00122210358845,20.1180217834542));
#104544=CARTESIAN_POINT('Ctrl Pts',(-1.84045385561639,2.68451195754086,
20.276913718938));
#104545=CARTESIAN_POINT('Ctrl Pts',(-3.25349828597628,-0.0928641587167671,
20.4358056544219));
#104546=CARTESIAN_POINT('Ctrl Pts',(-1.68433490870969,-2.78511952183474,
20.5946975899058));
#104547=CARTESIAN_POINT('Ctrl Pts',(1.42871638753743,-2.9244904397832,20.7535895253897));
#104548=CARTESIAN_POINT('Ctrl Pts',(3.23218373376165,-0.38322732329028,
20.9124814608735));
#104549=CARTESIAN_POINT('Ctrl Pts',(2.07298051381926,2.50930798586206,21.0713733963574));
#104550=CARTESIAN_POINT('Ctrl Pts',(-0.986349287101606,3.10177206973596,
21.2302653318412));
#104551=CARTESIAN_POINT('Ctrl Pts',(-3.14157584161525,0.851102946639152,
21.3891572673252));
#104552=CARTESIAN_POINT('Ctrl Pts',(-2.41718436132387,-2.17970046976106,
21.548049202809));
#104553=CARTESIAN_POINT('Ctrl Pts',(0.522836198430219,-3.21255623781816,
21.7069411382929));
#104554=CARTESIAN_POINT('Ctrl Pts',(2.98361724412315,-1.30073203070833,
21.8658330737767));
#104555=CARTESIAN_POINT('Ctrl Pts',(2.70956696485005,1.80336309018792,22.0247250092606));
#104556=CARTESIAN_POINT('Ctrl Pts',(-0.0481136935684708,3.254468260577,
22.1836169447445));
#104557=CARTESIAN_POINT('Ctrl Pts',(-2.76169526361428,1.72247447051088,
22.3425088802284));
#104558=CARTESIAN_POINT('Ctrl Pts',(-2.94385831113143,-1.38836263204452,
22.5014008157122));
#104559=CARTESIAN_POINT('Ctrl Pts',(-0.427644204365768,-3.22661217441425,
22.6602927511961));
#104560=CARTESIAN_POINT('Ctrl Pts',(2.48057396950494,-2.10728381055163,
22.8191846866799));
#104561=CARTESIAN_POINT('Ctrl Pts',(3.11502334931318,0.943586743892659,
22.9780766221639));
#104562=CARTESIAN_POINT('Ctrl Pts',(0.894261184887878,3.12960304662157,
23.1369685576477));
#104563=CARTESIAN_POINT('Ctrl Pts',(-2.14632458448094,2.44687617640059,
23.2958604931316));
#104564=CARTESIAN_POINT('Ctrl Pts',(-3.21930781471386,-0.47850565449158,
23.4547524286154));
#104565=CARTESIAN_POINT('Ctrl Pts',(-1.34189544060237,-2.96564494987165,
23.6136443640994));
#104566=CARTESIAN_POINT('Ctrl Pts',(1.76642218227432,-2.73373365138718,
23.7725362995832));
#104567=CARTESIAN_POINT('Ctrl Pts',(3.25388197267903,0.00263476266896457,
23.9314282350671));
#104568=CARTESIAN_POINT('Ctrl Pts',(1.76211703029526,2.73913811890468,24.0903201705509));
#104569=CARTESIAN_POINT('Ctrl Pts',(-1.35203650566515,2.95991020239352,
24.2492381724761));
#104570=CARTESIAN_POINT('Ctrl Pts',(-2.5917161935483,1.3048806588596,24.3551921959067));
#104571=CARTESIAN_POINT('Ctrl Pts',(-2.72415204890299,0.397871481308887,
24.4081822408425));
#104572=CARTESIAN_POINT('Ctrl Pts',(1.48546006159232,-2.08528497081503,
-0.108922561569808));
#104573=CARTESIAN_POINT('Ctrl Pts',(2.17977177658322,-1.59072995968249,
-0.0559326049298234));
#104574=CARTESIAN_POINT('Ctrl Pts',(3.02309439754947,0.137523069098973,
0.0500213302047839));
#104575=CARTESIAN_POINT('Ctrl Pts',(1.51865255465809,2.62069173036942,0.208939243834015));
#104576=CARTESIAN_POINT('Ctrl Pts',(-1.37888567991209,2.69361335216517,
0.367831179317886));
#104577=CARTESIAN_POINT('Ctrl Pts',(-3.01182090579545,0.301368262920637,
0.526723114801757));
#104578=CARTESIAN_POINT('Ctrl Pts',(-1.88443786280079,-2.3691080193925,
0.685615050285628));
#104579=CARTESIAN_POINT('Ctrl Pts',(0.970441480757242,-2.86698113346493,
0.844506985769499));
#104580=CARTESIAN_POINT('Ctrl Pts',(2.93569887827138,-0.737479474983559,
1.00339892125337));
#104581=CARTESIAN_POINT('Ctrl Pts',(2.21010079966783,2.0682931465622,1.16229085673724));
#104582=CARTESIAN_POINT('Ctrl Pts',(-0.54133794690907,2.97808602748199,
1.32118279222111));
#104583=CARTESIAN_POINT('Ctrl Pts',(-2.79656342279512,1.15819671584495,
1.48007472770498));
#104584=CARTESIAN_POINT('Ctrl Pts',(-2.48842232209177,-1.72335502950263,
1.63896666318885));
#104585=CARTESIAN_POINT('Ctrl Pts',(0.100649843392986,-3.02523087800956,
1.79785859867272));
#104586=CARTESIAN_POINT('Ctrl Pts',(2.59746270902568,-1.55414369665589,
1.95675053415659));
#104587=CARTESIAN_POINT('Ctrl Pts',(2.7134014013754,1.3415019961355,2.11564246964046));
#104588=CARTESIAN_POINT('Ctrl Pts',(0.342193037542567,3.00750272304177,
2.27453440512433));
#104589=CARTESIAN_POINT('Ctrl Pts',(-2.3426745603979,1.91678067516427,2.4334263406082));
#104590=CARTESIAN_POINT('Ctrl Pts',(-2.8802098904365,-0.930893597888221,
2.59231827609208));
#104591=CARTESIAN_POINT('Ctrl Pts',(-0.77769936000087,-2.92529568303992,
2.75121021157595));
#104592=CARTESIAN_POINT('Ctrl Pts',(2.03766261795009,-2.23832587423829,
2.91010214705982));
#104593=CARTESIAN_POINT('Ctrl Pts',(2.98527094824794,0.500328829931562,
3.06899408254369));
#104594=CARTESIAN_POINT('Ctrl Pts',(1.1965328665169,2.78037417923805,3.22788601802756));
#104595=CARTESIAN_POINT('Ctrl Pts',(-1.68896609238486,2.51188476948248,
3.38677795351144));
#104596=CARTESIAN_POINT('Ctrl Pts',(-3.0263321154034,-0.059037825902474,
3.5456698889953));
#104597=CARTESIAN_POINT('Ctrl Pts',(-1.58971442347893,-2.57584541040876,
3.70456182447918));
#104598=CARTESIAN_POINT('Ctrl Pts',(1.30406056269662,-2.73159250013523,
3.86345375996304));
#104599=CARTESIAN_POINT('Ctrl Pts',(3.00251308501958,-0.383518850657475,
4.02234569544692));
#104600=CARTESIAN_POINT('Ctrl Pts',(1.94881479249118,2.31609422043059,4.18123763093079));
#104601=CARTESIAN_POINT('Ctrl Pts',(-0.891197852855459,2.89273882713716,
4.34012956641466));
#104602=CARTESIAN_POINT('Ctrl Pts',(-2.91432450068511,0.81785343373588,
4.49902150189853));
#104603=CARTESIAN_POINT('Ctrl Pts',(-2.26613538016149,-2.00668930655468,
4.6579134373824));
#104604=CARTESIAN_POINT('Ctrl Pts',(0.459229145054833,-2.99186900228206,
4.81680537286627));
#104605=CARTESIAN_POINT('Ctrl Pts',(2.7636569982773,-1.23465441734085,4.97569730835014));
#104606=CARTESIAN_POINT('Ctrl Pts',(2.53487329046712,1.65426386518503,5.13458924383401));
#104607=CARTESIAN_POINT('Ctrl Pts',(-0.0174152260610237,3.02685781699636,
5.29348117931788));
#104608=CARTESIAN_POINT('Ctrl Pts',(-2.55374067191164,1.62498618917805,
5.45237311480176));
#104609=CARTESIAN_POINT('Ctrl Pts',(-2.749267169851,-1.26637339010859,5.61126505028562));
#104610=CARTESIAN_POINT('Ctrl Pts',(-0.424772050288417,-2.99695516144193,
5.7701569857695));
#104611=CARTESIAN_POINT('Ctrl Pts',(2.28907582515644,-1.98048059851179,
5.92904892125336));
#104612=CARTESIAN_POINT('Ctrl Pts',(2.90472072245671,0.851333694228085,
6.08794085673724));
#104613=CARTESIAN_POINT('Ctrl Pts',(0.857852825922402,2.90280210545861,
6.24683279222111));
#104614=CARTESIAN_POINT('Ctrl Pts',(-1.97533649097687,2.29351635743302,
6.40572472770499));
#104615=CARTESIAN_POINT('Ctrl Pts',(-2.99790124810567,-0.418042630606353,
6.56461666318884));
#104616=CARTESIAN_POINT('Ctrl Pts',(-1.27254247302535,-2.74641715490278,
6.72350859867273));
#104617=CARTESIAN_POINT('Ctrl Pts',(1.61924878863919,-2.55738243031585,
6.88240053415659));
#104618=CARTESIAN_POINT('Ctrl Pts',(3.02681109058924,-0.0242106646694371,
7.04129246964047));
#104619=CARTESIAN_POINT('Ctrl Pts',(1.65995064307836,2.53115297778335,7.20018440512434));
#104620=CARTESIAN_POINT('Ctrl Pts',(-1.22844672540447,2.7664219087552,7.3590763406082));
#104621=CARTESIAN_POINT('Ctrl Pts',(-2.99083046454003,0.465944918179204,
7.51796827609208));
#104622=CARTESIAN_POINT('Ctrl Pts',(-2.01177186312133,-2.26162452788943,
7.67686021157594));
#104623=CARTESIAN_POINT('Ctrl Pts',(0.811308534412381,-2.91615328753264,
7.83575214705982));
#104624=CARTESIAN_POINT('Ctrl Pts',(2.89073074273702,-0.897689984010518,
7.9946440825437));
#104625=CARTESIAN_POINT('Ctrl Pts',(2.32046359312609,1.94361010683061,8.15353601802756));
#104626=CARTESIAN_POINT('Ctrl Pts',(-0.376777057434817,3.00336654163099,
8.31242795351144));
#104627=CARTESIAN_POINT('Ctrl Pts',(-2.72865791898473,1.31018987004163,
8.4713198889953));
#104628=CARTESIAN_POINT('Ctrl Pts',(-2.57940792718688,-1.58392748557606,
8.63021182447918));
#104629=CARTESIAN_POINT('Ctrl Pts',(-0.0658319767663575,-3.02619194454561,
8.78910375996304));
#104630=CARTESIAN_POINT('Ctrl Pts',(2.50808660109806,-1.69460117307586,
8.94799569544693));
#104631=CARTESIAN_POINT('Ctrl Pts',(2.78305347188721,1.19028774126861,9.10688763093078));
#104632=CARTESIAN_POINT('Ctrl Pts',(0.507029668241175,2.98414015252653,
9.26577956641467));
#104633=CARTESIAN_POINT('Ctrl Pts',(-2.23374552031738,2.04268266866388,
9.42467150189852));
#104634=CARTESIAN_POINT('Ctrl Pts',(-2.92703436017603,-0.771129942841463,
9.58356343738241));
#104635=CARTESIAN_POINT('Ctrl Pts',(-0.93735737419411,-2.87811269540331,
9.74245537286627));
#104636=CARTESIAN_POINT('Ctrl Pts',(1.911516154124,-2.34697199108145,9.90134730835015));
#104637=CARTESIAN_POINT('Ctrl Pts',(3.00826384926654,0.335440229539894,
10.060239243834));
#104638=CARTESIAN_POINT('Ctrl Pts',(1.34758948865696,2.71038264908462,10.2191311793179));
#104639=CARTESIAN_POINT('Ctrl Pts',(-1.54830663583761,2.60094561569807,
10.3780231148017));
#104640=CARTESIAN_POINT('Ctrl Pts',(-3.02500049595403,0.10744083895636,
10.5369150502856));
#104641=CARTESIAN_POINT('Ctrl Pts',(-1.72893122618789,-2.48454590408593,
10.6958069857695));
#104642=CARTESIAN_POINT('Ctrl Pts',(1.15190365419162,-2.79915871394563,
10.8546989212533));
#104643=CARTESIAN_POINT('Ctrl Pts',(2.97688549064886,-0.548018530673967,
11.0135908567372));
#104644=CARTESIAN_POINT('Ctrl Pts',(2.07320716939916,2.20544407481798,11.1724827922211));
#104645=CARTESIAN_POINT('Ctrl Pts',(-0.730805517946308,2.93736188259754,
11.331374727705));
#104646=CARTESIAN_POINT('Ctrl Pts',(-2.86495034973719,0.976847494718856,
11.4902666631888));
#104647=CARTESIAN_POINT('Ctrl Pts',(-2.37303653812609,-1.87906070235006,
11.6491585986727));
#104648=CARTESIAN_POINT('Ctrl Pts',(0.294039964393921,-3.0125922448511,
11.8080505341566));
#104649=CARTESIAN_POINT('Ctrl Pts',(2.69159480135589,-1.38473425598983,
11.9669424696404));
#104650=CARTESIAN_POINT('Ctrl Pts',(2.62199142271915,1.51239297591101,12.1258344051243));
#104651=CARTESIAN_POINT('Ctrl Pts',(0.149029382320921,3.02323697013694,
12.2847263406082));
#104652=CARTESIAN_POINT('Ctrl Pts',(-2.46053533867895,1.76293431003818,
12.4436182760921));
#104653=CARTESIAN_POINT('Ctrl Pts',(-2.81473458916494,-1.11330172323418,
12.6025102115759));
#104654=CARTESIAN_POINT('Ctrl Pts',(-0.588903753811167,-2.96906785088264,
12.7614021470598));
#104655=CARTESIAN_POINT('Ctrl Pts',(2.1767255436589,-2.10333959264322,12.9202940825437));
#104656=CARTESIAN_POINT('Ctrl Pts',(2.94713390169327,0.690342885737227,
13.0791860180275));
#104657=CARTESIAN_POINT('Ctrl Pts',(1.01615287735504,2.85124619495422,13.2380779535114));
#104658=CARTESIAN_POINT('Ctrl Pts',(-1.84624988936723,2.39865230502655,
13.3969698889953));
#104659=CARTESIAN_POINT('Ctrl Pts',(-3.01635090981402,-0.252584091466298,
13.5558618244792));
#104660=CARTESIAN_POINT('Ctrl Pts',(-1.42161714735535,-2.67229792888874,
13.714753759963));
#104661=CARTESIAN_POINT('Ctrl Pts',(1.47619329765856,-2.64254136814274,
13.8736456954469));
#104662=CARTESIAN_POINT('Ctrl Pts',(3.02090170060603,-0.190589741784131,
14.0325376309308));
#104663=CARTESIAN_POINT('Ctrl Pts',(1.79660399408569,2.43605944566898,14.1914295664146));
#104664=CARTESIAN_POINT('Ctrl Pts',(-1.0744892486547,2.82977815189164,14.3503215018985));
#104665=CARTESIAN_POINT('Ctrl Pts',(-2.96068871167182,0.629677605586279,
14.5092134373824));
#104666=CARTESIAN_POINT('Ctrl Pts',(-2.13307423986045,-2.14759535798565,
14.6681053728662));
#104667=CARTESIAN_POINT('Ctrl Pts',(0.649749698361895,-2.95634856941403,
14.8269973083501));
#104668=CARTESIAN_POINT('Ctrl Pts',(2.83700282273485,-1.05526608880994,
14.985889243834));
#104669=CARTESIAN_POINT('Ctrl Pts',(2.42381444742106,1.81308992023858,15.1447811793179));
#104670=CARTESIAN_POINT('Ctrl Pts',(-0.21108045074281,3.01953913333011,
15.3036731148017));
#104671=CARTESIAN_POINT('Ctrl Pts',(-2.65249568103837,1.45823118759357,
15.4625650502856));
#104672=CARTESIAN_POINT('Ctrl Pts',(-2.66259156563698,-1.43971444703336,
15.6214569857695));
#104673=CARTESIAN_POINT('Ctrl Pts',(-0.232114057600147,-3.01799512899908,
15.7803489212533));
#104674=CARTESIAN_POINT('Ctrl Pts',(2.41112285384901,-1.82993391084071,
15.9392408567372));
#104675=CARTESIAN_POINT('Ctrl Pts',(2.84428655714113,1.03547357052898,16.0981327922211));
#104676=CARTESIAN_POINT('Ctrl Pts',(0.670332374994958,2.95174965764906,
16.257024727705));
#104677=CARTESIAN_POINT('Ctrl Pts',(-2.11805902679419,2.16240548774123,
16.4159166631888));
#104678=CARTESIAN_POINT('Ctrl Pts',(-2.96500414311501,-0.609033632658046,
16.5748085986727));
#104679=CARTESIAN_POINT('Ctrl Pts',(-1.09417973213347,-2.82222292673453,
16.7337005341566));
#104680=CARTESIAN_POINT('Ctrl Pts',(1.77958706605832,-2.44851820673558,
16.8925924696404));
#104681=CARTESIAN_POINT('Ctrl Pts',(3.02215631245399,0.169536891242848,
17.0514844051243));
#104682=CARTESIAN_POINT('Ctrl Pts',(1.49456945238876,2.63219180273477,17.2103763406082));
#104683=CARTESIAN_POINT('Ctrl Pts',(-1.40296332278459,2.68213822338054,
17.3692682760921));
#104684=CARTESIAN_POINT('Ctrl Pts',(-3.01451780499646,0.273594476839516,
17.5281602115759));
#104685=CARTESIAN_POINT('Ctrl Pts',(-1.86291775706917,-2.38573027913763,
17.6870521470598));
#104686=CARTESIAN_POINT('Ctrl Pts',(0.996262067361875,-2.85825706113596,
17.8459440825436));
#104687=CARTESIAN_POINT('Ctrl Pts',(2.94225237933618,-0.710860373553265,
18.0048360180275));
#104688=CARTESIAN_POINT('Ctrl Pts',(2.19132778926533,2.08812213588945,18.1637279535114));
#104689=CARTESIAN_POINT('Ctrl Pts',(-0.568202388701774,2.97309898588511,
18.3226198889953));
#104690=CARTESIAN_POINT('Ctrl Pts',(-2.80690930207393,1.13288644811743,
18.4815118244792));
#104691=CARTESIAN_POINT('Ctrl Pts',(-2.47275891108423,-1.74574766276608,
18.640403759963));
#104692=CARTESIAN_POINT('Ctrl Pts',(0.127961269535608,-3.02420195223377,
18.7992956954469));
#104693=CARTESIAN_POINT('Ctrl Pts',(2.61139013377353,-1.53062506957956,
18.9581876309307));
#104694=CARTESIAN_POINT('Ctrl Pts',(2.7011776447815,1.36594687515411,19.1170795664147));
#104695=CARTESIAN_POINT('Ctrl Pts',(0.315023154871148,3.01047038621467,
19.2759715018985));
#104696=CARTESIAN_POINT('Ctrl Pts',(-2.35988652368112,1.89554929498936,
19.4348634373824));
#104697=CARTESIAN_POINT('Ctrl Pts',(-2.8716870218366,-0.956862154701133,
19.5937553728662));
#104698=CARTESIAN_POINT('Ctrl Pts',(-0.751253936728898,-2.9321986728068,
19.7526473083501));
#104699=CARTESIAN_POINT('Ctrl Pts',(2.057790346785,-2.21983567478444,19.911539243834));
#104700=CARTESIAN_POINT('Ctrl Pts',(2.98063156694013,0.527263688415071,
20.0704311793178));
#104701=CARTESIAN_POINT('Ctrl Pts',(1.17137891652752,2.79106484468908,20.2293231148018));
#104702=CARTESIAN_POINT('Ctrl Pts',(-1.71157810964454,2.49653197638425,
20.3882150502856));
#104703=CARTESIAN_POINT('Ctrl Pts',(-3.02567566638506,-0.0863614486965333,
20.5471069857695));
#104704=CARTESIAN_POINT('Ctrl Pts',(-1.56639121935072,-2.59009460724541,
20.7059989212533));
#104705=CARTESIAN_POINT('Ctrl Pts',(1.32867210244754,-2.719706230788,20.8648908567372));
#104706=CARTESIAN_POINT('Ctrl Pts',(3.00585364211853,-0.356392253769203,
21.0237827922211));
#104707=CARTESIAN_POINT('Ctrl Pts',(1.92782234574661,2.33359646907276,21.182674727705));
#104708=CARTESIAN_POINT('Ctrl Pts',(-0.91728126902763,2.88457391065039,
21.3415666631888));
#104709=CARTESIAN_POINT('Ctrl Pts',(-2.92159046742086,0.791505403993785,
21.5004585986727));
#104710=CARTESIAN_POINT('Ctrl Pts',(-2.24792369946788,-2.02706935478992,
21.6593505341566));
#104711=CARTESIAN_POINT('Ctrl Pts',(0.486225171814051,-2.98760053987341,
21.8182424696404));
#104712=CARTESIAN_POINT('Ctrl Pts',(2.77469274603948,-1.20964970867379,
21.9771344051243));
#104713=CARTESIAN_POINT('Ctrl Pts',(2.51983253451372,1.67708458404834,22.1360263406082));
#104714=CARTESIAN_POINT('Ctrl Pts',(-0.0447445853828995,3.02657771958701,
22.2949182760921));
#104715=CARTESIAN_POINT('Ctrl Pts',(-2.56831060680309,1.60186010051345,
22.4538102115759));
#104716=CARTESIAN_POINT('Ctrl Pts',(-2.73771788836306,-1.29114407405777,
22.6127021470598));
#104717=CARTESIAN_POINT('Ctrl Pts',(-0.397698891865832,-3.00067222505312,
22.7715940825436));
#104718=CARTESIAN_POINT('Ctrl Pts',(2.3068745204355,-1.95972359205962,22.9304860180276));
#104719=CARTESIAN_POINT('Ctrl Pts',(2.89689728402915,0.877513125617889,
23.0893779535114));
#104720=CARTESIAN_POINT('Ctrl Pts',(0.831641534335725,2.91045605415649,
23.2482698889953));
#104721=CARTESIAN_POINT('Ctrl Pts',(-1.9960305789678,2.27553637802856,23.4071618244792));
#104722=CARTESIAN_POINT('Ctrl Pts',(-2.99387934506323,-0.44499882519174,
23.566053759963));
#104723=CARTESIAN_POINT('Ctrl Pts',(-1.24793069631059,-2.75797894181825,
23.7249456954469));
#104724=CARTESIAN_POINT('Ctrl Pts',(1.64273042236025,-2.54230697555083,
23.8838376309308));
#104725=CARTESIAN_POINT('Ctrl Pts',(3.02603248585074,0.00245026632671095,
24.0427295664146));
#104726=CARTESIAN_POINT('Ctrl Pts',(1.63872673388769,2.54733300120695,24.2016215018985));
#104727=CARTESIAN_POINT('Ctrl Pts',(-1.25736164450683,2.75264576369051,
24.3605395038237));
#104728=CARTESIAN_POINT('Ctrl Pts',(-2.41023413314696,1.21350783372652,
24.4664935272542));
#104729=CARTESIAN_POINT('Ctrl Pts',(-2.53339631418477,0.370010970816811,
24.5194835721902));
#104730=CARTESIAN_POINT('Ctrl Pts',(1.37361020065383,-1.92827042694857,
0.00237876977780734));
#104731=CARTESIAN_POINT('Ctrl Pts',(2.01564271219955,-1.47095364971531,
0.0553687264177913));
#104732=CARTESIAN_POINT('Ctrl Pts',(2.79546613832361,0.127168070972611,
0.161322661552399));
#104733=CARTESIAN_POINT('Ctrl Pts',(1.40430341701095,2.42336296119994,0.32024057518163));
#104734=CARTESIAN_POINT('Ctrl Pts',(-1.27506049097842,2.49079384415449,
0.479132510665502));
#104735=CARTESIAN_POINT('Ctrl Pts',(-2.78504150041466,0.278676304267241,
0.638024446149372));
#104736=CARTESIAN_POINT('Ctrl Pts',(-1.74254639203617,-2.19072260912893,
0.796916381633244));
#104737=CARTESIAN_POINT('Ctrl Pts',(0.897370687756388,-2.65110764794858,
0.955808317117115));
#104738=CARTESIAN_POINT('Ctrl Pts',(2.71465119090379,-0.681949892698155,
1.11470025260098));
#104739=CARTESIAN_POINT('Ctrl Pts',(2.04368806768372,1.91255802664586,1.27359218808486));
#104740=CARTESIAN_POINT('Ctrl Pts',(-0.500577124287141,2.75384673849052,
1.43248412356873));
#104741=CARTESIAN_POINT('Ctrl Pts',(-2.58599214051509,1.07098862122423,
1.5913760590526));
#104742=CARTESIAN_POINT('Ctrl Pts',(-2.3010529690687,-1.59359252333946,
1.75026799453647));
#104743=CARTESIAN_POINT('Ctrl Pts',(0.0930712680559027,-2.79744174940153,
1.90915993002034));
#104744=CARTESIAN_POINT('Ctrl Pts',(2.4018830025703,-1.43712220220855,2.06805186550421));
#104745=CARTESIAN_POINT('Ctrl Pts',(2.50909192361753,1.24049166566884,2.22694380098809));
#104746=CARTESIAN_POINT('Ctrl Pts',(0.316427118516644,2.78104846146861,
2.38583573647195));
#104747=CARTESIAN_POINT('Ctrl Pts',(-2.16627949560986,1.77245390562672,
2.54472767195583));
#104748=CARTESIAN_POINT('Ctrl Pts',(-2.66334032655633,-0.860800619851015,
2.7036196074397));
#104749=CARTESIAN_POINT('Ctrl Pts',(-0.719141363379423,-2.70503131928368,
2.86251154292357));
#104750=CARTESIAN_POINT('Ctrl Pts',(1.8842338679284,-2.06978789449606,3.02140347840744));
#104751=CARTESIAN_POINT('Ctrl Pts',(2.76049066026949,0.46265584800609,3.18029541389131));
#104752=CARTESIAN_POINT('Ctrl Pts',(1.10643819605854,2.57102188943541,3.33918734937518));
#104753=CARTESIAN_POINT('Ctrl Pts',(-1.56179295091342,2.32274877759393,
3.49807928485906));
#104754=CARTESIAN_POINT('Ctrl Pts',(-2.79846006753516,-0.0545924875268026,
3.65697122034292));
#104755=CARTESIAN_POINT('Ctrl Pts',(-1.47001457977705,-2.38189340967681,
3.8158631558268));
#104756=CARTESIAN_POINT('Ctrl Pts',(1.20586943904121,-2.52591329732098,
3.97475509131066));
#104757=CARTESIAN_POINT('Ctrl Pts',(2.77643452544834,-0.354641244841995,
4.13364702679454));
#104758=CARTESIAN_POINT('Ctrl Pts',(1.80207596781938,2.14170056073307,4.2925389622784));
#104759=CARTESIAN_POINT('Ctrl Pts',(-0.824093823277095,2.6749258788713,
4.45143089776229));
#104760=CARTESIAN_POINT('Ctrl Pts',(-2.69488622795106,0.756271978133945,
4.61032283324614));
#104761=CARTESIAN_POINT('Ctrl Pts',(-2.09550344350268,-1.8555927367524,
4.76921476873002));
#104762=CARTESIAN_POINT('Ctrl Pts',(0.424650823266605,-2.76659190429488,
4.92810670421389));
#104763=CARTESIAN_POINT('Ctrl Pts',(2.55556345276143,-1.14168932965037,
5.08699863969777));
#104764=CARTESIAN_POINT('Ctrl Pts',(2.34400634468638,1.52970367803454,5.24589057518163));
#104765=CARTESIAN_POINT('Ctrl Pts',(-0.0161039214601648,2.79894618566735,
5.40478251066551));
#104766=CARTESIAN_POINT('Ctrl Pts',(-2.36145307939294,1.50263050693126,
5.56367444614937));
#104767=CARTESIAN_POINT('Ctrl Pts',(-2.54225712725118,-1.17101997654861,
5.72256638163325));
#104768=CARTESIAN_POINT('Ctrl Pts',(-0.392788225220536,-2.77129509375434,
5.88145831711711));
#104769=CARTESIAN_POINT('Ctrl Pts',(2.11671655455651,-1.83135745123752,
6.040350252601));
#104770=CARTESIAN_POINT('Ctrl Pts',(2.6860055800761,0.787231294053425,6.19924218808485));
#104771=CARTESIAN_POINT('Ctrl Pts',(0.7932595583106,2.68423142811611,6.35813412356874));
#104772=CARTESIAN_POINT('Ctrl Pts',(-1.82660067670958,2.12082273054143,
6.5170260590526));
#104773=CARTESIAN_POINT('Ctrl Pts',(-2.7721699434562,-0.386565506913394,
6.67591799453647));
#104774=CARTESIAN_POINT('Ctrl Pts',(-1.17672454945654,-2.53962170829505,
6.83480993002035));
#104775=CARTESIAN_POINT('Ctrl Pts',(1.49732511225305,-2.36482062633797,
6.99370186550422));
#104776=CARTESIAN_POINT('Ctrl Pts',(2.79890297759256,-0.0223876877032405,
7.15259380098808));
#104777=CARTESIAN_POINT('Ctrl Pts',(1.53496226177243,2.34056615831974,7.31148573647197));
#104778=CARTESIAN_POINT('Ctrl Pts',(-1.13594905484471,2.55812017531127,
7.47037767195582));
#104779=CARTESIAN_POINT('Ctrl Pts',(-2.76563156475219,0.43086092255333,
7.6292696074397));
#104780=CARTESIAN_POINT('Ctrl Pts',(-1.86029259488113,-2.09133224236791,
7.78816154292357));
#104781=CARTESIAN_POINT('Ctrl Pts',(0.750219886458444,-2.69657731365141,
7.94705347840744));
#104782=CARTESIAN_POINT('Ctrl Pts',(2.67306899608655,-0.830097120039615,
8.10594541389131));
#104783=CARTESIAN_POINT('Ctrl Pts',(2.14574093520035,1.79726317648325,8.26483734937519));
#104784=CARTESIAN_POINT('Ctrl Pts',(-0.348407084677866,2.77722371981146,
8.42372928485904));
#104785=CARTESIAN_POINT('Ctrl Pts',(-2.52319967969691,1.21153723133653,
8.58262122034293));
#104786=CARTESIAN_POINT('Ctrl Pts',(-2.38518768160842,-1.4646633777222,
8.74151315582679));
#104787=CARTESIAN_POINT('Ctrl Pts',(-0.060875062987935,-2.79833045104458,
8.90040509131068));
#104788=CARTESIAN_POINT('Ctrl Pts',(2.31923659778409,-1.56700373006449,
9.05929702679454));
#104789=CARTESIAN_POINT('Ctrl Pts',(2.57349944087459,1.10066330653626,9.21818896227841));
#104790=CARTESIAN_POINT('Ctrl Pts',(0.468852137016506,2.75944500944524,
9.37708089776229));
#104791=CARTESIAN_POINT('Ctrl Pts',(-2.06555242493947,1.88887592667273,
9.53597283324615));
#104792=CARTESIAN_POINT('Ctrl Pts',(-2.70663908021347,-0.71306659997388,
9.69486476873003));
#104793=CARTESIAN_POINT('Ctrl Pts',(-0.86677769678369,-2.66140104285234,
9.85375670421389));
#104794=CARTESIAN_POINT('Ctrl Pts',(1.76758578430224,-2.17025334504288,
10.0126486396978));
#104795=CARTESIAN_POINT('Ctrl Pts',(2.78175227759491,0.310182772946269,
10.1715405751816));
#104796=CARTESIAN_POINT('Ctrl Pts',(1.24612079164814,2.50630047264078,10.3304325106655));
#104797=CARTESIAN_POINT('Ctrl Pts',(-1.43172465131564,2.40510365875409,
10.4893244461494));
#104798=CARTESIAN_POINT('Ctrl Pts',(-2.79722871429563,0.0993509257994383,
10.6482163816333));
#104799=CARTESIAN_POINT('Ctrl Pts',(-1.59874885224106,-2.29746843155571,
10.8071083171171));
#104800=CARTESIAN_POINT('Ctrl Pts',(1.06516940473778,-2.58839201546978,
10.966000252601));
#104801=CARTESIAN_POINT('Ctrl Pts',(2.7527365978123,-0.506754683848045,
11.1248921880849));
#104802=CARTESIAN_POINT('Ctrl Pts',(1.91710204103551,2.03938197765761,11.2837841235688));
#104803=CARTESIAN_POINT('Ctrl Pts',(-0.675778460895874,2.71618897691717,
11.4426760590526));
#104804=CARTESIAN_POINT('Ctrl Pts',(-2.64922977501486,0.903294351643931,
11.6015679945365));
#104805=CARTESIAN_POINT('Ctrl Pts',(-2.19435532437014,-1.73757411264833,
11.7604599300203));
#104806=CARTESIAN_POINT('Ctrl Pts',(0.271899800563075,-2.785754760382,11.9193518655042));
#104807=CARTESIAN_POINT('Ctrl Pts',(2.48892728304396,-1.28046869007272,
12.0782438009881));
#104808=CARTESIAN_POINT('Ctrl Pts',(2.42456479133692,1.39851516228695,12.237135736472));
#104809=CARTESIAN_POINT('Ctrl Pts',(0.137807999720803,2.79559797570218,
12.3960276719558));
#104810=CARTESIAN_POINT('Ctrl Pts',(-2.27526577635195,1.63019162477874,
12.5549196074397));
#104811=CARTESIAN_POINT('Ctrl Pts',(-2.60279508266664,-1.02947406192846,
12.7138115429236));
#104812=CARTESIAN_POINT('Ctrl Pts',(-0.544561395054448,-2.74550759852408,
12.8727034784075));
#104813=CARTESIAN_POINT('Ctrl Pts',(2.01282584978326,-1.94496559994811,
13.0315954138913));
#104814=CARTESIAN_POINT('Ctrl Pts',(2.72522519772037,0.638362521023264,
13.1904873493752));
#104815=CARTESIAN_POINT('Ctrl Pts',(0.939640178721769,2.63655749436058,
13.3493792848591));
#104816=CARTESIAN_POINT('Ctrl Pts',(-1.70723383722103,2.21804231510237,
13.5082712203429));
#104817=CARTESIAN_POINT('Ctrl Pts',(-2.78923041123751,-0.233565407466463,
13.6671631558268));
#104818=CARTESIAN_POINT('Ctrl Pts',(-1.31457443085917,-2.47108339646165,
13.8260550913107));
#104819=CARTESIAN_POINT('Ctrl Pts',(1.36504119109539,-2.44356739893747,
13.9849470267946));
#104820=CARTESIAN_POINT('Ctrl Pts',(2.79343854366366,-0.176239011888379,
14.1438389622784));
#104821=CARTESIAN_POINT('Ctrl Pts',(1.66132610133334,2.25263283105917,14.3027308977623));
#104822=CARTESIAN_POINT('Ctrl Pts',(-0.993584028683246,2.61670591860889,
14.4616228332461));
#104823=CARTESIAN_POINT('Ctrl Pts',(-2.73775937870298,0.582265120766335,
14.6205147687301));
#104824=CARTESIAN_POINT('Ctrl Pts',(-1.97246133395434,-1.98588906351594,
14.7794067042139));
#104825=CARTESIAN_POINT('Ctrl Pts',(0.600825856324219,-2.73374603372541,
14.9382986396978));
#104826=CARTESIAN_POINT('Ctrl Pts',(2.62338659742562,-0.975808304424984,
15.0971905751816));
#104827=CARTESIAN_POINT('Ctrl Pts',(2.24130983764105,1.67657069586423,15.2560825106655));
#104828=CARTESIAN_POINT('Ctrl Pts',(-0.195186843319176,2.79217857285889,
15.4149744461494));
#104829=CARTESIAN_POINT('Ctrl Pts',(-2.45277218746558,1.34843156405227,
15.5738663816333));
#104830=CARTESIAN_POINT('Ctrl Pts',(-2.46210788785084,-1.33130906821812,
15.7327583171171));
#104831=CARTESIAN_POINT('Ctrl Pts',(-0.214636694367242,-2.79075082656412,
15.891650252601));
#104832=CARTESIAN_POINT('Ctrl Pts',(2.22957387593874,-1.69214639386452,
16.0505421880849));
#104833=CARTESIAN_POINT('Ctrl Pts',(2.63012189252914,0.957506092396307,
16.2094341235687));
#104834=CARTESIAN_POINT('Ctrl Pts',(0.619858730590574,2.72949340366446,
16.3683260590526));
#104835=CARTESIAN_POINT('Ctrl Pts',(-1.95857671304387,1.99958404315983,
16.5272179945365));
#104836=CARTESIAN_POINT('Ctrl Pts',(-2.74174987350245,-0.563175565597893,
16.6861099300203));
#104837=CARTESIAN_POINT('Ctrl Pts',(-1.01179188876755,-2.60971957504275,
16.8450018655043));
#104838=CARTESIAN_POINT('Ctrl Pts',(1.64559048748105,-2.26415349171583,
17.0038938009881));
#104839=CARTESIAN_POINT('Ctrl Pts',(2.79459868770037,0.156771366137347,
17.162785736472));
#104840=CARTESIAN_POINT('Ctrl Pts',(1.38203368671266,2.43399711900581,17.3216776719558));
#104841=CARTESIAN_POINT('Ctrl Pts',(-1.29732517295305,2.48018275176639,
17.4805696074397));
#104842=CARTESIAN_POINT('Ctrl Pts',(-2.78753533269492,0.252993785525599,
17.6394615429236));
#104843=CARTESIAN_POINT('Ctrl Pts',(-1.72264667374927,-2.20609327181733,
17.7983534784075));
#104844=CARTESIAN_POINT('Ctrl Pts',(0.921247075997331,-2.64304046724668,
17.9572454138913));
#104845=CARTESIAN_POINT('Ctrl Pts',(2.72071123664003,-0.657335114958726,
18.1161373493752));
#104846=CARTESIAN_POINT('Ctrl Pts',(2.02632859821525,1.93089396358069,18.2750292848591));
#104847=CARTESIAN_POINT('Ctrl Pts',(-0.525418769132025,2.74923520339397,
18.4339212203429));
#104848=CARTESIAN_POINT('Ctrl Pts',(-2.59555901186999,1.04758412666344,
18.5928131558268));
#104849=CARTESIAN_POINT('Ctrl Pts',(-2.28656895721723,-1.61429907093739,
18.7517050913106));
#104850=CARTESIAN_POINT('Ctrl Pts',(0.118326240918447,-2.79649029807819,
18.9105970267946));
#104851=CARTESIAN_POINT('Ctrl Pts',(2.41476174175496,-1.41537444412829,
19.0694889622784));
#104852=CARTESIAN_POINT('Ctrl Pts',(2.49778857243239,1.26309593221353,19.2283808977623));
#104853=CARTESIAN_POINT('Ctrl Pts',(0.291303031405191,2.7837926701564,19.3872728332461));
#104854=CARTESIAN_POINT('Ctrl Pts',(-2.18219545925668,1.75282117288872,
19.54616476873));
#104855=CARTESIAN_POINT('Ctrl Pts',(-2.6554591996581,-0.884813836669676,
19.7050567042139));
#104856=CARTESIAN_POINT('Ctrl Pts',(-0.694687186450524,-2.71141453846537,
19.8639486396978));
#104857=CARTESIAN_POINT('Ctrl Pts',(1.90284605034815,-2.05268994131736,
20.0228405751816));
#104858=CARTESIAN_POINT('Ctrl Pts',(2.75620060787838,0.487562607415334,
20.1817325106655));
#104859=CARTESIAN_POINT('Ctrl Pts',(1.08317824906602,2.58090758578969,20.3406244461494));
#104860=CARTESIAN_POINT('Ctrl Pts',(-1.58270236367269,2.30855199522763,
20.4995163816333));
#104861=CARTESIAN_POINT('Ctrl Pts',(-2.79785304679384,-0.0798587386763005,
20.6584083171171));
#104862=CARTESIAN_POINT('Ctrl Pts',(-1.44844752999174,-2.39506969265607,
20.817300252601));
#104863=CARTESIAN_POINT('Ctrl Pts',(1.22862781735764,-2.51492202179281,
20.9761921880849));
#104864=CARTESIAN_POINT('Ctrl Pts',(2.77952355047542,-0.329557184248122,
21.1350841235687));
#104865=CARTESIAN_POINT('Ctrl Pts',(1.78266417767396,2.15788495228345,21.2939760590526));
#104866=CARTESIAN_POINT('Ctrl Pts',(-0.848213250953649,2.66737575156481,
21.4528679945365));
#104867=CARTESIAN_POINT('Ctrl Pts',(-2.70160509322647,0.731907861348415,
21.6117599300204));
#104868=CARTESIAN_POINT('Ctrl Pts',(-2.07866303761187,-1.8744382398188,
21.7706518655042));
#104869=CARTESIAN_POINT('Ctrl Pts',(0.449614145197882,-2.76264484192865,
21.9295438009881));
#104870=CARTESIAN_POINT('Ctrl Pts',(2.56576824795581,-1.11856738663923,
22.088435736472));
#104871=CARTESIAN_POINT('Ctrl Pts',(2.33009810417738,1.55080607790876,22.2473276719558));
#104872=CARTESIAN_POINT('Ctrl Pts',(-0.0413754771973295,2.79868717859702,
22.4062196074398));
#104873=CARTESIAN_POINT('Ctrl Pts',(-2.37492594999191,1.48124573051601,
22.5651115429236));
#104874=CARTESIAN_POINT('Ctrl Pts',(-2.53157746559467,-1.19392551607101,
22.7240034784075));
#104875=CARTESIAN_POINT('Ctrl Pts',(-0.367753579365892,-2.77473227569199,
22.8828954138913));
#104876=CARTESIAN_POINT('Ctrl Pts',(2.13317507136606,-1.81216337356762,
23.0417873493752));
#104877=CARTESIAN_POINT('Ctrl Pts',(2.67877121874512,0.811439507343116,
23.2006792848591));
#104878=CARTESIAN_POINT('Ctrl Pts',(0.769021883783568,2.6913090616914,23.3595712203429));
#104879=CARTESIAN_POINT('Ctrl Pts',(-1.84573657345466,2.10419657965654,
23.5184631558268));
#104880=CARTESIAN_POINT('Ctrl Pts',(-2.76845087541259,-0.411491995891901,
23.6773550913107));
#104881=CARTESIAN_POINT('Ctrl Pts',(-1.15396595201881,-2.55031293376487,
23.8362470267946));
#104882=CARTESIAN_POINT('Ctrl Pts',(1.51903866244618,-2.35088029971449,
23.9951389622784));
#104883=CARTESIAN_POINT('Ctrl Pts',(2.79818299902246,0.00226576998445874,
24.1540308977623));
#104884=CARTESIAN_POINT('Ctrl Pts',(1.51533643748012,2.35552788350921,24.3129228332461));
#104885=CARTESIAN_POINT('Ctrl Pts',(-1.16268678334851,2.5453813249875,24.4718408351714));
#104886=CARTESIAN_POINT('Ctrl Pts',(-2.22875207274563,1.12213500859344,
24.5777948586019));
#104887=CARTESIAN_POINT('Ctrl Pts',(-2.34264057946653,0.342150460324734,
24.6307849035378));
#104888=CARTESIAN_POINT('Ctrl Pts',(1.29201691215935,2.64852191642673,4.54887863488018E-15));
#104889=CARTESIAN_POINT('Ctrl Pts',(1.35230445507443,2.6121804996145,5.43378674156395E-15));
#104890=CARTESIAN_POINT('Ctrl Pts',(1.41110201644458,2.57358023305008,1.59117262741764E-15));
#104891=CARTESIAN_POINT('Ctrl Pts',(1.4682648448244,2.53271326293103,1.84054160801139E-15));
#104892=CARTESIAN_POINT('Ctrl Pts',(1.54796966940638,2.47573052122881,2.00750960553563E-15));
#104893=CARTESIAN_POINT('Ctrl Pts',(1.6244980979052,2.41434172809349,1.79546376567514E-15));
#104894=CARTESIAN_POINT('Ctrl Pts',(1.69767241980579,2.34892928422125,1.99493199737333E-15));
#104895=CARTESIAN_POINT('Ctrl Pts',(1.73624314581282,2.31444990150181,2.10007317684866E-15));
#104896=CARTESIAN_POINT('Ctrl Pts',(1.7738812599705,2.27885201635259,3.69427176174795E-15));
#104897=CARTESIAN_POINT('Ctrl Pts',(1.81055574615744,2.24218867772291,1.97064586870965E-15));
#104898=CARTESIAN_POINT('Ctrl Pts',(1.83140721175525,2.22134355012547,5.86266064330246E-16));
#104899=CARTESIAN_POINT('Ctrl Pts',(1.85194673165548,2.2001543900091,8.11396458076517E-16));
#104900=CARTESIAN_POINT('Ctrl Pts',(1.87216939098153,2.1786293341467,1.80411241501588E-15));
#104901=CARTESIAN_POINT('Ctrl Pts',(1.88524297304094,2.16471377637492,2.44588525584221E-15));
#104902=CARTESIAN_POINT('Ctrl Pts',(1.89818330708257,2.15065853098203,1.189897513384E-15));
#104903=CARTESIAN_POINT('Ctrl Pts',(1.91097839287718,2.13647800248694,1.09634523681734E-15));
#104904=CARTESIAN_POINT('Ctrl Pts',(1.97606835821047,2.06434014245464,3.44342342483582E-16));
#104905=CARTESIAN_POINT('Ctrl Pts',(2.03746495618161,1.98889786290504,8.29405017125788E-16));
#104906=CARTESIAN_POINT('Ctrl Pts',(2.0949947735992,1.91052554193752,7.63278329429795E-17));
#104907=CARTESIAN_POINT('Ctrl Pts',(2.15236598115915,1.83236929366463,-6.74673115466274E-16));
#104908=CARTESIAN_POINT('Ctrl Pts',(2.20589202711639,1.75129816353633,-1.41513655082523E-15));
#104909=CARTESIAN_POINT('Ctrl Pts',(2.25535281672612,1.66766527191713,-2.42861286636753E-15));
#104910=CARTESIAN_POINT('Ctrl Pts',(2.27484369419206,1.6347082881016,-2.827990693465E-15));
#104911=CARTESIAN_POINT('Ctrl Pts',(2.29370272849397,1.6013533709117,-3.52613603609337E-15));
#104912=CARTESIAN_POINT('Ctrl Pts',(2.31191421992203,1.56762185467499,-2.13717932240343E-15));
#104913=CARTESIAN_POINT('Ctrl Pts',(2.3215636330504,1.54974911004558,-1.4012364590331E-15));
#104914=CARTESIAN_POINT('Ctrl Pts',(2.33103139846528,1.53176995434509,-1.06177166968173E-15));
#104915=CARTESIAN_POINT('Ctrl Pts',(2.34030381034639,1.51371048032841,-1.2490009027033E-15));
#104916=CARTESIAN_POINT('Ctrl Pts',(2.38367085566508,1.42924636913981,-2.12467151974787E-15));
#104917=CARTESIAN_POINT('Ctrl Pts',(2.42283443804809,1.34290694301736,-9.36944287622972E-16));
#104918=CARTESIAN_POINT('Ctrl Pts',(2.45762895649157,1.2550365169234,-2.38697950294409E-15));
#104919=CARTESIAN_POINT('Ctrl Pts',(2.4920487142431,1.16811251524223,-3.82139685013631E-15));
#104920=CARTESIAN_POINT('Ctrl Pts',(2.52219321924462,1.07968940189563,-3.00090063764714E-15));
#104921=CARTESIAN_POINT('Ctrl Pts',(2.54785251130495,0.990091831681564,
-3.27515792264421E-15));
#104922=CARTESIAN_POINT('Ctrl Pts',(2.57275717075288,0.903129300981329,
-3.54134937749438E-15));
#104923=CARTESIAN_POINT('Ctrl Pts',(2.59343656824167,0.815059624988842,
-1.78047228398232E-15));
#104924=CARTESIAN_POINT('Ctrl Pts',(2.60965039179134,0.726183587939375,
-2.74780198594726E-15));
#104925=CARTESIAN_POINT('Ctrl Pts',(2.61912055200124,0.674272926206792,
-3.31279933067173E-15));
#104926=CARTESIAN_POINT('Ctrl Pts',(2.62706637598171,0.62208730687767,-6.0589320933173E-15));
#104927=CARTESIAN_POINT('Ctrl Pts',(2.63343195267653,0.56968881258124,-5.32907051820075E-15));
#104928=CARTESIAN_POINT('Ctrl Pts',(2.63584888151175,0.549793768053726,
-5.02254639302231E-15));
#104929=CARTESIAN_POINT('Ctrl Pts',(2.63803838941423,0.52986220654713,-1.31175086481935E-15));
#104930=CARTESIAN_POINT('Ctrl Pts',(2.63999431323799,0.509930525450882,
-2.02615701994091E-15));
#104931=CARTESIAN_POINT('Ctrl Pts',(2.64870355681473,0.42117969402649,-3.85326558685E-15));
#104932=CARTESIAN_POINT('Ctrl Pts',(2.65280061996473,0.332324654199259,
-3.41581273799203E-15));
#104933=CARTESIAN_POINT('Ctrl Pts',(2.65210228927602,0.24365609144491,-2.05391259555654E-15));
#104934=CARTESIAN_POINT('Ctrl Pts',(2.65178733264356,0.203665364440984,
-1.99754801784407E-15));
#104935=CARTESIAN_POINT('Ctrl Pts',(2.65049624272211,0.163712613523904,
-2.3425961516863E-15));
#104936=CARTESIAN_POINT('Ctrl Pts',(2.64820874432577,0.123825020344308,
-2.24820162486594E-15));
#104937=CARTESIAN_POINT('Ctrl Pts',(2.64295670172582,0.0322440430970331,
-2.21457773022915E-15));
#104938=CARTESIAN_POINT('Ctrl Pts',(2.63245536449145,-0.05899509673886,
-1.93770170853692E-15));
#104939=CARTESIAN_POINT('Ctrl Pts',(2.61690932751102,-0.149544955572229,
-3.13638004456607E-15));
#104940=CARTESIAN_POINT('Ctrl Pts',(2.6013632905306,-0.240094814405598,
-4.33505838059522E-15));
#104941=CARTESIAN_POINT('Ctrl Pts',(2.58077188138282,-0.329956281632541,
-1.29603811372711E-15));
#104942=CARTESIAN_POINT('Ctrl Pts',(2.55529474752967,-0.418751394683592,
-2.24820162486594E-15));
#104943=CARTESIAN_POINT('Ctrl Pts',(2.5508308695639,-0.434309288711294,
-2.57358246102794E-15));
#104944=CARTESIAN_POINT('Ctrl Pts',(2.54621690810265,-0.449834351812699,
3.60179654402708E-16));
#104945=CARTESIAN_POINT('Ctrl Pts',(2.54145360363441,-0.465324422952669,
-1.55431223447522E-15));
#104946=CARTESIAN_POINT('Ctrl Pts',(2.53754660451264,-0.478029824159677,
-3.18176020908992E-15));
#104947=CARTESIAN_POINT('Ctrl Pts',(2.5335420591532,-0.490702157165281,
9.72084519165929E-17));
#104948=CARTESIAN_POINT('Ctrl Pts',(2.52944084941284,-0.503340204338878,
-4.71844785465692E-16));
#104949=CARTESIAN_POINT('Ctrl Pts',(2.50206015777548,-0.587714936299748,
-2.72570571264101E-15));
#104950=CARTESIAN_POINT('Ctrl Pts',(2.47037373520267,-0.670566907612742,
-2.45628779146457E-15));
#104951=CARTESIAN_POINT('Ctrl Pts',(2.43459352459919,-0.751592967054325,
-2.44249065417534E-15));
#104952=CARTESIAN_POINT('Ctrl Pts',(2.39879623125327,-0.832657711212454,
-2.42868692964309E-15));
#104953=CARTESIAN_POINT('Ctrl Pts',(2.35890058949824,-0.911895594830773,
-2.48837357958352E-15));
#104954=CARTESIAN_POINT('Ctrl Pts',(2.31507655407985,-0.988972835355777,
-6.93889390390723E-16));
#104955=CARTESIAN_POINT('Ctrl Pts',(2.27205772689207,-1.06463388433495,
1.06762354398604E-15));
#104956=CARTESIAN_POINT('Ctrl Pts',(2.22525285000344,-1.13821355917498,
-1.39552169477871E-15));
#104957=CARTESIAN_POINT('Ctrl Pts',(2.17479201285555,-1.20935690519725,
-1.38777878078145E-15));
#104958=CARTESIAN_POINT('Ctrl Pts',(2.15736382618763,-1.23392842609816,
-1.38510452965671E-15));
#104959=CARTESIAN_POINT('Ctrl Pts',(2.1394993027235,-1.25820893371577,-8.89972469010783E-16));
#104960=CARTESIAN_POINT('Ctrl Pts',(2.12120315232448,-1.2821824919793,-1.22124532708767E-15));
#104961=CARTESIAN_POINT('Ctrl Pts',(2.11083609771111,-1.29576650732539,
-1.45441170047064E-15));
#104962=CARTESIAN_POINT('Ctrl Pts',(2.10033045792001,-1.30925195930262,
9.10990193106776E-16));
#104963=CARTESIAN_POINT('Ctrl Pts',(2.08968705080315,-1.32263584234787,
4.44089209850063E-16));
#104964=CARTESIAN_POINT('Ctrl Pts',(2.08126174077994,-1.33323051027069,
4.10545969975963E-17));
#104965=CARTESIAN_POINT('Ctrl Pts',(2.07275349646736,-1.34375719535956,
5.44615819269545E-16));
#104966=CARTESIAN_POINT('Ctrl Pts',(2.06416789660031,-1.35420866670935,
5.55111512312578E-16));
#104967=CARTESIAN_POINT('Ctrl Pts',(2.01002859219675,-1.42011383322463,
1.37201142676444E-15));
#104968=CARTESIAN_POINT('Ctrl Pts',(1.95275671705684,-1.48310619814664,
1.18076742119145E-15));
#104969=CARTESIAN_POINT('Ctrl Pts',(1.89251077597855,-1.54288980711619,
2.22044604925031E-16));
#104970=CARTESIAN_POINT('Ctrl Pts',(1.83320824964783,-1.60173724117744,
-6.61500643283973E-16));
#104971=CARTESIAN_POINT('Ctrl Pts',(1.77102343304878,-1.65747614431305,
2.34162966278675E-15));
#104972=CARTESIAN_POINT('Ctrl Pts',(1.70608147665216,-1.7097819039225,7.7715611723761E-16));
#104973=CARTESIAN_POINT('Ctrl Pts',(1.64316795857729,-1.76045391220805,
1.2348827422763E-16));
#104974=CARTESIAN_POINT('Ctrl Pts',(1.57766627853085,-1.80790418089787,
-3.2358106014976E-16));
#104975=CARTESIAN_POINT('Ctrl Pts',(1.50967443903864,-1.85179189330092,
-2.33146835171283E-15));
#104976=CARTESIAN_POINT('Ctrl Pts',(1.46645654143987,-1.87968839786154,
-2.59398396294788E-15));
#104977=CARTESIAN_POINT('Ctrl Pts',(1.42223225631607,-1.90614459401194,
8.75155213223675E-16));
#104978=CARTESIAN_POINT('Ctrl Pts',(1.37702479013102,-1.93106208855765,
7.7715611723761E-16));
#104979=CARTESIAN_POINT('Ctrl Pts',(-1.03676051102385,2.12842394760949,
-0.331722097696724));
#104980=CARTESIAN_POINT('Ctrl Pts',(-1.7455522477269,1.78318492571192,-0.278722164800846));
#104981=CARTESIAN_POINT('Ctrl Pts',(-2.77856061136894,0.334956131708931,
-0.172733943176718));
#104982=CARTESIAN_POINT('Ctrl Pts',(-1.78365806106894,-2.16005006104753,
-0.0137574328243411));
#104983=CARTESIAN_POINT('Ctrl Pts',(0.849859252582268,-2.66646553285166,
0.145207433360407));
#104984=CARTESIAN_POINT('Ctrl Pts',(2.70250349758136,-0.730105073536833,
0.304172299545154));
#104985=CARTESIAN_POINT('Ctrl Pts',(2.07654652319967,1.8778076872183,0.463137165729903));
#104986=CARTESIAN_POINT('Ctrl Pts',(-0.454739712339021,2.76212359428796,
0.62210203191465));
#104987=CARTESIAN_POINT('Ctrl Pts',(-2.56867903914637,1.11298801703124,
0.781066898099398));
#104988=CARTESIAN_POINT('Ctrl Pts',(-2.3262392006046,-1.55744028288047,
0.940031764284147));
#104989=CARTESIAN_POINT('Ctrl Pts',(0.0503084804544499,-2.79896185679702,
1.0989966304689));
#104990=CARTESIAN_POINT('Ctrl Pts',(2.38067870632853,-1.47282370987667,
1.25796149665364));
#104991=CARTESIAN_POINT('Ctrl Pts',(2.52706021534629,1.20449898638212,1.41692636283839));
#104992=CARTESIAN_POINT('Ctrl Pts',(0.355144551310132,2.77681184748758,
1.57589122902314));
#104993=CARTESIAN_POINT('Ctrl Pts',(-2.1425722229245,1.80172569768908,1.73485609520789));
#104994=CARTESIAN_POINT('Ctrl Pts',(-2.67472461252547,-0.826244041728367,
1.89382096139263));
#104995=CARTESIAN_POINT('Ctrl Pts',(-0.753120451482905,-2.6962261287845,
2.05278582757738));
#104996=CARTESIAN_POINT('Ctrl Pts',(1.85938553014776,-2.09272889546975,
2.21175069376213));
#104997=CARTESIAN_POINT('Ctrl Pts',(2.76611708141006,0.430609784178951,
2.37071555994688));
#104998=CARTESIAN_POINT('Ctrl Pts',(1.13525073787139,2.55891257909954,2.52968042613162));
#104999=CARTESIAN_POINT('Ctrl Pts',(-1.53707893828351,2.33970438741627,
2.68864529231638));
#105000=CARTESIAN_POINT('Ctrl Pts',(-2.79931358384604,-0.0259165258534752,
2.84761015850112));
#105001=CARTESIAN_POINT('Ctrl Pts',(-1.49349644210569,-2.36776191833878,
3.00657502468587));
#105002=CARTESIAN_POINT('Ctrl Pts',(1.18243377626383,-2.53745513396945,
3.16553989087062));
#105003=CARTESIAN_POINT('Ctrl Pts',(2.77361552270627,-0.379321906352915,
3.32450475705537));
#105004=CARTESIAN_POINT('Ctrl Pts',(1.82032054711271,2.12679601103407,3.48346962324011));
#105005=CARTESIAN_POINT('Ctrl Pts',(-0.802911451550624,2.68182053417896,
3.64243448942486));
#105006=CARTESIAN_POINT('Ctrl Pts',(-2.68956353241581,0.776579795495751,
3.8013993556096));
#105007=CARTESIAN_POINT('Ctrl Pts',(-2.10884703321116,-1.84108456165128,
3.96036422179436));
#105008=CARTESIAN_POINT('Ctrl Pts',(0.406496718972051,-2.76976327354607,
4.11932908797911));
#105009=CARTESIAN_POINT('Ctrl Pts',(2.54892597416715,-1.15749926640803,
4.27829395416385));
#105010=CARTESIAN_POINT('Ctrl Pts',(2.35300561059747,1.51663864183913,4.43725882034861));
#105011=CARTESIAN_POINT('Ctrl Pts',(-0.00152972572175765,2.79943312718021,
4.59622368653335));
#105012=CARTESIAN_POINT('Ctrl Pts',(-2.35466171272765,1.51406617825868,
4.7551885527181));
#105013=CARTESIAN_POINT('Ctrl Pts',(-2.54765944163499,-1.16028425093789,
4.91415341890285));
#105014=CARTESIAN_POINT('Ctrl Pts',(-0.403469451362134,-2.77020587238022,
5.0731182850876));
#105015=CARTESIAN_POINT('Ctrl Pts',(2.11085786236346,-1.83877874102286,
5.23208315127234));
#105016=CARTESIAN_POINT('Ctrl Pts',(2.68871321588955,0.77951870807597,5.39104801745709));
#105017=CARTESIAN_POINT('Ctrl Pts',(0.799980058451885,2.68269641957907,
5.55001288364184));
#105018=CARTESIAN_POINT('Ctrl Pts',(-1.82264379789626,2.12480534626852,
5.70897774982658));
#105019=CARTESIAN_POINT('Ctrl Pts',(-2.77319931132722,-0.382352917074548,
5.86794261601134));
#105020=CARTESIAN_POINT('Ctrl Pts',(-1.17965993226115,-2.53874587498616,
6.02690748219608));
#105021=CARTESIAN_POINT('Ctrl Pts',(1.49608323803294,-2.36612829711708,
6.18587234838083));
#105022=CARTESIAN_POINT('Ctrl Pts',(2.79934022996841,-0.0228571744051168,
6.34483721456558));
#105023=CARTESIAN_POINT('Ctrl Pts',(1.53452101031131,2.34138280562034,6.50380208075032));
#105024=CARTESIAN_POINT('Ctrl Pts',(-1.13804667113744,2.55767041423525,
6.66276694693508));
#105025=CARTESIAN_POINT('Ctrl Pts',(-2.76658599456728,0.42758637514024,
6.82173181311982));
#105026=CARTESIAN_POINT('Ctrl Pts',(-1.85709739130469,-2.09475952146081,
6.98069667930457));
#105027=CARTESIAN_POINT('Ctrl Pts',(0.756066807429931,-2.69540185431488,
7.13966154548932));
#105028=CARTESIAN_POINT('Ctrl Pts',(2.67562571955118,-0.823319611340344,
7.29862641167407));
#105029=CARTESIAN_POINT('Ctrl Pts',(2.14060240978145,1.80406471524147,7.4575912778588));
#105030=CARTESIAN_POINT('Ctrl Pts',(-0.358180098740468,2.77642489370911,
7.61655614404357));
#105031=CARTESIAN_POINT('Ctrl Pts',(-2.52837311278293,1.20173107478242,
7.7755210102283));
#105032=CARTESIAN_POINT('Ctrl Pts',(-2.37907142037402,-1.47541429785025,
7.93448587641306));
#105033=CARTESIAN_POINT('Ctrl Pts',(-0.0472423399272245,-2.79903489346946,
8.09345074259782));
#105034=CARTESIAN_POINT('Ctrl Pts',(2.32792621317397,-1.55485938899917,
8.25241560878254));
#105035=CARTESIAN_POINT('Ctrl Pts',(2.56748728762925,1.11572272604064,8.41138047496732));
#105036=CARTESIAN_POINT('Ctrl Pts',(0.451670849790703,2.76275616314411,
8.57034534115203));
#105037=CARTESIAN_POINT('Ctrl Pts',(-2.07850221122631,1.87527510820912,
8.72931020733681));
#105038=CARTESIAN_POINT('Ctrl Pts',(-2.70188594122545,-0.732557529583622,
8.88827507352154));
#105039=CARTESIAN_POINT('Ctrl Pts',(-0.846596683277061,-2.66835196880128,
9.04723993970629));
#105040=CARTESIAN_POINT('Ctrl Pts',(1.78534872381028,-2.1562370249883,9.20620480589104));
#105041=CARTESIAN_POINT('Ctrl Pts',(2.77943977581406,0.333980098455095,
9.36516967207578));
#105042=CARTESIAN_POINT('Ctrl Pts',(1.22371101906138,2.51780847471947,9.52413453826054));
#105043=CARTESIAN_POINT('Ctrl Pts',(-1.45463338986256,2.3918339981358,9.68309940444529));
#105044=CARTESIAN_POINT('Ctrl Pts',(-2.79851714084195,0.0716239202725503,
9.84206427063003));
#105045=CARTESIAN_POINT('Ctrl Pts',(-1.5750797708687,-2.31429295659422,
10.0010291368147));
#105046=CARTESIAN_POINT('Ctrl Pts',(1.0933141097943,-2.57710931682498,10.1599940029995));
#105047=CARTESIAN_POINT('Ctrl Pts',(2.75871666875113,-0.475721047564691,
10.3189588691842));
#105048=CARTESIAN_POINT('Ctrl Pts',(1.89331051224729,2.0620871654116,10.477923735369));
#105049=CARTESIAN_POINT('Ctrl Pts',(-0.70899265863458,2.70816498455018,
10.6368886015537));
#105050=CARTESIAN_POINT('Ctrl Pts',(-2.6608757193272,0.869809507786801,
10.7958534677385));
#105051=CARTESIAN_POINT('Ctrl Pts',(-2.17170800539298,-1.76649724394164,
10.9548183339232));
#105052=CARTESIAN_POINT('Ctrl Pts',(0.309754752733788,-2.78224372884552,
11.113783200108));
#105053=CARTESIAN_POINT('Ctrl Pts',(2.50705276253614,-1.24559809706071,
11.2727480662927));
#105054=CARTESIAN_POINT('Ctrl Pts',(2.40441506186246,1.43374209111343,11.4317129324775));
#105055=CARTESIAN_POINT('Ctrl Pts',(0.0960000651458504,2.79778701137764,
11.5906777986622));
#105056=CARTESIAN_POINT('Ctrl Pts',(-2.3004840704961,1.5951806214141,11.749642664847));
#105057=CARTESIAN_POINT('Ctrl Pts',(-2.58653577161565,-1.07082252296726,
11.9086075310317));
#105058=CARTESIAN_POINT('Ctrl Pts',(-0.499735143315288,-2.75446781794179,
12.0675723972165));
#105059=CARTESIAN_POINT('Ctrl Pts',(2.04551562973912,-1.91120223472933,
12.2265372634012));
#105060=CARTESIAN_POINT('Ctrl Pts',(2.71423850777836,0.685373982898722,
12.3855021295861));
#105061=CARTESIAN_POINT('Ctrl Pts',(0.892956323270132,2.6531975384945,12.5444669957707));
#105062=CARTESIAN_POINT('Ctrl Pts',(-1.7475117062567,2.18701417691729,12.7034318619554));
#105063=CARTESIAN_POINT('Ctrl Pts',(-2.78483654001413,-0.285505900015315,
12.8623967281402));
#105064=CARTESIAN_POINT('Ctrl Pts',(-1.2673906477906,-2.4961067924739,13.0213615943249));
#105065=CARTESIAN_POINT('Ctrl Pts',(1.41274198702393,-2.41681365678884,
13.1803264605097));
#105066=CARTESIAN_POINT('Ctrl Pts',(2.79684456048536,-0.120368924664381,
13.3392913266944));
#105067=CARTESIAN_POINT('Ctrl Pts',(1.61516041520069,2.28650060282304,13.4982561928792));
#105068=CARTESIAN_POINT('Ctrl Pts',(-1.04824967242495,2.59576593663651,
13.6572210590639));
#105069=CARTESIAN_POINT('Ctrl Pts',(-2.75000993315739,0.523711314635311,
13.8161859252487));
#105070=CARTESIAN_POINT('Ctrl Pts',(-1.92894891786922,-2.0287888618071,
13.9751507914334));
#105071=CARTESIAN_POINT('Ctrl Pts',(0.661703294775168,-2.72010604999605,
14.1341156576182));
#105072=CARTESIAN_POINT('Ctrl Pts',(2.6453180089931,-0.916035373136955,
14.2930805238029));
#105073=CARTESIAN_POINT('Ctrl Pts',(2.20215437799027,1.72839355155001,14.4520453899877));
#105074=CARTESIAN_POINT('Ctrl Pts',(-0.26123538052229,2.78721801255387,
14.6110102561724));
#105075=CARTESIAN_POINT('Ctrl Pts',(-2.48497139521209,1.28908701743486,
14.7699751223572));
#105076=CARTESIAN_POINT('Ctrl Pts',(-2.42902884199723,-1.3916346712722,
14.9289399885419));
#105077=CARTESIAN_POINT('Ctrl Pts',(-0.144728649498314,-2.79568985968684,
15.0879048547267));
#105078=CARTESIAN_POINT('Ctrl Pts',(2.27234361476724,-1.63501763598071,
15.2468697209114));
#105079=CARTESIAN_POINT('Ctrl Pts',(2.60479911141896,1.02559727119973,15.4058345870963));
#105080=CARTESIAN_POINT('Ctrl Pts',(0.547647741995679,2.74534335270262,
15.5647994532809));
#105081=CARTESIAN_POINT('Ctrl Pts',(-2.0119081309943,1.94654921488784,15.7237643194657));
#105082=CARTESIAN_POINT('Ctrl Pts',(-2.72576716592093,-0.63798239061021,
15.8827291856504));
#105083=CARTESIAN_POINT('Ctrl Pts',(-0.93904490593987,-2.63723772879309,
16.0416940518351));
#105084=CARTESIAN_POINT('Ctrl Pts',(1.70914423068041,-2.21712745963629,
16.2006589180199));
#105085=CARTESIAN_POINT('Ctrl Pts',(2.78938796573705,0.236945036121653,
16.3596237842046));
#105086=CARTESIAN_POINT('Ctrl Pts',(1.31068555947639,2.47364741580554,16.5185886503894));
#105087=CARTESIAN_POINT('Ctrl Pts',(-1.37042174567262,2.44105969048874,
16.6775535165741));
#105088=CARTESIAN_POINT('Ctrl Pts',(-2.79432299661122,0.169077391010992,
16.8365183827589));
#105089=CARTESIAN_POINT('Ctrl Pts',(-1.65475077680833,-2.25801418068922,
16.9954832489436));
#105090=CARTESIAN_POINT('Ctrl Pts',(1.00286703836107,-2.61363461044391,
17.1544481151284));
#105091=CARTESIAN_POINT('Ctrl Pts',(2.74046843071987,-0.571542608883376,
17.3134129813131));
#105092=CARTESIAN_POINT('Ctrl Pts',(1.96400179011519,1.99487471836346,17.4723778474979));
#105093=CARTESIAN_POINT('Ctrl Pts',(-0.614213070560955,2.73122142593629,
17.6313427136826));
#105094=CARTESIAN_POINT('Ctrl Pts',(-2.62895731109937,0.961983175507027,
17.7903075798675));
#105095=CARTESIAN_POINT('Ctrl Pts',(-2.2319322855622,-1.68976520446079,
17.9492724460521));
#105096=CARTESIAN_POINT('Ctrl Pts',(0.21263671018481,-2.79134623488795,
18.1082373122369));
#105097=CARTESIAN_POINT('Ctrl Pts',(2.4621357136205,-1.33218463482211,18.2672021784216));
#105098=CARTESIAN_POINT('Ctrl Pts',(2.45290528925346,1.34910482005423,18.4261670446065));
#105099=CARTESIAN_POINT('Ctrl Pts',(0.193413301399417,2.79274407498839,
18.5851319107911));
#105100=CARTESIAN_POINT('Ctrl Pts',(-2.24351338803655,1.67435834015417,
18.7440967769758));
#105101=CARTESIAN_POINT('Ctrl Pts',(-2.62227176319312,-0.980060698885337,
18.9030616431606));
#105102=CARTESIAN_POINT('Ctrl Pts',(-0.595394101940265,-2.7353855371618,
19.0620265093455));
#105103=CARTESIAN_POINT('Ctrl Pts',(1.977689916566,-1.98130531909285,19.2209913755301));
#105104=CARTESIAN_POINT('Ctrl Pts',(2.73646841612022,0.590397138460929,
19.379956241715));
#105105=CARTESIAN_POINT('Ctrl Pts',(0.984848441080798,2.620477384301,19.5389211078996));
#105106=CARTESIAN_POINT('Ctrl Pts',(-1.67025794355887,2.24656773225142,
19.6978859740844));
#105107=CARTESIAN_POINT('Ctrl Pts',(-2.79309267137315,-0.188312247462501,
19.8568508402691));
#105108=CARTESIAN_POINT('Ctrl Pts',(-1.35358261196975,-2.4504371622411,
20.0158157064539));
#105109=CARTESIAN_POINT('Ctrl Pts',(1.32768551221931,-2.46456473939368,
20.1747805726386));
#105110=CARTESIAN_POINT('Ctrl Pts',(2.79095321448688,-0.217734533731887,
20.3337454388233));
#105111=CARTESIAN_POINT('Ctrl Pts',(1.69383883831331,2.2288423370653,20.4927103050081));
#105112=CARTESIAN_POINT('Ctrl Pts',(-0.957179984086533,2.63070991457424,
20.6516751711928));
#105113=CARTESIAN_POINT('Ctrl Pts',(-2.73009505669085,0.619200410386925,
20.8106400373776));
#105114=CARTESIAN_POINT('Ctrl Pts',(-1.99845849072177,-1.96035502838096,
20.9696049035625));
#105115=CARTESIAN_POINT('Ctrl Pts',(0.566536405591253,-2.74150774087858,
21.1285697697471));
#105116=CARTESIAN_POINT('Ctrl Pts',(2.61179858446281,-1.00763896248394,
21.2875346359319));
#105117=CARTESIAN_POINT('Ctrl Pts',(2.26103270329154,1.65062391890566,21.4464995021166));
#105118=CARTESIAN_POINT('Ctrl Pts',(-0.163973521133312,2.79462716070978,
21.6054643683013));
#105119=CARTESIAN_POINT('Ctrl Pts',(-2.43855259750074,1.37487783258505,
21.7644292344861));
#105120=CARTESIAN_POINT('Ctrl Pts',(-2.47603725527275,-1.30616538187191,
21.9233941006708));
#105121=CARTESIAN_POINT('Ctrl Pts',(-0.242039052944788,-2.78895067659981,
22.0823589668556));
#105122=CARTESIAN_POINT('Ctrl Pts',(2.21400177968597,-1.71319055318707,
22.2413238330403));
#105123=CARTESIAN_POINT('Ctrl Pts',(2.63894911424742,0.934226172697978,
22.4002886992251));
#105124=CARTESIAN_POINT('Ctrl Pts',(0.642958410343447,2.72459826446569,
22.5592535654098));
#105125=CARTESIAN_POINT('Ctrl Pts',(-1.94286885474847,2.01545833544657,
22.7182184315946));
#105126=CARTESIAN_POINT('Ctrl Pts',(-2.74634381808181,-0.542629498889809,
22.8771832977793));
#105127=CARTESIAN_POINT('Ctrl Pts',(-1.03034384648533,-2.6029276480822,
23.036148163964));
#105128=CARTESIAN_POINT('Ctrl Pts',(1.63084712721742,-2.27531449840608,
23.1951130301488));
#105129=CARTESIAN_POINT('Ctrl Pts',(2.79598298084694,0.1396002291639,23.3540778963335));
#105130=CARTESIAN_POINT('Ctrl Pts',(1.39600493091336,2.42652520388118,23.5130427625183));
#105131=CARTESIAN_POINT('Ctrl Pts',(-1.284424361538,2.48724124595668,23.672007628703));
#105132=CARTESIAN_POINT('Ctrl Pts',(-2.78696897019498,0.26647914057034,
23.8309724948878));
#105133=CARTESIAN_POINT('Ctrl Pts',(-1.73196816232114,-2.19928735220062,
23.9899373610725));
#105134=CARTESIAN_POINT('Ctrl Pts',(0.910351149945236,-2.64642399680759,
24.1489022272573));
#105135=CARTESIAN_POINT('Ctrl Pts',(2.7205403994727,-0.667766635797716,
24.3078670934421));
#105136=CARTESIAN_POINT('Ctrl Pts',(2.0288526792701,1.92795307285542,24.4668579886134));
#105137=CARTESIAN_POINT('Ctrl Pts',(0.335086850842407,2.47282047565727,
24.5728605950565));
#105138=CARTESIAN_POINT('Ctrl Pts',(-0.439799363723413,2.32629260682496,
24.6258749127712));
#105139=CARTESIAN_POINT('Ctrl Pts',(-1.12118154143677,2.30173662773389,
-0.220420412161518));
#105140=CARTESIAN_POINT('Ctrl Pts',(-1.88768856351612,1.92838558415202,
-0.167420479265639));
#105141=CARTESIAN_POINT('Ctrl Pts',(-3.004812428816,0.362230841230852,-0.0614322576415114));
#105142=CARTESIAN_POINT('Ctrl Pts',(-1.92889724583594,-2.33593798304895,
0.0975442527108654));
#105143=CARTESIAN_POINT('Ctrl Pts',(0.919061342212502,-2.88358970516562,
0.256509118895613));
#105144=CARTESIAN_POINT('Ctrl Pts',(2.9225621587036,-0.789555855045466,
0.415473985080361));
#105145=CARTESIAN_POINT('Ctrl Pts',(2.24563494364476,2.03071326009328,0.574438851265108));
#105146=CARTESIAN_POINT('Ctrl Pts',(-0.491768124086146,2.98703698313542,
0.733403717449859));
#105147=CARTESIAN_POINT('Ctrl Pts',(-2.77784068156911,1.20361607841659,
0.892368583634605));
#105148=CARTESIAN_POINT('Ctrl Pts',(-2.51565952305497,-1.68425907284144,
1.05133344981935));
#105149=CARTESIAN_POINT('Ctrl Pts',(0.0544049846261753,-3.0268749008653,
1.2102983160041));
#105150=CARTESIAN_POINT('Ctrl Pts',(2.57453191286305,-1.5927523663815,1.36926318218884));
#105151=CARTESIAN_POINT('Ctrl Pts',(2.73283293240736,1.30257857610461,1.52822804837359));
#105152=CARTESIAN_POINT('Ctrl Pts',(0.384063157534352,3.00292126710289,
1.68719291455834));
#105153=CARTESIAN_POINT('Ctrl Pts',(-2.31703696465619,1.94843608866463,
1.84615778074309));
#105154=CARTESIAN_POINT('Ctrl Pts',(-2.89252130275355,-0.893523198904568,
2.00512264692783));
#105155=CARTESIAN_POINT('Ctrl Pts',(-0.814445322427711,-2.91577363816391,
2.16408751311259));
#105156=CARTESIAN_POINT('Ctrl Pts',(2.01079102902708,-2.26313500937155,
2.32305237929733));
#105157=CARTESIAN_POINT('Ctrl Pts',(2.99135565075408,0.465673351222398,
2.48201724548208));
#105158=CARTESIAN_POINT('Ctrl Pts',(1.22769160155114,2.76727896108183,2.64098211166683));
#105159=CARTESIAN_POINT('Ctrl Pts',(-1.66223975065641,2.53022114914384,
2.79994697785158));
#105160=CARTESIAN_POINT('Ctrl Pts',(-3.02725526824118,-0.0280268491094517,
2.95891184403632));
#105161=CARTESIAN_POINT('Ctrl Pts',(-1.61510843177923,-2.5605633404543,
3.11787671022108));
#105162=CARTESIAN_POINT('Ctrl Pts',(1.27871664653699,-2.74407428541136,
3.27684157640582));
#105163=CARTESIAN_POINT('Ctrl Pts',(2.99946467292601,-0.410209219143078,
3.43580644259057));
#105164=CARTESIAN_POINT('Ctrl Pts',(1.96854507402614,2.29997613201714,3.59477130877531));
#105165=CARTESIAN_POINT('Ctrl Pts',(-0.868290689426212,2.9001950290315,
3.75373617496007));
#105166=CARTESIAN_POINT('Ctrl Pts',(-2.9085685218548,0.83981490701523,3.91270104114481));
#105167=CARTESIAN_POINT('Ctrl Pts',(-2.28056561009935,-1.99099985464254,
4.07166590732956));
#105168=CARTESIAN_POINT('Ctrl Pts',(0.439596814423422,-2.99529874395252,
4.23063077351431));
#105169=CARTESIAN_POINT('Ctrl Pts',(2.7564791698159,-1.25175177673545,4.38959563969905));
#105170=CARTESIAN_POINT('Ctrl Pts',(2.5446054604199,1.64013504775611,4.54856050588381));
#105171=CARTESIAN_POINT('Ctrl Pts',(-0.00165428777859027,3.02738454571485,
4.70752537206855));
#105172=CARTESIAN_POINT('Ctrl Pts',(-2.54639641514797,1.63735311436671,
4.8664902382533));
#105173=CARTESIAN_POINT('Ctrl Pts',(-2.75510950644466,-1.25476353616774,
5.02545510443804));
#105174=CARTESIAN_POINT('Ctrl Pts',(-0.436323043355592,-2.99577738259457,
5.1844199706228));
#105175=CARTESIAN_POINT('Ctrl Pts',(2.28274017645734,-1.98850627632914,
5.34338483680754));
#105176=CARTESIAN_POINT('Ctrl Pts',(2.90764896600416,0.842993128505951,
5.50234970299229));
#105177=CARTESIAN_POINT('Ctrl Pts',(0.865120599711097,2.90114223577074,
5.66131456917704));
#105178=CARTESIAN_POINT('Ctrl Pts',(-1.97105750179221,2.29782337198566,
5.82027943536179));
#105179=CARTESIAN_POINT('Ctrl Pts',(-2.99901457040901,-0.413487038115629,
5.97924430154654));
#105180=CARTESIAN_POINT('Ctrl Pts',(-1.27571693477946,-2.74547012850852,
6.13820916773129));
#105181=CARTESIAN_POINT('Ctrl Pts',(1.61790586456557,-2.55879669720352,
6.29717403391604));
#105182=CARTESIAN_POINT('Ctrl Pts',(3.02728408409617,-0.0247183816898012,
6.45613890010078));
#105183=CARTESIAN_POINT('Ctrl Pts',(1.65947353647649,2.53203623709253,6.61510376628553));
#105184=CARTESIAN_POINT('Ctrl Pts',(-1.23071520125009,2.76593564958176,
6.77406863247027));
#105185=CARTESIAN_POINT('Ctrl Pts',(-2.99186274643416,0.462403752920377,
6.93303349865502));
#105186=CARTESIAN_POINT('Ctrl Pts',(-2.00831657228625,-2.26533098457947,
7.09199836483977));
#105187=CARTESIAN_POINT('Ctrl Pts',(0.817631593381527,-2.91488224491483,
7.25096323102452));
#105188=CARTESIAN_POINT('Ctrl Pts',(2.89349578485752,-0.890360638857735,
7.40992809720926));
#105189=CARTESIAN_POINT('Ctrl Pts',(2.31490675414699,1.95096556705137,7.56889296339402));
#105190=CARTESIAN_POINT('Ctrl Pts',(-0.387345882629388,3.00250280456578,
7.72785782957877));
#105191=CARTESIAN_POINT('Ctrl Pts',(-2.7342527360709,1.29958527981204,7.88682269576352));
#105192=CARTESIAN_POINT('Ctrl Pts',(-2.57279374929985,-1.59555389999179,
8.04578756194826));
#105193=CARTESIAN_POINT('Ctrl Pts',(-0.0510891753085383,-3.02695388474646,
8.204752428133));
#105194=CARTESIAN_POINT('Ctrl Pts',(2.51748390518839,-1.68146802269111,
8.36371729431776));
#105195=CARTESIAN_POINT('Ctrl Pts',(2.77655188845945,1.2065734685081,8.52268216050249));
#105196=CARTESIAN_POINT('Ctrl Pts',(0.488449371099479,2.98772106062261,
8.68164702668726));
#105197=CARTESIAN_POINT('Ctrl Pts',(-2.24774987886168,2.0279744589843,8.84061189287199));
#105198=CARTESIAN_POINT('Ctrl Pts',(-2.9218943161501,-0.792208008963017,
8.99957675905675));
#105199=CARTESIAN_POINT('Ctrl Pts',(-0.915533109372039,-2.88562974926773,
9.1585416252415));
#105200=CARTESIAN_POINT('Ctrl Pts',(1.93072557536648,-2.33181446020929,
9.31750649142625));
#105201=CARTESIAN_POINT('Ctrl Pts',(3.00576318160537,0.361175331827897,
9.476471357611));
#105202=CARTESIAN_POINT('Ctrl Pts',(1.32335500053861,2.72282784376186,9.63543622379573));
#105203=CARTESIAN_POINT('Ctrl Pts',(-1.57308085033148,2.58659555449547,
9.79440108998049));
#105204=CARTESIAN_POINT('Ctrl Pts',(-3.02639397271004,0.0774560918177764,
9.95336595616523));
#105205=CARTESIAN_POINT('Ctrl Pts',(-1.70333490387714,-2.50274052379573,
10.11233082235));
#105206=CARTESIAN_POINT('Ctrl Pts',(1.18234017003909,-2.78695741742269,
10.2712956885347));
#105207=CARTESIAN_POINT('Ctrl Pts',(2.98335263946653,-0.51445792131468,
10.4302605547195));
#105208=CARTESIAN_POINT('Ctrl Pts',(2.04747844460581,2.2299981935172,10.5892254209042));
#105209=CARTESIAN_POINT('Ctrl Pts',(-0.766724304622935,2.92868464757063,
10.748190287089));
#105210=CARTESIAN_POINT('Ctrl Pts',(-2.87754472594713,0.940636100938752,
10.9071551532737));
#105211=CARTESIAN_POINT('Ctrl Pts',(-2.34854520706281,-1.91033906273146,
11.0661200194585));
#105212=CARTESIAN_POINT('Ctrl Pts',(0.334977371769763,-3.0087954541008,
11.2250848856432));
#105213=CARTESIAN_POINT('Ctrl Pts',(2.71119631860565,-1.34702429309741,
11.384049751828));
#105214=CARTESIAN_POINT('Ctrl Pts',(2.60020106538442,1.55048842104322,11.5430146180127));
#105215=CARTESIAN_POINT('Ctrl Pts',(0.103817130256965,3.02560439047814,
11.7019794841975));
#105216=CARTESIAN_POINT('Ctrl Pts',(-2.48780721177585,1.72507252057746,
11.8609443503822));
#105217=CARTESIAN_POINT('Ctrl Pts',(-2.79715144680568,-1.15801714488529,
12.019909216567));
#105218=CARTESIAN_POINT('Ctrl Pts',(-0.540427429801531,-2.97875781448132,
12.1788740827517));
#105219=CARTESIAN_POINT('Ctrl Pts',(2.21207727570474,-2.06682704901162,
12.3378389489365));
#105220=CARTESIAN_POINT('Ctrl Pts',(2.93525272386455,0.741182414295655,
12.4968038151212));
#105221=CARTESIAN_POINT('Ctrl Pts',(0.965667708515435,2.86924132846054,
12.655768681306));
#105222=CARTESIAN_POINT('Ctrl Pts',(-1.88980757625962,2.36509772502683,
12.8147335474907));
#105223=CARTESIAN_POINT('Ctrl Pts',(-3.01159939193577,-0.308753990593601,
12.9736984136755));
#105224=CARTESIAN_POINT('Ctrl Pts',(-1.37059136124803,-2.69935904330781,
13.1326632798602));
#105225=CARTESIAN_POINT('Ctrl Pts',(1.5277783266453,-2.61360924945721,13.2916281460449));
#105226=CARTESIAN_POINT('Ctrl Pts',(3.02458519797139,-0.130170290111654,
13.4505930122297));
#105227=CARTESIAN_POINT('Ctrl Pts',(1.74667922314479,2.47268510240381,13.6095578784144));
#105228=CARTESIAN_POINT('Ctrl Pts',(-1.13360623889827,2.80713320299311,
13.7685227445992));
#105229=CARTESIAN_POINT('Ctrl Pts',(-2.97393693436389,0.566355925758412,
13.9274876107839));
#105230=CARTESIAN_POINT('Ctrl Pts',(-2.08601880385432,-2.19398848542593,
14.0864524769687));
#105231=CARTESIAN_POINT('Ctrl Pts',(0.715584276331253,-2.94159804658673,
14.2454173431534));
#105232=CARTESIAN_POINT('Ctrl Pts',(2.86072018694497,-0.990626032476896,
14.4043822093382));
#105233=CARTESIAN_POINT('Ctrl Pts',(2.38147075794636,1.86913267406616,14.5633470755229));
#105234=CARTESIAN_POINT('Ctrl Pts',(-0.282507178367135,3.0141747823221,
14.7223119417077));
#105235=CARTESIAN_POINT('Ctrl Pts',(-2.68731691618803,1.39405441650785,
14.8812768078924));
#105236=CARTESIAN_POINT('Ctrl Pts',(-2.62681908917938,-1.5049522905854,
15.0402416740772));
#105237=CARTESIAN_POINT('Ctrl Pts',(-0.156513571465329,-3.02333647253536,
15.1992065402619));
#105238=CARTESIAN_POINT('Ctrl Pts',(2.45737534328226,-1.76815337186677,
15.3581714064467));
#105239=CARTESIAN_POINT('Ctrl Pts',(2.81690192847887,1.1091093045987,15.5171362726314));
#105240=CARTESIAN_POINT('Ctrl Pts',(0.592241441496159,2.96889036496633,
15.6761011388162));
#105241=CARTESIAN_POINT('Ctrl Pts',(-2.17573319542207,2.10505225268967,
15.8350660050009));
#105242=CARTESIAN_POINT('Ctrl Pts',(-2.94772013419658,-0.689931833348374,
15.9940308711857));
#105243=CARTESIAN_POINT('Ctrl Pts',(-1.01550917875938,-2.85198194806187,
16.1529957373704));
#105244=CARTESIAN_POINT('Ctrl Pts',(1.84831592514999,-2.39766306328732,
16.3119606035552));
#105245=CARTESIAN_POINT('Ctrl Pts',(3.0165214298158,0.256238926936299,16.4709254697399));
#105246=CARTESIAN_POINT('Ctrl Pts',(1.41741167828759,2.67507085111204,16.6298903359247));
#105247=CARTESIAN_POINT('Ctrl Pts',(-1.48201204510996,2.63982958206858,
16.7888552021094));
#105248=CARTESIAN_POINT('Ctrl Pts',(-3.02185830893466,0.182844975151096,
16.9478200682941));
#105249=CARTESIAN_POINT('Ctrl Pts',(-1.7894933370904,-2.44187909625444,
17.1067849344789));
#105250=CARTESIAN_POINT('Ctrl Pts',(1.08452820103594,-2.82645688192358,
17.2657498006636));
#105251=CARTESIAN_POINT('Ctrl Pts',(2.96361848926806,-0.618082012587279,
17.4247146668484));
#105252=CARTESIAN_POINT('Ctrl Pts',(2.12392595108712,2.15731279106996,17.5836795330331));
#105253=CARTESIAN_POINT('Ctrl Pts',(-0.664227032086787,2.95361852209465,
17.7426443992179));
#105254=CARTESIAN_POINT('Ctrl Pts',(-2.84302727494801,1.04031525900428,
17.9016092654026));
#105255=CARTESIAN_POINT('Ctrl Pts',(-2.41367341223081,-1.82735890927465,
18.0605741315874));
#105256=CARTESIAN_POINT('Ctrl Pts',(0.229951229774008,-3.01863915633199,
18.2195389977721));
#105257=CARTESIAN_POINT('Ctrl Pts',(2.66262177742226,-1.44066137402666,
18.3785038639569));
#105258=CARTESIAN_POINT('Ctrl Pts',(2.65263974077067,1.45895933113273,18.5374687301416));
#105259=CARTESIAN_POINT('Ctrl Pts',(0.209162502903596,3.02015081934562,
18.6964335963264));
#105260=CARTESIAN_POINT('Ctrl Pts',(-2.42619753731628,1.81069749934597,
18.8553984625111));
#105261=CARTESIAN_POINT('Ctrl Pts',(-2.83579733821026,-1.0598647936472,
19.0143633286959));
#105262=CARTESIAN_POINT('Ctrl Pts',(-0.643875678016031,-2.95812170734611,
19.1733281948806));
#105263=CARTESIAN_POINT('Ctrl Pts',(2.13872867027862,-2.14263846674061,
19.3322930610654));
#105264=CARTESIAN_POINT('Ctrl Pts',(2.95929276265433,0.63847182326205,19.4912579272501));
#105265=CARTESIAN_POINT('Ctrl Pts',(1.06504239070805,2.8338568471607,19.6502227934348));
#105266=CARTESIAN_POINT('Ctrl Pts',(-1.80626321686095,2.42950058977487,
19.8091876596196));
#105267=CARTESIAN_POINT('Ctrl Pts',(-3.02052780113442,-0.203646081844827,
19.9681525258043));
#105268=CARTESIAN_POINT('Ctrl Pts',(-1.46380173937327,-2.6499706398368,
20.1271173919891));
#105269=CARTESIAN_POINT('Ctrl Pts',(1.43579589818991,-2.66524859319272,
20.2860822581738));
#105270=CARTESIAN_POINT('Ctrl Pts',(3.01821413318115,-0.235464157399701,
20.4450471243586));
#105271=CARTESIAN_POINT('Ctrl Pts',(1.83176424978813,2.41033185631518,20.6040119905434));
#105272=CARTESIAN_POINT('Ctrl Pts',(-1.03512095472343,2.8449225889039,20.7629768567281));
#105273=CARTESIAN_POINT('Ctrl Pts',(-2.95240043518508,0.669620479555379,
20.9219417229129));
#105274=CARTESIAN_POINT('Ctrl Pts',(-2.16118838179135,-2.11998224190941,
21.0809065890976));
#105275=CARTESIAN_POINT('Ctrl Pts',(0.612668165643748,-2.96474242806914,
21.2398714552823));
#105276=CARTESIAN_POINT('Ctrl Pts',(2.82447135255811,-1.08968869199482,
21.3988363214671));
#105277=CARTESIAN_POINT('Ctrl Pts',(2.44514341022872,1.78503043861445,21.5578011876518));
#105278=CARTESIAN_POINT('Ctrl Pts',(-0.177325508855966,3.0221872404181,
21.7167660538366));
#105279=CARTESIAN_POINT('Ctrl Pts',(-2.63711834224907,1.4868309809588,21.8757309200213));
#105280=CARTESIAN_POINT('Ctrl Pts',(-2.67765528972552,-1.41252343298867,
22.0346957862061));
#105281=CARTESIAN_POINT('Ctrl Pts',(-0.261747737865253,-3.01604853322711,
22.1936606523908));
#105282=CARTESIAN_POINT('Ctrl Pts',(2.39428286638798,-1.85269173041736,
22.3526255185756));
#105283=CARTESIAN_POINT('Ctrl Pts',(2.85383268770837,1.01029806712227,22.5115903847603));
#105284=CARTESIAN_POINT('Ctrl Pts',(0.695313038955047,2.94645605177694,
22.6705552509451));
#105285=CARTESIAN_POINT('Ctrl Pts',(-2.10107220926576,2.17957248487984,
22.8295201171298));
#105286=CARTESIAN_POINT('Ctrl Pts',(-2.96997229594661,-0.586814574364468,
22.9884849833146));
#105287=CARTESIAN_POINT('Ctrl Pts',(-1.11424238262265,-2.81487807617514,
23.1474498494993));
#105288=CARTESIAN_POINT('Ctrl Pts',(1.76364326814073,-2.46058813916154,
23.3064147156841));
#105289=CARTESIAN_POINT('Ctrl Pts',(3.02365346187921,0.150967555626084,
23.4653795818688));
#105290=CARTESIAN_POINT('Ctrl Pts',(1.50967841044511,2.62411158555409,23.6243444480536));
#105291=CARTESIAN_POINT('Ctrl Pts',(-1.38901209123598,2.68977159567244,
23.7833093142383));
#105292=CARTESIAN_POINT('Ctrl Pts',(-3.01390546101515,0.288177925768345,
23.942274180423));
#105293=CARTESIAN_POINT('Ctrl Pts',(-1.87299835719334,-2.37837027682274,
24.1012390466078));
#105294=CARTESIAN_POINT('Ctrl Pts',(0.984478956028511,-2.8619162328104,
24.2602039127925));
#105295=CARTESIAN_POINT('Ctrl Pts',(2.94206776414501,-0.722141341305858,
24.4191687789773));
#105296=CARTESIAN_POINT('Ctrl Pts',(2.19405749939855,2.08494186946522,24.5781596741486));
#105297=CARTESIAN_POINT('Ctrl Pts',(0.362372204523541,2.67417657512423,
24.6841622805916));
#105298=CARTESIAN_POINT('Ctrl Pts',(-0.475611217151184,2.51571727802135,
24.7371765983065));
#105299=CARTESIAN_POINT('Ctrl Pts',(-1.2056025718497,2.47504930785831,-0.109118726626311));
#105300=CARTESIAN_POINT('Ctrl Pts',(-2.02982487930536,2.07358624259213,
-0.0561187937304326));
#105301=CARTESIAN_POINT('Ctrl Pts',(-3.23106424626307,0.389505550752776,
0.0498694278936948));
#105302=CARTESIAN_POINT('Ctrl Pts',(-2.07413643060294,-2.51182590505037,
0.208845938246073));
#105303=CARTESIAN_POINT('Ctrl Pts',(0.988263431842728,-3.10071387747958,
0.36781080443082));
#105304=CARTESIAN_POINT('Ctrl Pts',(3.14262081982585,-0.849006636554098,
0.526775670615569));
#105305=CARTESIAN_POINT('Ctrl Pts',(2.41472336408983,2.18361883296827,0.685740536800315));
#105306=CARTESIAN_POINT('Ctrl Pts',(-0.528796535833263,3.21195037198289,
0.844705402985064));
#105307=CARTESIAN_POINT('Ctrl Pts',(-2.98700232399185,1.29424413980195,
1.00367026916981));
#105308=CARTESIAN_POINT('Ctrl Pts',(-2.70507984550533,-1.81107786280241,
1.16263513535456));
#105309=CARTESIAN_POINT('Ctrl Pts',(0.0585014887978986,-3.25478794493359,
1.32160000153931));
#105310=CARTESIAN_POINT('Ctrl Pts',(2.76838511939756,-1.71268102288631,
1.48056486772406));
#105311=CARTESIAN_POINT('Ctrl Pts',(2.93860564946843,1.4006581658271,1.6395297339088));
#105312=CARTESIAN_POINT('Ctrl Pts',(0.412981763758567,3.22903068671821,
1.79849460009355));
#105313=CARTESIAN_POINT('Ctrl Pts',(-2.49150170638785,2.09514647964018,
1.9574594662783));
#105314=CARTESIAN_POINT('Ctrl Pts',(-3.11031799298164,-0.960802356080768,
2.11642433246304));
#105315=CARTESIAN_POINT('Ctrl Pts',(-0.875770193372517,-3.13532114754331,
2.2753891986478));
#105316=CARTESIAN_POINT('Ctrl Pts',(2.16219652790641,-2.43354112327336,
2.43435406483254));
#105317=CARTESIAN_POINT('Ctrl Pts',(3.2165942200981,0.500736918265847,2.59331893101729));
#105318=CARTESIAN_POINT('Ctrl Pts',(1.3201324652309,2.97564534306413,2.75228379720204));
#105319=CARTESIAN_POINT('Ctrl Pts',(-1.7874005630293,2.7207379108714,2.91124866338679));
#105320=CARTESIAN_POINT('Ctrl Pts',(-3.25519695263632,-0.0301371723654253,
3.07021352957154));
#105321=CARTESIAN_POINT('Ctrl Pts',(-1.73672042145277,-2.75336476256983,
3.22917839575628));
#105322=CARTESIAN_POINT('Ctrl Pts',(1.37499951681013,-2.95069343685326,
3.38814326194103));
#105323=CARTESIAN_POINT('Ctrl Pts',(3.22531382314573,-0.441096531933247,
3.54710812812578));
#105324=CARTESIAN_POINT('Ctrl Pts',(2.11676960093958,2.4731562530002,3.70607299431053));
#105325=CARTESIAN_POINT('Ctrl Pts',(-0.933669927301801,3.11856952388404,
3.86503786049528));
#105326=CARTESIAN_POINT('Ctrl Pts',(-3.12757351129378,0.903050018534707,
4.02400272668002));
#105327=CARTESIAN_POINT('Ctrl Pts',(-2.45228418698753,-2.1409151476338,
4.18296759286477));
#105328=CARTESIAN_POINT('Ctrl Pts',(0.472696909874794,-3.22083421435897,
4.34193245904952));
#105329=CARTESIAN_POINT('Ctrl Pts',(2.96403236546465,-1.34600428706288,
4.50089732523426));
#105330=CARTESIAN_POINT('Ctrl Pts',(2.73620531024232,1.7636314536731,4.65986219141902));
#105331=CARTESIAN_POINT('Ctrl Pts',(-0.00177884983542148,3.2553359642495,
4.81882705760376));
#105332=CARTESIAN_POINT('Ctrl Pts',(-2.73813111756831,1.76064005047473,
4.97779192378851));
#105333=CARTESIAN_POINT('Ctrl Pts',(-2.96255957125432,-1.34924282139759,
5.13675678997326));
#105334=CARTESIAN_POINT('Ctrl Pts',(-0.469176635349051,-3.2213488928089,
5.29572165615801));
#105335=CARTESIAN_POINT('Ctrl Pts',(2.45462249055121,-2.13823381163544,
5.45468652234275));
#105336=CARTESIAN_POINT('Ctrl Pts',(3.12658471611875,0.906467548935932,
5.6136513885275));
#105337=CARTESIAN_POINT('Ctrl Pts',(0.930261140970313,3.1195880519624,5.77261625471225));
#105338=CARTESIAN_POINT('Ctrl Pts',(-2.11947120568816,2.4708413977028,5.931581120897));
#105339=CARTESIAN_POINT('Ctrl Pts',(-3.22482982949079,-0.444621159156713,
6.09054598708174));
#105340=CARTESIAN_POINT('Ctrl Pts',(-1.37177393729776,-2.95219438203088,
6.2495108532665));
#105341=CARTESIAN_POINT('Ctrl Pts',(1.7397284910982,-2.75146509728996,6.40847571945124));
#105342=CARTESIAN_POINT('Ctrl Pts',(3.25522793822394,-0.0265795889744855,
6.56744058563598));
#105343=CARTESIAN_POINT('Ctrl Pts',(1.78442606264166,2.7226896685647,6.72640545182074));
#105344=CARTESIAN_POINT('Ctrl Pts',(-1.32338373136274,2.97420088492828,
6.88537031800549));
#105345=CARTESIAN_POINT('Ctrl Pts',(-3.21713949830104,0.497221130700515,
7.04433518419023));
#105346=CARTESIAN_POINT('Ctrl Pts',(-2.15953575326782,-2.43590244769814,
7.20330005037498));
#105347=CARTESIAN_POINT('Ctrl Pts',(0.87919637933312,-3.13436263551479,
7.36226491655974));
#105348=CARTESIAN_POINT('Ctrl Pts',(3.11136585016387,-0.957401666375127,
7.52122978274447));
#105349=CARTESIAN_POINT('Ctrl Pts',(2.48921109851253,2.09786641886127,7.68019464892923));
#105350=CARTESIAN_POINT('Ctrl Pts',(-0.416511666518302,3.22858071542247,
7.83915951511398));
#105351=CARTESIAN_POINT('Ctrl Pts',(-2.94013235935888,1.39743948484165,
7.99812438129872));
#105352=CARTESIAN_POINT('Ctrl Pts',(-2.76651607822568,-1.71569350213334,
8.15708924748347));
#105353=CARTESIAN_POINT('Ctrl Pts',(-0.0549360106898553,-3.25487287602346,
8.31605411366822));
#105354=CARTESIAN_POINT('Ctrl Pts',(2.70704159720282,-1.80807665638305,
8.47501897985296));
#105355=CARTESIAN_POINT('Ctrl Pts',(2.98561648928963,1.29742421097557,8.63398384603771));
#105356=CARTESIAN_POINT('Ctrl Pts',(0.525227892408259,3.21268595810113,
8.79294871222246));
#105357=CARTESIAN_POINT('Ctrl Pts',(-2.41699754649706,2.18067380975948,
8.9519135784072));
#105358=CARTESIAN_POINT('Ctrl Pts',(-3.14190269107475,-0.851858488342414,
9.11087844459197));
#105359=CARTESIAN_POINT('Ctrl Pts',(-0.984469535467015,-3.10290752973419,
9.26984331077669));
#105360=CARTESIAN_POINT('Ctrl Pts',(2.07610242692268,-2.50739189543028,
9.42880817696146));
#105361=CARTESIAN_POINT('Ctrl Pts',(3.23208658739667,0.388370565200701,
9.58777304314619));
#105362=CARTESIAN_POINT('Ctrl Pts',(1.42299898201583,2.92784721280426,9.74673790933095));
#105363=CARTESIAN_POINT('Ctrl Pts',(-1.6915283108004,2.78135711085513,9.90570277551569));
#105364=CARTESIAN_POINT('Ctrl Pts',(-3.25427080457815,0.0832882633629985,
10.0646676417004));
#105365=CARTESIAN_POINT('Ctrl Pts',(-1.83159003688557,-2.69118809099722,
10.2236325078851));
#105366=CARTESIAN_POINT('Ctrl Pts',(1.27136623028387,-2.9968055180204,10.3825973740699));
#105367=CARTESIAN_POINT('Ctrl Pts',(3.20798861018195,-0.553194795064668,
10.5415622402546));
#105368=CARTESIAN_POINT('Ctrl Pts',(2.20164637696432,2.39790922162279,10.7005271064394));
#105369=CARTESIAN_POINT('Ctrl Pts',(-0.82445595061129,3.14920431059108,
10.8594919726241));
#105370=CARTESIAN_POINT('Ctrl Pts',(-3.09421373256705,1.0114626940907,11.0184568388089));
#105371=CARTESIAN_POINT('Ctrl Pts',(-2.52538240873262,-2.05418088152127,
11.1774217049936));
#105372=CARTESIAN_POINT('Ctrl Pts',(0.360199990805737,-3.23534717935607,
11.3363865711784));
#105373=CARTESIAN_POINT('Ctrl Pts',(2.91533987467515,-1.44845048913411,
11.4953514373631));
#105374=CARTESIAN_POINT('Ctrl Pts',(2.79598706890637,1.66723475097302,11.6543163035479));
#105375=CARTESIAN_POINT('Ctrl Pts',(0.111634195368079,3.25342176957865,
11.8132811697326));
#105376=CARTESIAN_POINT('Ctrl Pts',(-2.67513035305559,1.85496441974084,
11.9722460359174));
#105377=CARTESIAN_POINT('Ctrl Pts',(-3.0077671219957,-1.24521176680332,
12.1312109021021));
#105378=CARTESIAN_POINT('Ctrl Pts',(-0.581119716287773,-3.20304781102084,
12.2901757682869));
#105379=CARTESIAN_POINT('Ctrl Pts',(2.37863892167038,-2.22245186329391,
12.4491406344716));
#105380=CARTESIAN_POINT('Ctrl Pts',(3.15626693995073,0.79699084569259,12.6081055006564));
#105381=CARTESIAN_POINT('Ctrl Pts',(1.03837909376074,3.08528511842656,12.7670703668411));
#105382=CARTESIAN_POINT('Ctrl Pts',(-2.03210344626256,2.54318127313638,
12.9260352330259));
#105383=CARTESIAN_POINT('Ctrl Pts',(-3.23836224385742,-0.332002081171888,
13.0850000992106));
#105384=CARTESIAN_POINT('Ctrl Pts',(-1.47379207470547,-2.90261129414173,
13.2439649653954));
#105385=CARTESIAN_POINT('Ctrl Pts',(1.64281466626666,-2.81040484212558,
13.4029298315801));
#105386=CARTESIAN_POINT('Ctrl Pts',(3.25232583545743,-0.139971655558927,
13.5618946977649));
#105387=CARTESIAN_POINT('Ctrl Pts',(1.87819803108888,2.65886960198457,13.7208595639496));
#105388=CARTESIAN_POINT('Ctrl Pts',(-1.21896280537159,3.01850046934971,
13.8798244301343));
#105389=CARTESIAN_POINT('Ctrl Pts',(-3.1978639355704,0.609000536881513,
14.0387892963191));
#105390=CARTESIAN_POINT('Ctrl Pts',(-2.24308868983942,-2.35918810904475,
14.1977541625039));
#105391=CARTESIAN_POINT('Ctrl Pts',(0.769465257887335,-3.16309004317742,
14.3567190286886));
#105392=CARTESIAN_POINT('Ctrl Pts',(3.07612236489684,-1.06521669181684,
14.5156838948734));
#105393=CARTESIAN_POINT('Ctrl Pts',(2.56078713790247,2.00987179658232,14.6746487610581));
#105394=CARTESIAN_POINT('Ctrl Pts',(-0.303778976211977,3.24113155209031,
14.8336136272429));
#105395=CARTESIAN_POINT('Ctrl Pts',(-2.88966243716399,1.49902181558082,
14.9925784934276));
#105396=CARTESIAN_POINT('Ctrl Pts',(-2.8246093363615,-1.61826990989858,
15.1515433596124));
#105397=CARTESIAN_POINT('Ctrl Pts',(-0.168298493432347,-3.2509830853839,
15.3105082257971));
#105398=CARTESIAN_POINT('Ctrl Pts',(2.64240707179728,-1.90128910775282,
15.4694730919818));
#105399=CARTESIAN_POINT('Ctrl Pts',(3.02900474553876,1.19262133799767,15.6284379581666));
#105400=CARTESIAN_POINT('Ctrl Pts',(0.636835140996644,3.19243737723006,
15.7874028243514));
#105401=CARTESIAN_POINT('Ctrl Pts',(-2.33955825984986,2.2635552904915,15.9463676905361));
#105402=CARTESIAN_POINT('Ctrl Pts',(-3.16967310247223,-0.741881276086534,
16.1053325567208));
#105403=CARTESIAN_POINT('Ctrl Pts',(-1.0919734515789,-3.06672616733066,
16.2642974229056));
#105404=CARTESIAN_POINT('Ctrl Pts',(1.98748761961958,-2.57819866693835,
16.4232622890903));
#105405=CARTESIAN_POINT('Ctrl Pts',(3.24365489389454,0.275532817750943,
16.5822271552751));
#105406=CARTESIAN_POINT('Ctrl Pts',(1.52413779709881,2.87649428641854,16.7411920214598));
#105407=CARTESIAN_POINT('Ctrl Pts',(-1.5936023445473,2.83859947364843,16.9001568876446));
#105408=CARTESIAN_POINT('Ctrl Pts',(-3.24939362125808,0.196612559291201,
17.0591217538293));
#105409=CARTESIAN_POINT('Ctrl Pts',(-1.92423589737249,-2.62574401181966,
17.2180866200141));
#105410=CARTESIAN_POINT('Ctrl Pts',(1.16618936371082,-3.03927915340325,
17.3770514861988));
#105411=CARTESIAN_POINT('Ctrl Pts',(3.18676854781625,-0.664621416291182,
17.5360163523836));
#105412=CARTESIAN_POINT('Ctrl Pts',(2.28385011205904,2.31975086377646,17.6949812185683));
#105413=CARTESIAN_POINT('Ctrl Pts',(-0.714240993612621,3.176015618253,17.8539460847531));
#105414=CARTESIAN_POINT('Ctrl Pts',(-3.05709723879664,1.11864734250153,
18.0129109509378));
#105415=CARTESIAN_POINT('Ctrl Pts',(-2.59541453889942,-1.9649526140885,
18.1718758171225));
#105416=CARTESIAN_POINT('Ctrl Pts',(0.247265749363208,-3.24593207777605,
18.3308406833073));
#105417=CARTESIAN_POINT('Ctrl Pts',(2.86310784122402,-1.54913811323122,
18.4898055494921));
#105418=CARTESIAN_POINT('Ctrl Pts',(2.85237419228788,1.56881384221122,18.6487704156768));
#105419=CARTESIAN_POINT('Ctrl Pts',(0.224911704407769,3.24755756370285,
18.8077352818615));
#105420=CARTESIAN_POINT('Ctrl Pts',(-2.60888168659601,1.94703665853776,
18.9667001480463));
#105421=CARTESIAN_POINT('Ctrl Pts',(-3.04932291322741,-1.13966888840907,
19.125665014231));
#105422=CARTESIAN_POINT('Ctrl Pts',(-0.692357254091794,-3.18085787753041,
19.2846298804158));
#105423=CARTESIAN_POINT('Ctrl Pts',(2.29976742399123,-2.30397161438838,
19.4435947466005));
#105424=CARTESIAN_POINT('Ctrl Pts',(3.18211710918843,0.686546508063173,
19.6025596127853));
#105425=CARTESIAN_POINT('Ctrl Pts',(1.1452363403353,3.04723631002041,19.76152447897));
#105426=CARTESIAN_POINT('Ctrl Pts',(-1.94226849016302,2.61243344729831,
19.9204893451548));
#105427=CARTESIAN_POINT('Ctrl Pts',(-3.24796293089569,-0.218979916227147,
20.0794542113395));
#105428=CARTESIAN_POINT('Ctrl Pts',(-1.57402086677678,-2.84950411743251,
20.2384190775243));
#105429=CARTESIAN_POINT('Ctrl Pts',(1.54390628416051,-2.86593244699177,
20.397383943709));
#105430=CARTESIAN_POINT('Ctrl Pts',(3.2454750518754,-0.253193781067517,
20.5563488098938));
#105431=CARTESIAN_POINT('Ctrl Pts',(1.96968966126294,2.59182137556506,20.7153136760785));
#105432=CARTESIAN_POINT('Ctrl Pts',(-1.11306192536034,3.05913526323357,
20.8742785422633));
#105433=CARTESIAN_POINT('Ctrl Pts',(-3.17470581367933,0.720040548723835,
21.033243408448));
#105434=CARTESIAN_POINT('Ctrl Pts',(-2.32391827286092,-2.27960945543785,
21.1922082746328));
#105435=CARTESIAN_POINT('Ctrl Pts',(0.658799925696245,-3.18797711525971,
21.3511731408175));
#105436=CARTESIAN_POINT('Ctrl Pts',(3.03714412065341,-1.17173842150571,
21.5101380070023));
#105437=CARTESIAN_POINT('Ctrl Pts',(2.6292541171659,1.91943695832324,21.669102873187));
#105438=CARTESIAN_POINT('Ctrl Pts',(-0.190677496578619,3.24974732012642,
21.8280677393718));
#105439=CARTESIAN_POINT('Ctrl Pts',(-2.83568408699738,1.59878412933253,
21.9870326055565));
#105440=CARTESIAN_POINT('Ctrl Pts',(-2.87927332417827,-1.51888148410543,
22.1459974717412));
#105441=CARTESIAN_POINT('Ctrl Pts',(-0.281456422785714,-3.24314638985442,
22.304962337926));
#105442=CARTESIAN_POINT('Ctrl Pts',(2.57456395308999,-1.99219290764765,
22.4639272041107));
#105443=CARTESIAN_POINT('Ctrl Pts',(3.06871626116932,1.08636996154657,22.6228920702955));
#105444=CARTESIAN_POINT('Ctrl Pts',(0.747667667566643,3.16831383908819,
22.7818569364802));
#105445=CARTESIAN_POINT('Ctrl Pts',(-2.25927556378304,2.3436866343131,22.940821802665));
#105446=CARTESIAN_POINT('Ctrl Pts',(-3.1936007738114,-0.630999649839126,
23.0997866688497));
#105447=CARTESIAN_POINT('Ctrl Pts',(-1.19814091875997,-3.02682850426808,
23.2587515350345));
#105448=CARTESIAN_POINT('Ctrl Pts',(1.89643940906404,-2.64586177991698,
23.4177164012192));
#105449=CARTESIAN_POINT('Ctrl Pts',(3.25132394291147,0.16233488208827,23.576681267404));
#105450=CARTESIAN_POINT('Ctrl Pts',(1.62335188997686,2.82169796722699,23.7356461335887));
#105451=CARTESIAN_POINT('Ctrl Pts',(-1.49359982093395,2.8923019453882,23.8946109997735));
#105452=CARTESIAN_POINT('Ctrl Pts',(-3.24084195183531,0.309876710966349,
24.0535758659582));
#105453=CARTESIAN_POINT('Ctrl Pts',(-2.01402855206554,-2.55745320144486,
24.212540732143));
#105454=CARTESIAN_POINT('Ctrl Pts',(1.05860676211178,-3.0774084688132,24.3715055983277));
#105455=CARTESIAN_POINT('Ctrl Pts',(3.16359512881733,-0.776516046813999,
24.5304704645125));
#105456=CARTESIAN_POINT('Ctrl Pts',(2.35926231952699,2.24193066607503,24.6894613596838));
#105457=CARTESIAN_POINT('Ctrl Pts',(0.389657558204677,2.87553267459119,
24.7954639661269));
#105458=CARTESIAN_POINT('Ctrl Pts',(-0.511423070578954,2.70514194921774,
24.8484782838417));
#105459=CARTESIAN_POINT('Ctrl Pts',(-1.29002360226262,2.64836198798272,
0.00218295890889542));
#105460=CARTESIAN_POINT('Ctrl Pts',(-2.17196119509458,2.21878690103223,
0.0551828918047738));
#105461=CARTESIAN_POINT('Ctrl Pts',(-3.45731606371014,0.416780260274697,
0.161171113428902));
#105462=CARTESIAN_POINT('Ctrl Pts',(-2.21937561536994,-2.68771382705179,
0.320147623781279));
#105463=CARTESIAN_POINT('Ctrl Pts',(1.05746552147296,-3.31783804979352,
0.479112489966027));
#105464=CARTESIAN_POINT('Ctrl Pts',(3.36267948094808,-0.908457418062733,
0.638077356150774));
#105465=CARTESIAN_POINT('Ctrl Pts',(2.58381178453491,2.33652440584326,0.797042222335523));
#105466=CARTESIAN_POINT('Ctrl Pts',(-0.565824947580382,3.43686376083034,
0.956007088520271));
#105467=CARTESIAN_POINT('Ctrl Pts',(-3.1961639664146,1.3848722011873,1.11497195470501));
#105468=CARTESIAN_POINT('Ctrl Pts',(-2.89450016795568,-1.93789665276337,
1.27393682088976));
#105469=CARTESIAN_POINT('Ctrl Pts',(0.0625979929696191,-3.48270098900187,
1.43290168707451));
#105470=CARTESIAN_POINT('Ctrl Pts',(2.96223832593208,-1.83260967939114,
1.59186655325927));
#105471=CARTESIAN_POINT('Ctrl Pts',(3.14437836652949,1.49873775554959,1.75083141944401));
#105472=CARTESIAN_POINT('Ctrl Pts',(0.441900369982786,3.45514010633353,
1.90979628562875));
#105473=CARTESIAN_POINT('Ctrl Pts',(-2.66596644811953,2.24185687061573,
2.0687611518135));
#105474=CARTESIAN_POINT('Ctrl Pts',(-3.32811468320972,-1.02808151325697,
2.22772601799825));
#105475=CARTESIAN_POINT('Ctrl Pts',(-0.937095064317323,-3.35486865692271,
2.38669088418301));
#105476=CARTESIAN_POINT('Ctrl Pts',(2.31360202678571,-2.60394723717516,
2.54565575036775));
#105477=CARTESIAN_POINT('Ctrl Pts',(3.44183278944212,0.535800485309293,
2.70462061655249));
#105478=CARTESIAN_POINT('Ctrl Pts',(1.41257332891064,3.18401172504641,2.86358548273725));
#105479=CARTESIAN_POINT('Ctrl Pts',(-1.91256137540221,2.91125467259897,
3.022550348922));
#105480=CARTESIAN_POINT('Ctrl Pts',(-3.48313863703146,-0.0322474956213979,
3.18151521510675));
#105481=CARTESIAN_POINT('Ctrl Pts',(-1.85833241112631,-2.94616618468535,
3.34048008129148));
#105482=CARTESIAN_POINT('Ctrl Pts',(1.47128238708329,-3.15731258829517,
3.49944494747623));
#105483=CARTESIAN_POINT('Ctrl Pts',(3.45116297336547,-0.471983844723412,
3.65840981366099));
#105484=CARTESIAN_POINT('Ctrl Pts',(2.26499412785301,2.64633637398326,3.81737467984574));
#105485=CARTESIAN_POINT('Ctrl Pts',(-0.999049165177388,3.33694401873657,
3.97633954603049));
#105486=CARTESIAN_POINT('Ctrl Pts',(-3.34657850073276,0.966285130054183,
4.13530441221522));
#105487=CARTESIAN_POINT('Ctrl Pts',(-2.62400276387572,-2.29083044062507,
4.29426927839998));
#105488=CARTESIAN_POINT('Ctrl Pts',(0.505797005326167,-3.44636968476542,
4.45323414458472));
#105489=CARTESIAN_POINT('Ctrl Pts',(3.17158556111339,-1.4402567973903,4.61219901076946));
#105490=CARTESIAN_POINT('Ctrl Pts',(2.92780516006474,1.8871278595901,4.77116387695423));
#105491=CARTESIAN_POINT('Ctrl Pts',(-0.00190341189225514,3.48328738278414,
4.93012874313896));
#105492=CARTESIAN_POINT('Ctrl Pts',(-2.92986581998863,1.88392698658276,
5.08909360932372));
#105493=CARTESIAN_POINT('Ctrl Pts',(-3.17000963606399,-1.44372210662744,
5.24805847550846));
#105494=CARTESIAN_POINT('Ctrl Pts',(-0.502030227342508,-3.44692040302324,
5.4070233416932));
#105495=CARTESIAN_POINT('Ctrl Pts',(2.62650480464509,-2.28796134694173,
5.56598820787796));
#105496=CARTESIAN_POINT('Ctrl Pts',(3.34552046623336,0.969941969365909,
5.72495307406269));
#105497=CARTESIAN_POINT('Ctrl Pts',(0.995401682229525,3.33803386815407,
5.88391794024746));
#105498=CARTESIAN_POINT('Ctrl Pts',(-2.26788490958412,2.64385942341994,
6.0428828064322));
#105499=CARTESIAN_POINT('Ctrl Pts',(-3.45064508857258,-0.475755280197791,
6.20184767261695));
#105500=CARTESIAN_POINT('Ctrl Pts',(-1.46783093981607,-3.15891863555324,
6.36081253880171));
#105501=CARTESIAN_POINT('Ctrl Pts',(1.86155111763083,-2.94413349737639,
6.51977740498645));
#105502=CARTESIAN_POINT('Ctrl Pts',(3.48317179235171,-0.028440796259172,
6.6787422711712));
#105503=CARTESIAN_POINT('Ctrl Pts',(1.90937858880683,2.91334310003689,6.83770713735594));
#105504=CARTESIAN_POINT('Ctrl Pts',(-1.41605226147539,3.18246612027479,
6.99667200354068));
#105505=CARTESIAN_POINT('Ctrl Pts',(-3.44241625016792,0.53203850848065,
7.15563686972543));
#105506=CARTESIAN_POINT('Ctrl Pts',(-2.31075493424938,-2.60647391081679,
7.31460173591018));
#105507=CARTESIAN_POINT('Ctrl Pts',(0.940761165284715,-3.35384302611475,
7.47356660209493));
#105508=CARTESIAN_POINT('Ctrl Pts',(3.3292359154702,-1.02444269389252,7.63253146827967));
#105509=CARTESIAN_POINT('Ctrl Pts',(2.66351544287808,2.24476727067117,7.79149633446445));
#105510=CARTESIAN_POINT('Ctrl Pts',(-0.44567745040722,3.45465862627915,
7.95046120064917));
#105511=CARTESIAN_POINT('Ctrl Pts',(-3.14601198264685,1.49529368987125,
8.10942606683394));
#105512=CARTESIAN_POINT('Ctrl Pts',(-2.96023840715151,-1.83583310427489,
8.26839093301866));
#105513=CARTESIAN_POINT('Ctrl Pts',(-0.0587828460711719,-3.48279186730046,
8.42735579920343));
#105514=CARTESIAN_POINT('Ctrl Pts',(2.89659928921725,-1.93468529007499,
8.58632066538816));
#105515=CARTESIAN_POINT('Ctrl Pts',(3.19468109011983,1.38827495344303,8.74528553157291));
#105516=CARTESIAN_POINT('Ctrl Pts',(0.56200641371704,3.43765085557963,8.90425039775766));
#105517=CARTESIAN_POINT('Ctrl Pts',(-2.58624521413244,2.33337316053465,
9.06321526394242));
#105518=CARTESIAN_POINT('Ctrl Pts',(-3.3619110659994,-0.911508967721811,
9.22218013012717));
#105519=CARTESIAN_POINT('Ctrl Pts',(-1.05340596156199,-3.32018531020063,
9.38114499631191));
#105520=CARTESIAN_POINT('Ctrl Pts',(2.22147927847889,-2.68296933065128,
9.54010986249667));
#105521=CARTESIAN_POINT('Ctrl Pts',(3.45840999318797,0.415565798573505,
9.6990747286814));
#105522=CARTESIAN_POINT('Ctrl Pts',(1.52264296349306,3.13286658184666,9.85803959486615));
#105523=CARTESIAN_POINT('Ctrl Pts',(-1.80997577126933,2.9761186672148,10.0170044610509));
#105524=CARTESIAN_POINT('Ctrl Pts',(-3.48214763644626,0.0891204349082218,
10.1759693272357));
#105525=CARTESIAN_POINT('Ctrl Pts',(-1.959845169894,-2.87963565819873,10.3349341934204));
#105526=CARTESIAN_POINT('Ctrl Pts',(1.36039229052865,-3.20665361861812,
10.4938990596052));
#105527=CARTESIAN_POINT('Ctrl Pts',(3.43262458089735,-0.591931668814657,
10.6528639257899));
#105528=CARTESIAN_POINT('Ctrl Pts',(2.35581430932283,2.56582024972839,10.8118287919747));
#105529=CARTESIAN_POINT('Ctrl Pts',(-0.882187596599642,3.36972397361152,
10.9707936581594));
#105530=CARTESIAN_POINT('Ctrl Pts',(-3.31088273918698,1.08228928724265,
11.1297585243441));
#105531=CARTESIAN_POINT('Ctrl Pts',(-2.70221961040245,-2.1980227003111,
11.2887233905289));
#105532=CARTESIAN_POINT('Ctrl Pts',(0.38542260984171,-3.46189890461135,
11.4476882567136));
#105533=CARTESIAN_POINT('Ctrl Pts',(3.11948343074465,-1.54987668517082,
11.6066531228984));
#105534=CARTESIAN_POINT('Ctrl Pts',(2.99177307242833,1.78398108090281,11.7656179890831));
#105535=CARTESIAN_POINT('Ctrl Pts',(0.119451260479191,3.48123914867916,
11.9245828552679));
#105536=CARTESIAN_POINT('Ctrl Pts',(-2.86245349433533,1.9848563189042,12.0835477214526));
#105537=CARTESIAN_POINT('Ctrl Pts',(-3.21838279718572,-1.33240638872134,
12.2425125876374));
#105538=CARTESIAN_POINT('Ctrl Pts',(-0.621812002774014,-3.42733780756036,
12.4014774538221));
#105539=CARTESIAN_POINT('Ctrl Pts',(2.54520056763601,-2.37807667757619,
12.5604423200069));
#105540=CARTESIAN_POINT('Ctrl Pts',(3.37728115603691,0.852799277089526,
12.7194071861916));
#105541=CARTESIAN_POINT('Ctrl Pts',(1.11109047900605,3.30132890839259,12.8783720523764));
#105542=CARTESIAN_POINT('Ctrl Pts',(-2.1743993162655,2.72126482124593,13.0373369185611));
#105543=CARTESIAN_POINT('Ctrl Pts',(-3.46512509577907,-0.355250171750174,
13.1963017847459));
#105544=CARTESIAN_POINT('Ctrl Pts',(-1.57699278816291,-3.10586354497564,
13.3552666509306));
#105545=CARTESIAN_POINT('Ctrl Pts',(1.75785100588802,-3.00720043479395,
13.5142315171154));
#105546=CARTESIAN_POINT('Ctrl Pts',(3.48006647294345,-0.149773021006202,
13.6731963833001));
#105547=CARTESIAN_POINT('Ctrl Pts',(2.00971683903299,2.84505410156533,13.8321612494849));
#105548=CARTESIAN_POINT('Ctrl Pts',(-1.30431937184491,3.22986773570631,
13.9911261156696));
#105549=CARTESIAN_POINT('Ctrl Pts',(-3.42179093677689,0.651645148004609,
14.1500909818544));
#105550=CARTESIAN_POINT('Ctrl Pts',(-2.40015857582453,-2.52438773266358,
14.3090558480391));
#105551=CARTESIAN_POINT('Ctrl Pts',(0.823346239443419,-3.38458203976812,
14.4680207142239));
#105552=CARTESIAN_POINT('Ctrl Pts',(3.29152454284872,-1.13980735115677,
14.6269855804086));
#105553=CARTESIAN_POINT('Ctrl Pts',(2.74010351785857,2.15061091909846,14.7859504465933));
#105554=CARTESIAN_POINT('Ctrl Pts',(-0.325050774056821,3.46808832185853,
14.9449153127781));
#105555=CARTESIAN_POINT('Ctrl Pts',(-3.09200795813995,1.60398921465379,
15.1038801789628));
#105556=CARTESIAN_POINT('Ctrl Pts',(-3.02239958354363,-1.73158752921176,
15.2628450451476));
#105557=CARTESIAN_POINT('Ctrl Pts',(-0.180083415399364,-3.47862969823242,
15.4218099113323));
#105558=CARTESIAN_POINT('Ctrl Pts',(2.82743880031229,-2.03442484363887,
15.5807747775171));
#105559=CARTESIAN_POINT('Ctrl Pts',(3.24110756259866,1.27613337139665,15.7397396437018));
#105560=CARTESIAN_POINT('Ctrl Pts',(0.681428840497123,3.41598438949379,
15.8987045098866));
#105561=CARTESIAN_POINT('Ctrl Pts',(-2.50338332427764,2.42205832829334,
16.0576693760713));
#105562=CARTESIAN_POINT('Ctrl Pts',(-3.39162607074788,-0.793830718824695,
16.2166342422561));
#105563=CARTESIAN_POINT('Ctrl Pts',(-1.16843772439841,-3.28147038659945,
16.3755991084409));
#105564=CARTESIAN_POINT('Ctrl Pts',(2.12665931408915,-2.75873427058938,
16.5345639746256));
#105565=CARTESIAN_POINT('Ctrl Pts',(3.47078835797328,0.294826708565589,
16.6935288408103));
#105566=CARTESIAN_POINT('Ctrl Pts',(1.63086391591002,3.07791772172504,16.8524937069951));
#105567=CARTESIAN_POINT('Ctrl Pts',(-1.70519264398462,3.03736936522827,
17.0114585731798));
#105568=CARTESIAN_POINT('Ctrl Pts',(-3.47692893358152,0.210380143431305,
17.1704234393646));
#105569=CARTESIAN_POINT('Ctrl Pts',(-2.05897845765457,-2.80960892738488,
17.3293883055493));
#105570=CARTESIAN_POINT('Ctrl Pts',(1.24785052638568,-3.25210142488291,
17.4883531717341));
#105571=CARTESIAN_POINT('Ctrl Pts',(3.40991860636443,-0.711160819995082,
17.6473180379188));
#105572=CARTESIAN_POINT('Ctrl Pts',(2.44377427303097,2.48218893648296,17.8062829041036));
#105573=CARTESIAN_POINT('Ctrl Pts',(-0.764254955138454,3.39841271441135,
17.9652477702883));
#105574=CARTESIAN_POINT('Ctrl Pts',(-3.27116720264528,1.19697942599879,
18.1242126364731));
#105575=CARTESIAN_POINT('Ctrl Pts',(-2.77715566556803,-2.10254631890235,
18.2831775026578));
#105576=CARTESIAN_POINT('Ctrl Pts',(0.264580268952404,-3.4732249992201,
18.4421423688426));
#105577=CARTESIAN_POINT('Ctrl Pts',(3.06359390502579,-1.65761485243577,
18.6011072350273));
#105578=CARTESIAN_POINT('Ctrl Pts',(3.05210864380509,1.67866835328972,18.7600721012121));
#105579=CARTESIAN_POINT('Ctrl Pts',(0.240660905911945,3.47496430806008,
18.9190369673968));
#105580=CARTESIAN_POINT('Ctrl Pts',(-2.79156583587576,2.08337581772957,
19.0780018335815));
#105581=CARTESIAN_POINT('Ctrl Pts',(-3.26284848824455,-1.21947298317094,
19.2369666997663));
#105582=CARTESIAN_POINT('Ctrl Pts',(-0.74083883016756,-3.40359404771472,
19.395931565951));
#105583=CARTESIAN_POINT('Ctrl Pts',(2.46080617770385,-2.46530476203616,
19.5548964321358));
#105584=CARTESIAN_POINT('Ctrl Pts',(3.40494145572254,0.734621192864293,
19.7138612983205));
#105585=CARTESIAN_POINT('Ctrl Pts',(1.22543028996257,3.26061577288012,19.8728261645053));
#105586=CARTESIAN_POINT('Ctrl Pts',(-2.07827376346511,2.79536630482174,
20.03179103069));
#105587=CARTESIAN_POINT('Ctrl Pts',(-3.47539806065695,-0.234313750609469,
20.1907558968748));
#105588=CARTESIAN_POINT('Ctrl Pts',(-1.6842399941803,-3.04903759502821,
20.3497207630595));
#105589=CARTESIAN_POINT('Ctrl Pts',(1.6520166701311,-3.06661630079082,20.5086856292443));
#105590=CARTESIAN_POINT('Ctrl Pts',(3.47273597056966,-0.27092340473533,
20.667650495429));
#105591=CARTESIAN_POINT('Ctrl Pts',(2.10761507273776,2.77331089481495,20.8266153616138));
#105592=CARTESIAN_POINT('Ctrl Pts',(-1.19100289599724,3.27334793756324,
20.9855802277985));
#105593=CARTESIAN_POINT('Ctrl Pts',(-3.39701119217357,0.77046061789229,
21.1445450939833));
#105594=CARTESIAN_POINT('Ctrl Pts',(-2.4866481639305,-2.4392366689663,21.303509960168));
#105595=CARTESIAN_POINT('Ctrl Pts',(0.70493168574874,-3.41121180245027,
21.4624748263528));
#105596=CARTESIAN_POINT('Ctrl Pts',(3.2498168887487,-1.2537881510166,21.6214396925375));
#105597=CARTESIAN_POINT('Ctrl Pts',(2.81336482410308,2.05384347803204,21.7804045587223));
#105598=CARTESIAN_POINT('Ctrl Pts',(-0.20402948430127,3.47730739983474,
21.939369424907));
#105599=CARTESIAN_POINT('Ctrl Pts',(-3.03424983174571,1.71073727770627,
22.0983342910918));
#105600=CARTESIAN_POINT('Ctrl Pts',(-3.08089135863104,-1.62523953522219,
22.2572991572765));
#105601=CARTESIAN_POINT('Ctrl Pts',(-0.301165107706183,-3.47024424648171,
22.4162640234613));
#105602=CARTESIAN_POINT('Ctrl Pts',(2.75484503979201,-2.13169408487794,
22.575228889646));
#105603=CARTESIAN_POINT('Ctrl Pts',(3.28359983463026,1.16244185597087,22.7341937558308));
#105604=CARTESIAN_POINT('Ctrl Pts',(0.800022296178244,3.39017162639943,
22.8931586220155));
#105605=CARTESIAN_POINT('Ctrl Pts',(-2.41747891830033,2.50780078374637,
23.0521234882003));
#105606=CARTESIAN_POINT('Ctrl Pts',(-3.4172292516762,-0.675184725313785,
23.211088354385));
#105607=CARTESIAN_POINT('Ctrl Pts',(-1.28203945489728,-3.23877893236102,
23.3700532205698));
#105608=CARTESIAN_POINT('Ctrl Pts',(2.02923554998735,-2.83113542067243,
23.5290180867545));
#105609=CARTESIAN_POINT('Ctrl Pts',(3.47899442394374,0.173702208550458,
23.6879829529393));
#105610=CARTESIAN_POINT('Ctrl Pts',(1.73702536950861,3.0192843488999,23.846947819124));
#105611=CARTESIAN_POINT('Ctrl Pts',(-1.59818755063192,3.09483229510396,
24.0059126853087));
#105612=CARTESIAN_POINT('Ctrl Pts',(-3.46777844265547,0.331575496164351,
24.1648775514935));
#105613=CARTESIAN_POINT('Ctrl Pts',(-2.15505874693774,-2.73653612606696,
24.3238424176782));
#105614=CARTESIAN_POINT('Ctrl Pts',(1.13273456819505,-3.29290070481601,
24.482807283863));
#105615=CARTESIAN_POINT('Ctrl Pts',(3.38512249348965,-0.830890752322139,
24.6417721500477));
#105616=CARTESIAN_POINT('Ctrl Pts',(2.52446713965543,2.39891946268483,24.800763045219));
#105617=CARTESIAN_POINT('Ctrl Pts',(0.41694291188581,3.07688877405814,24.9067656516621));
#105618=CARTESIAN_POINT('Ctrl Pts',(-0.547234924006723,2.89456662041414,
24.9597799693768));
#105619=CARTESIAN_POINT('',(-1.37840024430538,-1.93245649864576,-0.0011160887762519));
#105620=CARTESIAN_POINT('Ctrl Pts',(-1.38000853228519,-1.93376988380877,
2.94035629178069E-16));
#105621=CARTESIAN_POINT('Ctrl Pts',(-1.4297549820204,-1.90670748712375,
-1.0940687484236E-15));
#105622=CARTESIAN_POINT('Ctrl Pts',(-1.47837306283675,-1.87779458035135,
1.7193541140338E-15));
#105623=CARTESIAN_POINT('Ctrl Pts',(-1.52574686801137,-1.84705383051901,
1.33053290607421E-15));
#105624=CARTESIAN_POINT('Ctrl Pts',(-1.59465901921528,-1.80233689902576,
5.8070168986626E-16));
#105625=CARTESIAN_POINT('Ctrl Pts',(-1.66093964424413,-1.75375486097636,
-7.47438015865648E-16));
#105626=CARTESIAN_POINT('Ctrl Pts',(-1.72450125496549,-1.7016761593034,
3.92047505570758E-16));
#105627=CARTESIAN_POINT('Ctrl Pts',(-1.77965763233737,-1.65648421891812,
1.3808502233884E-15));
#105628=CARTESIAN_POINT('Ctrl Pts',(-1.83276652858523,-1.60865813869483,
4.61594664290787E-15));
#105629=CARTESIAN_POINT('Ctrl Pts',(-1.88375802489245,-1.55840962235702,
2.91433543964104E-16));
#105630=CARTESIAN_POINT('Ctrl Pts',(-1.89644826437001,-1.54590428809742,
-8.1504500272814E-16));
#105631=CARTESIAN_POINT('Ctrl Pts',(-1.90900111730879,-1.53325481819968,
-1.74004399250644E-16));
#105632=CARTESIAN_POINT('Ctrl Pts',(-1.92141126720496,-1.52046950431021,
9.71445146547012E-17));
#105633=CARTESIAN_POINT('Ctrl Pts',(-1.98035838488981,-1.45974039073902,
1.67517006871711E-15));
#105634=CARTESIAN_POINT('Ctrl Pts',(-2.03612011880858,-1.39591828314059,
2.73356635213392E-15));
#105635=CARTESIAN_POINT('Ctrl Pts',(-2.08860296990658,-1.32938115129062,
1.77635683940025E-15));
#105636=CARTESIAN_POINT('Ctrl Pts',(-2.1424363494038,-1.26113183566471,
7.94515687876094E-16));
#105637=CARTESIAN_POINT('Ctrl Pts',(-2.19282057211837,-1.19002542991145,
-4.18623297150609E-16));
#105638=CARTESIAN_POINT('Ctrl Pts',(-2.23962715136483,-1.11642291402605,
5.27355936696949E-16));
#105639=CARTESIAN_POINT('Ctrl Pts',(-2.25367989982903,-1.09432521625106,
8.11367467546422E-16));
#105640=CARTESIAN_POINT('Ctrl Pts',(-2.26740994442307,-1.0720022413678,
1.01236449027613E-15));
#105641=CARTESIAN_POINT('Ctrl Pts',(-2.28081320143484,-1.0494630813435,
9.43689570931383E-16));
#105642=CARTESIAN_POINT('Ctrl Pts',(-2.28854016506294,-1.03646927919803,
1.06112055969545E-15));
#105643=CARTESIAN_POINT('Ctrl Pts',(-2.29615841050338,-1.02340363584216,
2.42274131692933E-15));
#105644=CARTESIAN_POINT('Ctrl Pts',(-2.30366012931239,-1.01028056907449,
2.42861286636753E-15));
#105645=CARTESIAN_POINT('Ctrl Pts',(-2.34788758313654,-0.932911656126013,
2.51960496077167E-15));
#105646=CARTESIAN_POINT('Ctrl Pts',(-2.38813169620358,-0.853443126245271,
2.56936708869013E-15));
#105647=CARTESIAN_POINT('Ctrl Pts',(-2.42429183936437,-0.772277775263675,
8.04911692853238E-16));
#105648=CARTESIAN_POINT('Ctrl Pts',(-2.46091595491175,-0.69007098809537,
-9.82183507738202E-16));
#105649=CARTESIAN_POINT('Ctrl Pts',(-2.49335125604467,-0.60612280514716,
-7.94941899479276E-16));
#105650=CARTESIAN_POINT('Ctrl Pts',(-2.52145944991457,-0.520809805332038,
-6.10622663543836E-16));
#105651=CARTESIAN_POINT('Ctrl Pts',(-2.5494808416252,-0.435760264372774,
-4.2687263201004E-16));
#105652=CARTESIAN_POINT('Ctrl Pts',(-2.57320236910088,-0.349353441725185,
5.04520330946943E-16));
#105653=CARTESIAN_POINT('Ctrl Pts',(-2.59244489102332,-0.261933481969527,
-2.77555756156289E-17));
#105654=CARTESIAN_POINT('Ctrl Pts',(-2.60035763856488,-0.225985383563911,
-2.4663358381342E-16));
#105655=CARTESIAN_POINT('Ctrl Pts',(-2.60751246699365,-0.189865704000582,
-9.27455087219583E-16));
#105656=CARTESIAN_POINT('Ctrl Pts',(-2.61389449998738,-0.153597483987339,
-7.7715611723761E-16));
#105657=CARTESIAN_POINT('Ctrl Pts',(-2.61683838977986,-0.136867761218229,
-7.7185221570313E-16));
#105658=CARTESIAN_POINT('Ctrl Pts',(-2.61961782537805,-0.120106427110366,
1.42601103290378E-15));
#105659=CARTESIAN_POINT('Ctrl Pts',(-2.62223123581086,-0.103315720290366,
1.11022302462516E-16));
#105660=CARTESIAN_POINT('Ctrl Pts',(-2.62432314157133,-0.0898755901530302,
-5.34901838098858E-16));
#105661=CARTESIAN_POINT('Ctrl Pts',(-2.62630726224861,-0.0764256097890602,
-1.48813852544152E-15));
#105662=CARTESIAN_POINT('Ctrl Pts',(-2.62818292774977,-0.0629691027470899,
-1.33226762955019E-15));
#105663=CARTESIAN_POINT('Ctrl Pts',(-2.64096297258636,0.0287182280877715,
-5.01642716975331E-16));
#105664=CARTESIAN_POINT('Ctrl Pts',(-2.64871616260283,0.120736677540811,
1.05235300008268E-15));
#105665=CARTESIAN_POINT('Ctrl Pts',(-2.65130675431473,0.212692240506512,
-7.49400541621981E-16));
#105666=CARTESIAN_POINT('Ctrl Pts',(-2.65228201510577,0.247310067262954,
-1.71122277691643E-15));
#105667=CARTESIAN_POINT('Ctrl Pts',(-2.65252517805866,0.28191928532423,
-1.61897482542291E-15));
#105668=CARTESIAN_POINT('Ctrl Pts',(-2.65202733419216,0.316499817063281,
-5.82867087928207E-16));
#105669=CARTESIAN_POINT('Ctrl Pts',(-2.65073859129207,0.406016667142018,
2.28695183531716E-15));
#105670=CARTESIAN_POINT('Ctrl Pts',(-2.64448830078811,0.495340674919477,
9.61036850291248E-16));
#105671=CARTESIAN_POINT('Ctrl Pts',(-2.63352875838965,0.584202228253877,
2.22044604925031E-16));
#105672=CARTESIAN_POINT('Ctrl Pts',(-2.62256921599118,0.673063781588278,
-5.16947640441185E-16));
#105673=CARTESIAN_POINT('Ctrl Pts',(-2.60690015250225,0.761463607059672,
4.96773921778048E-16));
#105674=CARTESIAN_POINT('Ctrl Pts',(-2.58672150741346,0.849135624308466,
-2.27595720048157E-15));
#105675=CARTESIAN_POINT('Ctrl Pts',(-2.58222377673817,0.86867732889812,
-2.64044297795768E-15));
#105676=CARTESIAN_POINT('Ctrl Pts',(-2.57750180222384,0.888182863298944,
1.57927706612469E-15));
#105677=CARTESIAN_POINT('Ctrl Pts',(-2.57255746459196,0.907649247569788,
-4.71844785465692E-16));
#105678=CARTESIAN_POINT('Ctrl Pts',(-2.56909036256595,0.921299597802606,
-1.81456717867258E-15));
#105679=CARTESIAN_POINT('Ctrl Pts',(-2.56551386203416,0.934930611625315,
-6.29501938009571E-17));
#105680=CARTESIAN_POINT('Ctrl Pts',(-2.56183256521565,0.948527398973697,
-2.22044604925031E-16));
#105681=CARTESIAN_POINT('Ctrl Pts',(-2.53769258385253,1.03768787947022,
-1.55526631325667E-15));
#105682=CARTESIAN_POINT('Ctrl Pts',(-2.5090134703751,1.12552579298916,2.14318453916703E-15));
#105683=CARTESIAN_POINT('Ctrl Pts',(-2.4760839832643,1.21175983132397,2.99760216648792E-15));
#105684=CARTESIAN_POINT('Ctrl Pts',(-2.44257162390528,1.29952026536694,
3.86714351321826E-15));
#105685=CARTESIAN_POINT('Ctrl Pts',(-2.40465691530913,1.38562031404822,
-6.57769690187563E-16));
#105686=CARTESIAN_POINT('Ctrl Pts',(-2.3625894351197,1.46976681490133,-1.63757896132211E-15));
#105687=CARTESIAN_POINT('Ctrl Pts',(-2.31999722978461,1.55496290999486,
-2.62960980028503E-15));
#105688=CARTESIAN_POINT('Ctrl Pts',(-2.27314775465957,1.63815729286034,
1.03894163369803E-15));
#105689=CARTESIAN_POINT('Ctrl Pts',(-2.22224770950079,1.71903655485284,
8.32667268468867E-16));
#105690=CARTESIAN_POINT('Ctrl Pts',(-2.19258578684687,1.76616881978589,
7.12461200913758E-16));
#105691=CARTESIAN_POINT('Ctrl Pts',(-2.16154735127789,1.8125146430568,-3.53624849731269E-16));
#105692=CARTESIAN_POINT('Ctrl Pts',(-2.12916581821013,1.85800875267655,
-4.44089209850063E-16));
#105693=CARTESIAN_POINT('Ctrl Pts',(-2.12064615841252,1.8699783631315,-5.70106170484684E-16));
#105694=CARTESIAN_POINT('Ctrl Pts',(-2.11203197224998,1.88189106910177,
4.99191063271152E-16));
#105695=CARTESIAN_POINT('Ctrl Pts',(-2.10332881249318,1.89373885098382,
4.44089209850063E-16));
#105696=CARTESIAN_POINT('Ctrl Pts',(-2.04513073725928,1.97296503096835,
6.63206793642155E-16));
#105697=CARTESIAN_POINT('Ctrl Pts',(-1.98310309941755,2.04909488477598,
2.85493467669587E-17));
#105698=CARTESIAN_POINT('Ctrl Pts',(-1.91752051055856,2.12182013150207,
1.27675647831893E-15));
#105699=CARTESIAN_POINT('Ctrl Pts',(-1.85172508404381,2.19478139622161,
2.51589036252178E-15));
#105700=CARTESIAN_POINT('Ctrl Pts',(-1.78235120221478,2.26431682197845,
2.36153937213606E-15));
#105701=CARTESIAN_POINT('Ctrl Pts',(-1.70962567801232,2.33010034792287,
1.66533453693773E-16));
#105702=CARTESIAN_POINT('Ctrl Pts',(-1.63825968478638,2.39465411660879,
-1.03982216055884E-15));
#105703=CARTESIAN_POINT('Ctrl Pts',(-1.56366566082645,2.45559572732805,
8.15654749631012E-16));
#105704=CARTESIAN_POINT('Ctrl Pts',(-1.48601649839977,2.51259054837298,
0.));
#105705=CARTESIAN_POINT('Ctrl Pts',(-1.42234737003875,2.55932396395166,
-4.16838681284198E-16));
#105706=CARTESIAN_POINT('Ctrl Pts',(-1.35662332229989,2.60340355803474,
-4.62859095806204E-17));
#105707=CARTESIAN_POINT('Ctrl Pts',(-1.28892185405323,2.64462557919717,
2.77555756156289E-16));
#105708=CARTESIAN_POINT('Ctrl Pts',(-1.37727721526601,-1.93088206134116,
-0.0011160887762518));
#105709=CARTESIAN_POINT('Ctrl Pts',(-1.36872530799275,-1.93698204397104,
-0.000744059184169721));
#105710=CARTESIAN_POINT('Ctrl Pts',(-1.36013287474801,-1.94302521096248,
-0.00037202959208763));
#105711=CARTESIAN_POINT('Ctrl Pts',(-1.35150067398999,-1.94901102888224,
-5.55111512312578E-15));
#105712=CARTESIAN_POINT('Origin',(-1.44337567297407,-2.5,-6.));
#105713=CARTESIAN_POINT('',(-1.44337567297407,-2.5,-6.));
#105714=CARTESIAN_POINT('',(1.44337567297406,-2.5,-6.));
#105715=CARTESIAN_POINT('',(-0.721687836487033,-2.5,-6.));
#105716=CARTESIAN_POINT('',(-1.44337567297407,-2.5,-3.));
#105717=CARTESIAN_POINT('',(-1.44337567297407,-2.5,-6.));
#105718=CARTESIAN_POINT('',(1.44337567297406,-2.5,-3.));
#105719=CARTESIAN_POINT('',(-1.44337567297407,-2.5,-3.));
#105720=CARTESIAN_POINT('',(1.44337567297406,-2.5,-6.));
#105721=CARTESIAN_POINT('Origin',(-2.88675134594813,3.53525079574969E-16,
-6.));
#105722=CARTESIAN_POINT('',(-2.88675134594813,3.53525079574969E-16,-6.));
#105723=CARTESIAN_POINT('',(-2.52590742770461,-0.625,-6.));
#105724=CARTESIAN_POINT('',(-2.88675134594813,5.55111512312578E-16,-3.));
#105725=CARTESIAN_POINT('',(-2.88675134594813,3.53525079574969E-16,-6.));
#105726=CARTESIAN_POINT('',(-2.88675134594813,3.53525079574969E-16,-3.));
#105727=CARTESIAN_POINT('Origin',(-1.44337567297406,2.5,-6.));
#105728=CARTESIAN_POINT('',(-1.44337567297406,2.5,-6.));
#105729=CARTESIAN_POINT('',(-1.80421959121758,1.875,-6.));
#105730=CARTESIAN_POINT('',(-1.44337567297406,2.5,-3.));
#105731=CARTESIAN_POINT('',(-1.44337567297406,2.5,-6.));
#105732=CARTESIAN_POINT('',(-1.44337567297406,2.5,-3.));
#105733=CARTESIAN_POINT('Origin',(1.44337567297406,2.5,-6.));
#105734=CARTESIAN_POINT('',(1.44337567297406,2.5,-6.));
#105735=CARTESIAN_POINT('',(0.721687836487033,2.5,-6.));
#105736=CARTESIAN_POINT('',(1.44337567297406,2.5,-3.));
#105737=CARTESIAN_POINT('',(1.44337567297406,2.5,-6.));
#105738=CARTESIAN_POINT('',(1.44337567297406,2.5,-3.));
#105739=CARTESIAN_POINT('Origin',(2.88675134594813,0.,-6.));
#105740=CARTESIAN_POINT('',(2.88675134594813,0.,-6.));
#105741=CARTESIAN_POINT('',(2.52590742770461,0.625,-6.));
#105742=CARTESIAN_POINT('',(2.88675134594813,0.,-3.));
#105743=CARTESIAN_POINT('',(2.88675134594813,0.,-6.));
#105744=CARTESIAN_POINT('',(2.88675134594813,0.,-3.));
#105745=CARTESIAN_POINT('Origin',(1.44337567297406,-2.5,-6.));
#105746=CARTESIAN_POINT('',(1.80421959121758,-1.875,-6.));
#105747=CARTESIAN_POINT('',(1.44337567297406,-2.5,-3.));
#105748=CARTESIAN_POINT('Origin',(0.,0.,-3.));
#105749=CARTESIAN_POINT('Origin',(0.,0.,0.));
#105750=CARTESIAN_POINT('',(-5.,-6.12323399573677E-16,0.));
#105751=CARTESIAN_POINT('Origin',(0.,0.,0.));
#105752=CARTESIAN_POINT('Origin',(0.,0.,-6.));
#105753=CARTESIAN_POINT('',(-5.,-6.12323399573677E-16,-6.));
#105754=CARTESIAN_POINT('',(-5.,-6.12323399573677E-16,-6.));
#105755=CARTESIAN_POINT('Origin',(0.,0.,-6.));
#105756=CARTESIAN_POINT('Origin',(0.,0.,-6.));
#105757=CARTESIAN_POINT('Origin',(0.,0.,25.));
#105791=UNCERTAINTY_MEASURE_WITH_UNIT(LENGTH_MEASURE(0.01),#105807,
'DISTANCE_ACCURACY_VALUE',
'Maximum model space distance between geometric entities at asserted c
onnectivities');
#105792=UNCERTAINTY_MEASURE_WITH_UNIT(LENGTH_MEASURE(0.01),#105807,
'DISTANCE_ACCURACY_VALUE',
'Maximum model space distance between geometric entities at asserted c
onnectivities');
#105805=(
GEOMETRIC_REPRESENTATION_CONTEXT(3)
GLOBAL_UNCERTAINTY_ASSIGNED_CONTEXT((#105791))
GLOBAL_UNIT_ASSIGNED_CONTEXT((#105807,#105809,#105810))
REPRESENTATION_CONTEXT('','3D')
);
#105806=(
GEOMETRIC_REPRESENTATION_CONTEXT(3)
GLOBAL_UNCERTAINTY_ASSIGNED_CONTEXT((#105792))
GLOBAL_UNIT_ASSIGNED_CONTEXT((#105807,#105809,#105810))
REPRESENTATION_CONTEXT('','3D')
);
#105807=(
LENGTH_UNIT()
NAMED_UNIT(*)
SI_UNIT(.MILLI.,.METRE.)
);
#105809=(
NAMED_UNIT(*)
PLANE_ANGLE_UNIT()
SI_UNIT($,.RADIAN.)
);
#105810=(
NAMED_UNIT(*)
SI_UNIT($,.STERADIAN.)
SOLID_ANGLE_UNIT()
);
#105823=SHAPE_DEFINITION_REPRESENTATION(#105836,#105870);
#105836=PRODUCT_DEFINITION_SHAPE('',$,#105884);
#105870=SHAPE_REPRESENTATION('',(#7676),#105805);
#105871=PRODUCT_DEFINITION_CONTEXT('part definition',#105912,'design');
#105884=PRODUCT_DEFINITION('Socket head cap screw M6x25',
'Socket head cap screw M6x25',#105897,#105871);
#105897=PRODUCT_DEFINITION_FORMATION('',$,#105926);
#105912=APPLICATION_CONTEXT(
'Core Data for Automotive Mechanical Design Process');
#105913=PRODUCT_CONTEXT('part definition',#105912,'mechanical');
#105926=PRODUCT('Socket head cap screw M6x25',
'Socket head cap screw M6x25',$,(#105913));
#105932=PRESENTATION_STYLE_ASSIGNMENT((#105938));
#105938=SURFACE_STYLE_USAGE(.BOTH.,#105944);
#105944=SURFACE_SIDE_STYLE('',(#105950));
#105950=SURFACE_STYLE_FILL_AREA(#105956);
#105956=FILL_AREA_STYLE('Opaque(64,72,82)',(#105962));
#105962=FILL_AREA_STYLE_COLOUR('Opaque(64,72,82)',#105968);
#105968=COLOUR_RGB('Opaque(64,72,82)',0.250980392156863,0.282352941176471,
0.32156862745098);
ENDSEC;
END-ISO-10303-21;
